ISO-10303-21;
HEADER;
/* Generated by software containing ST-Developer
 * from STEP Tools, Inc. (www.steptools.com) 
 */

FILE_DESCRIPTION(
/* description */ (''),
/* implementation_level */ '2;1');

FILE_NAME(
/* name */ 'Screw_right.step',
/* time_stamp */ '2026-10-04T22:13:49-07:00',
/* author */ (''),
/* organization */ (''),
/* preprocessor_version */ 'ST-DEVELOPER v20.2',
/* originating_system */ 'Autodesk Translation Framework v15.15.0.0',
/* authorisation */ '');

FILE_SCHEMA (('AUTOMOTIVE_DESIGN { 1 0 10303 214 3 1 1 }'));
ENDSEC;

DATA;
#10=MECHANICAL_DESIGN_GEOMETRIC_PRESENTATION_REPRESENTATION('',(#369),#40734);
#49=B_SPLINE_SURFACE_WITH_KNOTS('',3,3,((#39281,#39282,#39283,#39284,#39285,
#39286,#39287,#39288,#39289,#39290,#39291,#39292,#39293,#39294,#39295,#39296,
#39297,#39298,#39299,#39300,#39301,#39302,#39303,#39304,#39305,#39306,#39307,
#39308,#39309,#39310,#39311,#39312,#39313,#39314,#39315,#39316,#39317,#39318,
#39319,#39320,#39321,#39322,#39323,#39324,#39325,#39326,#39327,#39328,#39329,
#39330,#39331,#39332,#39333,#39334,#39335,#39336,#39337,#39338,#39339,#39340,
#39341,#39342,#39343,#39344,#39345,#39346,#39347,#39348,#39349,#39350,#39351,
#39352,#39353,#39354,#39355,#39356,#39357,#39358,#39359,#39360,#39361,#39362,
#39363,#39364,#39365,#39366,#39367,#39368,#39369,#39370,#39371,#39372,#39373,
#39374,#39375,#39376,#39377,#39378,#39379,#39380,#39381,#39382,#39383,#39384,
#39385,#39386,#39387,#39388,#39389,#39390,#39391,#39392,#39393,#39394,#39395,
#39396,#39397,#39398,#39399,#39400,#39401,#39402,#39403,#39404,#39405,#39406,
#39407,#39408,#39409,#39410,#39411,#39412,#39413,#39414,#39415,#39416,#39417,
#39418),(#39419,#39420,#39421,#39422,#39423,#39424,#39425,#39426,#39427,
#39428,#39429,#39430,#39431,#39432,#39433,#39434,#39435,#39436,#39437,#39438,
#39439,#39440,#39441,#39442,#39443,#39444,#39445,#39446,#39447,#39448,#39449,
#39450,#39451,#39452,#39453,#39454,#39455,#39456,#39457,#39458,#39459,#39460,
#39461,#39462,#39463,#39464,#39465,#39466,#39467,#39468,#39469,#39470,#39471,
#39472,#39473,#39474,#39475,#39476,#39477,#39478,#39479,#39480,#39481,#39482,
#39483,#39484,#39485,#39486,#39487,#39488,#39489,#39490,#39491,#39492,#39493,
#39494,#39495,#39496,#39497,#39498,#39499,#39500,#39501,#39502,#39503,#39504,
#39505,#39506,#39507,#39508,#39509,#39510,#39511,#39512,#39513,#39514,#39515,
#39516,#39517,#39518,#39519,#39520,#39521,#39522,#39523,#39524,#39525,#39526,
#39527,#39528,#39529,#39530,#39531,#39532,#39533,#39534,#39535,#39536,#39537,
#39538,#39539,#39540,#39541,#39542,#39543,#39544,#39545,#39546,#39547,#39548,
#39549,#39550,#39551,#39552,#39553,#39554,#39555,#39556),(#39557,#39558,
#39559,#39560,#39561,#39562,#39563,#39564,#39565,#39566,#39567,#39568,#39569,
#39570,#39571,#39572,#39573,#39574,#39575,#39576,#39577,#39578,#39579,#39580,
#39581,#39582,#39583,#39584,#39585,#39586,#39587,#39588,#39589,#39590,#39591,
#39592,#39593,#39594,#39595,#39596,#39597,#39598,#39599,#39600,#39601,#39602,
#39603,#39604,#39605,#39606,#39607,#39608,#39609,#39610,#39611,#39612,#39613,
#39614,#39615,#39616,#39617,#39618,#39619,#39620,#39621,#39622,#39623,#39624,
#39625,#39626,#39627,#39628,#39629,#39630,#39631,#39632,#39633,#39634,#39635,
#39636,#39637,#39638,#39639,#39640,#39641,#39642,#39643,#39644,#39645,#39646,
#39647,#39648,#39649,#39650,#39651,#39652,#39653,#39654,#39655,#39656,#39657,
#39658,#39659,#39660,#39661,#39662,#39663,#39664,#39665,#39666,#39667,#39668,
#39669,#39670,#39671,#39672,#39673,#39674,#39675,#39676,#39677,#39678,#39679,
#39680,#39681,#39682,#39683,#39684,#39685,#39686,#39687,#39688,#39689,#39690,
#39691,#39692,#39693,#39694),(#39695,#39696,#39697,#39698,#39699,#39700,
#39701,#39702,#39703,#39704,#39705,#39706,#39707,#39708,#39709,#39710,#39711,
#39712,#39713,#39714,#39715,#39716,#39717,#39718,#39719,#39720,#39721,#39722,
#39723,#39724,#39725,#39726,#39727,#39728,#39729,#39730,#39731,#39732,#39733,
#39734,#39735,#39736,#39737,#39738,#39739,#39740,#39741,#39742,#39743,#39744,
#39745,#39746,#39747,#39748,#39749,#39750,#39751,#39752,#39753,#39754,#39755,
#39756,#39757,#39758,#39759,#39760,#39761,#39762,#39763,#39764,#39765,#39766,
#39767,#39768,#39769,#39770,#39771,#39772,#39773,#39774,#39775,#39776,#39777,
#39778,#39779,#39780,#39781,#39782,#39783,#39784,#39785,#39786,#39787,#39788,
#39789,#39790,#39791,#39792,#39793,#39794,#39795,#39796,#39797,#39798,#39799,
#39800,#39801,#39802,#39803,#39804,#39805,#39806,#39807,#39808,#39809,#39810,
#39811,#39812,#39813,#39814,#39815,#39816,#39817,#39818,#39819,#39820,#39821,
#39822,#39823,#39824,#39825,#39826,#39827,#39828,#39829,#39830,#39831,#39832)),
 .UNSPECIFIED.,.F.,.F.,.F.,(4,4),(4,1,1,1,1,1,1,1,1,1,1,1,1,1,1,1,1,1,1,
1,1,1,1,1,1,1,1,1,1,1,1,1,1,1,1,1,1,1,1,1,1,1,1,1,1,1,1,1,1,1,1,1,1,1,1,
1,1,1,1,1,1,1,1,1,1,1,1,1,1,1,1,1,1,1,1,1,1,1,1,1,1,1,1,1,1,1,1,1,1,1,1,
1,1,1,1,1,1,1,1,1,1,1,1,1,1,1,1,1,1,1,1,1,1,1,1,1,1,1,1,1,1,1,1,1,1,1,1,
1,1,1,1,1,1,1,1,4),(-0.000234148554357844,0.0332108863658552),(8.30203615430837,
9.29477737004237,10.2875185857764,11.2802598015104,12.2730010172444,13.2657422329784,
14.2584834487124,15.2512246644464,16.2439658801804,17.2367070959144,18.2294483116484,
19.2221895273825,20.2149307431165,21.2076719588505,22.2004131745845,23.1931543903185,
24.1858956060525,25.1786368217865,26.1713780375205,27.1641192532545,28.1568604689885,
29.1496016847225,30.1423429004565,31.1350841161905,32.1278253319246,33.1205665476586,
34.1133077633926,35.1060489791266,36.0987901948606,37.0915314105946,38.0842726263286,
39.0770138420626,40.0697550577966,41.0624962735306,42.0552374892646,43.0479787049986,
44.0407199207326,45.0334611364667,46.0262023522007,47.0189435679347,48.0116847836687,
49.0044259994027,49.9971672151367,50.9899084308707,51.9826496466047,52.9753908623387,
53.9681320780727,54.9608732938067,55.9536145095407,56.9463557252747,57.9390969410088,
58.9318381567428,59.9245793724768,60.9173205882108,61.9100618039448,62.9028030196788,
63.8955442354128,64.8882854511468,65.8810266668808,66.8737678826148,67.8665090983488,
68.8592503140828,69.8519915298168,70.8447327455509,71.8374739612849,72.8302151770189,
73.8229563927529,74.8156976084869,75.8084388242209,76.8011800399549,77.7939212556889,
78.7866624714229,79.7794036871569,80.7721449028909,81.7648861186249,82.7576273343589,
83.750368550093,84.743109765827,85.735850981561,86.728592197295,87.721333413029,
88.714074628763,89.706815844497,90.699557060231,91.692298275965,92.685039491699,
93.677780707433,94.670521923167,95.663263138901,96.6560043546351,97.6487455703691,
98.6414867861031,99.6342280018371,100.626969217571,101.619710433305,102.612451649039,
103.605192864773,104.597934080507,105.590675296241,106.583416511975,107.576157727709,
108.568898943443,109.561640159177,110.554381374911,111.547122590645,112.539863806379,
113.532605022113,114.525346237847,115.518087453581,116.510828669315,117.503569885049,
118.496311100783,119.489052316517,120.481793532251,121.474534747985,122.467275963719,
123.460017179453,124.452758395187,125.445499610921,126.438240826655,127.430982042389,
128.423723258123,129.416464473857,130.409205689591,131.401946905325,132.394688121059,
133.387429336793,134.380170552527,135.372911768261,136.365652983995,137.358394199729,
138.351135415463,139.343876631197,140.336617846931,141.329359062665,142.322334426953),
 .UNSPECIFIED.);
#50=B_SPLINE_SURFACE_WITH_KNOTS('',3,3,((#39993,#39994,#39995,#39996,#39997,
#39998,#39999,#40000,#40001,#40002,#40003,#40004,#40005,#40006,#40007,#40008,
#40009,#40010,#40011,#40012,#40013,#40014,#40015,#40016,#40017,#40018,#40019,
#40020,#40021,#40022,#40023,#40024,#40025,#40026,#40027,#40028,#40029,#40030,
#40031,#40032,#40033,#40034,#40035,#40036,#40037,#40038,#40039,#40040,#40041,
#40042,#40043,#40044,#40045,#40046,#40047,#40048,#40049,#40050,#40051,#40052,
#40053,#40054,#40055,#40056,#40057,#40058,#40059,#40060,#40061,#40062,#40063,
#40064,#40065,#40066,#40067,#40068,#40069,#40070,#40071,#40072,#40073,#40074,
#40075,#40076,#40077,#40078,#40079,#40080,#40081,#40082,#40083,#40084,#40085,
#40086,#40087,#40088,#40089,#40090,#40091,#40092,#40093,#40094,#40095,#40096,
#40097,#40098,#40099,#40100,#40101,#40102,#40103,#40104,#40105,#40106,#40107,
#40108,#40109,#40110,#40111,#40112,#40113,#40114,#40115,#40116,#40117,#40118,
#40119,#40120,#40121,#40122,#40123,#40124,#40125,#40126,#40127,#40128,#40129,
#40130),(#40131,#40132,#40133,#40134,#40135,#40136,#40137,#40138,#40139,
#40140,#40141,#40142,#40143,#40144,#40145,#40146,#40147,#40148,#40149,#40150,
#40151,#40152,#40153,#40154,#40155,#40156,#40157,#40158,#40159,#40160,#40161,
#40162,#40163,#40164,#40165,#40166,#40167,#40168,#40169,#40170,#40171,#40172,
#40173,#40174,#40175,#40176,#40177,#40178,#40179,#40180,#40181,#40182,#40183,
#40184,#40185,#40186,#40187,#40188,#40189,#40190,#40191,#40192,#40193,#40194,
#40195,#40196,#40197,#40198,#40199,#40200,#40201,#40202,#40203,#40204,#40205,
#40206,#40207,#40208,#40209,#40210,#40211,#40212,#40213,#40214,#40215,#40216,
#40217,#40218,#40219,#40220,#40221,#40222,#40223,#40224,#40225,#40226,#40227,
#40228,#40229,#40230,#40231,#40232,#40233,#40234,#40235,#40236,#40237,#40238,
#40239,#40240,#40241,#40242,#40243,#40244,#40245,#40246,#40247,#40248,#40249,
#40250,#40251,#40252,#40253,#40254,#40255,#40256,#40257,#40258,#40259,#40260,
#40261,#40262,#40263,#40264,#40265,#40266,#40267,#40268),(#40269,#40270,
#40271,#40272,#40273,#40274,#40275,#40276,#40277,#40278,#40279,#40280,#40281,
#40282,#40283,#40284,#40285,#40286,#40287,#40288,#40289,#40290,#40291,#40292,
#40293,#40294,#40295,#40296,#40297,#40298,#40299,#40300,#40301,#40302,#40303,
#40304,#40305,#40306,#40307,#40308,#40309,#40310,#40311,#40312,#40313,#40314,
#40315,#40316,#40317,#40318,#40319,#40320,#40321,#40322,#40323,#40324,#40325,
#40326,#40327,#40328,#40329,#40330,#40331,#40332,#40333,#40334,#40335,#40336,
#40337,#40338,#40339,#40340,#40341,#40342,#40343,#40344,#40345,#40346,#40347,
#40348,#40349,#40350,#40351,#40352,#40353,#40354,#40355,#40356,#40357,#40358,
#40359,#40360,#40361,#40362,#40363,#40364,#40365,#40366,#40367,#40368,#40369,
#40370,#40371,#40372,#40373,#40374,#40375,#40376,#40377,#40378,#40379,#40380,
#40381,#40382,#40383,#40384,#40385,#40386,#40387,#40388,#40389,#40390,#40391,
#40392,#40393,#40394,#40395,#40396,#40397,#40398,#40399,#40400,#40401,#40402,
#40403,#40404,#40405,#40406),(#40407,#40408,#40409,#40410,#40411,#40412,
#40413,#40414,#40415,#40416,#40417,#40418,#40419,#40420,#40421,#40422,#40423,
#40424,#40425,#40426,#40427,#40428,#40429,#40430,#40431,#40432,#40433,#40434,
#40435,#40436,#40437,#40438,#40439,#40440,#40441,#40442,#40443,#40444,#40445,
#40446,#40447,#40448,#40449,#40450,#40451,#40452,#40453,#40454,#40455,#40456,
#40457,#40458,#40459,#40460,#40461,#40462,#40463,#40464,#40465,#40466,#40467,
#40468,#40469,#40470,#40471,#40472,#40473,#40474,#40475,#40476,#40477,#40478,
#40479,#40480,#40481,#40482,#40483,#40484,#40485,#40486,#40487,#40488,#40489,
#40490,#40491,#40492,#40493,#40494,#40495,#40496,#40497,#40498,#40499,#40500,
#40501,#40502,#40503,#40504,#40505,#40506,#40507,#40508,#40509,#40510,#40511,
#40512,#40513,#40514,#40515,#40516,#40517,#40518,#40519,#40520,#40521,#40522,
#40523,#40524,#40525,#40526,#40527,#40528,#40529,#40530,#40531,#40532,#40533,
#40534,#40535,#40536,#40537,#40538,#40539,#40540,#40541,#40542,#40543,#40544)),
 .UNSPECIFIED.,.F.,.F.,.F.,(4,4),(4,1,1,1,1,1,1,1,1,1,1,1,1,1,1,1,1,1,1,
1,1,1,1,1,1,1,1,1,1,1,1,1,1,1,1,1,1,1,1,1,1,1,1,1,1,1,1,1,1,1,1,1,1,1,1,
1,1,1,1,1,1,1,1,1,1,1,1,1,1,1,1,1,1,1,1,1,1,1,1,1,1,1,1,1,1,1,1,1,1,1,1,
1,1,1,1,1,1,1,1,1,1,1,1,1,1,1,1,1,1,1,1,1,1,1,1,1,1,1,1,1,1,1,1,1,1,1,1,
1,1,1,1,1,1,1,1,4),(-0.000206153515366958,0.0332359307550877),(11.6156993846295,
12.6086809632344,13.6014221789684,14.5941633947024,15.5869046104364,16.5796458261704,
17.5723870419044,18.5651282576385,19.5578694733725,20.5506106891065,21.5433519048405,
22.5360931205745,23.5288343363085,24.5215755520425,25.5143167677765,26.5070579835105,
27.4997991992445,28.4925404149785,29.4852816307125,30.4780228464465,31.4707640621806,
32.4635052779146,33.4562464936486,34.4489877093826,35.4417289251166,36.4344701408506,
37.4272113565846,38.4199525723186,39.4126937880526,40.4054350037866,41.3981762195206,
42.3909174352546,43.3836586509887,44.3763998667227,45.3691410824567,46.3618822981907,
47.3546235139247,48.3473647296587,49.3401059453927,50.3328471611267,51.3255883768607,
52.3183295925947,53.3110708083287,54.3038120240627,55.2965532397967,56.2892944555308,
57.2820356712648,58.2747768869988,59.2675181027328,60.2602593184668,61.2530005342008,
62.2457417499348,63.2384829656688,64.2312241814028,65.2239653971368,66.2167066128708,
67.2094478286048,68.2021890443388,69.1949302600729,70.1876714758069,71.1804126915409,
72.1731539072749,73.1658951230089,74.1586363387429,75.1513775544769,76.1441187702109,
77.1368599859449,78.1296012016789,79.1223424174129,80.1150836331469,81.107824848881,
82.100566064615,83.093307280349,84.086048496083,85.078789711817,86.071530927551,
87.064272143285,88.057013359019,89.049754574753,90.042495790487,91.035237006221,
92.027978221955,93.020719437689,94.0134606534231,95.0062018691571,95.9989430848911,
96.9916843006251,97.9844255163591,98.9771667320931,99.9699079478271,100.962649163561,
101.955390379295,102.948131595029,103.940872810763,104.933614026497,105.926355242231,
106.919096457965,107.911837673699,108.904578889433,109.897320105167,110.890061320901,
111.882802536635,112.875543752369,113.868284968103,114.861026183837,115.853767399571,
116.846508615305,117.839249831039,118.831991046773,119.824732262507,120.817473478241,
121.810214693975,122.802955909709,123.795697125443,124.788438341177,125.781179556911,
126.773920772645,127.766661988379,128.759403204113,129.752144419847,130.744885635581,
131.737626851315,132.730368067049,133.723109282783,134.715850498517,135.708591714251,
136.701332929985,137.694074145719,138.686815361453,139.679556577187,140.672297792921,
141.665039008655,142.657780224389,143.650521440123,144.643262655857,145.636003871591),
 .UNSPECIFIED.);
#229=B_SPLINE_CURVE_WITH_KNOTS('',3,(#22897,#22898,#22899,#22900,#22901,
#22902,#22903,#22904,#22905,#22906,#22907,#22908,#22909,#22910,#22911,#22912,
#22913,#22914,#22915,#22916,#22917,#22918,#22919,#22920,#22921,#22922,#22923,
#22924,#22925,#22926,#22927,#22928,#22929,#22930,#22931,#22932,#22933,#22934,
#22935,#22936,#22937,#22938,#22939,#22940,#22941,#22942,#22943,#22944,#22945,
#22946,#22947,#22948,#22949,#22950,#22951,#22952,#22953,#22954,#22955,#22956,
#22957,#22958,#22959,#22960,#22961,#22962,#22963,#22964,#22965,#22966,#22967,
#22968,#22969,#22970,#22971,#22972,#22973,#22974,#22975,#22976,#22977,#22978,
#22979,#22980,#22981,#22982,#22983,#22984,#22985,#22986,#22987,#22988,#22989,
#22990,#22991,#22992,#22993,#22994,#22995,#22996,#22997,#22998,#22999,#23000,
#23001,#23002,#23003,#23004,#23005,#23006),.UNSPECIFIED.,.F.,.F.,(4,2,2,
2,2,2,2,2,2,2,2,2,2,2,2,2,2,2,2,2,2,2,2,2,2,2,2,2,2,2,2,2,2,2,2,2,2,2,2,
2,2,2,2,2,2,2,2,2,2,2,2,2,2,2,4),(-0.388501056592863,-0.386820572871954,
-0.37137009344835,-0.346422087251238,-0.343921258609954,-0.342711393673856,
-0.3418454804417,-0.340904563019323,-0.33953517948609,-0.335881943037683,
-0.330289052303747,-0.310335625674568,-0.289142186338472,-0.285999939238393,
-0.283978855303575,-0.282356169521994,-0.280505558685679,-0.277309325459776,
-0.262246632946139,-0.247209707985575,-0.243654292750582,-0.228032928473727,
-0.226105223025318,-0.224926585294603,-0.224011568002013,-0.222935252360905,
-0.220965990434522,-0.209786460207454,-0.193816832175384,-0.171678092584887,
-0.168540235746571,-0.166508234742227,-0.164867556447226,-0.162986029098486,
-0.159708544545876,-0.143440725523142,-0.129248288257582,-0.112150650603508,
-0.109143404207764,-0.107951343042863,-0.10701247453129,-0.106034759822587,
-0.10460473073509,-0.102883612375124,-0.0996310274333393,-0.0913975068235331,
-0.0670909053345679,-0.0552672459457108,-0.0521232458976062,-0.0502599305992454,
-0.0487650651937886,-0.0467406787382857,-0.0428350448067549,-0.022839327136288,
-0.00170946157028903),.UNSPECIFIED.);
#230=B_SPLINE_CURVE_WITH_KNOTS('',3,(#23009,#23010,#23011,#23012,#23013,
#23014,#23015,#23016,#23017,#23018,#23019,#23020,#23021,#23022,#23023,#23024,
#23025,#23026,#23027,#23028,#23029,#23030,#23031,#23032,#23033,#23034,#23035,
#23036,#23037,#23038,#23039,#23040,#23041,#23042,#23043,#23044,#23045,#23046,
#23047,#23048,#23049,#23050,#23051,#23052,#23053,#23054,#23055,#23056,#23057,
#23058,#23059,#23060,#23061,#23062,#23063),.UNSPECIFIED.,.F.,.F.,(4,3,3,
3,3,3,3,3,3,3,3,3,3,3,3,3,3,3,4),(11.6159397475004,11.7400323994672,11.8624742267738,
11.9848874271838,12.107314791651,12.2326563345468,12.3553366947763,12.4820088290054,
12.6086809632344,12.7327736152012,12.851232493043,12.9695575437606,13.087803548112,
13.2060251446645,13.3243597220786,13.4427610123004,13.5613799833078,13.6014221789684,
13.6623826713879),.UNSPECIFIED.);
#231=B_SPLINE_CURVE_WITH_KNOTS('',3,(#23068,#23069,#23070,#23071,#23072,
#23073,#23074,#23075,#23076,#23077,#23078,#23079,#23080,#23081,#23082,#23083,
#23084,#23085,#23086,#23087,#23088,#23089,#23090,#23091,#23092,#23093,#23094,
#23095,#23096,#23097,#23098,#23099,#23100,#23101,#23102,#23103,#23104,#23105,
#23106,#23107,#23108,#23109,#23110,#23111,#23112,#23113,#23114,#23115,#23116,
#23117,#23118,#23119,#23120,#23121,#23122,#23123,#23124,#23125,#23126,#23127,
#23128,#23129,#23130,#23131,#23132,#23133,#23134,#23135,#23136,#23137,#23138,
#23139,#23140,#23141,#23142,#23143,#23144,#23145,#23146,#23147,#23148,#23149,
#23150,#23151,#23152,#23153,#23154,#23155,#23156,#23157,#23158,#23159,#23160,
#23161,#23162,#23163,#23164,#23165,#23166,#23167,#23168,#23169,#23170,#23171,
#23172,#23173,#23174,#23175,#23176,#23177,#23178,#23179,#23180,#23181,#23182,
#23183,#23184,#23185,#23186,#23187,#23188,#23189,#23190,#23191,#23192,#23193,
#23194,#23195,#23196,#23197,#23198,#23199,#23200,#23201,#23202,#23203,#23204,
#23205,#23206,#23207,#23208,#23209,#23210,#23211,#23212,#23213,#23214,#23215,
#23216,#23217,#23218,#23219,#23220,#23221,#23222,#23223,#23224,#23225,#23226,
#23227,#23228,#23229,#23230,#23231,#23232,#23233,#23234,#23235,#23236,#23237,
#23238,#23239,#23240,#23241,#23242,#23243,#23244,#23245,#23246,#23247,#23248,
#23249,#23250,#23251,#23252,#23253,#23254,#23255,#23256,#23257,#23258,#23259,
#23260,#23261,#23262,#23263,#23264,#23265,#23266,#23267,#23268,#23269,#23270,
#23271,#23272,#23273,#23274,#23275,#23276,#23277,#23278,#23279,#23280,#23281,
#23282,#23283,#23284,#23285,#23286,#23287),.UNSPECIFIED.,.F.,.F.,(4,2,2,
2,2,2,2,2,2,2,2,2,2,2,2,2,2,2,2,2,2,2,2,2,2,2,2,2,2,2,2,2,2,2,2,2,2,2,2,
2,2,2,2,2,2,2,2,2,2,2,2,2,2,2,2,2,2,2,2,2,2,2,2,2,2,2,2,2,2,2,2,2,2,2,2,
2,2,2,2,2,2,2,2,2,2,2,2,2,2,2,2,2,2,2,2,2,2,2,2,2,2,2,2,2,2,2,2,2,2,4),
(-1.13048491284919,-1.11742794727068,-1.11149198614902,-1.10702303107772,
-1.10490648610305,-1.10326505430796,-1.10145250216885,-1.09846406594016,
-1.08815110668756,-1.05798398520967,-1.0515135693742,-1.0474498029415,-1.04601701513843,
-1.04505926622458,-1.0442035640373,-1.04303259822145,-1.04008464381358,
-1.01887948305155,-1.00106301949291,-0.994659836513761,-0.989922397528697,
-0.98775646149669,-0.986108517098755,-0.984320033889488,-0.981441648574161,
-0.972173535529898,-0.947158676525079,-0.931458748178385,-0.9293662738169,
-0.928265275729413,-0.927350577703114,-0.926200224605055,-0.924377206456902,
-0.913959809977621,-0.90548264528034,-0.891073174472189,-0.875027394424812,
-0.871770045965304,-0.86989889302085,-0.868266713289335,-0.866244654298588,
-0.863121143913001,-0.84044750521824,-0.823088340431133,-0.816896597038623,
-0.81295901391849,-0.811543168567195,-0.810588792820048,-0.809729485834232,
-0.808545655586117,-0.805538298880899,-0.786555979884845,-0.767855788452594,
-0.757176428021775,-0.754262308099518,-0.752465443359327,-0.750818913694456,
-0.748704095477781,-0.744124291351968,-0.718297774601662,-0.703376021766843,
-0.698693728396099,-0.695486861899579,-0.694179963381556,-0.693246576081843,
-0.692363236406221,-0.690821456365581,-0.686300479467658,-0.678568926940036,
-0.66286883858718,-0.640953473960272,-0.637820624313029,-0.635796575481633,
-0.634165461383895,-0.632298477247327,-0.62905608813685,-0.613295493218393,
-0.589814136756139,-0.579623905635116,-0.577810701175702,-0.576663669346368,
-0.575749347912375,-0.574646052487432,-0.57254285101204,-0.556227058731184,
-0.52959774760129,-0.522113265644139,-0.519447865308257,-0.517878872190738,
-0.51622952295596,-0.514059603539153,-0.509304541808945,-0.502870030165085,
-0.484899961486914,-0.463920400614609,-0.460964544886845,-0.459788542767622,
-0.458930651950198,-0.457970143676417,-0.456535809789371,-0.452484206171058,
-0.446046225190043,-0.416260561592314,-0.405752168979231,-0.40274147907261,
-0.400921450622253,-0.399277008347685,-0.397161769427786,-0.392714962238584,
-0.388501056592863),.UNSPECIFIED.);
#232=B_SPLINE_CURVE_WITH_KNOTS('',3,(#23289,#23290,#23291,#23292,#23293,
#23294,#23295,#23296,#23297,#23298,#23299,#23300,#23301,#23302,#23303,#23304,
#23305,#23306,#23307,#23308,#23309,#23310,#23311,#23312,#23313,#23314,#23315,
#23316,#23317,#23318,#23319,#23320,#23321,#23322,#23323,#23324,#23325,#23326,
#23327,#23328,#23329,#23330,#23331,#23332,#23333,#23334,#23335,#23336,#23337,
#23338,#23339,#23340,#23341,#23342,#23343),.UNSPECIFIED.,.F.,.F.,(4,3,3,
3,3,3,3,3,3,3,3,3,3,3,3,3,3,3,4),(13.6623826713879,13.7821802303794,13.9018303726072,
14.021385637802,14.1408984130057,14.2605090576095,14.3801661535387,14.5000537598878,
14.5941633947024,14.7182560466692,14.838042915424,14.957714639234,15.0773235113992,
15.1969217157567,15.3166434180951,15.4364397332535,15.5564514304154,15.5869046104364,
15.7079632679489),.UNSPECIFIED.);
#233=B_SPLINE_CURVE_WITH_KNOTS('',3,(#23344,#23345,#23346,#23347,#23348,
#23349,#23350,#23351,#23352,#23353,#23354,#23355,#23356,#23357,#23358,#23359,
#23360,#23361,#23362,#23363,#23364,#23365,#23366,#23367,#23368,#23369,#23370,
#23371,#23372,#23373,#23374,#23375,#23376,#23377,#23378,#23379,#23380,#23381,
#23382,#23383,#23384,#23385,#23386,#23387,#23388,#23389,#23390,#23391,#23392,
#23393,#23394,#23395,#23396,#23397,#23398,#23399,#23400,#23401,#23402,#23403,
#23404,#23405,#23406,#23407,#23408,#23409,#23410,#23411,#23412,#23413,#23414,
#23415,#23416,#23417,#23418,#23419,#23420,#23421,#23422,#23423,#23424,#23425,
#23426,#23427,#23428,#23429,#23430,#23431,#23432,#23433,#23434,#23435,#23436,
#23437,#23438,#23439,#23440,#23441,#23442,#23443,#23444,#23445,#23446,#23447,
#23448,#23449,#23450,#23451,#23452,#23453,#23454,#23455,#23456,#23457,#23458,
#23459,#23460,#23461,#23462,#23463,#23464,#23465,#23466,#23467,#23468,#23469,
#23470,#23471,#23472,#23473,#23474,#23475,#23476,#23477,#23478,#23479,#23480,
#23481,#23482,#23483),.UNSPECIFIED.,.F.,.F.,(4,2,2,2,2,2,2,2,2,2,2,2,2,
2,2,2,2,2,2,2,2,2,2,2,2,2,2,2,2,2,2,2,2,2,2,2,2,2,2,2,2,2,2,2,2,2,2,2,2,
2,2,2,2,2,2,2,2,2,2,2,2,2,2,2,2,2,2,2,2,4),(-1.48450431841139,-1.4617611277698,
-1.44593454243558,-1.44270146431909,-1.44084323355285,-1.43922191691824,
-1.43721299573973,-1.4341097721629,-1.41163255113375,-1.39460054757425,
-1.38792774329617,-1.38511883993771,-1.38357795582617,-1.38228274348412,
-1.38135413076546,-1.38049548623494,-1.37931282111924,-1.37630565299905,
-1.35709232231919,-1.33852275952823,-1.32787689803448,-1.32496269215979,
-1.3231639751169,-1.32151450789825,-1.31939411267224,-1.31496062846687,
-1.28792632392131,-1.28256676732013,-1.26913107652234,-1.26624202927492,
-1.26498603957276,-1.26405865092523,-1.26302279612381,-1.26123676704593,
-1.25448185427391,-1.22352839734419,-1.2152993451098,-1.20957414247627,
-1.20724074097352,-1.20556474688588,-1.20403794966868,-1.20198652284865,
-1.1979800448179,-1.17021122788282,-1.15122108808407,-1.14876189022007,
-1.14758739428054,-1.14667172596313,-1.14559123102855,-1.1436486425439,
-1.13424769144913,-1.10318744586674,-1.09667715799843,-1.09188003707794,
-1.08970459528864,-1.08805657154721,-1.08649295753002,-1.08384691224912,
-1.07648685911044,-1.04634008698229,-1.03744853444824,-1.03238243373507,
-1.03082950190625,-1.02984645520666,-1.02891019607728,-1.02775551794013,
-1.02491673169677,-1.00161398686935,-0.98519209668673,-0.984038713564579),
 .UNSPECIFIED.);
#234=B_SPLINE_CURVE_WITH_KNOTS('',3,(#23489,#23490,#23491,#23492,#23493,
#23494,#23495,#23496,#23497,#23498,#23499,#23500,#23501,#23502,#23503,#23504,
#23505,#23506,#23507,#23508,#23509,#23510,#23511,#23512,#23513,#23514,#23515,
#23516,#23517,#23518,#23519,#23520,#23521,#23522,#23523,#23524,#23525,#23526,
#23527,#23528,#23529,#23530,#23531,#23532,#23533,#23534,#23535,#23536,#23537,
#23538,#23539,#23540,#23541,#23542,#23543,#23544,#23545,#23546,#23547,#23548,
#23549,#23550,#23551,#23552,#23553,#23554,#23555,#23556,#23557,#23558,#23559,
#23560,#23561,#23562,#23563,#23564,#23565,#23566,#23567,#23568,#23569,#23570,
#23571,#23572,#23573,#23574,#23575,#23576,#23577,#23578,#23579,#23580,#23581,
#23582,#23583,#23584,#23585,#23586,#23587,#23588,#23589,#23590,#23591,#23592,
#23593,#23594,#23595,#23596,#23597,#23598,#23599,#23600,#23601,#23602,#23603,
#23604,#23605,#23606,#23607,#23608,#23609,#23610,#23611,#23612,#23613,#23614,
#23615,#23616,#23617,#23618,#23619,#23620,#23621,#23622,#23623,#23624,#23625,
#23626,#23627,#23628,#23629,#23630,#23631,#23632,#23633,#23634,#23635,#23636,
#23637,#23638),.UNSPECIFIED.,.F.,.F.,(4,2,2,2,2,2,2,2,2,2,2,2,2,2,2,2,2,
2,2,2,2,2,2,2,2,2,2,2,2,2,2,2,2,2,2,2,2,2,2,2,2,2,2,2,2,2,2,2,2,2,2,2,2,
2,2,2,2,2,2,2,2,2,2,2,2,2,2,2,2,2,2,2,2,2,4),(-0.500694290278421,-0.497544488839605,
-0.495661357712548,-0.494492855323991,-0.493577002111409,-0.492490318556005,
-0.490466592203038,-0.477635817997283,-0.450094696254809,-0.440460302827894,
-0.43754182682963,-0.435744348790431,-0.43409863601131,-0.431950875806821,
-0.427314837357559,-0.421089139902201,-0.404126478228909,-0.381615394886978,
-0.378732636295032,-0.377570103137111,-0.376631545134818,-0.375650242287218,
-0.374108812827463,-0.369157227320466,-0.360566245051619,-0.334195806293179,
-0.323454453464546,-0.320412665249448,-0.318588298903664,-0.316949154199797,
-0.314853604473625,-0.310496759497856,-0.29347823375238,-0.274938529477881,
-0.263042839324536,-0.261166737053334,-0.260000367426982,-0.259084697255278,
-0.257996465962969,-0.255965256627442,-0.242880573285268,-0.212774006368426,
-0.205413445051682,-0.202765646017531,-0.20120052361162,-0.199550537622462,
-0.197371856384937,-0.192564705549658,-0.186037725262247,-0.154809411223525,
-0.145559982481404,-0.143624090127548,-0.142544422462605,-0.141627900072442,
-0.140473796262541,-0.138125815294119,-0.134961992463785,-0.127016727340287,
-0.100132859293806,-0.0889853560230274,-0.0859190418261268,-0.0840893010749391,
-0.0824511641418156,-0.0803649250865898,-0.0763578945436618,-0.0593578073915818,
-0.0449503960643063,-0.0286364519733591,-0.0267012887693669,-0.0255173386469702,
-0.0246003609189633,-0.023525195211802,-0.0223774179293482,-0.0205702953880954,
-0.000340360879008273),.UNSPECIFIED.);
#235=B_SPLINE_CURVE_WITH_KNOTS('',3,(#23639,#23640,#23641,#23642,#23643,
#23644,#23645,#23646,#23647,#23648,#23649,#23650,#23651,#23652,#23653,#23654,
#23655,#23656,#23657,#23658,#23659,#23660,#23661,#23662,#23663,#23664,#23665,
#23666,#23667,#23668,#23669,#23670,#23671,#23672,#23673,#23674,#23675,#23676,
#23677,#23678,#23679,#23680,#23681,#23682,#23683,#23684,#23685,#23686,#23687,
#23688,#23689,#23690,#23691,#23692,#23693,#23694,#23695,#23696,#23697,#23698,
#23699,#23700,#23701,#23702,#23703,#23704,#23705,#23706,#23707,#23708),
 .UNSPECIFIED.,.F.,.F.,(4,2,2,2,2,2,2,2,2,2,2,2,2,2,2,2,2,2,2,2,2,2,2,2,
2,2,2,2,2,2,2,2,2,2,4),(-1.37216423938497,-1.34558201548237,-1.34260950380171,
-1.34065849775233,-1.3387901421669,-1.33715832893005,-1.33513403494363,
-1.33200190257198,-1.31147073795144,-1.29387212379872,-1.28648518521141,
-1.28206143489466,-1.28060736088923,-1.27962515542679,-1.27868786372659,
-1.27752915199367,-1.27466699015011,-1.25191396248099,-1.23513446381467,
-1.22894897018639,-1.22437630025068,-1.22221853088604,-1.22057192564277,
-1.21878012495597,-1.21588577042803,-1.2064697950075,-1.1732599746904,-1.16539919001667,
-1.16360574159079,-1.16256895454495,-1.16164494831632,-1.16041970962888,
-1.15761540022164,-1.13307933462838,-1.13048491284919),.UNSPECIFIED.);
#236=B_SPLINE_CURVE_WITH_KNOTS('',3,(#23709,#23710,#23711,#23712,#23713,
#23714,#23715,#23716,#23717,#23718,#23719,#23720,#23721,#23722,#23723,#23724,
#23725,#23726,#23727,#23728,#23729,#23730,#23731,#23732,#23733,#23734,#23735,
#23736,#23737,#23738,#23739,#23740,#23741,#23742,#23743,#23744,#23745,#23746,
#23747,#23748,#23749,#23750,#23751,#23752,#23753,#23754,#23755,#23756,#23757,
#23758,#23759,#23760,#23761,#23762,#23763,#23764,#23765,#23766,#23767,#23768,
#23769,#23770,#23771,#23772,#23773,#23774,#23775,#23776,#23777,#23778,#23779,
#23780,#23781,#23782,#23783,#23784,#23785,#23786,#23787,#23788,#23789,#23790,
#23791,#23792,#23793,#23794,#23795,#23796,#23797,#23798,#23799,#23800,#23801,
#23802,#23803,#23804,#23805,#23806,#23807,#23808,#23809,#23810,#23811,#23812,
#23813,#23814,#23815,#23816,#23817,#23818,#23819,#23820,#23821,#23822,#23823,
#23824,#23825,#23826,#23827,#23828,#23829,#23830,#23831,#23832,#23833,#23834,
#23835,#23836,#23837,#23838,#23839,#23840,#23841,#23842,#23843,#23844,#23845,
#23846,#23847,#23848,#23849,#23850,#23851,#23852,#23853,#23854,#23855,#23856,
#23857,#23858,#23859,#23860,#23861,#23862,#23863,#23864,#23865,#23866,#23867,
#23868,#23869,#23870,#23871,#23872,#23873,#23874,#23875,#23876,#23877,#23878,
#23879,#23880,#23881,#23882,#23883,#23884,#23885,#23886,#23887,#23888,#23889,
#23890,#23891,#23892,#23893,#23894,#23895,#23896,#23897,#23898,#23899,#23900,
#23901,#23902,#23903,#23904,#23905,#23906,#23907,#23908,#23909,#23910,#23911,
#23912,#23913,#23914,#23915,#23916,#23917,#23918,#23919,#23920,#23921,#23922,
#23923,#23924,#23925,#23926,#23927,#23928,#23929,#23930),.UNSPECIFIED.,
 .F.,.F.,(4,2,2,2,2,2,2,2,2,2,2,2,2,2,2,2,2,2,2,2,2,2,2,2,2,2,2,2,2,2,2,
2,2,2,2,2,2,2,2,2,2,2,2,2,2,2,2,2,2,2,2,2,2,2,2,2,2,2,2,2,2,2,2,2,2,2,2,
2,2,2,2,2,2,2,2,2,2,2,2,2,2,2,2,2,2,2,2,2,2,2,2,2,2,2,2,2,2,2,2,2,2,2,2,
2,2,2,2,2,2,2,4),(-0.984038713564579,-0.979083382711775,-0.974514099266456,
-0.972378596647122,-0.970734461382103,-0.968930924076269,-0.965984892455485,
-0.956098893355456,-0.925490060350384,-0.918990582003603,-0.914913565602765,
-0.913478647123477,-0.912520177593105,-0.91166455259397,-0.910494325266551,
-0.90756634072051,-0.885984481222971,-0.868427902102175,-0.862078145649561,
-0.85737107091966,-0.855210580551665,-0.853563346040641,-0.851772278206197,
-0.848882273227625,-0.83950605601909,-0.814580008746206,-0.798913810932696,
-0.796821968301805,-0.795721125298328,-0.794806497580885,-0.79365615630539,
-0.791832943797292,-0.781406775136773,-0.772907111549027,-0.758429812593337,
-0.742480952275819,-0.739266899751719,-0.73738678374001,-0.735755776528335,
-0.733746710750133,-0.729829470622148,-0.724816977305916,-0.712860409646348,
-0.686724098553468,-0.68097019727523,-0.67928147801539,-0.678267767573056,
-0.677335980504339,-0.676038873637747,-0.672891576102773,-0.668325410868035,
-0.654043869396371,-0.627323133288759,-0.622797020398668,-0.620692447181739,
-0.619047800270467,-0.617246812812998,-0.614312051983835,-0.603382569448011,
-0.583879586004667,-0.565949166224158,-0.562936220062179,-0.561751739518097,
-0.560892520958884,-0.559938663596384,-0.558524818253106,-0.554600845578626,
-0.548439397457055,-0.531060002397481,-0.508378260428437,-0.505254989872259,
-0.503233037796786,-0.501600929657233,-0.499729844535093,-0.496472590770214,
-0.480430109939549,-0.466004582749208,-0.457518477831262,-0.44709677731593,
-0.445273444648482,-0.444122985930252,-0.443208241569681,-0.44210722014929,
-0.440014868547358,-0.424318411758726,-0.399308757887973,-0.390051168297601,
-0.387173762806587,-0.385385385252243,-0.383737198902599,-0.381570448161397,
-0.376829213981716,-0.370418754607422,-0.352568521687281,-0.331382310924339,
-0.328434538393741,-0.327262119328129,-0.326405992467733,-0.325448625648796,
-0.324017745883825,-0.319968283024939,-0.31353063342149,-0.29646643982214,
-0.273914165564096,-0.270788890007936,-0.268766344126854,-0.267134213645697,
-0.265263603785942,-0.262008475192572,-0.246010855207923,-0.242048471304312),
 .UNSPECIFIED.);
#237=B_SPLINE_CURVE_WITH_KNOTS('',3,(#23935,#23936,#23937,#23938,#23939,
#23940,#23941,#23942,#23943,#23944,#23945,#23946,#23947,#23948,#23949,#23950,
#23951,#23952,#23953,#23954,#23955,#23956,#23957,#23958,#23959,#23960,#23961,
#23962,#23963,#23964,#23965,#23966,#23967,#23968,#23969,#23970,#23971,#23972,
#23973,#23974,#23975,#23976,#23977,#23978,#23979,#23980,#23981,#23982,#23983,
#23984,#23985,#23986,#23987,#23988,#23989,#23990,#23991,#23992,#23993,#23994,
#23995,#23996,#23997,#23998,#23999,#24000,#24001,#24002,#24003,#24004,#24005,
#24006,#24007,#24008,#24009,#24010,#24011,#24012,#24013,#24014,#24015,#24016,
#24017,#24018,#24019,#24020,#24021,#24022,#24023,#24024,#24025,#24026,#24027,
#24028,#24029,#24030,#24031,#24032,#24033,#24034,#24035,#24036,#24037,#24038,
#24039,#24040,#24041,#24042,#24043,#24044,#24045,#24046,#24047,#24048,#24049,
#24050,#24051,#24052,#24053,#24054,#24055,#24056,#24057,#24058,#24059,#24060,
#24061,#24062,#24063,#24064,#24065,#24066,#24067,#24068,#24069,#24070,#24071,
#24072,#24073,#24074,#24075,#24076,#24077,#24078,#24079,#24080,#24081,#24082,
#24083,#24084,#24085,#24086,#24087,#24088,#24089,#24090,#24091,#24092,#24093,
#24094,#24095,#24096,#24097,#24098,#24099,#24100,#24101,#24102,#24103,#24104,
#24105,#24106,#24107,#24108,#24109,#24110,#24111,#24112,#24113,#24114,#24115,
#24116,#24117,#24118,#24119,#24120,#24121,#24122,#24123,#24124,#24125,#24126,
#24127,#24128,#24129,#24130,#24131,#24132,#24133,#24134,#24135,#24136,#24137,
#24138,#24139,#24140,#24141,#24142,#24143,#24144,#24145,#24146,#24147,#24148,
#24149,#24150,#24151,#24152),.UNSPECIFIED.,.F.,.F.,(4,2,2,2,2,2,2,2,2,2,
2,2,2,2,2,2,2,2,2,2,2,2,2,2,2,2,2,2,2,2,2,2,2,2,2,2,2,2,2,2,2,2,2,2,2,2,
2,2,2,2,2,2,2,2,2,2,2,2,2,2,2,2,2,2,2,2,2,2,2,2,2,2,2,2,2,2,2,2,2,2,2,2,
2,2,2,2,2,2,2,2,2,2,2,2,2,2,2,2,2,2,2,2,2,2,2,2,2,2,4),(-1.24281229412899,
-1.23823517134402,-1.21326017462496,-1.20489355448001,-1.20161975505772,
-1.19917814953849,-1.19800670320905,-1.19709060012867,-1.19600605128283,
-1.19404865521973,-1.18439141630898,-1.1604026271728,-1.14459122506566,
-1.1413445968791,-1.13947562613542,-1.13784301643643,-1.13581739756981,
-1.13268256535286,-1.11075412422281,-1.09502376403645,-1.08731420511488,
-1.08421321765552,-1.08187219128653,-1.08072043993349,-1.07989379286338,
-1.07883095317678,-1.07696947794716,-1.06894493296442,-1.06570174440512,
-1.05580034931728,-1.03732650538379,-1.02671796824432,-1.02381022009547,
-1.02201497047597,-1.02036840220475,-1.01825143614163,-1.01365851637043,
-0.988116047308891,-0.980509398572667,-0.967698761402144,-0.964877747211214,
-0.963636087701755,-0.962712599632508,-0.961672609248068,-0.959865471854731,
-0.952856005846949,-0.922129837401915,-0.91391540297594,-0.908197236100503,
-0.905864975208061,-0.904189237779933,-0.902662294837823,-0.90061010470269,
-0.896600383778468,-0.868905630287747,-0.8631419111951,-0.853652468501447,
-0.848360579796169,-0.846782285555594,-0.845792842470934,-0.844859427491579,
-0.84350187851855,-0.8409452467313,-0.816629540370137,-0.793814173284251,
-0.789989022974813,-0.787998307344609,-0.786367896299053,-0.784472366170217,
-0.781191641684948,-0.766110879440994,-0.742234622183565,-0.731906789792124,
-0.730087015630132,-0.728937518353579,-0.728022648202676,-0.726920394841888,
-0.724822741433705,-0.708844487496945,-0.683102623152255,-0.67467362275887,
-0.671889283589293,-0.670120906513703,-0.668465042154335,-0.666248908353811,
-0.661230650335449,-0.654325642225997,-0.633871752346058,-0.626179165452878,
-0.621584363691984,-0.614328384973159,-0.612522137548843,-0.611471950014313,
-0.610643292927963,-0.609473280095078,-0.607038889750075,-0.603777845190063,
-0.595460792427168,-0.570731071267607,-0.558184323631155,-0.555014160625655,
-0.553161801401082,-0.55169075703668,-0.549718453910335,-0.545983019762226,
-0.541265092616273,-0.530362481310411,-0.509637148706452,-0.500694290278421),
 .UNSPECIFIED.);
#238=B_SPLINE_CURVE_WITH_KNOTS('',3,(#24154,#24155,#24156,#24157,#24158,
#24159,#24160,#24161,#24162,#24163,#24164,#24165,#24166,#24167,#24168,#24169,
#24170,#24171,#24172,#24173,#24174,#24175,#24176,#24177,#24178,#24179,#24180,
#24181,#24182,#24183,#24184,#24185,#24186,#24187,#24188,#24189,#24190,#24191,
#24192,#24193,#24194,#24195,#24196,#24197,#24198,#24199,#24200,#24201,#24202,
#24203,#24204,#24205,#24206,#24207,#24208,#24209,#24210,#24211,#24212,#24213,
#24214,#24215,#24216,#24217,#24218,#24219,#24220,#24221,#24222,#24223,#24224,
#24225),.UNSPECIFIED.,.F.,.F.,(4,2,2,2,2,2,2,2,2,2,2,2,2,2,2,2,2,2,2,2,
2,2,2,2,2,2,2,2,2,2,2,2,2,2,2,4),(-0.242048471304312,-0.231554403723091,
-0.223053577267517,-0.212631651068731,-0.210808319157637,-0.209657860609199,
-0.208743118845369,-0.207642101892112,-0.205549745632317,-0.189851934316851,
-0.16484173116906,-0.155586910339118,-0.152709821721549,-0.15092152683397,
-0.149273339846562,-0.147106475332604,-0.142481241995114,-0.136206643895549,
-0.119012139413158,-0.0968518603501121,-0.0939519885653981,-0.0927866177273898,
-0.0918473914480129,-0.0908673859660855,-0.0894237017264087,-0.0851053334230332,
-0.0779574720188684,-0.0596249657259443,-0.0394613817161886,-0.0363332063582247,
-0.0343098187854399,-0.0326776805504764,-0.030807797978331,-0.0288547148409675,
-0.0258775913530729,-0.000340687906700261),.UNSPECIFIED.);
#239=B_SPLINE_CURVE_WITH_KNOTS('',3,(#24226,#24227,#24228,#24229,#24230,
#24231,#24232,#24233,#24234,#24235,#24236,#24237,#24238,#24239,#24240,#24241,
#24242,#24243,#24244,#24245,#24246,#24247,#24248,#24249,#24250,#24251,#24252,
#24253,#24254,#24255,#24256,#24257,#24258,#24259,#24260,#24261,#24262,#24263,
#24264,#24265,#24266,#24267,#24268,#24269,#24270,#24271,#24272,#24273,#24274,
#24275,#24276,#24277,#24278,#24279,#24280,#24281,#24282,#24283,#24284,#24285,
#24286,#24287,#24288,#24289,#24290,#24291,#24292,#24293,#24294,#24295,#24296,
#24297,#24298,#24299,#24300,#24301,#24302,#24303,#24304,#24305,#24306,#24307,
#24308,#24309,#24310,#24311,#24312,#24313,#24314,#24315,#24316,#24317,#24318,
#24319,#24320,#24321,#24322,#24323,#24324,#24325,#24326,#24327,#24328,#24329,
#24330,#24331,#24332,#24333,#24334,#24335,#24336,#24337,#24338,#24339,#24340,
#24341,#24342,#24343,#24344,#24345,#24346,#24347,#24348,#24349,#24350,#24351,
#24352,#24353,#24354,#24355,#24356,#24357,#24358,#24359,#24360,#24361,#24362,
#24363,#24364,#24365,#24366,#24367,#24368,#24369,#24370,#24371,#24372,#24373,
#24374,#24375,#24376,#24377,#24378,#24379,#24380,#24381,#24382,#24383),
 .UNSPECIFIED.,.F.,.F.,(4,2,2,2,2,2,2,2,2,2,2,2,2,2,2,2,2,2,2,2,2,2,2,2,
2,2,2,2,2,2,2,2,2,2,2,2,2,2,2,2,2,2,2,2,2,2,2,2,2,2,2,2,2,2,2,2,2,2,2,2,
2,2,2,2,2,2,2,2,2,2,2,2,2,2,2,2,2,2,4),(-1.48430386926941,-1.46653245415301,
-1.46301191802203,-1.46120515283548,-1.46005760821234,-1.45898269395285,
-1.45806588602968,-1.45688211279949,-1.45494716502168,-1.43810227494753,
-1.42412050259781,-1.40892041175522,-1.40379176762196,-1.40150491354494,
-1.3998375533479,-1.39830145062393,-1.39580812106899,-1.389499567781,-1.36287288999797,
-1.35051814156449,-1.34632668246337,-1.34340389296128,-1.34219418040405,
-1.34125847686484,-1.34037823588219,-1.33885441978669,-1.33640354760787,
-1.31523334121925,-1.29739251665676,-1.2909842242855,-1.28624381416137,
-1.28407724377567,-1.28242910837973,-1.28064070118657,-1.27776306416874,
-1.26850336685781,-1.24347938907165,-1.2277755788542,-1.22568290448192,
-1.22458181519565,-1.2236670691561,-1.22251668071253,-1.22069361090505,
-1.21027565538499,-1.20179862028053,-1.18738686595642,-1.17134688157405,
-1.16808991815495,-1.16621890295608,-1.16458679605956,-1.16256476834823,
-1.15944120328641,-1.13674977937359,-1.11936166223676,-1.11319450290552,
-1.10926827941543,-1.10785412865197,-1.10690022479071,-1.1060411299623,
-1.10485699149948,-1.10184581706413,-1.08306963647165,-1.06420424858992,
-1.05709344646599,-1.05196173420385,-1.0497261710511,-1.0480673441908,-1.04630655482708,
-1.043556703316,-1.03541377996334,-1.00616470818863,-0.997347043696302,
-0.992308073499113,-0.990756958282208,-0.989773540814691,-0.988836442150449,
-0.987679389918078,-0.984828314075721,-0.984009904944126),.UNSPECIFIED.);
#240=B_SPLINE_CURVE_WITH_KNOTS('',3,(#24389,#24390,#24391,#24392,#24393,
#24394,#24395,#24396,#24397,#24398,#24399,#24400,#24401,#24402,#24403,#24404,
#24405,#24406,#24407,#24408,#24409,#24410,#24411,#24412,#24413,#24414,#24415,
#24416,#24417,#24418,#24419,#24420,#24421,#24422,#24423,#24424,#24425,#24426,
#24427,#24428,#24429,#24430,#24431,#24432,#24433,#24434,#24435,#24436,#24437,
#24438,#24439,#24440,#24441,#24442,#24443,#24444,#24445,#24446,#24447,#24448,
#24449,#24450,#24451,#24452,#24453,#24454,#24455,#24456,#24457,#24458,#24459,
#24460,#24461,#24462,#24463,#24464,#24465,#24466,#24467,#24468,#24469,#24470,
#24471,#24472,#24473,#24474,#24475,#24476,#24477,#24478,#24479,#24480,#24481,
#24482,#24483,#24484,#24485,#24486,#24487,#24488,#24489,#24490,#24491,#24492,
#24493,#24494,#24495,#24496,#24497,#24498,#24499,#24500,#24501,#24502,#24503,
#24504,#24505,#24506,#24507,#24508,#24509,#24510,#24511,#24512,#24513,#24514,
#24515,#24516,#24517,#24518,#24519,#24520,#24521,#24522,#24523,#24524,#24525,
#24526,#24527,#24528,#24529,#24530,#24531,#24532,#24533,#24534,#24535,#24536,
#24537,#24538,#24539,#24540,#24541,#24542,#24543,#24544),.UNSPECIFIED.,
 .F.,.F.,(4,2,2,2,2,2,2,2,2,2,2,2,2,2,2,2,2,2,2,2,2,2,2,2,2,2,2,2,2,2,2,
2,2,2,2,2,2,2,2,2,2,2,2,2,2,2,2,2,2,2,2,2,2,2,2,2,2,2,2,2,2,2,2,2,2,2,2,
2,2,2,2,2,2,2,2,2,2,4),(-0.500918874538835,-0.493729283290626,-0.481227039374831,
-0.478096659133442,-0.476235156695093,-0.474617166932814,-0.472588241309173,
-0.468574202577156,-0.463403476454992,-0.450860905284672,-0.431807810733804,
-0.427786646560088,-0.420183640185763,-0.418351148640682,-0.41729488808885,
-0.416467182695655,-0.415305960627832,-0.41291704794769,-0.409734480839948,
-0.401718598209421,-0.378190358497151,-0.364163038685052,-0.360935707274224,
-0.359052161850098,-0.357420774093964,-0.355414543566555,-0.35151354127568,
-0.328585937674148,-0.304510491538616,-0.301652902497553,-0.300528471513784,
-0.299599538386361,-0.29860167729446,-0.296985630064722,-0.291321263688311,
-0.280790039047186,-0.256675361679246,-0.24637393203707,-0.243385967550815,
-0.241573128394394,-0.23993106781524,-0.237813195361913,-0.233339498974164,
-0.227395350281804,-0.211711913427668,-0.187188907166548,-0.184372544429671,
-0.183144933029173,-0.182220313064407,-0.181184136788051,-0.179394684184911,
-0.171600372616162,-0.139234087204213,-0.129060581538441,-0.126084741605259,
-0.124274614667218,-0.122664708414234,-0.120738536918804,-0.118540543195545,
-0.114967194231283,-0.107719961407809,-0.0881813356869555,-0.0702913549404585,
-0.0672782632698932,-0.0660936630632054,-0.0652343393737278,-0.0642802943988998,
-0.062866129214121,-0.0589410146506339,-0.0527774767385878,-0.0183603635020737,
-0.0110828695650004,-0.00844907915857034,-0.00688652083307198,-0.00531417154097046,
-0.00371122492596661,-0.00203843401347154,-0.000340248170157266),
 .UNSPECIFIED.);
#241=B_SPLINE_CURVE_WITH_KNOTS('',3,(#24545,#24546,#24547,#24548,#24549,
#24550,#24551,#24552,#24553,#24554,#24555,#24556,#24557,#24558,#24559,#24560,
#24561,#24562,#24563,#24564,#24565,#24566,#24567,#24568,#24569,#24570,#24571,
#24572,#24573,#24574,#24575,#24576,#24577,#24578,#24579,#24580,#24581,#24582,
#24583,#24584,#24585,#24586,#24587,#24588,#24589,#24590,#24591,#24592,#24593,
#24594,#24595,#24596,#24597,#24598,#24599,#24600,#24601,#24602,#24603,#24604,
#24605,#24606,#24607,#24608,#24609,#24610,#24611,#24612,#24613,#24614,#24615,
#24616,#24617,#24618,#24619,#24620,#24621,#24622,#24623,#24624),
 .UNSPECIFIED.,.F.,.F.,(4,2,2,2,2,2,2,2,2,2,2,2,2,2,2,2,2,2,2,2,2,2,2,2,
2,2,2,2,2,2,2,2,2,2,2,2,2,2,2,4),(-1.484428834093,-1.48054199923031,-1.44819876680698,
-1.43954244786739,-1.43456582256332,-1.433021565382,-1.4320396319046,-1.43110147473606,
-1.42994050820837,-1.42706690860662,-1.40446331814616,-1.3827964218617,
-1.37896070958198,-1.37665631910656,-1.37465654399446,-1.37462546049038,
-1.37459299209241,-1.37455895845735,-1.37298760352077,-1.37120341845313,
-1.36834614543548,-1.35928455012788,-1.33113078566982,-1.32234322774752,
-1.31896227105564,-1.31645911480328,-1.31527586076659,-1.31435886885517,
-1.31328303482637,-1.31136429422616,-1.3024234939432,-1.27852599892734,
-1.26749043433603,-1.26273424659767,-1.25897468290425,-1.2569973714755,
-1.25552581078917,-1.25367702645904,-1.25052352740852,-1.24281229412899),
 .UNSPECIFIED.);
#242=B_SPLINE_CURVE_WITH_KNOTS('',3,(#24625,#24626,#24627,#24628,#24629,
#24630,#24631,#24632,#24633,#24634,#24635,#24636,#24637,#24638,#24639,#24640,
#24641,#24642,#24643,#24644,#24645,#24646,#24647,#24648,#24649,#24650,#24651,
#24652,#24653,#24654,#24655,#24656,#24657,#24658,#24659,#24660,#24661,#24662,
#24663,#24664,#24665,#24666,#24667,#24668,#24669,#24670,#24671,#24672,#24673,
#24674,#24675,#24676,#24677,#24678,#24679,#24680,#24681,#24682,#24683,#24684,
#24685,#24686,#24687,#24688,#24689,#24690,#24691,#24692,#24693,#24694,#24695,
#24696,#24697,#24698,#24699,#24700,#24701,#24702,#24703,#24704,#24705,#24706,
#24707,#24708,#24709,#24710,#24711,#24712,#24713,#24714,#24715,#24716,#24717,
#24718,#24719,#24720,#24721,#24722,#24723,#24724,#24725,#24726,#24727,#24728,
#24729,#24730,#24731,#24732,#24733,#24734,#24735,#24736,#24737,#24738,#24739,
#24740,#24741,#24742,#24743,#24744,#24745,#24746,#24747,#24748,#24749,#24750,
#24751,#24752,#24753,#24754,#24755,#24756,#24757,#24758,#24759,#24760,#24761,
#24762,#24763,#24764,#24765,#24766,#24767,#24768,#24769,#24770,#24771,#24772,
#24773,#24774,#24775,#24776,#24777,#24778,#24779,#24780,#24781,#24782,#24783,
#24784,#24785,#24786,#24787,#24788,#24789,#24790,#24791,#24792,#24793,#24794,
#24795,#24796,#24797,#24798,#24799,#24800,#24801,#24802,#24803,#24804,#24805,
#24806,#24807,#24808,#24809,#24810,#24811,#24812,#24813,#24814,#24815,#24816,
#24817,#24818,#24819,#24820,#24821,#24822,#24823,#24824,#24825,#24826,#24827,
#24828,#24829,#24830,#24831,#24832,#24833,#24834),.UNSPECIFIED.,.F.,.F.,
(4,2,2,2,2,2,2,2,2,2,2,2,2,2,2,2,2,2,2,2,2,2,2,2,2,2,2,2,2,2,2,2,2,2,2,
2,2,2,2,2,2,2,2,2,2,2,2,2,2,2,2,2,2,2,2,2,2,2,2,2,2,2,2,2,2,2,2,2,2,2,2,
2,2,2,2,2,2,2,2,2,2,2,2,2,2,2,2,2,2,2,2,2,2,2,2,2,2,2,2,2,2,2,2,2,4),(-0.984009904944126,
-0.961823534427199,-0.945195306252899,-0.939041443571138,-0.934446193655206,
-0.932305920577051,-0.930661196563781,-0.928860089942887,-0.925925060339749,
-0.916138104967741,-0.91207595714914,-0.887983807976547,-0.87979473307276,
-0.876566997483682,-0.874152070093205,-0.872985846154686,-0.872157654540614,
-0.871104997304057,-0.869287951302992,-0.861891600062579,-0.828857887531441,
-0.822194217371007,-0.817309812771511,-0.815117350561738,-0.813465295773428,
-0.811687780770774,-0.80886067874769,-0.80006226638829,-0.774632035453004,
-0.759364241953133,-0.756898528797663,-0.755722523075203,-0.754806198822679,
-0.753725331435031,-0.751783946388736,-0.742429814717131,-0.728395940025744,
-0.7045998991639,-0.69994722095481,-0.697819598376388,-0.696171664681408,
-0.694381864280427,-0.691498409294805,-0.681164420729508,-0.66101064452863,
-0.643045424406669,-0.640020575434316,-0.638834112941866,-0.637974400631664,
-0.637021087375945,-0.635609991488778,-0.631706152056529,-0.625588603678782,
-0.608092311262583,-0.585454202895747,-0.582330758723305,-0.580308698757551,
-0.578676506552808,-0.576805328229851,-0.573547919673089,-0.557504716755464,
-0.543078998107933,-0.534593194621034,-0.524170828774063,-0.522347387900391,
-0.52119685886378,-0.520282056713186,-0.519180961569566,-0.517088456235864,
-0.50138952306028,-0.476374215858401,-0.467121382497707,-0.464244364526069,
-0.462456000152752,-0.460807673144654,-0.45864051313973,-0.453897457069288,
-0.447483899476263,-0.429619180084874,-0.408452204479977,-0.40549510076717,
-0.404325496014753,-0.403470035376363,-0.40251172713355,-0.401076501375177,
-0.396994837311345,-0.39048558233509,-0.359714952843162,-0.349966969742027,
-0.347036448951131,-0.345236468629042,-0.343591695099338,-0.34144981021662,
-0.336844991260212,-0.330673547526229,-0.313962880636645,-0.291059627270006,
-0.288203554379225,-0.287045692396799,-0.286108440409246,-0.285125466761232,
-0.283576124848773,-0.278552309547939,-0.269774735303037,-0.241902829928485),
 .UNSPECIFIED.);
#243=B_SPLINE_CURVE_WITH_KNOTS('',3,(#24839,#24840,#24841,#24842,#24843,
#24844,#24845,#24846,#24847,#24848,#24849,#24850,#24851,#24852,#24853,#24854,
#24855,#24856,#24857,#24858,#24859,#24860,#24861,#24862,#24863,#24864,#24865,
#24866,#24867,#24868,#24869,#24870,#24871,#24872,#24873,#24874,#24875,#24876,
#24877,#24878,#24879,#24880,#24881,#24882,#24883,#24884,#24885,#24886,#24887,
#24888,#24889,#24890,#24891,#24892,#24893,#24894,#24895,#24896,#24897,#24898,
#24899,#24900,#24901,#24902,#24903,#24904,#24905,#24906,#24907,#24908,#24909,
#24910,#24911,#24912,#24913,#24914,#24915,#24916,#24917,#24918,#24919,#24920,
#24921,#24922,#24923,#24924,#24925,#24926,#24927,#24928,#24929,#24930,#24931,
#24932,#24933,#24934,#24935,#24936,#24937,#24938,#24939,#24940,#24941,#24942,
#24943,#24944,#24945,#24946,#24947,#24948,#24949,#24950,#24951,#24952,#24953,
#24954,#24955,#24956,#24957,#24958,#24959,#24960,#24961,#24962,#24963,#24964,
#24965,#24966,#24967,#24968,#24969,#24970,#24971,#24972,#24973,#24974,#24975,
#24976,#24977,#24978,#24979,#24980,#24981,#24982,#24983,#24984,#24985,#24986,
#24987,#24988,#24989,#24990,#24991,#24992,#24993,#24994,#24995,#24996,#24997,
#24998,#24999,#25000,#25001,#25002,#25003,#25004,#25005,#25006,#25007,#25008,
#25009,#25010,#25011,#25012,#25013,#25014,#25015,#25016,#25017,#25018,#25019,
#25020,#25021,#25022,#25023,#25024,#25025,#25026,#25027,#25028,#25029,#25030,
#25031,#25032,#25033,#25034,#25035,#25036,#25037,#25038,#25039,#25040,#25041,
#25042,#25043,#25044,#25045,#25046,#25047,#25048,#25049,#25050,#25051,#25052,
#25053,#25054,#25055,#25056,#25057,#25058),.UNSPECIFIED.,.F.,.F.,(4,2,2,
2,2,2,2,2,2,2,2,2,2,2,2,2,2,2,2,2,2,2,2,2,2,2,2,2,2,2,2,2,2,2,2,2,2,2,2,
2,2,2,2,2,2,2,2,2,2,2,2,2,2,2,2,2,2,2,2,2,2,2,2,2,2,2,2,2,2,2,2,2,2,2,2,
2,2,2,2,2,2,2,2,2,2,2,2,2,2,2,2,2,2,2,2,2,2,2,2,2,2,2,2,2,2,2,2,2,2,4),
(-1.24300538673529,-1.2401076602996,-1.23867315968935,-1.23771505767543,
-1.23685955737713,-1.23568962472891,-1.2327301582961,-1.21164802544438,
-1.19374966498115,-1.18732972550532,-1.18258269622164,-1.18041489176712,
-1.17876653800613,-1.17697859281537,-1.17410324096957,-1.16486562072408,
-1.13982471522782,-1.12411473949377,-1.12202192607441,-1.12092078744097,
-1.1200060120584,-1.11885559365772,-1.11703248430546,-1.10661411685994,
-1.09814086903657,-1.08373365899801,-1.06768956408412,-1.06443236880306,
-1.06256126807125,-1.06092911219803,-1.05890705464857,-1.05578349675363,
-1.03309324686783,-1.01570512165146,-1.00953932273506,-1.00561371817511,
-1.00419962769855,-1.00324571576042,-1.00238657163031,-1.00120230670449,
-0.998190493157122,-0.980337453497084,-0.963307904897578,-0.950166593197001,
-0.947069094429297,-0.945232612494161,-0.943595782504044,-0.941521204963318,
-0.93727350782546,-0.907678649802125,-0.904497804750764,-0.894309621728063,
-0.888765802241242,-0.88716180508812,-0.886166715910977,-0.885236563944614,
-0.884106736499347,-0.881214145464196,-0.857669174478239,-0.841401721951798,
-0.835326901869917,-0.830777208047939,-0.828645339272115,-0.827001691523599,
-0.825196388889853,-0.822242235297532,-0.812287196951743,-0.781724872283551,
-0.775226734626685,-0.771150258077749,-0.769715565673442,-0.768757261567959,
-0.767901523645287,-0.766731194434354,-0.763770341694089,-0.742696147585277,
-0.718172832549207,-0.713540651441771,-0.711416562028089,-0.70976896300983,
-0.707977117835005,-0.705085003227308,-0.694656226705977,-0.674156662841869,
-0.666059795982463,-0.662822546383895,-0.654774240561229,-0.652911108557263,
-0.651847885413859,-0.651021272715207,-0.649870012407224,-0.647531515250833,
-0.629198984754756,-0.600476933631467,-0.596129941273214,-0.59403620395498,
-0.592397186911814,-0.590571632870533,-0.587524702010141,-0.575135247469739,
-0.544630197788277,-0.537381444353269,-0.535575649839366,-0.534525498983972,
-0.533696726951843,-0.532526364007551,-0.530090548346005,-0.526827138453678,
-0.518501390079531,-0.500918874538835),.UNSPECIFIED.);
#244=B_SPLINE_CURVE_WITH_KNOTS('',3,(#25060,#25061,#25062,#25063,#25064,
#25065,#25066,#25067,#25068,#25069,#25070,#25071,#25072,#25073,#25074,#25075,
#25076,#25077,#25078,#25079,#25080,#25081,#25082,#25083,#25084,#25085,#25086,
#25087,#25088,#25089,#25090,#25091,#25092,#25093,#25094,#25095,#25096,#25097,
#25098,#25099,#25100,#25101,#25102,#25103,#25104,#25105,#25106,#25107,#25108,
#25109,#25110,#25111,#25112,#25113,#25114,#25115,#25116,#25117,#25118,#25119,
#25120,#25121,#25122,#25123,#25124,#25125,#25126,#25127,#25128,#25129,#25130,
#25131,#25132,#25133,#25134,#25135,#25136,#25137,#25138,#25139,#25140,#25141,
#25142,#25143,#25144,#25145,#25146,#25147,#25148,#25149,#25150,#25151,#25152,
#25153,#25154,#25155,#25156,#25157,#25158,#25159,#25160,#25161,#25162,#25163),
 .UNSPECIFIED.,.F.,.F.,(4,2,2,2,2,2,2,2,2,2,2,2,2,2,2,2,2,2,2,2,2,2,2,2,
2,2,2,2,2,2,2,2,2,2,2,2,2,2,2,2,2,2,2,2,2,2,2,2,2,2,2,4),(-0.241902829928485,
-0.241235095552837,-0.232498724410631,-0.229678875365911,-0.227903015268497,
-0.226250506802044,-0.224054461234132,-0.219149343198562,-0.212447672973761,
-0.193108617620372,-0.174036634756401,-0.171029143259472,-0.169845638469247,
-0.168986729277969,-0.168032690142907,-0.166617766914246,-0.162685611602245,
-0.156506198619109,-0.139146666803432,-0.116485689341663,-0.11335724721356,
-0.111333768510963,-0.1097420786436,-0.109666710484884,-0.10962984118605,
-0.10956028055288,-0.109498224048938,-0.109442381974887,-0.109391752542218,
-0.109345544019743,-0.109303121300336,-0.109263968090822,-0.109227659854679,
-0.109193843831824,-0.109162224164724,-0.109132550654296,-0.109104610058547,
-0.109078219341809,-0.107077758985253,-0.104796295575755,-0.101016965016604,
-0.0804882390455822,-0.0564855802506454,-0.0536229642185044,-0.0524979140069384,
-0.0515690019114021,-0.0505718399758018,-0.0489581966699216,-0.0433156083799494,
-0.0328459798865186,-0.0193890757200365,-0.000340612923464106),
 .UNSPECIFIED.);
#245=B_SPLINE_CURVE_WITH_KNOTS('',3,(#25164,#25165,#25166,#25167,#25168,
#25169,#25170,#25171,#25172,#25173,#25174,#25175,#25176,#25177,#25178,#25179,
#25180,#25181,#25182,#25183,#25184,#25185,#25186,#25187,#25188,#25189,#25190,
#25191,#25192,#25193,#25194,#25195,#25196,#25197,#25198,#25199,#25200,#25201,
#25202,#25203,#25204,#25205,#25206,#25207,#25208,#25209,#25210,#25211,#25212,
#25213,#25214,#25215,#25216,#25217,#25218,#25219,#25220,#25221,#25222,#25223,
#25224,#25225,#25226,#25227,#25228,#25229,#25230,#25231,#25232,#25233,#25234,
#25235,#25236,#25237,#25238,#25239,#25240,#25241,#25242,#25243,#25244,#25245,
#25246,#25247,#25248,#25249,#25250,#25251,#25252,#25253,#25254,#25255,#25256,
#25257,#25258,#25259,#25260,#25261,#25262,#25263,#25264,#25265,#25266,#25267,
#25268,#25269,#25270,#25271,#25272,#25273,#25274,#25275,#25276,#25277,#25278,
#25279,#25280,#25281,#25282,#25283,#25284,#25285,#25286,#25287,#25288,#25289,
#25290,#25291,#25292,#25293,#25294,#25295,#25296,#25297,#25298,#25299,#25300,
#25301,#25302,#25303,#25304,#25305,#25306,#25307,#25308,#25309,#25310,#25311,
#25312,#25313,#25314,#25315,#25316,#25317),.UNSPECIFIED.,.F.,.F.,(4,2,2,
2,2,2,2,2,2,2,2,2,2,2,2,2,2,2,2,2,2,2,2,2,2,2,2,2,2,2,2,2,2,2,2,2,2,2,2,
2,2,2,2,2,2,2,2,2,2,2,2,2,2,2,2,2,2,2,2,2,2,2,2,2,2,2,2,2,2,2,2,2,2,2,2,
2,4),(-1.48429374019444,-1.48208298361065,-1.48001002368649,-1.47838838880993,
-1.47683260671731,-1.47508675568846,-1.47240399049729,-1.46475589808267,
-1.43473308594258,-1.42602539635362,-1.42102958109654,-1.4194836706342,
-1.41850168443352,-1.41756434191149,-1.41640529833117,-1.41354098980554,
-1.39083238707803,-1.36928321980456,-1.36544568595439,-1.36314092235335,
-1.3610670934118,-1.35945246340073,-1.35766389759325,-1.35478391861388,
-1.34549655724287,-1.31421128218915,-1.30766835496553,-1.30357236516067,
-1.30213549942183,-1.30117705255872,-1.30032220070988,-1.29915435582538,
-1.29620696254842,-1.27485328121104,-1.25714433572781,-1.25076353626861,
-1.24603895611784,-1.24387551427642,-1.24222809398535,-1.24043883945829,
-1.23755623786655,-1.22824582883302,-1.20327245215956,-1.1875894250323,
-1.18549749419664,-1.18439669399194,-1.1834821290127,-1.18233189379625,
-1.18050893065373,-1.17008659443793,-1.16159109665915,-1.14712713329275,
-1.13116630040875,-1.12791351583137,-1.12604363844312,-1.12441178456757,
-1.12238911242253,-1.11926271092811,-1.09671372620601,-1.07964247930974,
-1.07319747557486,-1.06914528578361,-1.06771419487868,-1.06675690837535,
-1.06590100850812,-1.0647291199385,-1.06178171411255,-1.04061416071021,
-1.022775200704,-1.01636762878247,-1.01162776298925,-1.00946145181498,-1.00781351781457,
-1.00602533325033,-1.00314806349783,-0.993889634336018,-0.983954477832344),
 .UNSPECIFIED.);
#246=B_SPLINE_CURVE_WITH_KNOTS('',3,(#25323,#25324,#25325,#25326,#25327,
#25328,#25329,#25330,#25331,#25332,#25333,#25334,#25335,#25336,#25337,#25338,
#25339,#25340,#25341,#25342,#25343,#25344,#25345,#25346,#25347,#25348,#25349,
#25350,#25351,#25352,#25353,#25354,#25355,#25356,#25357,#25358,#25359,#25360,
#25361,#25362,#25363,#25364,#25365,#25366,#25367,#25368,#25369,#25370,#25371,
#25372,#25373,#25374,#25375,#25376,#25377,#25378,#25379,#25380,#25381,#25382,
#25383,#25384,#25385,#25386,#25387,#25388,#25389,#25390,#25391,#25392,#25393,
#25394,#25395,#25396,#25397,#25398,#25399,#25400,#25401,#25402,#25403,#25404,
#25405,#25406,#25407,#25408,#25409,#25410,#25411,#25412,#25413,#25414,#25415,
#25416,#25417,#25418,#25419,#25420,#25421,#25422,#25423,#25424,#25425,#25426,
#25427,#25428,#25429,#25430,#25431,#25432,#25433,#25434,#25435,#25436,#25437,
#25438,#25439,#25440,#25441,#25442,#25443,#25444,#25445,#25446,#25447,#25448,
#25449,#25450,#25451,#25452,#25453,#25454,#25455,#25456,#25457,#25458,#25459,
#25460,#25461,#25462,#25463,#25464,#25465,#25466),.UNSPECIFIED.,.F.,.F.,
(4,2,2,2,2,2,2,2,2,2,2,2,2,2,2,2,2,2,2,2,2,2,2,2,2,2,2,2,2,2,2,2,2,2,2,
2,2,2,2,2,2,2,2,2,2,2,2,2,2,2,2,2,2,2,2,2,2,2,2,2,2,2,2,2,2,2,2,2,2,2,2,
4),(-0.500810674765781,-0.493763997975324,-0.479343838874954,-0.470862672363058,
-0.46044030020236,-0.458616925055466,-0.457466435887697,-0.456551662356445,
-0.455450590638109,-0.453358092466655,-0.437654725138245,-0.412625980248117,
-0.403393575844477,-0.400518790032286,-0.398730949720771,-0.397082524951323,
-0.394914382057417,-0.390165635960305,-0.38374194195318,-0.365826223518783,
-0.344741174014523,-0.341781252562763,-0.340610762999099,-0.339755101282576,
-0.338797108669497,-0.33736328374844,-0.333291885928938,-0.326805381007299,
-0.296372437889619,-0.28632500980634,-0.28336056594681,-0.28155321931724,
-0.279910459444584,-0.277783648842673,-0.27325999921489,-0.267229219376008,
-0.251158195752625,-0.227285441490762,-0.224413386411133,-0.223286872301924,
-0.222357626374446,-0.22136120073813,-0.219750780971,-0.214140555211819,
-0.203763530308994,-0.180283500567982,-0.169277718806919,-0.166221296568094,
-0.164393867620123,-0.162755553573591,-0.160666000833089,-0.156339841161414,
-0.139563400149093,-0.112879349242939,-0.107947730715232,-0.106352596766125,
-0.105359514347856,-0.104436295556282,-0.103187085909334,-0.101715303326176,
-0.0990955069060905,-0.093086120761574,-0.0684081952874672,-0.0525792148884451,
-0.0492653612654853,-0.0473624791550844,-0.0457482525158989,-0.0437738540592276,
-0.0400276938112811,-0.0352924223120453,-0.0243287202206848,-0.000340767018293399),
 .UNSPECIFIED.);
#247=B_SPLINE_CURVE_WITH_KNOTS('',3,(#25467,#25468,#25469,#25470,#25471,
#25472,#25473,#25474,#25475,#25476,#25477,#25478,#25479,#25480,#25481,#25482,
#25483,#25484,#25485,#25486,#25487,#25488,#25489,#25490,#25491,#25492,#25493,
#25494,#25495,#25496,#25497,#25498,#25499,#25500,#25501,#25502,#25503,#25504,
#25505,#25506,#25507,#25508,#25509,#25510,#25511,#25512,#25513,#25514,#25515,
#25516,#25517,#25518,#25519,#25520,#25521,#25522,#25523,#25524,#25525,#25526,
#25527,#25528,#25529,#25530,#25531,#25532,#25533,#25534,#25535,#25536,#25537,
#25538,#25539,#25540,#25541,#25542,#25543,#25544,#25545,#25546,#25547,#25548,
#25549,#25550,#25551,#25552,#25553,#25554,#25555,#25556,#25557,#25558,#25559,
#25560,#25561,#25562,#25563,#25564,#25565,#25566,#25567,#25568,#25569,#25570,
#25571,#25572,#25573,#25574,#25575,#25576,#25577,#25578,#25579,#25580,#25581,
#25582,#25583,#25584,#25585,#25586,#25587,#25588,#25589,#25590,#25591,#25592,
#25593,#25594,#25595,#25596,#25597,#25598,#25599,#25600,#25601,#25602,#25603,
#25604,#25605,#25606,#25607,#25608,#25609,#25610,#25611,#25612,#25613,#25614,
#25615,#25616,#25617,#25618,#25619,#25620,#25621,#25622,#25623,#25624,#25625,
#25626,#25627,#25628,#25629,#25630,#25631,#25632,#25633,#25634,#25635,#25636,
#25637,#25638,#25639,#25640,#25641,#25642,#25643,#25644,#25645,#25646,#25647,
#25648,#25649,#25650,#25651,#25652,#25653,#25654),.UNSPECIFIED.,.F.,.F.,
(4,2,2,2,2,2,2,2,2,2,2,2,2,2,2,2,2,2,2,2,2,2,2,2,2,2,2,2,2,2,2,2,2,2,2,
2,2,2,2,2,2,2,2,2,2,2,2,2,2,2,2,2,2,2,2,2,2,2,2,2,2,2,2,2,2,2,2,2,2,2,2,
2,2,2,2,2,2,2,2,2,2,2,2,2,2,2,2,2,2,2,2,2,2,4),(-1.48452413958049,-1.4784429304074,
-1.47512352499763,-1.47386473256755,-1.47293655958983,-1.472065482934,-1.47106651165108,
-1.46944417051658,-1.46428483722046,-1.45654241215069,-1.42936559743042,
-1.41871316119289,-1.41580239765065,-1.41400693704685,-1.41236126653133,
-1.41024697066382,-1.40583133784541,-1.37839802722197,-1.37242614775626,
-1.36926311670616,-1.36189881745768,-1.35889177242019,-1.35662511794588,
-1.35550052783905,-1.3554962227811,-1.35549187782454,-1.35548749258201,
-1.35548306638497,-1.35547859880842,-1.3554740893391,-1.35546953748773,
-1.35546494273987,-1.35546030464082,-1.3554556226107,-1.35545089611522,
-1.35544612456033,-1.35544130745021,-1.35543644423668,-1.35543153422422,
-1.35542657678914,-1.35542157148871,-1.35541651780225,-1.3554114149066,
-1.35540626230105,-1.35540105939099,-1.35539580552704,-1.35539049999029,
-1.35538514219486,-1.35537973157735,-1.35537426737185,-1.35536874884142,
-1.35536317543888,-1.35535754641141,-1.35535186095732,-1.35534611835286,
-1.35534115712002,-1.35533596964344,-1.35533054543398,-1.35532487328584,
-1.35531894164037,-1.35531273827813,-1.35530625042951,-1.35529946469499,
-1.35529236709083,-1.35528494287048,-1.35527717642616,-1.35526905161778,
-1.35526055144018,-1.35525165799427,-1.3552423525241,-1.35523261549278,
-1.35522242639285,-1.35521176363457,-1.3552006046248,-1.35518953070745,
-1.35517596990946,-1.35515936733245,-1.3551390467402,-1.35509835217385,
-1.35416888884173,-1.35304120289169,-1.35016118296104,-1.32671771010661,
-1.3103745565863,-1.30428365799597,-1.29972493834902,-1.29759171330962,
-1.29594822591923,-1.2941443039396,-1.29119516593943,-1.28127912217326,
-1.25068358274672,-1.24418434366141,-1.24300538673529),.UNSPECIFIED.);
#248=B_SPLINE_CURVE_WITH_KNOTS('',3,(#25655,#25656,#25657,#25658,#25659,
#25660,#25661,#25662,#25663,#25664,#25665,#25666,#25667,#25668,#25669,#25670,
#25671,#25672,#25673,#25674,#25675,#25676,#25677,#25678,#25679,#25680,#25681,
#25682,#25683,#25684,#25685,#25686,#25687,#25688,#25689,#25690,#25691,#25692,
#25693,#25694,#25695,#25696,#25697,#25698,#25699,#25700,#25701,#25702,#25703,
#25704,#25705,#25706,#25707,#25708,#25709,#25710,#25711,#25712,#25713,#25714,
#25715,#25716,#25717,#25718,#25719,#25720,#25721,#25722,#25723,#25724,#25725,
#25726,#25727,#25728,#25729,#25730,#25731,#25732,#25733,#25734,#25735,#25736,
#25737,#25738,#25739,#25740,#25741,#25742,#25743,#25744,#25745,#25746,#25747,
#25748,#25749,#25750,#25751,#25752,#25753,#25754,#25755,#25756,#25757,#25758,
#25759,#25760,#25761,#25762,#25763,#25764,#25765,#25766,#25767,#25768,#25769,
#25770,#25771,#25772,#25773,#25774,#25775,#25776,#25777,#25778,#25779,#25780,
#25781,#25782,#25783,#25784,#25785,#25786,#25787,#25788,#25789,#25790,#25791,
#25792,#25793,#25794,#25795,#25796,#25797,#25798,#25799,#25800,#25801,#25802,
#25803,#25804,#25805,#25806,#25807,#25808,#25809,#25810,#25811,#25812,#25813,
#25814,#25815,#25816,#25817,#25818,#25819,#25820,#25821,#25822,#25823,#25824,
#25825,#25826,#25827,#25828,#25829,#25830,#25831,#25832,#25833,#25834,#25835,
#25836,#25837,#25838,#25839,#25840,#25841,#25842,#25843,#25844,#25845,#25846,
#25847,#25848,#25849,#25850,#25851,#25852,#25853,#25854,#25855,#25856,#25857,
#25858,#25859,#25860,#25861,#25862,#25863,#25864,#25865,#25866,#25867,#25868,
#25869,#25870,#25871,#25872),.UNSPECIFIED.,.F.,.F.,(4,2,2,2,2,2,2,2,2,2,
2,2,2,2,2,2,2,2,2,2,2,2,2,2,2,2,2,2,2,2,2,2,2,2,2,2,2,2,2,2,2,2,2,2,2,2,
2,2,2,2,2,2,2,2,2,2,2,2,2,2,2,2,2,2,2,2,2,2,2,2,2,2,2,2,2,2,2,2,2,2,2,2,
2,2,2,2,2,2,2,2,2,2,2,2,2,2,2,2,2,2,2,2,2,2,2,2,2,2,4),(-0.983954477832344,
-0.968868638508017,-0.953166724759176,-0.951074306613063,-0.949973352227744,
-0.9490587183943,-0.947908471159131,-0.946085625100627,-0.935668945765655,
-0.927192952418088,-0.912782957367132,-0.896744966698653,-0.893488404504935,
-0.891617619380803,-0.889985712932694,-0.887963933233468,-0.884840750664748,
-0.862147866182155,-0.84475358069355,-0.838595020900477,-0.834672877626706,
-0.833259396390993,-0.832305711720418,-0.831446632176123,-0.830262283477115,
-0.827249331906869,-0.809126776339629,-0.789105104974024,-0.77880841300617,
-0.775928644710211,-0.774139827322274,-0.772491923622991,-0.770363109984292,
-0.76570277250765,-0.742272925841974,-0.720060305264201,-0.717159747474094,
-0.715994277868525,-0.715055042395106,-0.714075114170517,-0.712539453835846,
-0.707637798195469,-0.699173761350993,-0.673644462929149,-0.662005878491625,
-0.658897513439,-0.657058832256574,-0.655586296554883,-0.653595917379173,
-0.649771107742804,-0.624664531686292,-0.602847498623458,-0.599923513817372,
-0.598754034219578,-0.597898645370193,-0.596940393384362,-0.595505210046815,
-0.591423382144515,-0.584913573523478,-0.554129466025904,-0.544396415059281,
-0.541467651588219,-0.539668138414914,-0.538023389948223,-0.535880960189099,
-0.531272674746425,-0.525095062817244,-0.508354966292686,-0.485499830618691,
-0.482641648942825,-0.481483470251986,-0.480546180320971,-0.479563436227032,
-0.478014927172715,-0.472998013858148,-0.464238030225078,-0.435992997289897,
-0.427000993123812,-0.424151303747702,-0.422369041321594,-0.420718985637325,
-0.418538696411346,-0.413721658821508,-0.407176917836962,-0.37572818820882,
-0.366709973772506,-0.364787014616994,-0.36371034223593,-0.3627936263392,
-0.361612027954384,-0.359116905559313,-0.355750165659295,-0.347018754400621,
-0.319215201911636,-0.309821128283198,-0.306928982634031,-0.305137385784263,
-0.303490193216075,-0.301330529042793,-0.296628438329255,-0.290286876090216,
-0.272772109346323,-0.251090592894792,-0.24816705740505,-0.246997640327601,
-0.246142255360121,-0.245183956516744,-0.243748614346413,-0.241908569806093),
 .UNSPECIFIED.);
#249=B_SPLINE_CURVE_WITH_KNOTS('',3,(#25877,#25878,#25879,#25880,#25881,
#25882,#25883,#25884,#25885,#25886,#25887,#25888,#25889,#25890,#25891,#25892,
#25893,#25894,#25895,#25896,#25897,#25898,#25899,#25900,#25901,#25902,#25903,
#25904,#25905,#25906,#25907,#25908,#25909,#25910,#25911,#25912,#25913,#25914,
#25915,#25916,#25917,#25918,#25919,#25920,#25921,#25922,#25923,#25924,#25925,
#25926,#25927,#25928,#25929,#25930,#25931,#25932,#25933,#25934,#25935,#25936,
#25937,#25938,#25939,#25940,#25941,#25942,#25943,#25944,#25945,#25946,#25947,
#25948,#25949,#25950,#25951,#25952,#25953,#25954,#25955,#25956,#25957,#25958,
#25959,#25960,#25961,#25962,#25963,#25964,#25965,#25966,#25967,#25968,#25969,
#25970,#25971,#25972,#25973,#25974,#25975,#25976,#25977,#25978,#25979,#25980,
#25981,#25982,#25983,#25984,#25985,#25986,#25987,#25988,#25989,#25990,#25991,
#25992,#25993,#25994,#25995,#25996,#25997,#25998,#25999,#26000,#26001,#26002,
#26003,#26004,#26005,#26006,#26007,#26008,#26009,#26010,#26011,#26012,#26013,
#26014,#26015,#26016,#26017,#26018,#26019,#26020,#26021,#26022,#26023,#26024,
#26025,#26026,#26027,#26028,#26029,#26030,#26031,#26032,#26033,#26034,#26035,
#26036,#26037,#26038,#26039,#26040,#26041,#26042,#26043,#26044,#26045,#26046,
#26047,#26048,#26049,#26050,#26051,#26052,#26053,#26054,#26055,#26056,#26057,
#26058,#26059,#26060,#26061,#26062,#26063,#26064,#26065,#26066,#26067,#26068,
#26069,#26070,#26071,#26072,#26073,#26074,#26075,#26076,#26077,#26078,#26079,
#26080,#26081,#26082,#26083,#26084,#26085,#26086,#26087,#26088,#26089,#26090,
#26091,#26092,#26093,#26094,#26095,#26096),.UNSPECIFIED.,.F.,.F.,(4,2,2,
2,2,2,2,2,2,2,2,2,2,2,2,2,2,2,2,2,2,2,2,2,2,2,2,2,2,2,2,2,2,2,2,2,2,2,2,
2,2,2,2,2,2,2,2,2,2,2,2,2,2,2,2,2,2,2,2,2,2,2,2,2,2,2,2,2,2,2,2,2,2,2,2,
2,2,2,2,2,2,2,2,2,2,2,2,2,2,2,2,2,2,2,2,2,2,2,2,2,2,2,2,2,2,2,2,2,2,4),
(-1.24277962970854,-1.23412966373543,-1.22741005871783,-1.22249463988393,
-1.22029694619587,-1.21864434600835,-1.21708539526387,-1.21446904165843,
-1.20733392187946,-1.17702478227368,-1.16805907342439,-1.16296381083007,
-1.16140672726362,-1.16042211146713,-1.15948607423148,-1.15833263541782,
-1.15550168011246,-1.13203242805169,-1.11572196681001,-1.10963814963226,
-1.105083467593,-1.10295092969087,-1.10130746684272,-1.09950306753541,-1.09655199534884,
-1.08662009767472,-1.06218433081072,-1.05156119895492,-1.04586622071375,
-1.04424751512979,-1.04324927653661,-1.04232100142987,-1.04119842094369,
-1.03835110454978,-1.01419358187509,-0.998316397697683,-0.99232906098506,
-0.987830186697089,-0.985707990865551,-0.984065803704339,-0.982256076084012,
-0.97928077859667,-0.969108557526195,-0.942126827523083,-0.933463181284425,
-0.928483897929747,-0.926939460140422,-0.925957561489534,-0.925019566806886,
-0.92385893726383,-0.920986845991631,-0.898370413946775,-0.881493997925063,
-0.875286990624912,-0.870661321910824,-0.868515555929468,-0.866870202539996,
-0.865071960955131,-0.862149640011554,-0.852478469822047,-0.827812479964596,
-0.812247343682553,-0.8101571160069,-0.809056484770628,-0.808141636065454,
-0.806990502179923,-0.805165120257801,-0.794691935011586,-0.767279905622326,
-0.755348955916304,-0.752335519454585,-0.750517393691155,-0.748877024456409,
-0.74677039987178,-0.742354853180554,-0.724861715068614,-0.706506740457486,
-0.701560154790389,-0.694522194070815,-0.692712817320951,-0.691672440540991,
-0.690749232647188,-0.68950881276234,-0.686694124094588,-0.673941764204985,
-0.667390994497136,-0.640653917426471,-0.636129384357236,-0.634025143437769,
-0.632380586052915,-0.630579522932804,-0.627644243225624,-0.616707739600309,
-0.597181227651071,-0.579283183877282,-0.576270569478968,-0.575086175082451,
-0.574227006930266,-0.573273142164785,-0.571859256917569,-0.567935001968803,
-0.561772895381529,-0.544395779055861,-0.521716350416832,-0.518593117598922,
-0.516571157791766,-0.514939020119211,-0.513067873366136,-0.5098104327551,
-0.500810674765781),.UNSPECIFIED.);
#250=B_SPLINE_CURVE_WITH_KNOTS('',3,(#26098,#26099,#26100,#26101,#26102,
#26103,#26104,#26105,#26106,#26107,#26108,#26109,#26110,#26111,#26112,#26113,
#26114,#26115,#26116,#26117,#26118,#26119,#26120,#26121,#26122,#26123,#26124,
#26125,#26126,#26127,#26128,#26129,#26130,#26131,#26132,#26133,#26134,#26135,
#26136,#26137,#26138,#26139,#26140,#26141,#26142,#26143,#26144,#26145,#26146,
#26147,#26148,#26149,#26150,#26151,#26152,#26153,#26154,#26155,#26156,#26157,
#26158,#26159,#26160,#26161,#26162,#26163,#26164,#26165,#26166,#26167,#26168,
#26169,#26170,#26171,#26172,#26173,#26174,#26175),.UNSPECIFIED.,.F.,.F.,
(4,2,2,2,2,2,2,2,2,2,2,2,2,2,2,2,2,2,2,2,2,2,2,2,2,2,2,2,2,2,2,2,2,2,2,
2,2,2,4),(-0.241908569806093,-0.239665731678708,-0.233153621010589,-0.202335542846139,
-0.192632530864902,-0.189706977527231,-0.187908141035259,-0.186263159733702,
-0.184119201847845,-0.179502753495191,-0.173310959974035,-0.156505251655551,
-0.133750872788444,-0.130886135550159,-0.129726810989271,-0.128789205314897,
-0.127826604430165,-0.126336873585595,-0.124561298104256,-0.121127754815419,
-0.112129159235787,-0.0817443573993051,-0.0747175042380305,-0.0721163544391079,
-0.0705602358057474,-0.0689060117117186,-0.0666982153744462,-0.061725774537956,
-0.054903011115217,-0.025924018582589,-0.0183732371213993,-0.0141208835930925,
-0.0126150873274648,-0.0117383796533788,-0.0108668402608708,-0.00993909372422445,
-0.00868160291576745,-0.00563143718800878,-0.000340074931059168),
 .UNSPECIFIED.);
#251=B_SPLINE_CURVE_WITH_KNOTS('',3,(#26176,#26177,#26178,#26179,#26180,
#26181,#26182,#26183,#26184,#26185,#26186,#26187,#26188,#26189,#26190,#26191,
#26192,#26193,#26194,#26195,#26196,#26197,#26198,#26199,#26200,#26201,#26202,
#26203,#26204,#26205,#26206,#26207,#26208,#26209,#26210,#26211,#26212,#26213,
#26214,#26215,#26216,#26217,#26218,#26219,#26220,#26221,#26222,#26223,#26224,
#26225,#26226,#26227,#26228,#26229,#26230,#26231,#26232,#26233,#26234,#26235,
#26236,#26237,#26238,#26239,#26240,#26241,#26242,#26243,#26244,#26245,#26246,
#26247,#26248,#26249,#26250,#26251,#26252,#26253,#26254,#26255,#26256,#26257,
#26258,#26259,#26260,#26261,#26262,#26263,#26264,#26265,#26266,#26267,#26268,
#26269,#26270,#26271,#26272,#26273,#26274,#26275,#26276,#26277,#26278,#26279,
#26280,#26281,#26282,#26283,#26284,#26285,#26286,#26287,#26288,#26289,#26290,
#26291,#26292,#26293,#26294,#26295,#26296,#26297,#26298,#26299,#26300,#26301,
#26302,#26303,#26304,#26305,#26306,#26307,#26308,#26309,#26310,#26311,#26312,
#26313,#26314,#26315,#26316,#26317,#26318,#26319,#26320,#26321),
 .UNSPECIFIED.,.F.,.F.,(4,2,2,2,2,2,2,2,2,2,2,2,2,2,2,2,2,2,2,2,2,2,2,2,
2,2,2,2,2,2,2,2,2,2,2,2,2,2,2,2,2,2,2,2,2,2,2,2,2,2,2,2,2,2,2,2,2,2,2,2,
2,2,2,2,2,2,2,2,2,2,2,2,4),(-1.48451778638364,-1.46066201472305,-1.44895628021111,
-1.44401265830151,-1.4401374685125,-1.43813699952084,-1.43650661364363,
-1.43462010883433,-1.43137749338801,-1.41705735181162,-1.3922953247286,
-1.38529004156106,-1.38238243621184,-1.38080094696952,-1.37947675470059,
-1.37853757846013,-1.37768257102024,-1.37651429016597,-1.37356487970255,
-1.35221184560742,-1.33450158186885,-1.32812028024024,-1.32339532208566,
-1.32123170151447,-1.31958414283739,-1.31779473577959,-1.31491188349838,
-1.30560061704466,-1.28062519729804,-1.26494087202525,-1.26284876524312,
-1.26174787231249,-1.26083323021122,-1.25968289789646,-1.2578597806812,
-1.24743655671786,-1.23894033381647,-1.2244751106091,-1.2085129859683,-1.20525992963476,
-1.20338989512212,-1.20175790359319,-1.19973506014053,-1.19660839254029,
-1.17405755413047,-1.15698487328093,-1.15053929559783,-1.14648675040522,
-1.14505553698962,-1.14409816938358,-1.14324219765871,-1.14207021152182,
-1.13912255359797,-1.11795321845521,-1.10011275218442,-1.09370463955401,
-1.08896437385642,-1.08679787997681,-1.0851498070183,-1.08336147169593,
-1.0804839594233,-1.07122475044398,-1.04620164413103,-1.03049840612559,
-1.02840581154371,-1.02730476432478,-1.02639005336872,-1.02523970914546,
-1.02341670938952,-1.01299915182339,-1.00452216175146,-0.990110426008559,
-0.984125170450909),.UNSPECIFIED.);
#252=B_SPLINE_CURVE_WITH_KNOTS('',3,(#26327,#26328,#26329,#26330,#26331,
#26332,#26333,#26334,#26335,#26336,#26337,#26338,#26339,#26340,#26341,#26342,
#26343,#26344,#26345,#26346,#26347,#26348,#26349,#26350,#26351,#26352,#26353,
#26354,#26355,#26356,#26357,#26358,#26359,#26360,#26361,#26362,#26363,#26364,
#26365,#26366,#26367,#26368,#26369,#26370,#26371,#26372,#26373,#26374,#26375,
#26376,#26377,#26378,#26379,#26380,#26381,#26382,#26383,#26384,#26385,#26386,
#26387,#26388,#26389,#26390,#26391,#26392,#26393,#26394,#26395,#26396,#26397,
#26398,#26399,#26400,#26401,#26402,#26403,#26404,#26405,#26406,#26407,#26408,
#26409,#26410,#26411,#26412,#26413,#26414,#26415,#26416,#26417,#26418,#26419,
#26420,#26421,#26422,#26423,#26424,#26425,#26426,#26427,#26428,#26429,#26430,
#26431,#26432,#26433,#26434,#26435,#26436,#26437,#26438,#26439,#26440,#26441,
#26442,#26443,#26444,#26445,#26446,#26447,#26448,#26449,#26450,#26451,#26452,
#26453,#26454,#26455,#26456,#26457,#26458,#26459,#26460,#26461,#26462,#26463,
#26464,#26465,#26466,#26467,#26468,#26469,#26470,#26471,#26472,#26473,#26474,
#26475,#26476,#26477,#26478,#26479,#26480),.UNSPECIFIED.,.F.,.F.,(4,2,2,
2,2,2,2,2,2,2,2,2,2,2,2,2,2,2,2,2,2,2,2,2,2,2,2,2,2,2,2,2,2,2,2,2,2,2,2,
2,2,2,2,2,2,2,2,2,2,2,2,2,2,2,2,2,2,2,2,2,2,2,2,2,2,2,2,2,2,2,2,2,2,2,2,
2,4),(-0.500647391340917,-0.499639498486703,-0.49800539474486,-0.497003639325043,
-0.496066234440156,-0.494737354861665,-0.49139217980479,-0.486437587803248,
-0.46991231738142,-0.446301415675732,-0.441644678250074,-0.439516225225528,
-0.437868064843415,-0.436078432509876,-0.433196162657974,-0.422876997138652,
-0.402777235394939,-0.384734007803615,-0.38171425531961,-0.380528603712869,
-0.379669054522658,-0.378715406522772,-0.377302930974548,-0.373389589300195,
-0.367251506663444,-0.349846300274575,-0.327151004569,-0.324027407598899,
-0.322005219126954,-0.320372901475535,-0.318501553434403,-0.31524377551086,
-0.299196030475438,-0.284773965386116,-0.276291664139459,-0.265868172486806,
-0.264044597858373,-0.262893982468024,-0.261979108326631,-0.260877915210355,
-0.258785185523965,-0.243080017238911,-0.218048328667486,-0.208815128571274,
-0.205940049704668,-0.204152017778155,-0.202503410059391,-0.200335017329256,
-0.195585686059944,-0.189161174619783,-0.171242939055352,-0.150156380747205,
-0.147205541538612,-0.146031415904382,-0.145174786298885,-0.144217770601365,
-0.142860930542293,-0.139161761110379,-0.133430805034786,-0.11551471264295,
-0.092674529818609,-0.0895504613273472,-0.087528158531183,-0.0858958725695207,
-0.0840246968858895,-0.0810395411596259,-0.0678015620629751,-0.0503895066295616,
-0.0418844031631154,-0.0313964545750801,-0.0295703216737137,-0.0284189473413277,
-0.0275040594930109,-0.0264035584067737,-0.0252196469170199,-0.0233239747058074,
-0.000340432792623708),.UNSPECIFIED.);
#253=B_SPLINE_CURVE_WITH_KNOTS('',3,(#26481,#26482,#26483,#26484,#26485,
#26486,#26487,#26488,#26489,#26490,#26491,#26492,#26493,#26494,#26495,#26496,
#26497,#26498,#26499,#26500,#26501,#26502,#26503,#26504,#26505,#26506,#26507,
#26508,#26509,#26510,#26511,#26512,#26513,#26514,#26515,#26516,#26517,#26518,
#26519,#26520,#26521,#26522,#26523,#26524,#26525,#26526,#26527,#26528,#26529,
#26530,#26531,#26532,#26533,#26534,#26535,#26536,#26537,#26538,#26539,#26540,
#26541,#26542,#26543,#26544,#26545,#26546,#26547,#26548,#26549,#26550,#26551,
#26552),.UNSPECIFIED.,.F.,.F.,(4,2,2,2,2,2,2,2,2,2,2,2,2,2,2,2,2,2,2,2,
2,2,2,2,2,2,2,2,2,2,2,2,2,2,2,4),(-1.48443446178175,-1.46089065681018,-1.45788661713376,
-1.45592251976316,-1.45404488572894,-1.45241367689662,-1.45040133918318,
-1.44730909539555,-1.42950435627513,-1.41442207851342,-1.40338697946608,
-1.39813471340563,-1.39623049618969,-1.39514680960526,-1.39423097514338,
-1.39305929255334,-1.39116495026636,-1.37877035124615,-1.35307080871119,
-1.34176281806496,-1.33869030069849,-1.33681960244217,-1.33518779769318,
-1.33316617520752,-1.33004328948931,-1.30735913496712,-1.2899771230153,
-1.28381041051754,-1.27988462302829,-1.27847069523388,-1.27751695939325,
-1.27665802588238,-1.27547411727258,-1.27246356423765,-1.25356928446698,
-1.24277962970854),.UNSPECIFIED.);
#254=B_SPLINE_CURVE_WITH_KNOTS('',3,(#26553,#26554,#26555,#26556,#26557,
#26558,#26559,#26560,#26561,#26562,#26563,#26564,#26565,#26566,#26567,#26568,
#26569,#26570,#26571,#26572,#26573,#26574,#26575,#26576,#26577,#26578,#26579,
#26580,#26581,#26582,#26583,#26584,#26585,#26586,#26587,#26588,#26589,#26590,
#26591,#26592,#26593,#26594,#26595,#26596,#26597,#26598,#26599,#26600,#26601,
#26602,#26603,#26604,#26605,#26606,#26607,#26608,#26609,#26610,#26611,#26612,
#26613,#26614,#26615,#26616,#26617,#26618,#26619,#26620,#26621,#26622,#26623,
#26624,#26625,#26626,#26627,#26628,#26629,#26630,#26631,#26632,#26633,#26634,
#26635,#26636,#26637,#26638,#26639,#26640,#26641,#26642,#26643,#26644,#26645,
#26646,#26647,#26648,#26649,#26650,#26651,#26652,#26653,#26654,#26655,#26656,
#26657,#26658,#26659,#26660,#26661,#26662,#26663,#26664,#26665,#26666,#26667,
#26668,#26669,#26670,#26671,#26672,#26673,#26674,#26675,#26676,#26677,#26678,
#26679,#26680,#26681,#26682,#26683,#26684,#26685,#26686,#26687,#26688,#26689,
#26690,#26691,#26692,#26693,#26694,#26695,#26696,#26697,#26698,#26699,#26700,
#26701,#26702,#26703,#26704,#26705,#26706,#26707,#26708,#26709,#26710,#26711,
#26712,#26713,#26714,#26715,#26716,#26717,#26718,#26719,#26720,#26721,#26722,
#26723,#26724,#26725,#26726,#26727,#26728,#26729,#26730,#26731,#26732,#26733,
#26734,#26735,#26736,#26737,#26738,#26739,#26740,#26741,#26742,#26743,#26744,
#26745,#26746,#26747,#26748,#26749,#26750,#26751,#26752,#26753,#26754,#26755,
#26756,#26757,#26758,#26759,#26760,#26761,#26762,#26763,#26764,#26765,#26766,
#26767,#26768,#26769,#26770,#26771,#26772),.UNSPECIFIED.,.F.,.F.,(4,2,2,
2,2,2,2,2,2,2,2,2,2,2,2,2,2,2,2,2,2,2,2,2,2,2,2,2,2,2,2,2,2,2,2,2,2,2,2,
2,2,2,2,2,2,2,2,2,2,2,2,2,2,2,2,2,2,2,2,2,2,2,2,2,2,2,2,2,2,2,2,2,2,2,2,
2,2,2,2,2,2,2,2,2,2,2,2,2,2,2,2,2,2,2,2,2,2,2,2,2,2,2,2,2,2,2,2,2,2,4),
(-0.984125170450909,-0.97407182850143,-0.970815026141635,-0.968944090705639,
-0.96731204591619,-0.965290085476164,-0.962166605751026,-0.939512479383253,
-0.92199453602018,-0.915886379681188,-0.911987317587578,-0.910576952629664,
-0.909623851686047,-0.908764104586927,-0.90757731833726,-0.90455023494979,
-0.886650923156437,-0.866473158707528,-0.856132910536406,-0.853249088092647,
-0.851459290146421,-0.849811510631094,-0.847684298960911,-0.843033436833498,
-0.819125754082017,-0.80515467357207,-0.798799627098277,-0.794787830999968,
-0.793362028861912,-0.792405734577381,-0.791548744173856,-0.790372873751615,
-0.787411093245368,-0.76659029702288,-0.742556196047015,-0.737544994545705,
-0.735496907400908,-0.733971130726448,-0.732294820393593,-0.729958311495741,
-0.724211841866047,-0.715941008890753,-0.684524884674582,-0.678168947510021,
-0.67642009919006,-0.675393000118325,-0.674465942141049,-0.673198840031539,
-0.67023100924564,-0.666007197355681,-0.653494958947578,-0.623980232755666,
-0.619724831776662,-0.617648791607647,-0.616011836412843,-0.614176292059367,
-0.611083009889578,-0.598007766065222,-0.581159515513287,-0.563022814900155,
-0.560008464887938,-0.558823773800337,-0.557964523288482,-0.557010731664748,
-0.555597242480497,-0.551675954767237,-0.545520405511775,-0.528133871327585,
-0.505447855231891,-0.502324474460695,-0.500302455058573,-0.498670295283407,
-0.496799153795069,-0.493541808469324,-0.477498892960424,-0.463073482991047,
-0.454587861537948,-0.44416570118901,-0.442342296453984,-0.441191790235998,
-0.440277006243833,-0.439175932973491,-0.437083469240241,-0.421384850782953,
-0.396370048037415,-0.387117389551859,-0.384240427773661,-0.382452098706696,
-0.380803804493003,-0.378636687975238,-0.373893728598252,-0.367480302789346,
-0.349615959939549,-0.328449372292195,-0.325492328793118,-0.324322747544248,
-0.323467303960574,-0.322509014660337,-0.321073816989163,-0.316992230873438,
-0.310483098222279,-0.279712973462818,-0.269965280240216,-0.26703482812587,
-0.265234885836784,-0.263590144338347,-0.261448297256017,-0.256843544035796,
-0.250672178107061,-0.242054869217963),.UNSPECIFIED.);
#255=B_SPLINE_CURVE_WITH_KNOTS('',3,(#26777,#26778,#26779,#26780,#26781,
#26782,#26783,#26784,#26785,#26786,#26787,#26788,#26789,#26790,#26791,#26792,
#26793,#26794,#26795,#26796,#26797,#26798,#26799,#26800,#26801,#26802,#26803,
#26804,#26805,#26806,#26807,#26808,#26809,#26810,#26811,#26812,#26813,#26814,
#26815,#26816,#26817,#26818,#26819,#26820,#26821,#26822,#26823,#26824,#26825,
#26826,#26827,#26828,#26829,#26830,#26831,#26832,#26833,#26834,#26835,#26836,
#26837,#26838,#26839,#26840,#26841,#26842,#26843,#26844,#26845,#26846,#26847,
#26848,#26849,#26850,#26851,#26852,#26853,#26854,#26855,#26856,#26857,#26858,
#26859,#26860,#26861,#26862,#26863,#26864,#26865,#26866,#26867,#26868,#26869,
#26870,#26871,#26872,#26873,#26874,#26875,#26876,#26877,#26878,#26879,#26880,
#26881,#26882,#26883,#26884,#26885,#26886,#26887,#26888,#26889,#26890,#26891,
#26892,#26893,#26894,#26895,#26896,#26897,#26898,#26899,#26900,#26901,#26902,
#26903,#26904,#26905,#26906,#26907,#26908,#26909,#26910,#26911,#26912,#26913,
#26914,#26915,#26916,#26917,#26918,#26919,#26920,#26921,#26922,#26923,#26924,
#26925,#26926,#26927,#26928,#26929,#26930,#26931,#26932,#26933,#26934,#26935,
#26936,#26937,#26938,#26939,#26940,#26941,#26942,#26943,#26944,#26945,#26946,
#26947,#26948,#26949,#26950,#26951,#26952,#26953,#26954,#26955,#26956,#26957,
#26958,#26959,#26960,#26961,#26962,#26963,#26964,#26965,#26966,#26967,#26968,
#26969,#26970,#26971,#26972,#26973,#26974,#26975,#26976,#26977,#26978,#26979,
#26980,#26981,#26982,#26983,#26984),.UNSPECIFIED.,.F.,.F.,(4,2,2,2,2,2,
2,2,2,2,2,2,2,2,2,2,2,2,2,2,2,2,2,2,2,2,2,2,2,2,2,2,2,2,2,2,2,2,2,2,2,2,
2,2,2,2,2,2,2,2,2,2,2,2,2,2,2,2,2,2,2,2,2,2,2,2,2,2,2,2,2,2,2,2,2,2,2,2,
2,2,2,2,2,2,2,2,2,2,2,2,2,2,2,2,2,2,2,2,2,2,2,2,2,4),(-1.24263702846597,
-1.21318204125405,-1.20668394162792,-1.2026079522997,-1.20117368459524,
-1.20021573497816,-1.19936036831268,-1.19819061535303,-1.19523158708895,
-1.17415333775118,-1.15625741807759,-1.14983841312723,-1.14509208811516,
-1.14292461731375,-1.14127652211616,-1.1394888621142,-1.13661397937199,
-1.12737796729563,-1.10234087453071,-1.08663332268865,-1.08454083805351,
-1.08343987270461,-1.0825252414519,-1.08137500452467,-1.07955218315156,
-1.06913547580294,-1.06066302248118,-1.04625712501536,-1.03021692183133,
-1.02696030267285,-1.0250895103207,-1.02345761023854,-1.02143585249069,
-1.01831272488349,-0.995673761011148,-0.978176214080962,-0.972051717356255,
-0.968145257884437,-0.966733947595452,-0.965780711316288,-0.96492123366464,
-0.963735312041772,-0.960712907556075,-0.942754067174463,-0.923307836845784,
-0.912396341343931,-0.909463460698849,-0.907663068389353,-0.906018596350264,
-0.90391373711316,-0.899385000741499,-0.872697190659421,-0.866911669328857,
-0.856828816303559,-0.85132266614208,-0.849722645100682,-0.84872855869881,
-0.84779814828582,-0.846666767923126,-0.843878943672105,-0.819468487625621,
-0.80374533106142,-0.797792922152787,-0.7933143730306,-0.791196025174085,
-0.789554368042603,-0.787742753837772,-0.784758625013523,-0.774491004888847,
-0.742217401027794,-0.734556201747298,-0.73271976552013,-0.731662714385639,
-0.730835309910871,-0.729675702444195,-0.727294411249541,-0.724124765209694,
-0.716157177941159,-0.69265620664322,-0.678546369365,-0.675314852353816,
-0.67343055937763,-0.671962655776449,-0.670030086160236,-0.666484890115924,
-0.641390254293036,-0.619048416234183,-0.6161506160245,-0.614985507410493,
-0.61404626461817,-0.613065956967291,-0.611529052542682,-0.606617777449525,
-0.598129789399926,-0.572459425364615,-0.560963779758772,-0.557870980775725,
-0.556035496943811,-0.554562180195069,-0.552566357253889,-0.548715797012864,
-0.527532513346686,-0.504896939276271,-0.500647391340917),.UNSPECIFIED.);
#256=B_SPLINE_CURVE_WITH_KNOTS('',3,(#26986,#26987,#26988,#26989,#26990,
#26991,#26992,#26993,#26994,#26995,#26996,#26997,#26998,#26999,#27000,#27001,
#27002,#27003,#27004,#27005,#27006,#27007,#27008,#27009,#27010,#27011,#27012,
#27013,#27014,#27015,#27016,#27017,#27018,#27019,#27020,#27021,#27022,#27023,
#27024,#27025,#27026,#27027,#27028,#27029,#27030,#27031,#27032,#27033,#27034,
#27035,#27036,#27037,#27038,#27039,#27040,#27041,#27042,#27043,#27044,#27045,
#27046,#27047,#27048,#27049,#27050,#27051,#27052,#27053,#27054,#27055,#27056,
#27057),.UNSPECIFIED.,.F.,.F.,(4,2,2,2,2,2,2,2,2,2,2,2,2,2,2,2,2,2,2,2,
2,2,2,2,2,2,2,2,2,2,2,2,2,2,2,4),(-0.242054869217963,-0.233961635944292,
-0.211059150468313,-0.208203119345212,-0.207045277770996,-0.206108043714239,
-0.205125090610733,-0.2035757841274,-0.198552110910142,-0.189774820774933,
-0.16214525028512,-0.152668588143719,-0.149765271130868,-0.147971264397082,
-0.146324848842791,-0.144296933346305,-0.139974595621538,-0.134225302276008,
-0.119377292428596,-0.0979828763116323,-0.0918935951311966,-0.0901705991383185,
-0.0891492783533216,-0.0882204133828071,-0.0869410689661844,-0.0840209540877586,
-0.0719012620377772,-0.0544965872382285,-0.036441255927238,-0.0333421070009472,
-0.0313275138753943,-0.0296959552808848,-0.0278195547636938,-0.0258572145078923,
-0.0228576454510606,-0.000340382138819982),.UNSPECIFIED.);
#257=B_SPLINE_CURVE_WITH_KNOTS('',3,(#27058,#27059,#27060,#27061,#27062,
#27063,#27064,#27065,#27066,#27067,#27068,#27069,#27070,#27071,#27072,#27073,
#27074,#27075,#27076,#27077,#27078,#27079,#27080,#27081,#27082,#27083,#27084,
#27085,#27086,#27087,#27088,#27089,#27090,#27091,#27092,#27093,#27094,#27095,
#27096,#27097,#27098,#27099,#27100,#27101,#27102,#27103,#27104,#27105,#27106,
#27107,#27108,#27109,#27110,#27111,#27112,#27113,#27114,#27115,#27116,#27117,
#27118,#27119,#27120,#27121,#27122,#27123,#27124,#27125,#27126,#27127,#27128,
#27129,#27130,#27131,#27132,#27133,#27134,#27135,#27136,#27137,#27138,#27139,
#27140,#27141,#27142,#27143,#27144,#27145,#27146,#27147,#27148,#27149,#27150,
#27151,#27152,#27153,#27154,#27155,#27156,#27157,#27158,#27159,#27160,#27161,
#27162,#27163,#27164,#27165,#27166,#27167,#27168,#27169,#27170,#27171,#27172,
#27173,#27174,#27175,#27176,#27177,#27178,#27179,#27180,#27181,#27182,#27183,
#27184,#27185,#27186,#27187,#27188,#27189,#27190,#27191,#27192,#27193,#27194,
#27195,#27196,#27197,#27198,#27199,#27200,#27201,#27202,#27203,#27204,#27205,
#27206,#27207,#27208,#27209,#27210,#27211),.UNSPECIFIED.,.F.,.F.,(4,2,2,
2,2,2,2,2,2,2,2,2,2,2,2,2,2,2,2,2,2,2,2,2,2,2,2,2,2,2,2,2,2,2,2,2,2,2,2,
2,2,2,2,2,2,2,2,2,2,2,2,2,2,2,2,2,2,2,2,2,2,2,2,2,2,2,2,2,2,2,2,2,2,2,2,
2,4),(-1.48458759282926,-1.46058697544366,-1.45866771350882,-1.45747422433994,
-1.45636704735927,-1.45545247293161,-1.45430884437518,-1.45250830884724,
-1.44255926386911,-1.43962645768021,-1.4331831010642,-1.41717709970874,
-1.40296091072758,-1.39991153561542,-1.39834225269685,-1.3967251338865,
-1.39485812141508,-1.39170288973667,-1.37881620306246,-1.35128299416862,
-1.34501066975361,-1.34105977743947,-1.33962819745971,-1.33867058345057,
-1.33781439048956,-1.33664210027279,-1.33369368708015,-1.31251888695154,
-1.29467382174839,-1.28826405676497,-1.28352256866965,-1.28135551600932,
-1.27970701794204,-1.27791822129416,-1.27503996664619,-1.26577836806808,
-1.24074880814399,-1.22504151992479,-1.22294838556946,-1.22184705434025,
-1.22093210743715,-1.21978146648348,-1.21795799648213,-1.20753775159071,
-1.19905887010152,-1.18464396698514,-1.16860045217859,-1.16534277370507,
-1.16347134788721,-1.16183888288917,-1.15981641163107,-1.15669216159334,
-1.13399890515511,-1.11661311965169,-1.11043880635247,-1.10650906136972,
-1.10509423407258,-1.10414004559071,-1.10328082915723,-1.10209669380087,
-1.0990864434082,-1.08014901481529,-1.06139257796928,-1.05069311927257,
-1.04777743005807,-1.04598038395088,-1.04433422133456,-1.04222062911883,
-1.03764662189543,-1.01169550990352,-0.996854830014449,-0.992186646215384,
-0.988986906274839,-0.987681081609704,-0.986747645672439,-0.98573699111287,
-0.984187833277004),.UNSPECIFIED.);
#258=B_SPLINE_CURVE_WITH_KNOTS('',3,(#27217,#27218,#27219,#27220,#27221,
#27222,#27223,#27224,#27225,#27226,#27227,#27228,#27229,#27230,#27231,#27232,
#27233,#27234,#27235,#27236,#27237,#27238,#27239,#27240,#27241,#27242,#27243,
#27244,#27245,#27246,#27247,#27248,#27249,#27250,#27251,#27252,#27253,#27254,
#27255,#27256,#27257,#27258,#27259,#27260,#27261,#27262,#27263,#27264,#27265,
#27266,#27267,#27268,#27269,#27270,#27271,#27272,#27273,#27274,#27275,#27276,
#27277,#27278,#27279,#27280,#27281,#27282,#27283,#27284,#27285,#27286,#27287,
#27288,#27289,#27290,#27291,#27292,#27293,#27294,#27295,#27296,#27297,#27298,
#27299,#27300,#27301,#27302,#27303,#27304,#27305,#27306,#27307,#27308,#27309,
#27310,#27311,#27312,#27313,#27314,#27315,#27316,#27317,#27318,#27319,#27320,
#27321,#27322,#27323,#27324,#27325,#27326,#27327,#27328,#27329,#27330,#27331,
#27332,#27333,#27334,#27335,#27336,#27337,#27338,#27339,#27340,#27341,#27342,
#27343,#27344,#27345,#27346,#27347,#27348,#27349,#27350,#27351,#27352,#27353,
#27354,#27355,#27356,#27357,#27358,#27359,#27360,#27361,#27362,#27363,#27364,
#27365,#27366,#27367,#27368,#27369,#27370,#27371,#27372),.UNSPECIFIED.,
 .F.,.F.,(4,2,2,2,2,2,2,2,2,2,2,2,2,2,2,2,2,2,2,2,2,2,2,2,2,2,2,2,2,2,2,
2,2,2,2,2,2,2,2,2,2,2,2,2,2,2,2,2,2,2,2,2,2,2,2,2,2,2,2,2,2,2,2,2,2,2,2,
2,2,2,2,2,2,2,2,2,2,4),(-0.500904416667459,-0.488914936864186,-0.482753931044674,
-0.480282045965134,-0.478749662876254,-0.477078835279314,-0.474773500539124,
-0.469223350727045,-0.448226833297894,-0.424766938789263,-0.421933650815843,
-0.42077966519421,-0.419843357066977,-0.418858654971897,-0.41730180004511,
-0.412210393844688,-0.403256835821251,-0.372993911786864,-0.365820246994291,
-0.363198158870924,-0.361637886018321,-0.359985417112075,-0.357790528858627,
-0.352892711957206,-0.346204284411774,-0.312830303232384,-0.305749199823953,
-0.303936007185761,-0.302894683371461,-0.301971508569885,-0.300732312691038,
-0.297925247255231,-0.285246569714141,-0.281204120939117,-0.251379284141169,
-0.247161814559687,-0.245092965453389,-0.243456571176483,-0.241616284144362,
-0.238501868889925,-0.225100708636843,-0.208788184800751,-0.190471595618797,
-0.187462636303479,-0.186278755528788,-0.185419642396299,-0.184465455524613,
-0.183050439980223,-0.179118832938403,-0.172941019127285,-0.155577318348858,
-0.132903586014866,-0.129779571939499,-0.127757229975083,-0.126202956225671,
-0.124401598177523,-0.122500883026045,-0.119651487100752,-0.114420828537869,
-0.10165075677646,-0.0830288291128392,-0.0787527746289728,-0.0713027843680808,
-0.0694816105326993,-0.0684279823263795,-0.067599904919146,-0.0664349943354398,
-0.0640269665966417,-0.0608114600192663,-0.0526697262820125,-0.0229582393288504,
-0.0143963324163041,-0.0115986933566161,-0.00982746605347513,-0.00825927673259034,
-0.00665175994948807,-0.00386382252695999,-0.000340186971329014),
 .UNSPECIFIED.);
#259=B_SPLINE_CURVE_WITH_KNOTS('',3,(#27373,#27374,#27375,#27376,#27377,
#27378,#27379,#27380,#27381,#27382,#27383,#27384,#27385,#27386,#27387,#27388,
#27389,#27390,#27391,#27392,#27393,#27394,#27395,#27396,#27397,#27398,#27399,
#27400,#27401,#27402,#27403,#27404,#27405,#27406,#27407,#27408,#27409,#27410,
#27411,#27412,#27413,#27414,#27415,#27416,#27417,#27418,#27419,#27420,#27421,
#27422,#27423,#27424,#27425,#27426,#27427,#27428,#27429,#27430,#27431,#27432,
#27433,#27434,#27435,#27436,#27437,#27438,#27439,#27440,#27441,#27442,#27443,
#27444),.UNSPECIFIED.,.F.,.F.,(4,2,2,2,2,2,2,2,2,2,2,2,2,2,2,2,2,2,2,2,
2,2,2,2,2,2,2,2,2,2,2,2,2,2,2,4),(-1.48415219493652,-1.45250665935878,-1.43944929105978,
-1.43660293167591,-1.43535716127721,-1.43443347557021,-1.43339645273249,
-1.43160142939977,-1.42472731610342,-1.39388168211648,-1.38566028126054,
-1.3817626330946,-1.3794336443774,-1.37740835295126,-1.37581764842499,-1.37406145438945,
-1.37133086339452,-1.3633397768778,-1.33411460502419,-1.32516815228624,
-1.32008057132548,-1.31852452873993,-1.31754027375196,-1.31660432588514,
-1.31545073133081,-1.31261810310143,-1.28919955682737,-1.2728623832405,
-1.26677319357932,-1.26221562455362,-1.26008281571874,-1.25843959769232,
-1.25663592016143,-1.25368706467827,-1.24377101569511,-1.24263702846597),
 .UNSPECIFIED.);
#260=B_SPLINE_CURVE_WITH_KNOTS('',3,(#27445,#27446,#27447,#27448,#27449,
#27450,#27451,#27452,#27453,#27454,#27455,#27456,#27457,#27458,#27459,#27460,
#27461,#27462,#27463,#27464,#27465,#27466,#27467,#27468,#27469,#27470,#27471,
#27472,#27473,#27474,#27475,#27476,#27477,#27478,#27479,#27480,#27481,#27482,
#27483,#27484,#27485,#27486,#27487,#27488,#27489,#27490,#27491,#27492,#27493,
#27494,#27495,#27496,#27497,#27498,#27499,#27500,#27501,#27502,#27503,#27504,
#27505,#27506,#27507,#27508,#27509,#27510,#27511,#27512,#27513,#27514,#27515,
#27516,#27517,#27518,#27519,#27520,#27521,#27522,#27523,#27524,#27525,#27526,
#27527,#27528,#27529,#27530,#27531,#27532,#27533,#27534,#27535,#27536,#27537,
#27538,#27539,#27540,#27541,#27542,#27543,#27544,#27545,#27546,#27547,#27548,
#27549,#27550,#27551,#27552,#27553,#27554,#27555,#27556,#27557,#27558,#27559,
#27560,#27561,#27562,#27563,#27564,#27565,#27566,#27567,#27568,#27569,#27570,
#27571,#27572,#27573,#27574,#27575,#27576,#27577,#27578,#27579,#27580,#27581,
#27582,#27583,#27584,#27585,#27586,#27587,#27588,#27589,#27590,#27591,#27592,
#27593,#27594,#27595,#27596,#27597,#27598,#27599,#27600,#27601,#27602,#27603,
#27604,#27605,#27606,#27607,#27608,#27609,#27610,#27611,#27612,#27613,#27614,
#27615,#27616,#27617,#27618,#27619,#27620,#27621,#27622,#27623,#27624,#27625,
#27626,#27627,#27628,#27629,#27630,#27631,#27632,#27633,#27634,#27635,#27636,
#27637,#27638,#27639,#27640,#27641,#27642,#27643,#27644,#27645,#27646,#27647,
#27648,#27649,#27650,#27651,#27652),.UNSPECIFIED.,.F.,.F.,(4,2,2,2,2,2,
2,2,2,2,2,2,2,2,2,2,2,2,2,2,2,2,2,2,2,2,2,2,2,2,2,2,2,2,2,2,2,2,2,2,2,2,
2,2,2,2,2,2,2,2,2,2,2,2,2,2,2,2,2,2,2,2,2,2,2,2,2,2,2,2,2,2,2,2,2,2,2,2,
2,2,2,2,2,2,2,2,2,2,2,2,2,2,2,2,2,2,2,2,2,2,2,2,2,4),(-0.984187833277004,
-0.984063074238169,-0.978450970218995,-0.946255889702368,-0.933671315699779,
-0.930610757768473,-0.928782191797354,-0.927143696133262,-0.925055065774211,
-0.920735070982084,-0.891741437880094,-0.873935118102472,-0.871384090055669,
-0.870191716335036,-0.869282132623342,-0.868215878699228,-0.866339583889734,
-0.858088985999228,-0.837676606763139,-0.820197434904205,-0.814744510263714,
-0.812454814896139,-0.810786564171258,-0.809250462259531,-0.807161527518278,
-0.803003906840926,-0.77798118750282,-0.77051401785999,-0.757155451106151,
-0.754276937838385,-0.753025141909919,-0.752100220133899,-0.75106540712829,
-0.749281982408049,-0.742548236253123,-0.728171352650195,-0.7015813823746,
-0.697045603661932,-0.694939064384009,-0.693293943636355,-0.691493518778946,
-0.688562133239908,-0.677676895975676,-0.658323046831343,-0.64018079092848,
-0.637166050881948,-0.635981179168268,-0.635121788266104,-0.634167829492333,
-0.632754073338513,-0.628831920967881,-0.622674892176426,-0.605285878494386,
-0.58259625897793,-0.579472349815046,-0.577449988229246,-0.575817552172951,
-0.573946093869864,-0.570688196814293,-0.55464255837595,-0.54021471160418,
-0.53172765678937,-0.52130373187606,-0.519480018465419,-0.518329317488355,
-0.517414378642223,-0.516313118986224,-0.514220301059465,-0.498519026007381,
-0.473499990978974,-0.464245763688528,-0.461368314635313,-0.459579682783899,
-0.457931109566543,-0.455763626331094,-0.451019864790236,-0.444605354592505,
-0.426737993928148,-0.405567813974401,-0.402610270336967,-0.401440491180134,
-0.4005849028065,-0.399626451261733,-0.398191010520867,-0.394108732576942,
-0.387598496056274,-0.356823131798161,-0.347073816342459,-0.344142871193565,
-0.342342624871686,-0.340697604766851,-0.338555393741221,-0.333949853585836,
-0.327777430014588,-0.311063999139821,-0.288157727357864,-0.285301208436593,
-0.284143170112735,-0.283205777201962,-0.282222657999818,-0.28067309059857,
-0.275648579221517,-0.266869835047864,-0.24195210917092),.UNSPECIFIED.);
#261=B_SPLINE_CURVE_WITH_KNOTS('',3,(#27657,#27658,#27659,#27660,#27661,
#27662,#27663,#27664,#27665,#27666,#27667,#27668,#27669,#27670,#27671,#27672,
#27673,#27674,#27675,#27676,#27677,#27678,#27679,#27680,#27681,#27682,#27683,
#27684,#27685,#27686,#27687,#27688,#27689,#27690,#27691,#27692,#27693,#27694,
#27695,#27696,#27697,#27698,#27699,#27700,#27701,#27702,#27703,#27704,#27705,
#27706,#27707,#27708,#27709,#27710,#27711,#27712,#27713,#27714,#27715,#27716,
#27717,#27718,#27719,#27720,#27721,#27722,#27723,#27724,#27725,#27726,#27727,
#27728,#27729,#27730,#27731,#27732,#27733,#27734,#27735,#27736,#27737,#27738,
#27739,#27740,#27741,#27742,#27743,#27744,#27745,#27746,#27747,#27748,#27749,
#27750,#27751,#27752,#27753,#27754,#27755,#27756,#27757,#27758,#27759,#27760,
#27761,#27762,#27763,#27764,#27765,#27766,#27767,#27768,#27769,#27770,#27771,
#27772,#27773,#27774,#27775,#27776,#27777,#27778,#27779,#27780,#27781,#27782,
#27783,#27784,#27785,#27786,#27787,#27788,#27789,#27790,#27791,#27792,#27793,
#27794,#27795,#27796,#27797,#27798,#27799,#27800,#27801,#27802,#27803,#27804,
#27805,#27806,#27807,#27808,#27809,#27810,#27811,#27812,#27813,#27814,#27815,
#27816,#27817,#27818,#27819,#27820,#27821,#27822,#27823,#27824,#27825,#27826,
#27827,#27828,#27829,#27830,#27831,#27832,#27833,#27834,#27835,#27836,#27837,
#27838,#27839,#27840,#27841,#27842,#27843,#27844,#27845,#27846,#27847,#27848,
#27849,#27850,#27851,#27852,#27853,#27854,#27855,#27856,#27857,#27858,#27859,
#27860,#27861,#27862,#27863,#27864,#27865,#27866,#27867,#27868,#27869,#27870,
#27871,#27872,#27873,#27874,#27875,#27876),.UNSPECIFIED.,.F.,.F.,(4,2,2,
2,2,2,2,2,2,2,2,2,2,2,2,2,2,2,2,2,2,2,2,2,2,2,2,2,2,2,2,2,2,2,2,2,2,2,2,
2,2,2,2,2,2,2,2,2,2,2,2,2,2,2,2,2,2,2,2,2,2,2,2,2,2,2,2,2,2,2,2,2,2,2,2,
2,2,2,2,2,2,2,2,2,2,2,2,2,2,2,2,2,2,2,2,2,2,2,2,2,2,2,2,2,2,2,2,2,2,4),
(-1.24297521476333,-1.24178430330719,-1.2407892377459,-1.2398594153016,
-1.23873030622846,-1.23584128673268,-1.21225132719135,-1.19602034423567,
-1.18995416829667,-1.18540971178841,-1.1832791163697,-1.18163595351687,
-1.17983068646783,-1.176875451765,-1.16690786539197,-1.136369321897,-1.12987381025455,
-1.12579878310798,-1.12436449258101,-1.12340642663823,-1.12255087799421,
-1.12138077834746,-1.11845314324577,-1.09686490306256,-1.07931013273746,
-1.07296052444913,-1.06825343285418,-1.06609284780836,-1.06444550374562,
-1.06265427832567,-1.05976392697298,-1.05038554422044,-1.01919080192893,
-1.0126523011671,-1.00855791829819,-1.00712096149052,-1.00616227001806,
-1.00530705435517,-1.00413852527222,-1.00118876385751,-0.979881373816018,
-0.970179038659431,-0.959040382489031,-0.9542549889917,-0.95047733223311,
-0.948496383874068,-0.947024558171151,-0.945178625829668,-0.942037900888435,
-0.929941866463692,-0.904800335910472,-0.896402661586025,-0.893120935736141,
-0.890674791609677,-0.889502513112402,-0.888586405601287,-0.887502614532241,
-0.885548408230798,-0.875951478474062,-0.847727392713301,-0.835664287092581,
-0.832641003931838,-0.830820673514944,-0.829180684903721,-0.827077848656834,
-0.82268265679223,-0.794400138325365,-0.789120013035911,-0.779642858053847,
-0.77435557114362,-0.772777799555301,-0.771788497314846,-0.770855059290487,
-0.769497243191671,-0.766939491179242,-0.742639181609929,-0.719225679507449,
-0.716092905355166,-0.714067982967697,-0.71243553693369,-0.710566318056714,
-0.707318141091196,-0.6914732664365,-0.667192625678609,-0.657814376218448,
-0.655871527380021,-0.654790284353407,-0.653873914277331,-0.652698202928157,
-0.650234293968244,-0.646922062453605,-0.638405858242854,-0.612559902350962,
-0.601252591386285,-0.598173839350377,-0.596341369014647,-0.594867498273093,
-0.592867005260843,-0.588993687962437,-0.584053049682493,-0.572359328853213,
-0.550729594376325,-0.540644767981708,-0.538834996304174,-0.537688545525651,
-0.536773825614432,-0.535669009110655,-0.533558934009499,-0.516791755470417,
-0.500904416667459),.UNSPECIFIED.);
#262=B_SPLINE_CURVE_WITH_KNOTS('',3,(#27878,#27879,#27880,#27881,#27882,
#27883,#27884,#27885,#27886,#27887,#27888,#27889,#27890,#27891,#27892,#27893,
#27894,#27895,#27896,#27897,#27898,#27899,#27900,#27901,#27902,#27903,#27904,
#27905,#27906,#27907,#27908,#27909,#27910,#27911,#27912,#27913,#27914,#27915,
#27916,#27917,#27918,#27919,#27920,#27921,#27922,#27923,#27924,#27925,#27926,
#27927,#27928,#27929,#27930,#27931,#27932,#27933,#27934,#27935,#27936,#27937,
#27938,#27939,#27940,#27941,#27942,#27943,#27944,#27945,#27946,#27947,#27948,
#27949,#27950,#27951,#27952,#27953,#27954,#27955,#27956,#27957,#27958,#27959,
#27960,#27961,#27962,#27963,#27964,#27965,#27966,#27967,#27968,#27969,#27970,
#27971,#27972,#27973),.UNSPECIFIED.,.F.,.F.,(4,2,2,2,2,2,2,2,2,2,2,2,2,
2,2,2,2,2,2,2,2,2,2,2,2,2,2,2,2,2,2,2,2,2,2,2,2,2,2,2,2,2,2,2,2,2,2,4),
(-0.24195210917092,-0.238328488327181,-0.229588572179531,-0.226768044860348,
-0.224991863617181,-0.223339128956458,-0.221142891645517,-0.216237812400091,
-0.209536522718923,-0.190201936325325,-0.17111711888477,-0.168109251654614,
-0.166925582219484,-0.166066547761138,-0.165112362510809,-0.163697210693321,
-0.159764343264134,-0.153583735231869,-0.127098530275104,-0.113201832761435,
-0.109963132552584,-0.108077153460812,-0.106515775731751,-0.106468973102604,
-0.106426895041746,-0.106388872976778,-0.106354360927049,-0.106322908301707,
-0.106294139580394,-0.106267739191376,-0.106243439735482,-0.106221013094132,
-0.106200263406243,-0.106181021379253,-0.104140310014139,-0.10185746950122,
-0.0980749726181405,-0.0902054561595218,-0.0762115215929237,-0.0536776523592188,
-0.0507964390220819,-0.0496341658065563,-0.0486956722841141,-0.0477142621794448,
-0.0461723714497,-0.0412167655535401,-0.0326156466268484,-0.000340676557468298),
 .UNSPECIFIED.);
#263=B_SPLINE_CURVE_WITH_KNOTS('',3,(#27974,#27975,#27976,#27977,#27978,
#27979,#27980,#27981,#27982,#27983,#27984,#27985,#27986,#27987,#27988,#27989,
#27990,#27991,#27992,#27993,#27994,#27995,#27996,#27997,#27998,#27999,#28000,
#28001,#28002,#28003,#28004,#28005,#28006,#28007,#28008,#28009,#28010,#28011,
#28012,#28013,#28014,#28015,#28016,#28017,#28018,#28019,#28020,#28021,#28022,
#28023,#28024,#28025,#28026,#28027,#28028,#28029,#28030,#28031,#28032,#28033,
#28034,#28035,#28036,#28037,#28038,#28039,#28040,#28041,#28042,#28043,#28044,
#28045,#28046,#28047,#28048,#28049,#28050,#28051,#28052,#28053,#28054,#28055,
#28056,#28057,#28058,#28059,#28060,#28061,#28062,#28063,#28064,#28065,#28066,
#28067,#28068,#28069,#28070,#28071,#28072,#28073,#28074,#28075,#28076,#28077,
#28078,#28079,#28080,#28081,#28082,#28083,#28084,#28085,#28086,#28087,#28088,
#28089,#28090,#28091,#28092,#28093,#28094,#28095,#28096,#28097,#28098,#28099,
#28100,#28101,#28102,#28103,#28104,#28105,#28106,#28107,#28108,#28109,#28110,
#28111,#28112,#28113,#28114,#28115,#28116,#28117,#28118,#28119,#28120,#28121,
#28122,#28123,#28124,#28125,#28126,#28127,#28128,#28129,#28130,#28131),
 .UNSPECIFIED.,.F.,.F.,(4,2,2,2,2,2,2,2,2,2,2,2,2,2,2,2,2,2,2,2,2,2,2,2,
2,2,2,2,2,2,2,2,2,2,2,2,2,2,2,2,2,2,2,2,2,2,2,2,2,2,2,2,2,2,2,2,2,2,2,2,
2,2,2,2,2,2,2,2,2,2,2,2,2,2,2,2,2,2,4),(-1.48414639998802,-1.47879596711116,
-1.47672811482419,-1.47513078917331,-1.47355491489769,-1.47176712386732,
-1.46889001650299,-1.45962481974856,-1.4303154511884,-1.42248294561508,
-1.4193496963634,-1.4169900760554,-1.41583505940126,-1.4150084929214,-1.41394912438853,
-1.41210121870852,-1.40426639083598,-1.38357072828186,-1.36965356907349,
-1.36413094592819,-1.3611725882687,-1.35922749315818,-1.35785980986077,
-1.3562535279143,-1.35443282884722,-1.35140522134449,-1.34081341629944,
-1.31097581125902,-1.30452929211255,-1.3004765952843,-1.29904557068101,
-1.2980883975217,-1.29723265241524,-1.29606104276559,-1.29312323915568,
-1.27179471894925,-1.25407071477623,-1.24768703116408,-1.24296089283786,
-1.24079726407342,-1.23914991497618,-1.23736094604149,-1.23447926685457,
-1.22517629163125,-1.20019888619625,-1.18451474018673,-1.18242292043329,
-1.18132219180586,-1.18040769389663,-1.17925755260603,-1.177434755803,-1.16701401108436,
-1.15852001135506,-1.14406096663784,-1.12809609592202,-1.12484330607293,
-1.12297351262465,-1.12134178294259,-1.11931933073128,-1.11619339605062,
-1.09364164715054,-1.07657104027939,-1.0701293754927,-1.066078771608,-1.06464795804046,
-1.06369077751449,-1.0628349108017,-1.06166299032605,-1.05871614006145,
-1.03754977192699,-1.01971235405795,-1.01330529838588,-1.00856580598276,
-1.00639965774219,-1.0047518445645,-1.00296378806579,-1.00008671764343,
-0.990828864930486,-0.983855788104838),.UNSPECIFIED.);
#264=B_SPLINE_CURVE_WITH_KNOTS('',3,(#28137,#28138,#28139,#28140,#28141,
#28142,#28143,#28144,#28145,#28146,#28147,#28148,#28149,#28150,#28151,#28152,
#28153,#28154,#28155,#28156,#28157,#28158,#28159,#28160,#28161,#28162,#28163,
#28164,#28165,#28166,#28167,#28168,#28169,#28170,#28171,#28172,#28173,#28174,
#28175,#28176,#28177,#28178,#28179,#28180,#28181,#28182,#28183,#28184,#28185,
#28186,#28187,#28188,#28189,#28190,#28191,#28192,#28193,#28194,#28195,#28196,
#28197,#28198,#28199,#28200,#28201,#28202,#28203,#28204,#28205,#28206,#28207,
#28208,#28209,#28210,#28211,#28212,#28213,#28214,#28215,#28216,#28217,#28218,
#28219,#28220,#28221,#28222,#28223,#28224,#28225,#28226,#28227,#28228,#28229,
#28230,#28231,#28232,#28233,#28234,#28235,#28236,#28237,#28238,#28239,#28240,
#28241,#28242,#28243,#28244,#28245,#28246,#28247,#28248,#28249,#28250,#28251,
#28252,#28253,#28254,#28255,#28256,#28257,#28258,#28259,#28260,#28261,#28262,
#28263,#28264,#28265,#28266,#28267,#28268,#28269,#28270,#28271,#28272,#28273,
#28274,#28275,#28276,#28277,#28278,#28279,#28280,#28281,#28282,#28283,#28284,
#28285,#28286,#28287,#28288,#28289,#28290,#28291,#28292,#28293,#28294,#28295,
#28296,#28297,#28298,#28299,#28300,#28301,#28302,#28303,#28304,#28305,#28306,
#28307,#28308,#28309,#28310,#28311,#28312),.UNSPECIFIED.,.F.,.F.,(4,2,2,
2,2,2,2,2,2,2,2,2,2,2,2,2,2,2,2,2,2,2,2,2,2,2,2,2,2,2,2,2,2,2,2,2,2,2,2,
2,2,2,2,2,2,2,2,2,2,2,2,2,2,2,2,2,2,2,2,2,2,2,2,2,2,2,2,2,2,2,2,2,2,2,2,
2,2,2,2,2,2,2,2,2,2,2,2,4),(-0.500748493306363,-0.49428692095435,-0.484922197772312,
-0.464917275796128,-0.461933188638434,-0.460753645807397,-0.459895791679644,
-0.458940716612863,-0.457520474447514,-0.453548867408227,-0.447282813202204,
-0.433688506878275,-0.409274829434102,-0.404640682058993,-0.402516634232706,
-0.400869454990949,-0.399078454711964,-0.396188568931295,-0.385778132769649,
-0.365340749507521,-0.35778139146162,-0.352681271788409,-0.34574068117324,
-0.343939730573339,-0.342901304730169,-0.341977787907235,-0.340734188676198,
-0.337900836587531,-0.324970390781765,-0.31596860700133,-0.292093305837505,
-0.287443722188799,-0.285316879102415,-0.283669285805314,-0.281879589823099,
-0.27899570893954,-0.268653041192708,-0.248463825045924,-0.23054057302486,
-0.227528186485945,-0.226343923968489,-0.225484866009631,-0.224531141102751,
-0.223117492994218,-0.219194088543173,-0.213033507100442,-0.195658058721139,
-0.172981378241405,-0.169858574019207,-0.167836891831768,-0.166204978352811,
-0.164334088730973,-0.161077096032481,-0.145032875160836,-0.121429840704774,
-0.111647275020201,-0.109678777977246,-0.108591909625912,-0.107704495495276,
-0.107698414936022,-0.107692449169858,-0.107686594814106,-0.107680848348299,
-0.107675206756756,-0.107669666820321,-0.107664225280265,-0.107658879427332,
-0.107653626655327,-0.107648464394768,-0.107643389723269,-0.107638399987156,
-0.107633493353716,-0.10762866745188,-0.10762391987864,-0.107619248728151,
-0.106453069992474,-0.105145280717095,-0.102942585751177,-0.0982663456840263,
-0.0833750968508959,-0.0575424237070847,-0.0529662632000266,-0.0508527080196141,
-0.0492069928625414,-0.0474108571577775,-0.0444975950420383,-0.0338192939406861,
-0.0003407532546169),.UNSPECIFIED.);
#265=B_SPLINE_CURVE_WITH_KNOTS('',3,(#28313,#28314,#28315,#28316,#28317,
#28318,#28319,#28320,#28321,#28322,#28323,#28324,#28325,#28326,#28327,#28328,
#28329,#28330,#28331,#28332,#28333,#28334,#28335,#28336,#28337,#28338,#28339,
#28340,#28341,#28342,#28343,#28344,#28345,#28346,#28347,#28348,#28349,#28350,
#28351,#28352,#28353,#28354,#28355,#28356,#28357,#28358,#28359,#28360,#28361,
#28362,#28363,#28364,#28365,#28366,#28367,#28368,#28369,#28370,#28371,#28372,
#28373,#28374,#28375,#28376,#28377,#28378,#28379,#28380,#28381,#28382,#28383,
#28384,#28385,#28386,#28387,#28388,#28389,#28390),.UNSPECIFIED.,.F.,.F.,
(4,2,2,2,2,2,2,2,2,2,2,2,2,2,2,2,2,2,2,2,2,2,2,2,2,2,2,2,2,2,2,2,2,2,2,
2,2,2,4),(-1.4845396710087,-1.47825139841739,-1.47693547624366,-1.47598577733424,
-1.47512798895945,-1.4742724086583,-1.47310213361687,-1.47014318743695,
-1.46279099408039,-1.43184755347238,-1.42158280980162,-1.41870593319078,
-1.41691775279343,-1.41526965765706,-1.41313950038778,-1.40847165261581,
-1.38564972473863,-1.36850507613455,-1.36345178115162,-1.3611272845425,
-1.35977109015024,-1.35856925747271,-1.35766369141969,-1.35662573750668,
-1.35482701010589,-1.34791232985656,-1.31710109178158,-1.30888142439269,
-1.30316099809011,-1.30082880731301,-1.29915345656426,-1.29762709434516,
-1.29557602800734,-1.29054642150204,-1.26148084161633,-1.2591535564171,
-1.24894087425676,-1.24338887098085,-1.24297521476333),.UNSPECIFIED.);
#266=B_SPLINE_CURVE_WITH_KNOTS('',3,(#28391,#28392,#28393,#28394,#28395,
#28396,#28397,#28398,#28399,#28400,#28401,#28402,#28403,#28404,#28405,#28406,
#28407,#28408,#28409,#28410,#28411,#28412,#28413,#28414,#28415,#28416,#28417,
#28418,#28419,#28420,#28421,#28422,#28423,#28424,#28425,#28426,#28427,#28428,
#28429,#28430,#28431,#28432,#28433,#28434,#28435,#28436,#28437,#28438,#28439,
#28440,#28441,#28442,#28443,#28444,#28445,#28446,#28447,#28448,#28449,#28450,
#28451,#28452,#28453,#28454,#28455,#28456,#28457,#28458,#28459,#28460,#28461,
#28462,#28463,#28464,#28465,#28466,#28467,#28468,#28469,#28470,#28471,#28472,
#28473,#28474,#28475,#28476,#28477,#28478,#28479,#28480,#28481,#28482,#28483,
#28484,#28485,#28486,#28487,#28488,#28489,#28490,#28491,#28492,#28493,#28494,
#28495,#28496,#28497,#28498,#28499,#28500,#28501,#28502,#28503,#28504,#28505,
#28506,#28507,#28508,#28509,#28510,#28511,#28512,#28513,#28514,#28515,#28516,
#28517,#28518,#28519,#28520,#28521,#28522,#28523,#28524,#28525,#28526,#28527,
#28528,#28529,#28530,#28531,#28532,#28533,#28534,#28535,#28536,#28537,#28538,
#28539,#28540,#28541,#28542,#28543,#28544,#28545,#28546,#28547,#28548,#28549,
#28550,#28551,#28552,#28553,#28554,#28555,#28556,#28557,#28558,#28559,#28560,
#28561,#28562,#28563,#28564,#28565,#28566,#28567,#28568,#28569,#28570,#28571,
#28572,#28573,#28574,#28575,#28576,#28577,#28578,#28579,#28580,#28581,#28582,
#28583,#28584,#28585,#28586,#28587,#28588,#28589,#28590,#28591,#28592,#28593,
#28594,#28595,#28596,#28597,#28598,#28599,#28600,#28601,#28602,#28603,#28604,
#28605,#28606),.UNSPECIFIED.,.F.,.F.,(4,2,2,2,2,2,2,2,2,2,2,2,2,2,2,2,2,
2,2,2,2,2,2,2,2,2,2,2,2,2,2,2,2,2,2,2,2,2,2,2,2,2,2,2,2,2,2,2,2,2,2,2,2,
2,2,2,2,2,2,2,2,2,2,2,2,2,2,2,2,2,2,2,2,2,2,2,2,2,2,2,2,2,2,2,2,2,2,2,2,
2,2,2,2,2,2,2,2,2,2,2,2,2,2,2,2,2,2,4),(-0.983855788104838,-0.965809777789558,
-0.950109041312935,-0.948016776262846,-0.946915902240519,-0.946001335059476,
-0.944851171507917,-0.943028457812708,-0.932612525586969,-0.924135814794796,
-0.903475602414132,-0.896535907110599,-0.891498414251561,-0.889279396724808,
-0.887623518238953,-0.886070729696273,-0.883486783921482,-0.876579308626038,
-0.846070805215775,-0.837035067306361,-0.833592482985266,-0.831054356812462,
-0.829864673453913,-0.828947366190847,-0.827876601616018,-0.825979424848689,
-0.817387058739746,-0.792773610314513,-0.776467420910509,-0.773198765935964,
-0.771325413425742,-0.769693821747222,-0.76767573005686,-0.764564561227109,
-0.742158727986369,-0.718372188321029,-0.714458202767508,-0.713001840444135,
-0.712134793876668,-0.711189080498951,-0.709815355129405,-0.706172999867635,
-0.700611864858019,-0.680893449506599,-0.659613177578876,-0.656474670260101,
-0.654448205543137,-0.652815917961458,-0.650948414851934,-0.647707187672623,
-0.631999140297674,-0.608990551083149,-0.598315311597118,-0.596481949013811,
-0.595328493033816,-0.594413654402313,-0.593315262268302,-0.591235337667744,
-0.576174440874272,-0.552773189977835,-0.541623316051212,-0.538557176063239,
-0.53672768106786,-0.535089855039159,-0.533004139294621,-0.528697725471281,
-0.512076598720576,-0.506718548796849,-0.482318524299208,-0.479768087862753,
-0.478412319073975,-0.477479380395934,-0.476489669375229,-0.474909575517582,
-0.469598277720327,-0.4600563960465,-0.45254867384428,-0.426917611851322,
-0.422331241682865,-0.420215792150934,-0.418569775819305,-0.416774497920194,
-0.41386529928985,-0.403235032277134,-0.384690536708838,-0.365441217666579,
-0.362436574851348,-0.361253558961388,-0.360394786799302,-0.359440636924612,
-0.358025101151982,-0.354088342340681,-0.347898825130568,-0.330550558740069,
-0.307885384806987,-0.304762317169975,-0.302740494935786,-0.301108490709808,
-0.299237523593117,-0.295980471554556,-0.279938725486797,-0.265514938704909,
-0.257030275753172,-0.246609090184405,-0.244785858177224,-0.243635461160612,
-0.24272076414252,-0.241877241928533),.UNSPECIFIED.);
#267=B_SPLINE_CURVE_WITH_KNOTS('',3,(#28611,#28612,#28613,#28614,#28615,
#28616,#28617,#28618,#28619,#28620,#28621,#28622,#28623,#28624,#28625,#28626,
#28627,#28628,#28629,#28630,#28631,#28632,#28633,#28634,#28635,#28636,#28637,
#28638,#28639,#28640,#28641,#28642,#28643,#28644,#28645,#28646,#28647,#28648,
#28649,#28650,#28651,#28652,#28653,#28654,#28655,#28656,#28657,#28658,#28659,
#28660,#28661,#28662,#28663,#28664,#28665,#28666,#28667,#28668,#28669,#28670,
#28671,#28672,#28673,#28674,#28675,#28676,#28677,#28678,#28679,#28680,#28681,
#28682,#28683,#28684,#28685,#28686,#28687,#28688,#28689,#28690,#28691,#28692,
#28693,#28694,#28695,#28696,#28697,#28698,#28699,#28700,#28701,#28702,#28703,
#28704,#28705,#28706,#28707,#28708,#28709,#28710,#28711,#28712,#28713,#28714,
#28715,#28716,#28717,#28718,#28719,#28720,#28721,#28722,#28723,#28724,#28725,
#28726,#28727,#28728,#28729,#28730,#28731,#28732,#28733,#28734,#28735,#28736,
#28737,#28738,#28739,#28740,#28741,#28742,#28743,#28744,#28745,#28746,#28747,
#28748,#28749,#28750,#28751,#28752,#28753,#28754,#28755,#28756,#28757,#28758,
#28759,#28760,#28761,#28762,#28763,#28764,#28765,#28766,#28767,#28768,#28769,
#28770,#28771,#28772,#28773,#28774,#28775,#28776,#28777,#28778,#28779,#28780,
#28781,#28782,#28783,#28784,#28785,#28786,#28787,#28788,#28789,#28790,#28791,
#28792,#28793,#28794,#28795,#28796,#28797,#28798,#28799,#28800,#28801,#28802,
#28803,#28804,#28805,#28806,#28807,#28808,#28809,#28810,#28811,#28812,#28813,
#28814,#28815,#28816,#28817,#28818,#28819,#28820,#28821,#28822,#28823,#28824,
#28825,#28826,#28827,#28828,#28829,#28830,#28831,#28832,#28833,#28834),
 .UNSPECIFIED.,.F.,.F.,(4,2,2,2,2,2,2,2,2,2,2,2,2,2,2,2,2,2,2,2,2,2,2,2,
2,2,2,2,2,2,2,2,2,2,2,2,2,2,2,2,2,2,2,2,2,2,2,2,2,2,2,2,2,2,2,2,2,2,2,2,
2,2,2,2,2,2,2,2,2,2,2,2,2,2,2,2,2,2,2,2,2,2,2,2,2,2,2,2,2,2,2,2,2,2,2,2,
2,2,2,2,2,2,2,2,2,2,2,2,2,2,2,4),(-1.24268594727471,-1.22755581692661,-1.22432347418344,
-1.22245781579084,-1.22082520574043,-1.21879581845494,-1.21564787247119,
-1.19369863506161,-1.17787628935238,-1.16660182088411,-1.16463204259183,
-1.16355693602476,-1.16264004536171,-1.16145626216942,-1.15952148159293,
-1.14290544250946,-1.14031384061548,-1.12004351463544,-1.10967801598931,
-1.10679191268082,-1.10500158874819,-1.10335391673355,-1.10122767071859,
-1.0965823204256,-1.07247287634745,-1.05864564918267,-1.05232390861533,
-1.04832720624053,-1.04690342782924,-1.04594753729696,-1.04509016260734,
-1.04391281937489,-1.04094236936503,-1.02037193114212,-0.994354415997967,
-0.990382185316445,-0.988361935933999,-0.986730011197086,-0.984857825740183,
-0.981679223001586,-0.968458238618318,-0.944298963011325,-0.936096468314974,
-0.932865405007933,-0.93044862619079,-0.929282131400289,-0.928453995807091,
-0.927401744395747,-0.925586114114291,-0.918206194702676,-0.892477557667124,
-0.881499054283819,-0.876759459693661,-0.873010372474889,-0.871035447096061,
-0.869564357328636,-0.86771445549058,-0.864554783621135,-0.85216491102753,
-0.829563440267243,-0.816313274741673,-0.813446397677439,-0.812196827591933,
-0.811272410555561,-0.810236887632161,-0.808449483398962,-0.801666860940497,
-0.795091525755241,-0.776105621024928,-0.762036472673339,-0.756652062138215,
-0.754373994147937,-0.752708071502994,-0.751169820092415,-0.74866514730882,
-0.742273599084137,-0.732454671033082,-0.717256136422843,-0.716267613065891,
-0.709836627486398,-0.697899151248068,-0.696021774109766,-0.694855094029024,
-0.693939502098999,-0.692851745128487,-0.690822416681446,-0.67779529566062,
-0.647806365400008,-0.640312943408168,-0.637647327979162,-0.636078917953427,
-0.634430700929729,-0.632263147368133,-0.627516995138471,-0.621097697146585,
-0.603202373629714,-0.58209146851319,-0.5791423891782,-0.577968838660747,
-0.577112466532503,-0.576155540932334,-0.574726524667804,-0.570690395294082,
-0.564282073127849,-0.534962743979483,-0.523876297780399,-0.52081292074943,
-0.518984087625428,-0.517346235808414,-0.515259636324544,-0.510948267202939,
-0.500748493306363),.UNSPECIFIED.);
#268=B_SPLINE_CURVE_WITH_KNOTS('',3,(#28836,#28837,#28838,#28839,#28840,
#28841,#28842,#28843,#28844,#28845,#28846,#28847,#28848,#28849,#28850,#28851,
#28852,#28853,#28854,#28855,#28856,#28857,#28858,#28859,#28860,#28861,#28862,
#28863,#28864,#28865,#28866,#28867,#28868,#28869,#28870,#28871,#28872,#28873,
#28874,#28875,#28876,#28877,#28878,#28879,#28880,#28881,#28882,#28883,#28884,
#28885,#28886,#28887,#28888,#28889,#28890,#28891,#28892,#28893,#28894,#28895,
#28896,#28897,#28898,#28899,#28900,#28901,#28902,#28903,#28904,#28905,#28906,
#28907,#28908,#28909,#28910,#28911,#28912,#28913),.UNSPECIFIED.,.F.,.F.,
(4,2,2,2,2,2,2,2,2,2,2,2,2,2,2,2,2,2,2,2,2,2,2,2,2,2,2,2,2,2,2,2,2,2,2,
2,2,2,4),(-0.241877241928533,-0.241619795735405,-0.239527531769983,-0.223830450244459,
-0.198818140520498,-0.189566229696313,-0.186689527539865,-0.18490136548066,
-0.183253228964646,-0.18108632530501,-0.1763438545345,-0.16993110489117,
-0.152068786838454,-0.130903271091689,-0.127946836819323,-0.126777426883858,
-0.125922079540128,-0.12498314209916,-0.123597336807539,-0.121977159984821,
-0.118966747174926,-0.111591014881524,-0.0956008125452895,-0.0734238926969615,
-0.0703071856780489,-0.0682873153153312,-0.0666554782071564,-0.0647831551336937,
-0.0615197191439157,-0.0453375296941648,-0.0198558688782215,-0.0125674908445179,
-0.0103143655522347,-0.00916539692384771,-0.00830733410877659,-0.0074399773927748,
-0.00637126135853562,-0.00397532333556067,-0.000340107566605497),
 .UNSPECIFIED.);
#269=B_SPLINE_CURVE_WITH_KNOTS('',3,(#28914,#28915,#28916,#28917,#28918,
#28919,#28920,#28921,#28922,#28923,#28924,#28925,#28926,#28927,#28928,#28929,
#28930,#28931,#28932,#28933,#28934,#28935,#28936,#28937,#28938,#28939,#28940,
#28941,#28942,#28943,#28944,#28945,#28946,#28947,#28948,#28949,#28950,#28951,
#28952,#28953,#28954,#28955,#28956,#28957,#28958,#28959,#28960,#28961,#28962,
#28963,#28964,#28965,#28966,#28967,#28968,#28969,#28970,#28971,#28972,#28973,
#28974,#28975,#28976,#28977,#28978,#28979,#28980,#28981,#28982,#28983,#28984,
#28985,#28986,#28987,#28988,#28989,#28990,#28991,#28992,#28993,#28994,#28995,
#28996,#28997,#28998,#28999,#29000,#29001,#29002,#29003,#29004,#29005,#29006,
#29007,#29008,#29009,#29010,#29011,#29012,#29013,#29014,#29015,#29016,#29017,
#29018,#29019,#29020,#29021,#29022,#29023,#29024,#29025,#29026,#29027,#29028,
#29029,#29030,#29031,#29032,#29033,#29034,#29035,#29036,#29037,#29038,#29039,
#29040,#29041,#29042,#29043,#29044,#29045,#29046,#29047,#29048,#29049,#29050,
#29051,#29052,#29053,#29054,#29055,#29056,#29057,#29058,#29059,#29060,#29061,
#29062,#29063,#29064,#29065,#29066,#29067,#29068,#29069,#29070,#29071,#29072,
#29073,#29074,#29075,#29076,#29077,#29078,#29079,#29080,#29081,#29082,#29083,
#29084,#29085,#29086,#29087,#29088,#29089,#29090,#29091,#29092,#29093,#29094,
#29095,#29096,#29097,#29098,#29099,#29100,#29101,#29102,#29103,#29104,#29105,
#29106,#29107,#29108,#29109,#29110,#29111,#29112,#29113,#29114,#29115,#29116,
#29117,#29118,#29119,#29120,#29121,#29122,#29123,#29124,#29125,#29126,#29127,
#29128,#29129),.UNSPECIFIED.,.F.,.F.,(4,2,2,2,2,2,2,2,2,2,2,2,2,2,2,2,2,
2,2,2,2,2,2,2,2,2,2,2,2,2,2,2,2,2,2,2,2,2,2,2,2,2,2,2,2,2,2,2,2,2,2,2,2,
2,2,2,2,2,2,2,2,2,2,2,2,2,2,2,2,2,2,2,2,2,2,2,2,2,2,2,2,2,2,2,2,2,2,2,2,
2,2,2,2,2,2,2,2,2,2,2,2,2,2,2,2,2,2,4),(-1.48447813887855,-1.44993276123579,
-1.43927478434815,-1.43636367976403,-1.43456823207176,-1.43292272299963,
-1.43080884476849,-1.42622965472528,-1.4004434401445,-1.3855033320513,-1.38081848943171,
-1.37861317048929,-1.37730443095426,-1.37614079035221,-1.37613605869907,
-1.37613125331992,-1.37612637225832,-1.37612141321535,-1.37611637423337,
-1.37611125273326,-1.37610604652552,-1.37610075312672,-1.37609536991382,
-1.3760898940988,-1.37608432296462,-1.37607865368691,-1.37607288307957,
-1.37606700803392,-1.37606102528906,-1.37605493150694,-1.37604872296438,
-1.37604239585419,-1.37603594645505,-1.37602937069825,-1.37602266430301,
-1.37601582273936,-1.37600884136323,-1.37600171541581,-1.37599443974402,
-1.37598700887642,-1.37597941731928,-1.37597165902972,-1.3759637280546,
-1.37595561801138,-1.37594732184286,-1.37593883240099,-1.37593014241902,
-1.37592124375391,-1.37591212815086,-1.37590278676235,-1.37589321016808,
-1.37588338865127,-1.37587331194629,-1.37498866611297,-1.37381651593659,
-1.37192039595824,-1.3591470933345,-1.33820005982344,-1.32266967375351,
-1.31943763208308,-1.3175723091197,-1.31594009015537,-1.31391131850543,
-1.31076458408937,-1.28881473386802,-1.27299023212113,-1.26172354491973,
-1.25975441002599,-1.25867959255592,-1.25776291208425,-1.25657936100898,
-1.25464488755773,-1.2379426226308,-1.22238556063083,-1.21121795724662,
-1.20642481677116,-1.20264259182654,-1.20066107801255,-1.1991895928448,
-1.19734507984015,-1.19420923329042,-1.18217622009633,-1.15698640207302,
-1.1485807886006,-1.14529733714547,-1.14285035998046,-1.14167813590655,
-1.14084943818705,-1.13980127523412,-1.13800297259332,-1.13083968860688,
-1.10027943698269,-1.08788812530975,-1.08484197076202,-1.08301703865256,
-1.08137867826305,-1.07928591849728,-1.07494150809859,-1.04619586832003,
-1.02807759218667,-1.02560935266101,-1.02443303813311,-1.02351689909638,
-1.02243675107123,-1.02049784122899,-1.01118306214216,-0.98781186896046,
-0.984053158365659),.UNSPECIFIED.);
#270=B_SPLINE_CURVE_WITH_KNOTS('',3,(#29135,#29136,#29137,#29138,#29139,
#29140,#29141,#29142,#29143,#29144,#29145,#29146,#29147,#29148,#29149,#29150,
#29151,#29152,#29153,#29154,#29155,#29156,#29157,#29158,#29159,#29160,#29161,
#29162,#29163,#29164,#29165,#29166,#29167,#29168,#29169,#29170,#29171,#29172,
#29173,#29174,#29175,#29176,#29177,#29178,#29179,#29180,#29181,#29182,#29183,
#29184,#29185,#29186,#29187,#29188,#29189,#29190,#29191,#29192,#29193,#29194,
#29195,#29196,#29197,#29198,#29199,#29200,#29201,#29202,#29203,#29204,#29205,
#29206,#29207,#29208,#29209,#29210,#29211,#29212,#29213,#29214,#29215,#29216,
#29217,#29218,#29219,#29220,#29221,#29222,#29223,#29224,#29225,#29226,#29227,
#29228,#29229,#29230,#29231,#29232,#29233,#29234,#29235,#29236,#29237,#29238,
#29239,#29240,#29241,#29242,#29243,#29244,#29245,#29246,#29247,#29248,#29249,
#29250,#29251,#29252,#29253,#29254,#29255,#29256,#29257,#29258,#29259,#29260,
#29261,#29262,#29263,#29264,#29265,#29266,#29267,#29268,#29269,#29270,#29271,
#29272,#29273,#29274,#29275,#29276,#29277,#29278,#29279,#29280,#29281,#29282),
 .UNSPECIFIED.,.F.,.F.,(4,2,2,2,2,2,2,2,2,2,2,2,2,2,2,2,2,2,2,2,2,2,2,2,
2,2,2,2,2,2,2,2,2,2,2,2,2,2,2,2,2,2,2,2,2,2,2,2,2,2,2,2,2,2,2,2,2,2,2,2,
2,2,2,2,2,2,2,2,2,2,2,2,2,4),(-0.500718660599513,-0.500400110751097,-0.499485194754859,
-0.498383951653016,-0.496291128044058,-0.480585339217535,-0.455552758774148,
-0.446318844691955,-0.443443603602185,-0.441655483213064,-0.4400068022588,
-0.437838325418924,-0.433088860312599,-0.426664202145293,-0.408745872232347,
-0.387657274117378,-0.38469691583698,-0.383526242184164,-0.382670446764753,
-0.381712305522132,-0.380278259986341,-0.376206248176301,-0.369718777818682,
-0.339281763618541,-0.329232131553156,-0.3262671757704,-0.32445953670125,
-0.32281652375529,-0.320689403586707,-0.316165165775265,-0.310133647655511,
-0.294061021399678,-0.270183115964008,-0.267310718879712,-0.266184045913166,
-0.265254659316578,-0.264258070727483,-0.262647365048782,-0.25703590953585,
-0.246656247942295,-0.223171151518339,-0.212166094743792,-0.209109414932852,
-0.207281748994032,-0.205643170510959,-0.203553208998678,-0.19922593986097,
-0.182443437973725,-0.177168294017118,-0.152890594518186,-0.150051337484662,
-0.148929896799405,-0.148001770147206,-0.147002675151922,-0.145380684613584,
-0.139743376234368,-0.129247968276644,-0.0975350303846231,-0.0928880002702371,
-0.0907613711845579,-0.0891135527506156,-0.0873232211707997,-0.0846943827588374,
-0.0757706437612646,-0.0600534964439603,-0.0355967045487589,-0.0328105664360528,
-0.0316793483313575,-0.0307488626859592,-0.0297544200010428,-0.028153331282767,
-0.0262405493043127,-0.0224210226223817,-0.000340524436432586),
 .UNSPECIFIED.);
#271=B_SPLINE_CURVE_WITH_KNOTS('',3,(#29283,#29284,#29285,#29286,#29287,
#29288,#29289,#29290,#29291,#29292,#29293,#29294,#29295,#29296,#29297,#29298,
#29299,#29300,#29301,#29302,#29303,#29304,#29305,#29306,#29307,#29308,#29309,
#29310,#29311,#29312,#29313,#29314,#29315,#29316,#29317,#29318,#29319,#29320,
#29321,#29322,#29323,#29324,#29325,#29326,#29327,#29328,#29329,#29330,#29331,
#29332,#29333,#29334,#29335,#29336,#29337,#29338,#29339,#29340,#29341,#29342,
#29343,#29344,#29345,#29346,#29347,#29348,#29349,#29350,#29351,#29352,#29353,
#29354),.UNSPECIFIED.,.F.,.F.,(4,2,2,2,2,2,2,2,2,2,2,2,2,2,2,2,2,2,2,2,
2,2,2,2,2,2,2,2,2,2,2,2,2,2,2,4),(-1.48436044637623,-1.46363610470996,-1.46068896284307,
-1.45874821980611,-1.45718862764179,-1.45555887871019,-1.45365730467275,
-1.45034881516589,-1.43463884215802,-1.42021635804648,-1.40262751754562,
-1.39967722319634,-1.39839279491649,-1.39746314436856,-1.39644410144448,
-1.39473132793389,-1.38874376399468,-1.36461110167954,-1.35155221209812,
-1.34624658357989,-1.3421873911038,-1.34020994604938,-1.33857067988293,
-1.33674843809142,-1.33371556245394,-1.32307255532416,-1.29657665364041,
-1.28390853466999,-1.28188995060368,-1.28080445990665,-1.27988865565304,
-1.27871900136947,-1.27683172631911,-1.26462104590702,-1.24308133150857,
-1.24268594727471),.UNSPECIFIED.);
#272=B_SPLINE_CURVE_WITH_KNOTS('',3,(#29355,#29356,#29357,#29358,#29359,
#29360,#29361,#29362,#29363,#29364,#29365,#29366,#29367,#29368,#29369,#29370,
#29371,#29372,#29373,#29374,#29375,#29376,#29377,#29378,#29379,#29380,#29381,
#29382,#29383,#29384,#29385,#29386,#29387,#29388,#29389,#29390,#29391,#29392,
#29393,#29394,#29395,#29396,#29397,#29398,#29399,#29400,#29401,#29402,#29403,
#29404,#29405,#29406,#29407,#29408,#29409,#29410,#29411,#29412,#29413,#29414,
#29415,#29416,#29417,#29418,#29419,#29420,#29421,#29422,#29423,#29424,#29425,
#29426,#29427,#29428,#29429,#29430,#29431,#29432,#29433,#29434,#29435,#29436,
#29437,#29438,#29439,#29440,#29441,#29442,#29443,#29444,#29445,#29446,#29447,
#29448,#29449,#29450,#29451,#29452,#29453,#29454,#29455,#29456,#29457,#29458,
#29459,#29460,#29461,#29462,#29463,#29464,#29465,#29466,#29467,#29468,#29469,
#29470,#29471,#29472,#29473,#29474,#29475,#29476,#29477,#29478,#29479,#29480,
#29481,#29482,#29483,#29484,#29485,#29486,#29487,#29488,#29489,#29490,#29491,
#29492,#29493,#29494,#29495,#29496,#29497,#29498,#29499,#29500,#29501,#29502,
#29503,#29504,#29505,#29506,#29507,#29508,#29509,#29510,#29511,#29512,#29513,
#29514,#29515,#29516,#29517,#29518,#29519,#29520,#29521,#29522,#29523,#29524,
#29525,#29526,#29527,#29528,#29529,#29530,#29531,#29532,#29533,#29534,#29535,
#29536,#29537,#29538,#29539,#29540,#29541,#29542,#29543,#29544,#29545,#29546,
#29547,#29548,#29549,#29550,#29551,#29552,#29553,#29554,#29555,#29556,#29557,
#29558,#29559,#29560,#29561,#29562,#29563,#29564,#29565,#29566,#29567,#29568,
#29569,#29570,#29571,#29572,#29573,#29574,#29575,#29576,#29577,#29578,#29579,
#29580,#29581,#29582),.UNSPECIFIED.,.F.,.F.,(4,2,2,2,2,2,2,2,2,2,2,2,2,
2,2,2,2,2,2,2,2,2,2,2,2,2,2,2,2,2,2,2,2,2,2,2,2,2,2,2,2,2,2,2,2,2,2,2,2,
2,2,2,2,2,2,2,2,2,2,2,2,2,2,2,2,2,2,2,2,2,2,2,2,2,2,2,2,2,2,2,2,2,2,2,2,
2,2,2,2,2,2,2,2,2,2,2,2,2,2,2,2,2,2,2,2,2,2,2,2,2,2,2,2,4),(-0.984053158365659,
-0.976712214041789,-0.971938326079979,-0.968168042193585,-0.966188961947261,
-0.964717695965065,-0.962871387267738,-0.959727351554003,-0.947571129667715,
-0.922489498362212,-0.914103868233824,-0.9108255446165,-0.90838151843392,
-0.9072098554621,-0.906381217433222,-0.90533266880774,-0.903532722358874,
-0.896349507928024,-0.870543513232499,-0.859473608806476,-0.854708173774071,
-0.850943138830566,-0.84896513230403,-0.84749396486923,-0.845646866275643,
-0.842499214437275,-0.83028799089571,-0.805254535093528,-0.7968779395003,
-0.793601939096763,-0.791159251771831,-0.78998784530935,-0.789159236268877,
-0.788110515683509,-0.786309829345756,-0.779117582648423,-0.773186504838792,
-0.754131010132862,-0.742554441257789,-0.735376790812867,-0.732754482784648,
-0.73119439673305,-0.729542360984107,-0.727348452454022,-0.722454571965926,
-0.715772781417891,-0.682486535913121,-0.675324631505821,-0.673526115415097,
-0.672477796291944,-0.671648943625247,-0.670476477744319,-0.66802887530248,
-0.656800353861006,-0.633140999369956,-0.619348152390165,-0.616134707900035,
-0.614254591994021,-0.612623361630794,-0.610613732337479,-0.60669443748868,
-0.601678733498216,-0.589710902974336,-0.563749878213513,-0.557865332505684,
-0.556162893592807,-0.555146068428914,-0.554215438867957,-0.552925471012426,
-0.549821522909534,-0.545338915834534,-0.531505575690141,-0.504112789416371,
-0.499693826973797,-0.497578602710253,-0.495932504309026,-0.494136877236163,
-0.491226529294816,-0.480584881549858,-0.462006164841777,-0.442799051953094,
-0.43979489528577,-0.438611902128175,-0.437753088318309,-0.436798821947255,
-0.435382993596101,-0.431444645446266,-0.425251861771903,-0.40790502918907,
-0.385239412731637,-0.382116080563427,-0.380094086933948,-0.378461944266476,
-0.376590818334384,-0.3733334895627,-0.357290373499673,-0.342865369498245,
-0.334379990628789,-0.323957920559101,-0.322134533860992,-0.3209840392454,
-0.320069264630318,-0.318968202829638,-0.316875761391885,-0.301177349361784,
-0.276162920683849,-0.266910221622156,-0.264033275071036,-0.262244961239208,
-0.260596684931616,-0.258429597620231,-0.253686725490098,-0.247273433524857,
-0.24206462708761),.UNSPECIFIED.);
#273=B_SPLINE_CURVE_WITH_KNOTS('',3,(#29587,#29588,#29589,#29590,#29591,
#29592,#29593,#29594,#29595,#29596,#29597,#29598,#29599,#29600,#29601,#29602,
#29603,#29604,#29605,#29606,#29607,#29608,#29609,#29610,#29611,#29612,#29613,
#29614,#29615,#29616,#29617,#29618,#29619,#29620,#29621,#29622,#29623,#29624,
#29625,#29626,#29627,#29628,#29629,#29630,#29631,#29632,#29633,#29634,#29635,
#29636,#29637,#29638,#29639,#29640,#29641,#29642,#29643,#29644,#29645,#29646,
#29647,#29648,#29649,#29650,#29651,#29652,#29653,#29654,#29655,#29656,#29657,
#29658,#29659,#29660,#29661,#29662,#29663,#29664,#29665,#29666,#29667,#29668,
#29669,#29670,#29671,#29672,#29673,#29674,#29675,#29676,#29677,#29678,#29679,
#29680,#29681,#29682,#29683,#29684,#29685,#29686,#29687,#29688,#29689,#29690,
#29691,#29692,#29693,#29694,#29695,#29696,#29697,#29698,#29699,#29700,#29701,
#29702,#29703,#29704,#29705,#29706,#29707,#29708,#29709,#29710,#29711,#29712,
#29713,#29714,#29715,#29716,#29717,#29718,#29719,#29720,#29721,#29722,#29723,
#29724,#29725,#29726,#29727,#29728,#29729,#29730,#29731,#29732,#29733,#29734,
#29735,#29736,#29737,#29738,#29739,#29740,#29741,#29742,#29743,#29744,#29745,
#29746,#29747,#29748,#29749,#29750,#29751,#29752,#29753,#29754,#29755,#29756,
#29757,#29758,#29759,#29760,#29761,#29762,#29763,#29764,#29765,#29766,#29767,
#29768,#29769,#29770,#29771,#29772,#29773,#29774,#29775,#29776,#29777,#29778,
#29779,#29780,#29781,#29782,#29783,#29784,#29785,#29786,#29787,#29788,#29789,
#29790,#29791,#29792,#29793,#29794,#29795,#29796,#29797,#29798),
 .UNSPECIFIED.,.F.,.F.,(4,2,2,2,2,2,2,2,2,2,2,2,2,2,2,2,2,2,2,2,2,2,2,2,
2,2,2,2,2,2,2,2,2,2,2,2,2,2,2,2,2,2,2,2,2,2,2,2,2,2,2,2,2,2,2,2,2,2,2,2,
2,2,2,2,2,2,2,2,2,2,2,2,2,2,2,2,2,2,2,2,2,2,2,2,2,2,2,2,2,2,2,2,2,2,2,2,
2,2,2,2,2,2,2,2,2,4),(-1.24280763943444,-1.22268571771476,-1.20697442025643,
-1.2048814307625,-1.20378019948657,-1.20286534714334,-1.2017148319585,-1.19989156922864,
-1.1894723252949,-1.18099836452278,-1.16658994224282,-1.15054449778414,
-1.14728702848753,-1.14541577034329,-1.14378347715707,-1.14176124948906,
-1.13863742880102,-1.11594522248837,-1.09855554159171,-1.0923893115782,
-1.08846341695498,-1.0870492130481,-1.08609522199718,-1.08523600457854,
-1.08405163604696,-1.08103954513751,-1.0617017711617,-1.04324572085829,
-1.03264315039829,-1.02973601405698,-1.02794095392827,-1.02629443483638,
-1.02417735867814,-1.01974970957412,-0.992437002652213,-0.978532823637424,
-0.974036597449419,-0.970925752719812,-0.969634549199411,-0.968703633052056,
-0.967687135350315,-0.965986532964893,-0.960120815296411,-0.934401571214883,
-0.917788636619313,-0.913482654270816,-0.911396766655546,-0.90975862877382,
-0.907928599426175,-0.904861117363274,-0.893700887775741,-0.867697487506419,
-0.859154922406015,-0.854222569158852,-0.85268321140019,-0.851702324373684,
-0.850763374019604,-0.849599536642928,-0.846709405654708,-0.824299533813988,
-0.79996898507792,-0.796013090677606,-0.793995899347205,-0.792363921691072,
-0.790488896037379,-0.787298702047962,-0.773897769001144,-0.751683479680263,
-0.742292270469208,-0.737132641237955,-0.735509917857048,-0.734510653143797,
-0.733571906241908,-0.732235819355497,-0.728844613182002,-0.723798008273827,
-0.70669760969028,-0.683831903439715,-0.679164246231147,-0.677033765165119,
-0.675385244130325,-0.673596427602753,-0.670718147175711,-0.660444524376605,
-0.640509338269064,-0.622230902008625,-0.619221211409352,-0.618037195126648,
-0.617178036025954,-0.616223861290774,-0.614808971413012,-0.61087840916066,
-0.604702924108123,-0.587336260307222,-0.564660018034641,-0.561536305481998,
-0.559514032810818,-0.557881641107584,-0.556010201494232,-0.552752246819358,
-0.536703166304568,-0.522280864721184,-0.513798442718789,-0.503374438652297,
-0.501550779193074,-0.500718660599513),.UNSPECIFIED.);
#274=B_SPLINE_CURVE_WITH_KNOTS('',3,(#29800,#29801,#29802,#29803,#29804,
#29805,#29806,#29807,#29808,#29809,#29810,#29811,#29812,#29813,#29814,#29815,
#29816,#29817,#29818,#29819,#29820,#29821,#29822,#29823,#29824,#29825,#29826,
#29827,#29828,#29829,#29830,#29831,#29832,#29833,#29834,#29835,#29836,#29837,
#29838,#29839,#29840,#29841,#29842,#29843,#29844,#29845,#29846,#29847,#29848,
#29849,#29850,#29851,#29852,#29853,#29854,#29855,#29856,#29857,#29858,#29859,
#29860,#29861,#29862,#29863,#29864,#29865,#29866,#29867,#29868,#29869,#29870,
#29871),.UNSPECIFIED.,.F.,.F.,(4,2,2,2,2,2,2,2,2,2,2,2,2,2,2,2,2,2,2,2,
2,2,2,2,2,2,2,2,2,2,2,2,2,2,2,4),(-0.24206462708761,-0.229409608471203,
-0.208242742972339,-0.205285752764569,-0.204116187756894,-0.203260754000776,
-0.202302473198574,-0.200867283906088,-0.196785692057573,-0.190276519887479,
-0.159505080654677,-0.149758964950301,-0.146828703665975,-0.14502881492429,
-0.14338408059051,-0.141367135341366,-0.137096545683497,-0.131439646267583,
-0.116977336489474,-0.0949351853640112,-0.0889165580126861,-0.0872005837593868,
-0.086180807865097,-0.0852513721303828,-0.0839684884640444,-0.0810276964737433,
-0.0614872094232513,-0.0478088219577944,-0.0332185623453336,-0.0299611576291717,
-0.0280710561831135,-0.0264405409194214,-0.0248773107901266,-0.0229234421895695,
-0.0199444790809123,-0.000340292378937216),.UNSPECIFIED.);
#275=B_SPLINE_CURVE_WITH_KNOTS('',3,(#29872,#29873,#29874,#29875,#29876,
#29877,#29878,#29879,#29880,#29881,#29882,#29883,#29884,#29885,#29886,#29887,
#29888,#29889,#29890,#29891,#29892,#29893,#29894,#29895,#29896,#29897,#29898,
#29899,#29900,#29901,#29902,#29903,#29904,#29905,#29906,#29907,#29908,#29909,
#29910,#29911,#29912,#29913,#29914,#29915,#29916,#29917,#29918,#29919,#29920,
#29921,#29922,#29923,#29924,#29925,#29926,#29927,#29928,#29929,#29930,#29931,
#29932,#29933,#29934,#29935,#29936,#29937,#29938,#29939,#29940,#29941,#29942,
#29943,#29944,#29945,#29946,#29947,#29948,#29949,#29950,#29951,#29952,#29953,
#29954,#29955,#29956,#29957,#29958,#29959,#29960,#29961,#29962,#29963,#29964,
#29965,#29966,#29967,#29968,#29969,#29970,#29971,#29972,#29973,#29974,#29975,
#29976,#29977,#29978,#29979,#29980,#29981,#29982,#29983,#29984,#29985,#29986,
#29987,#29988,#29989,#29990,#29991,#29992,#29993,#29994,#29995,#29996,#29997,
#29998,#29999,#30000,#30001,#30002,#30003,#30004,#30005,#30006,#30007,#30008,
#30009,#30010,#30011,#30012,#30013,#30014,#30015,#30016,#30017,#30018,#30019),
 .UNSPECIFIED.,.F.,.F.,(4,2,2,2,2,2,2,2,2,2,2,2,2,2,2,2,2,2,2,2,2,2,2,2,
2,2,2,2,2,2,2,2,2,2,2,2,2,2,2,2,2,2,2,2,2,2,2,2,2,2,2,2,2,2,2,2,2,2,2,2,
2,2,2,2,2,2,2,2,2,2,2,2,2,4),(-1.48430358760489,-1.4597246532768,-1.45666928759006,
-1.45503241734088,-1.4536170060634,-1.45266294653794,-1.4518042556676,-1.4506213636504,
-1.44761705387336,-1.42846664822781,-1.41207606660783,-1.39953211121336,
-1.39658933449029,-1.39502968458839,-1.39355793220374,-1.39171433500767,
-1.38858313733914,-1.37662208235956,-1.3481760858305,-1.34183125745421,
-1.33785051793992,-1.33641336227839,-1.33545472247536,-1.33459969888755,
-1.33343161981659,-1.33048363578237,-1.30912557320389,-1.29141312718798,
-1.28503105702883,-1.28030553386675,-1.27814165825848,-1.27649390687085,
-1.27470429196992,-1.27182110807929,-1.26250880178412,-1.23753042492945,
-1.22184425250862,-1.21975190116346,-1.21865087963237,-1.21773613073978,
-1.21658566418178,-1.21476233433302,-1.20433789918159,-1.195840689987,-1.18137380408734,
-1.16540978038666,-1.16215634257817,-1.1602860893635,-1.1586539073184,-1.15663082817078,
-1.15350379712415,-1.13095029453175,-1.11387561667634,-1.10742930633547,
-1.10337629692999,-1.10194491760816,-1.10098743847175,-1.1001313666006,
-1.09895924280717,-1.09601124304522,-1.07483943412046,-1.05699688614121,
-1.05058802556939,-1.04584720654982,-1.04368045973566,-1.04203219434918,
-1.0402436502048,-1.03736580189195,-1.02810551124147,-1.00307948367819,
-0.987374412326566,-0.98528157341315,-0.984180397635834,-0.984002691704062),
 .UNSPECIFIED.);
#276=B_SPLINE_CURVE_WITH_KNOTS('',3,(#30025,#30026,#30027,#30028,#30029,
#30030,#30031,#30032,#30033,#30034,#30035,#30036,#30037,#30038,#30039,#30040,
#30041,#30042,#30043,#30044,#30045,#30046,#30047,#30048,#30049,#30050,#30051,
#30052,#30053,#30054,#30055,#30056,#30057,#30058,#30059,#30060,#30061,#30062,
#30063,#30064,#30065,#30066,#30067,#30068,#30069,#30070,#30071,#30072,#30073,
#30074,#30075,#30076,#30077,#30078,#30079,#30080,#30081,#30082,#30083,#30084,
#30085,#30086,#30087,#30088,#30089,#30090,#30091,#30092,#30093,#30094,#30095,
#30096,#30097,#30098,#30099,#30100,#30101,#30102,#30103,#30104,#30105,#30106,
#30107,#30108,#30109,#30110,#30111,#30112,#30113,#30114,#30115,#30116,#30117,
#30118,#30119,#30120,#30121,#30122,#30123,#30124,#30125,#30126,#30127,#30128,
#30129,#30130,#30131,#30132,#30133,#30134,#30135,#30136,#30137,#30138,#30139,
#30140,#30141,#30142,#30143,#30144,#30145,#30146,#30147,#30148,#30149,#30150,
#30151,#30152,#30153,#30154,#30155,#30156,#30157,#30158,#30159,#30160,#30161,
#30162,#30163,#30164,#30165,#30166,#30167,#30168,#30169,#30170,#30171,#30172,
#30173,#30174,#30175,#30176,#30177,#30178,#30179,#30180),.UNSPECIFIED.,
 .F.,.F.,(4,2,2,2,2,2,2,2,2,2,2,2,2,2,2,2,2,2,2,2,2,2,2,2,2,2,2,2,2,2,2,
2,2,2,2,2,2,2,2,2,2,2,2,2,2,2,2,2,2,2,2,2,2,2,2,2,2,2,2,2,2,2,2,2,2,2,2,
2,2,2,2,2,2,2,2,2,2,4),(-0.500846823737344,-0.487606703081641,-0.484483003251093,
-0.482460739216415,-0.480828354744568,-0.478956923707451,-0.475698984702297,
-0.459650001234931,-0.445227745706519,-0.436745349986905,-0.426321393802306,
-0.424497742511653,-0.423347079203627,-0.42243216727492,-0.421330929051376,
-0.419238114666127,-0.403532391399216,-0.378499911225953,-0.369266050860534,
-0.366390823885218,-0.364602711733264,-0.362954038010901,-0.360785570154017,
-0.356036122533534,-0.349611486527616,-0.331693204732785,-0.310604747112755,
-0.307644398212804,-0.306473729904561,-0.305617938322044,-0.304659801291414,
-0.303225761916063,-0.299153766635581,-0.292666321621788,-0.262229390742629,
-0.252179852923616,-0.249214914212792,-0.247407284024581,-0.245764278162907,
-0.243637165763318,-0.239112939019434,-0.233081432093515,-0.217008807348068,
-0.193131119263884,-0.190258726762178,-0.189132057512633,-0.188202674730495,
-0.187206091172668,-0.185595395376335,-0.179983992450302,-0.169604456258818,
-0.14603173450636,-0.135101689611372,-0.132051609445832,-0.130225387997182,
-0.128619156439092,-0.127247968759405,-0.125306358799174,-0.122357382842953,
-0.116860991140866,-0.103052857908684,-0.0826668163600495,-0.0743661800669981,
-0.0724865950543069,-0.0714196619645263,-0.0705102806790766,-0.069319195194738,
-0.066774601339198,-0.0633212231158481,-0.0542433421583409,-0.0283444858439824,
-0.0179670642535147,-0.0148615777933429,-0.0130232913170418,-0.011420793302306,
-0.00984244810923627,-0.00783663028624213,-0.000340145515886172),
 .UNSPECIFIED.);
#277=B_SPLINE_CURVE_WITH_KNOTS('',3,(#30181,#30182,#30183,#30184,#30185,
#30186,#30187,#30188,#30189,#30190,#30191,#30192,#30193,#30194,#30195,#30196,
#30197,#30198,#30199,#30200,#30201,#30202,#30203,#30204,#30205,#30206,#30207,
#30208,#30209,#30210,#30211,#30212,#30213,#30214,#30215,#30216,#30217,#30218,
#30219,#30220,#30221,#30222,#30223,#30224,#30225,#30226,#30227,#30228,#30229,
#30230,#30231,#30232,#30233,#30234,#30235,#30236,#30237,#30238,#30239,#30240,
#30241,#30242,#30243,#30244,#30245,#30246,#30247,#30248,#30249,#30250,#30251,
#30252,#30253,#30254,#30255,#30256,#30257,#30258,#30259,#30260),
 .UNSPECIFIED.,.F.,.F.,(4,2,2,2,2,2,2,2,2,2,2,2,2,2,2,2,2,2,2,2,2,2,2,2,
2,2,2,2,2,2,2,2,2,2,2,2,2,2,2,4),(-1.48436245928363,-1.45697626582871,-1.44145867048246,
-1.43936947323549,-1.43826910742382,-1.43735431844207,-1.43620305700907,
-1.43437710222971,-1.42388697285354,-1.3964930501114,-1.3885998090499,-1.38480948759865,
-1.38252355478692,-1.38047273681414,-1.38045595817035,-1.38043776423287,
-1.38041799710493,-1.38039647477197,-1.37882236344308,-1.37701828969799,
-1.37406890358588,-1.36415202553159,-1.33355391205358,-1.32705412617481,
-1.3229770998334,-1.32154247853527,-1.32058429591438,-1.319728723641,-1.31855869256389,
-1.31559897714232,-1.29451507063247,-1.27661520431747,-1.27019472471291,
-1.26544729604828,-1.26327930921085,-1.26163081676943,-1.25984272115395,
-1.25696712739865,-1.2477287299737,-1.24280763943444),.UNSPECIFIED.);
#278=B_SPLINE_CURVE_WITH_KNOTS('',3,(#30261,#30262,#30263,#30264,#30265,
#30266,#30267,#30268,#30269,#30270,#30271,#30272,#30273,#30274,#30275,#30276,
#30277,#30278,#30279,#30280,#30281,#30282,#30283,#30284,#30285,#30286,#30287,
#30288,#30289,#30290,#30291,#30292,#30293,#30294,#30295,#30296,#30297,#30298,
#30299,#30300,#30301,#30302,#30303,#30304,#30305,#30306,#30307,#30308,#30309,
#30310,#30311,#30312,#30313,#30314,#30315,#30316,#30317,#30318,#30319,#30320,
#30321,#30322,#30323,#30324,#30325,#30326,#30327,#30328,#30329,#30330,#30331,
#30332,#30333,#30334,#30335,#30336,#30337,#30338,#30339,#30340,#30341,#30342,
#30343,#30344,#30345,#30346,#30347,#30348,#30349,#30350,#30351,#30352,#30353,
#30354,#30355,#30356,#30357,#30358,#30359,#30360,#30361,#30362,#30363,#30364,
#30365,#30366,#30367,#30368,#30369,#30370,#30371,#30372,#30373,#30374,#30375,
#30376,#30377,#30378,#30379,#30380,#30381,#30382,#30383,#30384,#30385,#30386,
#30387,#30388,#30389,#30390,#30391,#30392,#30393,#30394,#30395,#30396,#30397,
#30398,#30399,#30400,#30401,#30402,#30403,#30404,#30405,#30406,#30407,#30408,
#30409,#30410,#30411,#30412,#30413,#30414,#30415,#30416,#30417,#30418,#30419,
#30420,#30421,#30422,#30423,#30424,#30425,#30426,#30427,#30428,#30429,#30430,
#30431,#30432,#30433,#30434,#30435,#30436,#30437,#30438,#30439,#30440,#30441,
#30442,#30443,#30444,#30445,#30446,#30447,#30448,#30449,#30450,#30451,#30452,
#30453,#30454,#30455,#30456,#30457,#30458,#30459,#30460,#30461,#30462,#30463,
#30464,#30465,#30466,#30467,#30468,#30469,#30470,#30471,#30472,#30473,#30474,
#30475,#30476,#30477,#30478),.UNSPECIFIED.,.F.,.F.,(4,2,2,2,2,2,2,2,2,2,
2,2,2,2,2,2,2,2,2,2,2,2,2,2,2,2,2,2,2,2,2,2,2,2,2,2,2,2,2,2,2,2,2,2,2,2,
2,2,2,2,2,2,2,2,2,2,2,2,2,2,2,2,2,2,2,2,2,2,2,2,2,2,2,2,2,2,2,2,2,2,2,2,
2,2,2,2,2,2,2,2,2,2,2,2,2,2,2,2,2,2,2,2,2,2,2,2,2,2,4),(-0.984002691704062,
-0.983265579879282,-0.982115101342455,-0.98029188872968,-0.969873114741405,
-0.961395403523032,-0.946982485815175,-0.930941305467715,-0.927684090046827,
-0.925812929079602,-0.924180694436495,-0.922158507690352,-0.919034695475286,
-0.896334175187465,-0.878930388345964,-0.872776257329012,-0.868855926680461,
-0.867442519897269,-0.866488717189068,-0.865629399334593,-0.864444554557963,
-0.86142944006154,-0.843454637902599,-0.823316440839283,-0.812986537088207,
-0.810103407345437,-0.808313624475316,-0.806665581652403,-0.804537641222769,
-0.799883576699916,-0.776084945864894,-0.759679675084305,-0.754744262178868,
-0.751409009640127,-0.750081698988863,-0.749144596367316,-0.748266105096901,
-0.74675164702973,-0.742438018774673,-0.735211431508296,-0.719037524177743,
-0.696844320877178,-0.693707727904646,-0.69168164615558,-0.690049115134306,
-0.68818073020362,-0.684936415094689,-0.669173484735883,-0.645679776641144,
-0.635501171275532,-0.63368753033417,-0.63253991242042,-0.631625155715052,
-0.630521380238969,-0.628416287372753,-0.611981641479028,-0.585024778655133,
-0.577914827331452,-0.57530161156218,-0.573742995230213,-0.572089607893275,
-0.569888924856837,-0.564958501340524,-0.558211733620303,-0.538633053837819,
-0.53801465694927,-0.519887524301152,-0.516872493203845,-0.515687652933693,
-0.514828334885846,-0.513874517320948,-0.512461073139244,-0.508540447608072,
-0.502386467179895,-0.484997001677238,-0.462308755731776,-0.459185207759204,
-0.457163080613137,-0.455530834192337,-0.453659593727591,-0.450402077025643,
-0.434358342227161,-0.419932144090225,-0.411446058694533,-0.401023346719223,
-0.399199845278794,-0.398049278024558,-0.397134445485913,-0.39603331376506,
-0.393940738908263,-0.378241283270627,-0.353225142505801,-0.343972005043057,
-0.341094891854124,-0.339306468156209,-0.33765808637706,-0.335490854225948,
-0.330747639699413,-0.324333867464797,-0.306468546748124,-0.285300879846517,
-0.282343677369006,-0.281174033670358,-0.280318544594259,-0.279360204556625,
-0.277924931282514,-0.273843132786132,-0.267333664141669,-0.241916328248978),
 .UNSPECIFIED.);
#279=B_SPLINE_CURVE_WITH_KNOTS('',3,(#30483,#30484,#30485,#30486,#30487,
#30488,#30489,#30490,#30491,#30492,#30493,#30494,#30495,#30496,#30497,#30498,
#30499,#30500,#30501,#30502,#30503,#30504,#30505,#30506,#30507,#30508,#30509,
#30510,#30511,#30512,#30513,#30514,#30515,#30516,#30517,#30518,#30519,#30520,
#30521,#30522,#30523,#30524,#30525,#30526,#30527,#30528,#30529,#30530,#30531,
#30532,#30533,#30534,#30535,#30536,#30537,#30538,#30539,#30540,#30541,#30542,
#30543,#30544,#30545,#30546,#30547,#30548,#30549,#30550,#30551,#30552,#30553,
#30554,#30555,#30556,#30557,#30558,#30559,#30560,#30561,#30562,#30563,#30564,
#30565,#30566,#30567,#30568,#30569,#30570,#30571,#30572,#30573,#30574,#30575,
#30576,#30577,#30578,#30579,#30580,#30581,#30582,#30583,#30584,#30585,#30586,
#30587,#30588,#30589,#30590,#30591,#30592,#30593,#30594,#30595,#30596,#30597,
#30598,#30599,#30600,#30601,#30602,#30603,#30604,#30605,#30606,#30607,#30608,
#30609,#30610,#30611,#30612,#30613,#30614,#30615,#30616,#30617,#30618,#30619,
#30620,#30621,#30622,#30623,#30624,#30625,#30626,#30627,#30628,#30629,#30630,
#30631,#30632,#30633,#30634,#30635,#30636,#30637,#30638,#30639,#30640,#30641,
#30642,#30643,#30644,#30645,#30646,#30647,#30648,#30649,#30650,#30651,#30652,
#30653,#30654,#30655,#30656,#30657,#30658,#30659,#30660,#30661,#30662,#30663,
#30664,#30665,#30666,#30667,#30668,#30669,#30670,#30671,#30672,#30673,#30674,
#30675,#30676,#30677,#30678,#30679,#30680,#30681,#30682,#30683,#30684,#30685,
#30686,#30687,#30688,#30689,#30690,#30691,#30692,#30693,#30694),
 .UNSPECIFIED.,.F.,.F.,(4,2,2,2,2,2,2,2,2,2,2,2,2,2,2,2,2,2,2,2,2,2,2,2,
2,2,2,2,2,2,2,2,2,2,2,2,2,2,2,2,2,2,2,2,2,2,2,2,2,2,2,2,2,2,2,2,2,2,2,2,
2,2,2,2,2,2,2,2,2,2,2,2,2,2,2,2,2,2,2,2,2,2,2,2,2,2,2,2,2,2,2,2,2,2,2,2,
2,2,2,2,2,2,2,2,2,4),(-1.24301555874646,-1.24280678210364,-1.24164937253616,
-1.23879642287787,-1.21583894977737,-1.20211326195524,-1.19034727950917,
-1.18734594005223,-1.18553030458148,-1.18388911289608,-1.18177713532705,
-1.17733409199837,-1.14954091908435,-1.13074392557291,-1.12818555667396,
-1.12699181497948,-1.12608210959619,-1.12501679355969,-1.12314456580738,
-1.11495676763724,-1.08271293902672,-1.07610667431467,-1.07125435240713,
-1.06906745881062,-1.06741610561402,-1.06563599387225,-1.06279748095302,
-1.0539173283568,-1.02552264243608,-1.0167492763692,-1.01337188112954,-1.01087075703067,
-1.00968788531127,-1.00877091908418,-1.00769479847151,-1.00577480994069,
-0.996812153231707,-0.976921462576252,-0.959710502782217,-0.954263975461164,
-0.951975402469816,-0.950307410444432,-0.948771156501619,-0.946681412061269,
-0.942520268426617,-0.917613676933456,-0.909454695141724,-0.89660817274771,
-0.893783358840923,-0.892541033383309,-0.891617461381184,-0.890577836607942,
-0.888772343503266,-0.881782246024147,-0.848334195570448,-0.841642044160709,
-0.836741667048819,-0.834546302006329,-0.832893730206289,-0.831333541959309,
-0.828712057001917,-0.821543117196986,-0.791253015809147,-0.782295507970897,
-0.778872052174502,-0.77634465718312,-0.775156808162071,-0.77424772480152,
-0.773178553436826,-0.771289189757746,-0.762838915587905,-0.742576682293863,
-0.722126792506872,-0.718994879402654,-0.716970169060304,-0.715337670778208,
-0.713468147743128,-0.710218810167517,-0.694351792420643,-0.66986831634356,
-0.660694620291853,-0.658762777639333,-0.657683982342627,-0.656767307407488,
-0.655588137459173,-0.653106390464633,-0.637841737676232,-0.612351866017475,
-0.603638537489341,-0.600820966941319,-0.599045356300897,-0.597392264764845,
-0.595194219024158,-0.590279348572559,-0.583560605660456,-0.564133031249619,
-0.54517834487597,-0.542167968185322,-0.540983841148447,-0.54012465641764,
-0.539170519261211,-0.537755797621785,-0.533826429388241,-0.52765353779518,
-0.510284232297328,-0.500846823737344),.UNSPECIFIED.);
#280=B_SPLINE_CURVE_WITH_KNOTS('',3,(#30696,#30697,#30698,#30699,#30700,
#30701,#30702,#30703,#30704,#30705,#30706,#30707,#30708,#30709,#30710,#30711,
#30712,#30713,#30714,#30715,#30716,#30717,#30718,#30719,#30720,#30721,#30722,
#30723,#30724,#30725,#30726,#30727,#30728,#30729,#30730,#30731,#30732,#30733,
#30734,#30735,#30736,#30737,#30738,#30739,#30740,#30741,#30742,#30743,#30744,
#30745,#30746,#30747,#30748,#30749,#30750,#30751,#30752,#30753,#30754,#30755,
#30756,#30757,#30758,#30759,#30760,#30761,#30762,#30763,#30764,#30765,#30766,
#30767,#30768,#30769,#30770,#30771,#30772,#30773),.UNSPECIFIED.,.F.,.F.,
(4,2,2,2,2,2,2,2,2,2,2,2,2,2,2,2,2,2,2,2,2,2,2,2,2,2,2,2,2,2,2,2,2,2,2,
2,2,2,4),(-0.241916328248978,-0.236562051352221,-0.226813709406645,-0.223883087469065,
-0.222083046533686,-0.220438218608943,-0.218296264316374,-0.213691301802682,
-0.207519669427203,-0.190808523118788,-0.167904394656517,-0.165048232361707,
-0.16389033286731,-0.162953050000126,-0.161970043329616,-0.160420648258423,
-0.155396650676668,-0.146618744887094,-0.119029162039518,-0.109535578023307,
-0.10661954439565,-0.104822703424011,-0.103247809715307,-0.103229170337593,
-0.103212052745656,-0.103196304164034,-0.101141341876507,-0.0988529194085211,
-0.0950564235044132,-0.0871442297293138,-0.0595982870658473,-0.0492481992942097,
-0.0474276568445735,-0.0462779936179891,-0.0453632141980915,-0.0442613455262378,
-0.0421651843025551,-0.0262630380286178,-0.0003407087586844),
 .UNSPECIFIED.);
#281=B_SPLINE_CURVE_WITH_KNOTS('',3,(#30774,#30775,#30776,#30777,#30778,
#30779,#30780,#30781,#30782,#30783,#30784,#30785,#30786,#30787,#30788,#30789,
#30790,#30791,#30792,#30793,#30794,#30795,#30796,#30797,#30798,#30799,#30800,
#30801,#30802,#30803,#30804,#30805,#30806,#30807,#30808,#30809,#30810,#30811,
#30812,#30813,#30814,#30815,#30816,#30817,#30818,#30819,#30820,#30821,#30822,
#30823,#30824,#30825,#30826,#30827,#30828,#30829,#30830,#30831,#30832,#30833,
#30834,#30835,#30836,#30837,#30838,#30839,#30840,#30841,#30842,#30843,#30844,
#30845,#30846,#30847,#30848,#30849,#30850,#30851,#30852,#30853,#30854,#30855,
#30856,#30857,#30858,#30859,#30860,#30861,#30862,#30863,#30864,#30865,#30866,
#30867,#30868,#30869,#30870,#30871,#30872,#30873,#30874,#30875,#30876,#30877,
#30878,#30879,#30880,#30881,#30882,#30883,#30884,#30885,#30886,#30887,#30888,
#30889,#30890,#30891,#30892,#30893,#30894,#30895,#30896,#30897,#30898,#30899,
#30900,#30901,#30902,#30903,#30904,#30905,#30906,#30907,#30908,#30909,#30910,
#30911,#30912,#30913,#30914,#30915,#30916,#30917,#30918,#30919,#30920,#30921,
#30922,#30923,#30924,#30925,#30926,#30927,#30928,#30929,#30930,#30931,#30932,
#30933,#30934,#30935,#30936,#30937,#30938,#30939),.UNSPECIFIED.,.F.,.F.,
(4,2,2,2,2,2,2,2,2,2,2,2,2,2,2,2,2,2,2,2,2,2,2,2,2,2,2,2,2,2,2,2,2,2,2,
2,2,2,2,2,2,2,2,2,2,2,2,2,2,2,2,2,2,2,2,2,2,2,2,2,2,2,2,2,2,2,2,2,2,2,2,
2,2,2,2,2,2,2,2,2,2,2,4),(-1.48419118738283,-1.47921164972554,-1.47564836502954,
-1.47364501573966,-1.47206793642528,-1.47046570329038,-1.46862719724292,
-1.46551799142764,-1.45411967840977,-1.42385030441413,-1.41826632819307,
-1.4146135825172,-1.41323851531508,-1.41229269107301,-1.41142619362586,
-1.40997201289101,-1.40607144333268,-1.37193939764168,-1.36349629958902,
-1.3595268825577,-1.35629775870598,-1.35445321303051,-1.35442928284637,
-1.35439733448367,-1.3543547378575,-1.35429804700801,-1.35276370461461,
-1.35074218620048,-1.34761882012523,-1.32493705492615,-1.307552352111,-1.30139141264108,
-1.29746850112217,-1.29605517174715,-1.29510171406355,-1.29424293662532,
-1.29305912831267,-1.29004821714032,-1.27216274147199,-1.2519708500577,
-1.24162853439811,-1.23874527283915,-1.23695603791654,-1.23530892028595,
-1.23318276435052,-1.22853504276312,-1.20458170028576,-1.19065441478453,
-1.18431063867901,-1.18030437578359,-1.17887965722658,-1.17792383865088,
-1.17706707932346,-1.17589128006043,-1.17292839237909,-1.15217302071374,
-1.15091052317974,-1.13371420660334,-1.12744023820528,-1.12277666137749,
-1.12062448318291,-1.11897881018088,-1.1171847492777,-1.11427941380768,
-1.10476046252644,-1.07708845402743,-1.06836584945626,-1.06336422736914,
-1.06181765189496,-1.06083550510258,-1.05989823474671,-1.0587395173517,
-1.05587718506041,-1.03313573509099,-1.01634725762738,-1.01015987187919,
-1.00554580923614,-1.00340262046433,-1.00175808269149,-0.999959585418396,
-0.997034259152756,-0.987329249751594,-0.983859778380464),.UNSPECIFIED.);
#282=B_SPLINE_CURVE_WITH_KNOTS('',3,(#30945,#30946,#30947,#30948,#30949,
#30950,#30951,#30952,#30953,#30954,#30955,#30956,#30957,#30958,#30959,#30960,
#30961,#30962,#30963,#30964,#30965,#30966,#30967,#30968,#30969,#30970,#30971,
#30972,#30973,#30974,#30975,#30976,#30977,#30978,#30979,#30980,#30981,#30982,
#30983,#30984,#30985,#30986,#30987,#30988,#30989,#30990,#30991,#30992,#30993,
#30994,#30995,#30996,#30997,#30998,#30999,#31000,#31001,#31002,#31003,#31004,
#31005,#31006,#31007,#31008,#31009,#31010,#31011,#31012,#31013,#31014,#31015,
#31016,#31017,#31018,#31019,#31020,#31021,#31022,#31023,#31024,#31025,#31026,
#31027,#31028,#31029,#31030,#31031,#31032,#31033,#31034,#31035,#31036,#31037,
#31038,#31039,#31040,#31041,#31042,#31043,#31044,#31045,#31046,#31047,#31048,
#31049,#31050,#31051,#31052,#31053,#31054,#31055,#31056,#31057,#31058,#31059,
#31060,#31061,#31062,#31063,#31064,#31065,#31066,#31067,#31068,#31069,#31070,
#31071,#31072,#31073,#31074,#31075,#31076,#31077,#31078,#31079,#31080,#31081,
#31082),.UNSPECIFIED.,.F.,.F.,(4,2,2,2,2,2,2,2,2,2,2,2,2,2,2,2,2,2,2,2,
2,2,2,2,2,2,2,2,2,2,2,2,2,2,2,2,2,2,2,2,2,2,2,2,2,2,2,2,2,2,2,2,2,2,2,2,
2,2,2,2,2,2,2,2,2,2,2,2,4),(-0.500851044544667,-0.470894244201872,-0.465649373246299,
-0.464016774608514,-0.463015383174412,-0.462077864007863,-0.460748168974234,
-0.457397540441704,-0.452431991446596,-0.435838474650016,-0.412319264901858,
-0.407661000237684,-0.405532331804943,-0.403884202026082,-0.402094800157889,
-0.399213339085658,-0.388902201358566,-0.368830641023063,-0.350748574800594,
-0.347731367777153,-0.346546169047475,-0.345686760952296,-0.344733042471823,
-0.343320078712556,-0.339402918202136,-0.333256418499153,-0.315861217289976,
-0.293171659297553,-0.290048210487714,-0.288026114714526,-0.286393869772687,
-0.284522602736839,-0.281264959620612,-0.265217698604029,-0.250796482663248,
-0.242314702381025,-0.231891666712883,-0.230068172840124,-0.228917608321084,
-0.228002775010712,-0.226901631551511,-0.224808995620849,-0.209104479502421,
-0.184073770533595,-0.174841177479061,-0.171966249281754,-0.170178303133175,
-0.168529769197121,-0.166361465738672,-0.161612298021905,-0.155187986383279,
-0.137270113651277,-0.116185846134633,-0.113234634624075,-0.112060477173242,
-0.11120386541438,-0.110270629096301,-0.108945310054627,-0.107372092485822,
-0.104486831862825,-0.0720408047135209,-0.0582880063787682,-0.0550768717875946,
-0.0531972605332543,-0.0515659551181552,-0.0495555746376407,-0.0456326536754258,
-0.0246874792708936,-0.000340715134129704),.UNSPECIFIED.);
#283=B_SPLINE_CURVE_WITH_KNOTS('',3,(#31083,#31084,#31085,#31086,#31087,
#31088,#31089,#31090,#31091,#31092,#31093,#31094,#31095,#31096,#31097,#31098,
#31099,#31100,#31101,#31102,#31103,#31104,#31105,#31106,#31107,#31108,#31109,
#31110,#31111,#31112,#31113,#31114,#31115,#31116,#31117,#31118,#31119,#31120,
#31121,#31122,#31123,#31124,#31125,#31126,#31127,#31128,#31129,#31130,#31131,
#31132,#31133,#31134,#31135,#31136,#31137,#31138,#31139,#31140,#31141,#31142,
#31143,#31144,#31145,#31146,#31147,#31148,#31149,#31150,#31151,#31152,#31153,
#31154,#31155,#31156,#31157,#31158,#31159,#31160),.UNSPECIFIED.,.F.,.F.,
(4,2,2,2,2,2,2,2,2,2,2,2,2,2,2,2,2,2,2,2,2,2,2,2,2,2,2,2,2,2,2,2,2,2,2,
2,2,2,4),(-1.48461435640971,-1.48095567937514,-1.47974240158655,-1.47883059476506,
-1.47794354751819,-1.47691361604675,-1.47515157681881,-1.46865992468335,
-1.44929217834935,-1.42650225485955,-1.42256245148621,-1.42054875108082,
-1.41891732349596,-1.41704041715532,-1.41384087999495,-1.400282318118,-1.36771184950226,
-1.36476891410112,-1.36317400325097,-1.36180480368685,-1.3608695765384,
-1.36001083242486,-1.35882820169348,-1.35582634070192,-1.33871521949899,
-1.3179113197633,-1.31094598563399,-1.30589405601771,-1.30367217148542,
-1.30201548127954,-1.30024947393576,-1.29747573874274,-1.28913522682116,
-1.26011876050653,-1.25131260692672,-1.24627803778347,-1.24472735988065,
-1.24374400664924,-1.24301555874646),.UNSPECIFIED.);
#284=B_SPLINE_CURVE_WITH_KNOTS('',3,(#31161,#31162,#31163,#31164,#31165,
#31166,#31167,#31168,#31169,#31170,#31171,#31172,#31173,#31174,#31175,#31176,
#31177,#31178,#31179,#31180,#31181,#31182,#31183,#31184,#31185,#31186,#31187,
#31188,#31189,#31190,#31191,#31192,#31193,#31194,#31195,#31196,#31197,#31198,
#31199,#31200,#31201,#31202,#31203,#31204,#31205,#31206,#31207,#31208,#31209,
#31210,#31211,#31212,#31213,#31214,#31215,#31216,#31217,#31218,#31219,#31220,
#31221,#31222,#31223,#31224,#31225,#31226,#31227,#31228,#31229,#31230,#31231,
#31232,#31233,#31234,#31235,#31236,#31237,#31238,#31239,#31240,#31241,#31242,
#31243,#31244,#31245,#31246,#31247,#31248,#31249,#31250,#31251,#31252,#31253,
#31254,#31255,#31256,#31257,#31258,#31259,#31260,#31261,#31262,#31263,#31264,
#31265,#31266,#31267,#31268,#31269,#31270,#31271,#31272,#31273,#31274,#31275,
#31276,#31277,#31278,#31279,#31280,#31281,#31282,#31283,#31284,#31285,#31286,
#31287,#31288,#31289,#31290,#31291,#31292,#31293,#31294,#31295,#31296,#31297,
#31298,#31299,#31300,#31301,#31302,#31303,#31304,#31305,#31306,#31307,#31308,
#31309,#31310,#31311,#31312,#31313,#31314,#31315,#31316,#31317,#31318,#31319,
#31320,#31321,#31322,#31323,#31324,#31325,#31326,#31327,#31328,#31329,#31330,
#31331,#31332,#31333,#31334,#31335,#31336,#31337,#31338,#31339,#31340,#31341,
#31342,#31343,#31344,#31345,#31346,#31347,#31348,#31349,#31350,#31351,#31352,
#31353,#31354,#31355,#31356,#31357,#31358,#31359,#31360,#31361,#31362,#31363,
#31364,#31365,#31366),.UNSPECIFIED.,.F.,.F.,(4,2,2,2,2,2,2,2,2,2,2,2,2,
2,2,2,2,2,2,2,2,2,2,2,2,2,2,2,2,2,2,2,2,2,2,2,2,2,2,2,2,2,2,2,2,2,2,2,2,
2,2,2,2,2,2,2,2,2,2,2,2,2,2,2,2,2,2,2,2,2,2,2,2,2,2,2,2,2,2,2,2,2,2,2,2,
2,2,2,2,2,2,2,2,2,2,2,2,2,2,2,2,2,4),(-0.983859778380464,-0.956504322260066,
-0.949990619817789,-0.945907656089805,-0.944472491112579,-0.94351437847939,
-0.942659206983767,-0.941490152443025,-0.938537859202834,-0.917332862261902,
-0.899520681043165,-0.893118682458089,-0.888382026189533,-0.886216351454495,
-0.884568565581389,-0.8827802145083,-0.87990195187403,-0.870633334570441,
-0.845622578781929,-0.829924881779486,-0.827832617921649,-0.826731724218592,
-0.825817128910256,-0.824666915160807,-0.822844094873349,-0.812426562834528,
-0.803964432365397,-0.789576630597031,-0.77350823421958,-0.770250378464962,
-0.768379364120978,-0.766747558273291,-0.764726292123414,-0.761604649487132,
-0.742185020241834,-0.726888864122854,-0.712777138059242,-0.710861168394497,
-0.709683061650375,-0.708766760155919,-0.707687869288201,-0.705699914213867,
-0.693932804271416,-0.670440108515074,-0.656315300476018,-0.653083468215382,
-0.651199366351649,-0.649731815794533,-0.647799964512289,-0.644256897049762,
-0.619263397012194,-0.596808923862333,-0.593921997393029,-0.592758904546354,
-0.591820344534971,-0.590839596829148,-0.589300015442163,-0.584362923889726,
-0.575808244920175,-0.549698234382592,-0.538680644571589,-0.535623394671848,
-0.533795924912142,-0.532157860650581,-0.530069022833586,-0.525745814953144,
-0.508990969644128,-0.494870477813161,-0.478357825960762,-0.476423050565638,
-0.475239368364634,-0.474322614561491,-0.473247733329158,-0.471278556459339,
-0.460011379886193,-0.444199836384678,-0.422254400401983,-0.41911064692152,
-0.417082675807384,-0.415450389596015,-0.413584213706913,-0.410348705206556,
-0.394754795609124,-0.372716756975284,-0.367134511753262,-0.360497204350288,
-0.358722776699775,-0.357690189049464,-0.35676509042552,-0.355510117523619,
-0.352611700451612,-0.339054781104996,-0.335061952140706,-0.306431703458366,
-0.302076518480185,-0.299981611743217,-0.298342899413162,-0.296518943141558,
-0.293477681225447,-0.281159033943898,-0.25118057349547,-0.243408795535128,
-0.241907325797883),.UNSPECIFIED.);
#285=B_SPLINE_CURVE_WITH_KNOTS('',3,(#31371,#31372,#31373,#31374,#31375,
#31376,#31377,#31378,#31379,#31380,#31381,#31382,#31383,#31384,#31385,#31386,
#31387,#31388,#31389,#31390,#31391,#31392,#31393,#31394,#31395,#31396,#31397,
#31398,#31399,#31400,#31401,#31402,#31403,#31404,#31405,#31406,#31407,#31408,
#31409,#31410,#31411,#31412,#31413,#31414,#31415,#31416,#31417,#31418,#31419,
#31420,#31421,#31422,#31423,#31424,#31425,#31426,#31427,#31428,#31429,#31430,
#31431,#31432,#31433,#31434,#31435,#31436,#31437,#31438,#31439,#31440,#31441,
#31442,#31443,#31444,#31445,#31446,#31447,#31448,#31449,#31450,#31451,#31452,
#31453,#31454,#31455,#31456,#31457,#31458,#31459,#31460,#31461,#31462,#31463,
#31464,#31465,#31466,#31467,#31468,#31469,#31470,#31471,#31472,#31473,#31474,
#31475,#31476,#31477,#31478,#31479,#31480,#31481,#31482,#31483,#31484,#31485,
#31486,#31487,#31488,#31489,#31490,#31491,#31492,#31493,#31494,#31495,#31496,
#31497,#31498,#31499,#31500,#31501,#31502,#31503,#31504,#31505,#31506,#31507,
#31508,#31509,#31510,#31511,#31512,#31513,#31514,#31515,#31516,#31517,#31518,
#31519,#31520,#31521,#31522,#31523,#31524,#31525,#31526,#31527,#31528,#31529,
#31530,#31531,#31532,#31533,#31534,#31535,#31536,#31537,#31538,#31539,#31540,
#31541,#31542,#31543,#31544,#31545,#31546,#31547,#31548,#31549,#31550,#31551,
#31552,#31553,#31554,#31555,#31556,#31557,#31558,#31559,#31560,#31561,#31562,
#31563,#31564,#31565,#31566,#31567,#31568,#31569,#31570,#31571,#31572,#31573,
#31574,#31575,#31576,#31577,#31578,#31579,#31580,#31581,#31582,#31583,#31584,
#31585,#31586,#31587,#31588,#31589,#31590),.UNSPECIFIED.,.F.,.F.,(4,2,2,
2,2,2,2,2,2,2,2,2,2,2,2,2,2,2,2,2,2,2,2,2,2,2,2,2,2,2,2,2,2,2,2,2,2,2,2,
2,2,2,2,2,2,2,2,2,2,2,2,2,2,2,2,2,2,2,2,2,2,2,2,2,2,2,2,2,2,2,2,2,2,2,2,
2,2,2,2,2,2,2,2,2,2,2,2,2,2,2,2,2,2,2,2,2,2,2,2,2,2,2,2,2,2,2,2,2,2,4),
(-1.2427255514666,-1.23060639702225,-1.22734995878737,-1.22547924039624,
-1.22384738677346,-1.2218256634024,-1.21870254924936,-1.19599880834317,
-1.17858368190725,-1.17244529391067,-1.16853251114878,-1.16712041934795,
-1.16616709789873,-1.16530792723202,-1.1641228860977,-1.16110513657904,
-1.14308012134878,-1.12299513858127,-1.11268157357094,-1.10980059671523,
-1.10801169641925,-1.10636416351028,-1.1042364574599,-1.09958115577374,
-1.07591712084999,-1.06177958613118,-1.05538720100713,-1.05135878925255,
-1.04993095819828,-1.04897439716279,-1.04811792428216,-1.04694382727023,
-1.04399201665834,-1.0229712970852,-1.00503526460183,-0.998607946502903,
-0.993856820084637,-0.991688375720636,-0.990040030279437,-0.988252573869962,
-0.985379064781073,-0.976157428830489,-0.951108805714289,-0.93539687307613,
-0.933304157500287,-0.932203074612696,-0.931288375468315,-0.930138077140012,
-0.928315145539022,-0.91789723601422,-0.909425950442992,-0.89502035921056,
-0.878978888820759,-0.875722134865666,-0.87385127700113,-0.872219326820631,
-0.870197516313012,-0.867074326196596,-0.844384905671827,-0.826995860488933,
-0.820833303343909,-0.816909327136579,-0.815495580962352,-0.814541831431272,
-0.813682779619426,-0.812498575102276,-0.80948655641407,-0.790609908013162,
-0.771155266060003,-0.764432591104257,-0.759515363871419,-0.757317245885591,
-0.755664477296493,-0.753889572141093,-0.751073898163996,-0.742373361690178,
-0.726899212117861,-0.702037861028191,-0.6992589620858,-0.698038179503742,
-0.697114789673177,-0.696075504625279,-0.694270921341789,-0.686242128345383,
-0.666913550870398,-0.644940258253765,-0.641801216129891,-0.639774546274086,
-0.638142181373455,-0.636274683570456,-0.633033700117319,-0.617332040787526,
-0.594373451152823,-0.589357020035347,-0.583119770253274,-0.581382332131788,
-0.580357811938072,-0.579430029637448,-0.578157702095767,-0.575158706713002,
-0.570875962911844,-0.558070181845823,-0.529054678352759,-0.524741928417015,
-0.522654986779741,-0.521017005459846,-0.519188171415971,-0.516125144550386,
-0.503498200677261,-0.500851044544667),.UNSPECIFIED.);
#286=B_SPLINE_CURVE_WITH_KNOTS('',3,(#31592,#31593,#31594,#31595,#31596,
#31597,#31598,#31599,#31600,#31601,#31602,#31603,#31604,#31605,#31606,#31607,
#31608,#31609,#31610,#31611,#31612,#31613,#31614,#31615,#31616,#31617,#31618,
#31619,#31620,#31621,#31622,#31623,#31624,#31625,#31626,#31627,#31628,#31629,
#31630,#31631,#31632,#31633,#31634,#31635,#31636,#31637,#31638,#31639,#31640,
#31641,#31642,#31643,#31644,#31645,#31646,#31647,#31648,#31649,#31650,#31651,
#31652,#31653,#31654,#31655,#31656,#31657,#31658,#31659,#31660,#31661,#31662,
#31663,#31664,#31665,#31666,#31667,#31668,#31669,#31670,#31671,#31672,#31673,
#31674,#31675,#31676,#31677,#31678,#31679),.UNSPECIFIED.,.F.,.F.,(4,2,2,
2,2,2,2,2,2,2,2,2,2,2,2,2,2,2,2,2,2,2,2,2,2,2,2,2,2,2,2,2,2,2,2,2,2,2,2,
2,2,2,2,4),(-0.241907325797883,-0.241564736786382,-0.2405060295345,-0.239679017943203,
-0.238522152108265,-0.236154348097133,-0.233007704473341,-0.225126565777923,
-0.201723109279611,-0.187408074081491,-0.184165567342836,-0.182278938034591,
-0.180648332175155,-0.178647450960559,-0.174771021102985,-0.169825066938676,
-0.158111036262439,-0.144624591959884,-0.126640701292084,-0.124722421562707,
-0.123543586682625,-0.122644011424788,-0.121598200755175,-0.120466219902755,
-0.118697580026735,-0.115283174764137,-0.106361259804418,-0.0761777649382564,
-0.0689124259559693,-0.0662779636630842,-0.0647155665043315,-0.0630646866011098,
-0.0608784413088461,-0.0560277048481825,-0.0494229319742788,-0.0456307667643694,
-0.0142563478955802,-0.00858120041559184,-0.00690292372145922,-0.00589149484902674,
-0.00501412596607927,-0.00409312851683857,-0.00241291697315785,-0.000340185083165174),
 .UNSPECIFIED.);
#287=B_SPLINE_CURVE_WITH_KNOTS('',3,(#31680,#31681,#31682,#31683,#31684,
#31685,#31686,#31687,#31688,#31689,#31690,#31691,#31692,#31693,#31694,#31695,
#31696,#31697,#31698,#31699,#31700,#31701,#31702,#31703,#31704,#31705,#31706,
#31707,#31708,#31709,#31710,#31711,#31712,#31713,#31714,#31715,#31716,#31717,
#31718,#31719,#31720,#31721,#31722,#31723,#31724,#31725,#31726,#31727,#31728,
#31729,#31730,#31731,#31732,#31733,#31734,#31735,#31736,#31737,#31738,#31739,
#31740,#31741,#31742,#31743,#31744,#31745,#31746,#31747,#31748,#31749,#31750,
#31751,#31752,#31753,#31754,#31755,#31756,#31757,#31758,#31759,#31760,#31761,
#31762,#31763,#31764,#31765,#31766,#31767,#31768,#31769,#31770,#31771,#31772,
#31773,#31774,#31775,#31776,#31777,#31778,#31779,#31780,#31781,#31782,#31783,
#31784,#31785,#31786,#31787,#31788,#31789,#31790,#31791,#31792,#31793,#31794),
 .UNSPECIFIED.,.F.,.F.,(4,3,3,3,3,3,3,3,3,3,3,3,3,3,3,3,3,3,3,3,3,3,3,3,
3,3,3,3,3,3,3,3,3,3,3,3,3,3,4),(128.805298797903,128.92420180571,129.042936368382,
129.161556941574,129.280117790517,129.398763160983,129.517442871689,129.636361003745,
129.752144419847,129.876237071814,129.995823264793,130.115290605822,130.234691814404,
130.354079495645,130.47358802796,130.593169404387,130.71296572914,130.744885635581,
130.868978287548,130.988564594503,131.10803205027,131.227433374119,131.346821170921,
131.466329818357,131.585911309774,131.705707748165,131.737626851315,131.861719503282,
131.981305352592,132.100772351382,132.22017321981,132.339560563643,132.459068765062,
132.578649814039,132.698445819611,132.730368067049,132.850162222238,132.969754516053,
133.043121691919),.UNSPECIFIED.);
#288=B_SPLINE_CURVE_WITH_KNOTS('',3,(#31800,#31801,#31802,#31803,#31804,
#31805,#31806,#31807,#31808,#31809,#31810,#31811,#31812,#31813,#31814,#31815,
#31816,#31817,#31818,#31819,#31820,#31821,#31822,#31823,#31824,#31825,#31826,
#31827,#31828,#31829,#31830,#31831,#31832,#31833,#31834,#31835,#31836,#31837,
#31838,#31839,#31840,#31841,#31842,#31843,#31844,#31845,#31846,#31847,#31848,
#31849,#31850,#31851,#31852,#31853,#31854,#31855,#31856,#31857,#31858,#31859,
#31860,#31861,#31862,#31863,#31864,#31865,#31866,#31867,#31868,#31869,#31870,
#31871,#31872,#31873,#31874,#31875,#31876,#31877,#31878,#31879,#31880,#31881,
#31882,#31883,#31884,#31885,#31886,#31887,#31888,#31889,#31890,#31891,#31892,
#31893,#31894,#31895,#31896,#31897,#31898,#31899,#31900,#31901,#31902,#31903,
#31904,#31905,#31906,#31907,#31908,#31909,#31910,#31911),.UNSPECIFIED.,
 .F.,.F.,(4,3,3,3,3,3,3,3,3,3,3,3,3,3,3,3,3,3,3,3,3,3,3,3,3,3,3,3,3,3,3,
3,3,3,3,3,3,4),(135.088484104816,135.235319650575,135.372911768261,135.497004420228,
135.616613963295,135.736104467611,135.855528609251,135.974938949634,136.094469573001,
136.214072732833,136.33389017762,136.365652983995,136.489745635962,136.609357211818,
136.728850230044,136.848277355743,136.967691140023,137.087225850178,137.206833475805,
137.326655887354,137.358394199729,137.482486851696,137.601928623404,137.721251639095,
137.840508895953,137.959753276841,138.079120520349,138.198561623553,138.318220556655,
138.351135415463,138.472967083591,138.592769381413,138.712449797914,138.832060644392,
138.955492673417,139.075196120745,139.200492440618,139.325788760491),
 .UNSPECIFIED.);
#289=B_SPLINE_CURVE_WITH_KNOTS('',3,(#31912,#31913,#31914,#31915,#31916,
#31917,#31918,#31919,#31920,#31921,#31922,#31923,#31924,#31925,#31926,#31927,
#31928,#31929,#31930,#31931,#31932,#31933,#31934,#31935,#31936,#31937,#31938,
#31939,#31940,#31941,#31942,#31943,#31944,#31945,#31946,#31947,#31948,#31949,
#31950,#31951,#31952,#31953,#31954,#31955,#31956,#31957,#31958,#31959,#31960,
#31961,#31962,#31963,#31964,#31965,#31966,#31967,#31968,#31969,#31970,#31971,
#31972,#31973,#31974,#31975,#31976,#31977,#31978,#31979,#31980,#31981,#31982,
#31983,#31984,#31985),.UNSPECIFIED.,.F.,.F.,(4,2,2,2,2,2,2,2,2,2,2,2,2,
2,2,2,2,2,2,2,2,2,2,2,2,2,2,2,2,2,2,2,2,2,2,2,4),(-1.48433664459609,-1.46671782054178,
-1.46371943846842,-1.461758308634,-1.46019416291955,-1.45856476614673,-1.45668477152549,
-1.45346669170546,-1.43956052911776,-1.42476392374183,-1.41144205555522,
-1.40368120358948,-1.40189154794862,-1.40085624895909,-1.39993245513015,
-1.39870663663035,-1.39589864627127,-1.37133735902695,-1.35570646797292,
-1.34977485815692,-1.34534046054347,-1.34329373304463,-1.34164426587415,
-1.33985883508753,-1.336995700033,-1.32787579135332,-1.30275607210206,-1.28701833701235,
-1.28492474437849,-1.28382323918716,-1.28290836603037,-1.28175799058702,
-1.2799348673473,-1.26951253007453,-1.261048704623,-1.24664495753197,-1.2427255514666),
 .UNSPECIFIED.);
#290=B_SPLINE_CURVE_WITH_KNOTS('',3,(#31987,#31988,#31989,#31990,#31991,
#31992,#31993,#31994,#31995,#31996,#31997,#31998,#31999,#32000,#32001,#32002,
#32003,#32004,#32005,#32006,#32007,#32008,#32009,#32010,#32011,#32012,#32013,
#32014,#32015,#32016,#32017,#32018,#32019,#32020,#32021,#32022,#32023,#32024,
#32025,#32026,#32027,#32028,#32029,#32030,#32031,#32032,#32033,#32034,#32035,
#32036,#32037,#32038,#32039,#32040,#32041),.UNSPECIFIED.,.F.,.F.,(4,3,3,
3,3,3,3,3,3,3,3,3,3,3,3,3,3,3,4),(133.043121691919,133.16254457611,133.281931744498,
133.401423904568,133.520968990874,133.640744469938,133.723109282783,133.84720193475,
133.966788928961,134.086257075103,134.205659091046,134.325047580267,134.444556915418,
134.56413909254,134.683936206814,134.715850498517,134.851216151486,134.985568509351,
135.088484103636),.UNSPECIFIED.);
#291=B_SPLINE_CURVE_WITH_KNOTS('',3,(#32042,#32043,#32044,#32045,#32046,
#32047,#32048,#32049,#32050,#32051,#32052,#32053,#32054,#32055,#32056,#32057,
#32058,#32059,#32060,#32061,#32062,#32063,#32064,#32065,#32066,#32067,#32068,
#32069,#32070,#32071,#32072,#32073,#32074,#32075,#32076,#32077,#32078,#32079,
#32080,#32081,#32082,#32083,#32084,#32085,#32086,#32087,#32088,#32089,#32090,
#32091,#32092,#32093,#32094,#32095,#32096,#32097,#32098,#32099,#32100,#32101,
#32102,#32103,#32104,#32105,#32106,#32107,#32108,#32109,#32110,#32111,#32112,
#32113,#32114,#32115,#32116,#32117,#32118,#32119,#32120,#32121,#32122,#32123,
#32124,#32125,#32126,#32127,#32128,#32129,#32130,#32131,#32132,#32133,#32134,
#32135,#32136,#32137,#32138,#32139,#32140,#32141,#32142,#32143,#32144,#32145,
#32146,#32147,#32148,#32149,#32150,#32151,#32152,#32153,#32154,#32155,#32156,
#32157,#32158,#32159,#32160,#32161,#32162,#32163,#32164,#32165,#32166,#32167,
#32168,#32169,#32170,#32171,#32172,#32173,#32174,#32175,#32176,#32177,#32178,
#32179,#32180,#32181,#32182,#32183,#32184,#32185,#32186,#32187,#32188,#32189,
#32190,#32191,#32192,#32193,#32194,#32195),.UNSPECIFIED.,.F.,.F.,(4,2,2,
2,2,2,2,2,2,2,2,2,2,2,2,2,2,2,2,2,2,2,2,2,2,2,2,2,2,2,2,2,2,2,2,2,2,2,2,
2,2,2,2,2,2,2,2,2,2,2,2,2,2,2,2,2,2,2,2,2,2,2,2,2,2,2,2,2,2,2,2,2,2,2,2,
2,4),(0.500786432389318,0.512128357748242,0.515212285446151,0.517046105357922,
0.518520106997671,0.520519510482704,0.524386314514495,0.529315375315604,
0.540964201475301,0.559881492768139,0.562846546633378,0.572769307541564,
0.574567560361756,0.57571031546824,0.576624314654795,0.57773081720011,0.579852194656469,
0.597599957817087,0.627349344461373,0.631646249968152,0.633728953812867,
0.635365090787654,0.637193378608985,0.640259064057918,0.652953175769306,
0.686280538407828,0.690882046830322,0.692434278844384,0.693319577537061,
0.694251550172155,0.695550980788332,0.698712808466119,0.703307756442877,
0.717746353397341,0.744260486092286,0.748350882736053,0.750423186768318,
0.751955117939803,0.753626638816482,0.755935134568518,0.761504157214373,
0.782949708419264,0.805845372659464,0.808699585127555,0.8098573260419,0.810794755757872,
0.811777965195418,0.813328434968161,0.818362519764478,0.827168181138911,
0.855641342762716,0.864409188682483,0.867232411448932,0.869008841809705,
0.870627939153777,0.872750076516439,0.875104279531898,0.879064300347567,
0.88747727406923,0.921039827713324,0.925427952290645,0.926952410093915,
0.927832712943928,0.928768170478391,0.930087463870695,0.933373504830684,
0.938211794778996,0.954036446931215,0.968368149659771,0.979680459449246,
0.983222018779296,0.985345229338978,0.9869922044933,0.988519355524955,0.990278595138859,
0.992780135022167,1.00127085069662),.UNSPECIFIED.);
#292=B_SPLINE_CURVE_WITH_KNOTS('',3,(#32201,#32202,#32203,#32204,#32205,
#32206),.UNSPECIFIED.,.F.,.F.,(4,1,1,4),(-4.09202352044853,-3.97096486293603,
-2.97822364720202,-2.07364390538107),.UNSPECIFIED.);
#293=B_SPLINE_CURVE_WITH_KNOTS('',3,(#32209,#32210,#32211,#32212,#32213),
 .UNSPECIFIED.,.F.,.F.,(4,1,4),(0.,0.992741215733998,1.12274180646084),
 .UNSPECIFIED.);
#294=B_SPLINE_CURVE_WITH_KNOTS('',3,(#32218,#32219,#32220,#32221,#32222,
#32223,#32224,#32225,#32226,#32227),.UNSPECIFIED.,.F.,.F.,(4,1,1,1,1,1,
1,4),(-10.3752053909602,-9.92741215734008,-8.93467094160607,-7.94192972587206,
-6.94918851013805,-5.95644729440404,-4.96370607867004,-4.09202352044853),
 .UNSPECIFIED.);
#295=B_SPLINE_CURVE_WITH_KNOTS('',3,(#32228,#32229,#32230,#32231,#32232,
#32233,#32234,#32235,#32236,#32237,#32238,#32239,#32240,#32241,#32242,#32243,
#32244,#32245,#32246,#32247,#32248,#32249,#32250,#32251,#32252,#32253,#32254,
#32255,#32256,#32257,#32258,#32259,#32260,#32261,#32262,#32263,#32264,#32265,
#32266,#32267,#32268,#32269,#32270,#32271,#32272,#32273,#32274,#32275,#32276,
#32277,#32278,#32279,#32280,#32281,#32282,#32283,#32284,#32285,#32286,#32287,
#32288,#32289,#32290,#32291,#32292,#32293,#32294,#32295,#32296,#32297,#32298,
#32299,#32300,#32301,#32302,#32303,#32304,#32305,#32306,#32307,#32308,#32309,
#32310,#32311,#32312,#32313,#32314,#32315,#32316,#32317,#32318,#32319,#32320,
#32321,#32322,#32323,#32324,#32325,#32326,#32327,#32328,#32329,#32330,#32331,
#32332,#32333,#32334,#32335,#32336,#32337,#32338,#32339,#32340,#32341,#32342,
#32343,#32344,#32345,#32346,#32347,#32348,#32349,#32350,#32351,#32352,#32353,
#32354,#32355,#32356,#32357,#32358,#32359,#32360,#32361,#32362,#32363,#32364,
#32365,#32366,#32367,#32368,#32369,#32370,#32371,#32372,#32373,#32374,#32375,
#32376,#32377,#32378,#32379,#32380,#32381,#32382,#32383,#32384,#32385,#32386,
#32387,#32388,#32389,#32390,#32391,#32392,#32393,#32394,#32395,#32396,#32397,
#32398,#32399),.UNSPECIFIED.,.F.,.F.,(4,3,3,3,3,3,3,3,3,3,3,3,3,3,3,3,3,
3,3,3,3,3,3,3,3,3,3,3,3,3,3,3,3,3,3,3,3,3,3,3,3,3,3,3,3,3,3,3,3,3,3,3,3,
3,3,3,3,4),(1.12274180646084,1.23355937374209,1.34423918815353,1.45482944455971,
1.56537815734206,1.67601277927824,1.78668774769182,1.89757125282276,1.98548243146801,
2.09908269663091,2.21248030600278,2.32576514911402,2.43898180620018,2.55217475654608,
2.66546889339697,2.77881317901057,2.89236747726848,2.97822364720202,3.09188643018773,
3.20535340945894,3.31871176665814,3.43200594742818,3.54528030150624,3.65866123708271,
3.77209545052106,3.88574371923928,3.97096486293603,4.0843145896902,4.19745986938771,
4.31049148709486,4.4234544918255,4.536393830391,4.64943648022474,4.76253007371526,
4.87583814693796,4.96370607867004,5.07720989041121,5.19051208640097,5.30370223548262,
5.41682510052755,5.52992534434195,5.64312923773688,5.75638451459586,5.86985297185556,
5.95644729440405,6.06994635889941,6.18324442746533,6.29643083241813,6.40955034376972,
6.522647631939,6.63584921520513,6.74910253713155,6.86256965122693,6.94918851013806,
7.07058636504131,7.19168899525419,7.3123612953248,7.40592711324594),
 .UNSPECIFIED.);
#296=B_SPLINE_CURVE_WITH_KNOTS('',3,(#32404,#32405,#32406,#32407,#32408,
#32409,#32410,#32411,#32412,#32413,#32414,#32415,#32416,#32417,#32418,#32419,
#32420,#32421,#32422,#32423,#32424,#32425,#32426,#32427,#32428,#32429,#32430,
#32431,#32432,#32433,#32434,#32435,#32436,#32437,#32438,#32439,#32440,#32441,
#32442,#32443,#32444,#32445,#32446,#32447,#32448,#32449,#32450,#32451,#32452,
#32453,#32454,#32455,#32456,#32457,#32458,#32459,#32460,#32461,#32462,#32463,
#32464,#32465,#32466,#32467,#32468,#32469,#32470,#32471,#32472,#32473,#32474,
#32475,#32476,#32477,#32478,#32479,#32480,#32481,#32482,#32483,#32484,#32485,
#32486,#32487,#32488,#32489,#32490,#32491,#32492,#32493,#32494,#32495,#32496,
#32497,#32498,#32499,#32500,#32501,#32502,#32503,#32504,#32505,#32506,#32507,
#32508,#32509,#32510,#32511,#32512,#32513,#32514,#32515,#32516,#32517,#32518,
#32519,#32520,#32521,#32522,#32523,#32524,#32525,#32526,#32527,#32528,#32529,
#32530,#32531,#32532,#32533,#32534,#32535,#32536,#32537,#32538,#32539,#32540,
#32541,#32542,#32543,#32544,#32545,#32546,#32547,#32548,#32549,#32550,#32551,
#32552,#32553,#32554,#32555,#32556,#32557,#32558,#32559,#32560,#32561,#32562,
#32563,#32564,#32565,#32566,#32567,#32568,#32569,#32570,#32571,#32572,#32573,
#32574,#32575),.UNSPECIFIED.,.F.,.F.,(4,3,3,3,3,3,3,3,3,3,3,3,3,3,3,3,3,
3,3,3,3,3,3,3,3,3,3,3,3,3,3,3,3,3,3,3,3,3,3,3,3,3,3,3,3,3,3,3,3,3,3,3,3,
3,3,3,3,4),(-16.6583941342588,-16.5466839297704,-16.4350647570386,-16.3234895832408,
-16.2118304445513,-16.1001347697573,-15.9882254957626,-15.8838594517441,
-15.7703802606902,-15.6571027547231,-15.5439373184522,-15.4308391434175,
-15.3177635212612,-15.2045839431989,-15.0913528487032,-14.9779080503663,
-14.8911182360101,-14.7776389385898,-14.6643613248847,-14.5511957801209,
-14.4380974960384,-14.325021764479,-14.2118420773477,-14.098610873801,-13.985165967815,
-13.8983770202761,-13.7848981557516,-13.671620974954,-13.5584558627794,
-13.4453580102098,-13.3322827083287,-13.2191034446402,-13.1058726617254,
-12.9924281665408,-12.9056358045421,-12.7921564211267,-12.6788787267111,
-12.5657131045183,-12.4526147463851,-12.3395389442535,-12.2263591924163,
-12.1131279273202,-11.9996829656535,-11.9128945888081,-11.7994146477071,
-11.6861363842348,-11.5729701864831,-11.4598712473816,-11.3467948599574,
-11.2336145209221,-11.1203826666689,-11.0069371201003,-10.9201533730741,
-10.8031896759694,-10.6865155346278,-10.5700128234899,-10.4536777554397,
-10.3752088276281),.UNSPECIFIED.);
#297=B_SPLINE_CURVE_WITH_KNOTS('',3,(#32576,#32577,#32578,#32579,#32580,
#32581,#32582,#32583,#32584,#32585,#32586,#32587,#32588,#32589,#32590,#32591,
#32592,#32593,#32594,#32595,#32596,#32597,#32598,#32599,#32600,#32601,#32602,
#32603,#32604,#32605,#32606,#32607,#32608,#32609,#32610,#32611,#32612,#32613,
#32614,#32615,#32616,#32617,#32618,#32619,#32620,#32621,#32622,#32623,#32624,
#32625,#32626,#32627,#32628,#32629,#32630,#32631,#32632,#32633,#32634,#32635,
#32636,#32637,#32638,#32639,#32640,#32641,#32642,#32643,#32644,#32645,#32646,
#32647,#32648,#32649,#32650,#32651,#32652,#32653,#32654,#32655,#32656,#32657,
#32658,#32659,#32660,#32661,#32662,#32663,#32664,#32665,#32666,#32667,#32668,
#32669,#32670,#32671,#32672,#32673,#32674,#32675,#32676,#32677,#32678,#32679,
#32680,#32681,#32682,#32683,#32684,#32685,#32686,#32687,#32688,#32689,#32690,
#32691,#32692,#32693,#32694,#32695,#32696,#32697,#32698,#32699,#32700,#32701,
#32702,#32703,#32704,#32705,#32706,#32707,#32708,#32709,#32710,#32711,#32712,
#32713,#32714,#32715,#32716,#32717,#32718,#32719,#32720,#32721,#32722,#32723,
#32724,#32725,#32726,#32727,#32728,#32729,#32730,#32731,#32732,#32733,#32734,
#32735,#32736,#32737,#32738,#32739,#32740,#32741,#32742,#32743,#32744,#32745,
#32746,#32747),.UNSPECIFIED.,.F.,.F.,(4,3,3,3,3,3,3,3,3,3,3,3,3,3,3,3,3,
3,3,3,3,3,3,3,3,3,3,3,3,3,3,3,3,3,3,3,3,3,3,3,3,3,3,3,3,3,3,3,3,3,3,3,3,
3,3,3,3,4),(7.40592711364043,7.52254421271226,7.63940844128119,7.75640405188725,
7.87369086241296,7.94192972587207,8.05541344444123,8.16869552285997,8.28186555550056,
8.39496834237503,8.50804858342432,8.62123275397868,8.73446843335694,8.84791774642208,
8.93467094160608,9.04815210392042,9.16143166055977,9.27459919455485,9.38769951052788,
9.50077731305781,9.61395911540794,9.72719246201059,9.84063953017342,9.92741215734009,
10.0408890554138,10.1541642137661,10.267327270786,10.3804230392832,10.4934962319243,
10.6066733642354,10.7199020001953,10.8333443496985,10.9201533730741,11.0336333034009,
11.1469115595896,11.260077752197,11.3731766882899,11.4862530748409,11.5994334163036,
11.7126652748211,11.826110828601,11.9128945888081,12.0263739369873,12.1396516092528,
12.2528172173109,12.3659155693028,12.4789913732743,12.5921711392499,12.7054024253357,
12.8188474189226,12.9056358045421,13.0175007058498,13.1292062137034,13.2407996694667,
13.3528778571923,13.4644298780027,13.5767711491859,13.6891124203691),
 .UNSPECIFIED.);
#298=B_SPLINE_CURVE_WITH_KNOTS('',3,(#32752,#32753,#32754,#32755,#32756,
#32757,#32758,#32759,#32760,#32761,#32762,#32763,#32764,#32765,#32766,#32767,
#32768,#32769,#32770,#32771,#32772,#32773,#32774,#32775,#32776,#32777,#32778,
#32779,#32780,#32781,#32782,#32783,#32784,#32785,#32786,#32787,#32788,#32789,
#32790,#32791,#32792,#32793,#32794,#32795,#32796,#32797,#32798,#32799,#32800,
#32801,#32802,#32803,#32804,#32805,#32806,#32807,#32808,#32809,#32810,#32811,
#32812,#32813,#32814,#32815,#32816,#32817,#32818,#32819,#32820,#32821,#32822,
#32823,#32824,#32825,#32826,#32827,#32828,#32829,#32830,#32831,#32832,#32833,
#32834,#32835,#32836,#32837,#32838,#32839,#32840,#32841,#32842,#32843,#32844,
#32845,#32846,#32847,#32848,#32849,#32850,#32851,#32852,#32853,#32854,#32855,
#32856,#32857,#32858,#32859,#32860,#32861,#32862,#32863,#32864,#32865,#32866,
#32867,#32868,#32869,#32870,#32871,#32872,#32873,#32874,#32875,#32876,#32877,
#32878,#32879,#32880,#32881,#32882,#32883,#32884,#32885,#32886,#32887,#32888,
#32889,#32890,#32891,#32892,#32893,#32894,#32895,#32896,#32897,#32898,#32899,
#32900,#32901,#32902,#32903,#32904,#32905,#32906,#32907,#32908,#32909,#32910,
#32911,#32912,#32913,#32914,#32915,#32916,#32917,#32918,#32919,#32920,#32921,
#32922,#32923),.UNSPECIFIED.,.F.,.F.,(4,3,3,3,3,3,3,3,3,3,3,3,3,3,3,3,3,
3,3,3,3,3,3,3,3,3,3,3,3,3,3,3,3,3,3,3,3,3,3,3,3,3,3,3,3,3,3,3,3,3,3,3,3,
3,3,3,3,4),(-22.9415794419873,-22.8330479618822,-22.7195687853659,-22.6062912933183,
-22.4931258705797,-22.3800277086708,-22.2669520992146,-22.1537725331014,
-22.0405414501564,-21.9270966625821,-21.8403067461482,-21.7268275693145,
-21.6135500769637,-21.500384653931,-21.3872864917374,-21.2742108820062,
-21.1610313156354,-21.0478002324418,-20.9343554446367,-20.8475655304142,
-20.734086350754,-20.6208088555591,-20.5076434296737,-20.3945452646239,
-20.2814696520382,-20.1682900828382,-20.0550589968252,-19.941614206252,
-19.8548243146802,-19.7413451423172,-19.6280676544019,-19.5149022357798,
-19.4018040779645,-19.2887284725718,-19.175548910444,-19.0623178314471,
-18.9488730477109,-18.8620830989461,-18.7486039218275,-18.6353264292627,
-18.5221610060591,-18.4090628437377,-18.2959872339214,-18.1828076675315,
-18.0695765843554,-17.9561317966267,-17.8693418832121,-17.7558626881208,
-17.6425851774241,-17.5294197360051,-17.416321555418,-17.3032459273188,
-17.1900663427658,-17.0768352414653,-16.9633904359026,-16.8766006674781,
-16.7220055544691,-16.6583941348077),.UNSPECIFIED.);
#299=B_SPLINE_CURVE_WITH_KNOTS('',3,(#32924,#32925,#32926,#32927,#32928,
#32929,#32930,#32931,#32932,#32933,#32934,#32935,#32936,#32937,#32938,#32939,
#32940,#32941,#32942,#32943,#32944,#32945,#32946,#32947,#32948,#32949,#32950,
#32951,#32952,#32953,#32954,#32955,#32956,#32957,#32958,#32959,#32960,#32961,
#32962,#32963,#32964,#32965,#32966,#32967,#32968,#32969,#32970,#32971,#32972,
#32973,#32974,#32975,#32976,#32977,#32978,#32979,#32980,#32981,#32982,#32983,
#32984,#32985,#32986,#32987,#32988,#32989,#32990,#32991,#32992,#32993,#32994,
#32995,#32996,#32997,#32998,#32999,#33000,#33001,#33002,#33003,#33004,#33005,
#33006,#33007,#33008,#33009,#33010,#33011,#33012,#33013,#33014,#33015,#33016,
#33017,#33018,#33019,#33020,#33021,#33022,#33023,#33024,#33025,#33026,#33027,
#33028,#33029,#33030,#33031,#33032,#33033,#33034,#33035,#33036,#33037,#33038,
#33039,#33040,#33041,#33042,#33043,#33044,#33045,#33046,#33047,#33048,#33049,
#33050,#33051,#33052,#33053,#33054,#33055,#33056,#33057,#33058,#33059,#33060,
#33061,#33062,#33063,#33064,#33065,#33066,#33067,#33068,#33069,#33070,#33071,
#33072,#33073,#33074,#33075,#33076,#33077,#33078,#33079,#33080,#33081,#33082,
#33083,#33084,#33085,#33086,#33087,#33088,#33089,#33090,#33091,#33092,#33093,
#33094,#33095),.UNSPECIFIED.,.F.,.F.,(4,3,3,3,3,3,3,3,3,3,3,3,3,3,3,3,3,
3,3,3,3,3,3,3,3,3,3,3,3,3,3,3,3,3,3,3,3,3,3,3,3,3,3,3,3,3,3,3,3,3,3,3,3,
3,3,3,3,4),(13.68911242082,13.8466881871004,13.8983770202761,14.0118563143335,
14.1251339258355,14.2382994691069,14.3513977524058,14.4644734838899,14.5776531720396,
14.6908843772135,14.804329285801,14.8911182360101,15.0045974231147,15.1178749266047,
15.2310403613002,15.3441385356588,15.4572141580369,15.5703937377043,15.6836248345758,
15.7970696365178,15.8838594517441,15.9973385929408,16.1106160486916,16.2237814345631,
16.3368795591022,16.4499551307528,16.5631346586859,16.676365703184,16.789810452353,
16.8766006674781,16.9900798618807,17.1033573721298,17.2165228132485,17.3296209936827,
17.4426966217761,17.5558762065502,17.6691073081982,17.7825521143103,17.8693418832121,
17.9828210599164,18.0960985522228,18.2092639752631,18.3223621375165,18.4354377473594,
18.5486173139223,18.6618483973528,18.7752931854659,18.8620830989461,18.9755622717187,
19.0888397598947,19.2020051786863,19.3151033365802,19.4281789419606,19.541358503936,
19.6545895827026,19.7680343660839,19.8548243146801,19.9722977279996),
 .UNSPECIFIED.);
#300=B_SPLINE_CURVE_WITH_KNOTS('',3,(#33100,#33101,#33102,#33103,#33104,
#33105,#33106,#33107,#33108,#33109,#33110,#33111,#33112,#33113,#33114,#33115,
#33116,#33117,#33118,#33119,#33120,#33121,#33122,#33123,#33124,#33125,#33126,
#33127,#33128,#33129,#33130,#33131,#33132,#33133,#33134,#33135,#33136,#33137,
#33138,#33139,#33140,#33141,#33142,#33143,#33144,#33145,#33146,#33147,#33148,
#33149,#33150,#33151,#33152,#33153,#33154,#33155,#33156,#33157,#33158,#33159,
#33160,#33161,#33162,#33163,#33164,#33165,#33166,#33167,#33168,#33169,#33170,
#33171,#33172,#33173,#33174,#33175,#33176,#33177,#33178,#33179,#33180,#33181,
#33182,#33183,#33184,#33185,#33186,#33187,#33188,#33189,#33190,#33191,#33192,
#33193,#33194,#33195,#33196,#33197,#33198,#33199,#33200,#33201,#33202,#33203,
#33204,#33205,#33206,#33207,#33208,#33209,#33210,#33211,#33212,#33213,#33214,
#33215,#33216,#33217,#33218,#33219,#33220,#33221,#33222,#33223,#33224,#33225,
#33226,#33227,#33228,#33229,#33230,#33231,#33232,#33233,#33234,#33235,#33236,
#33237,#33238,#33239,#33240,#33241,#33242,#33243,#33244,#33245,#33246,#33247,
#33248,#33249,#33250,#33251,#33252,#33253,#33254,#33255,#33256,#33257,#33258,
#33259,#33260,#33261,#33262,#33263,#33264,#33265,#33266,#33267,#33268,#33269,
#33270,#33271),.UNSPECIFIED.,.F.,.F.,(4,3,3,3,3,3,3,3,3,3,3,3,3,3,3,3,3,
3,3,3,3,3,3,3,3,3,3,3,3,3,3,3,3,3,3,3,3,3,3,3,3,3,3,3,3,3,3,3,3,3,3,3,3,
3,3,3,3,4),(-29.2247647485903,-29.1026702317892,-28.9802494953267,-28.8573319787146,
-28.7894952562862,-28.6760160792305,-28.5627385866474,-28.449573163376,
-28.336475000938,-28.2233993909572,-28.1102198243307,-27.9969887408777,
-27.8835439528106,-27.7967540405522,-27.6832748635018,-27.5699973709241,
-27.4568319476583,-27.3437337852261,-27.2306581752511,-27.1174786086306,
-27.0042475251837,-26.8908027371227,-26.8040128248182,-26.690533647707,
-26.5772561550685,-26.4640907317418,-26.3509925692487,-26.237916959213,
-26.1247373925325,-26.011506309026,-25.8980615209065,-25.8112716090842,
-25.6977924320825,-25.5845149395528,-25.4713495163346,-25.3582513539493,
-25.2451757440206,-25.131996177445,-25.0187650940424,-24.905320306024,-24.8185303933502,
-24.7050512163485,-24.5917737238206,-24.4786083006053,-24.3655101382241,
-24.2524345283007,-24.139254961732,-24.0260238783372,-23.912579090328,-23.8257891776162,
-23.7138259496525,-23.6020187560681,-23.4903204007749,-23.3786838657664,
-23.2669922326728,-23.1552793919515,-23.0433808076553,-22.941579442425),
 .UNSPECIFIED.);
#301=B_SPLINE_CURVE_WITH_KNOTS('',3,(#33272,#33273,#33274,#33275,#33276,
#33277,#33278,#33279,#33280,#33281,#33282,#33283,#33284,#33285,#33286,#33287,
#33288,#33289,#33290,#33291,#33292,#33293,#33294,#33295,#33296,#33297,#33298,
#33299,#33300,#33301,#33302,#33303,#33304,#33305,#33306,#33307,#33308,#33309,
#33310,#33311,#33312,#33313,#33314,#33315,#33316,#33317,#33318,#33319,#33320,
#33321,#33322,#33323,#33324,#33325,#33326,#33327,#33328,#33329,#33330,#33331,
#33332,#33333,#33334,#33335,#33336,#33337,#33338,#33339,#33340,#33341,#33342,
#33343,#33344,#33345,#33346,#33347,#33348,#33349,#33350,#33351,#33352,#33353,
#33354,#33355,#33356,#33357,#33358,#33359,#33360,#33361,#33362,#33363,#33364,
#33365,#33366,#33367,#33368,#33369,#33370,#33371,#33372,#33373,#33374,#33375,
#33376,#33377,#33378,#33379,#33380,#33381,#33382,#33383,#33384,#33385,#33386,
#33387,#33388,#33389,#33390,#33391,#33392,#33393,#33394,#33395,#33396,#33397,
#33398,#33399,#33400,#33401,#33402,#33403,#33404,#33405,#33406,#33407,#33408,
#33409,#33410,#33411,#33412,#33413,#33414,#33415,#33416,#33417,#33418,#33419,
#33420,#33421,#33422,#33423,#33424,#33425,#33426,#33427,#33428,#33429,#33430,
#33431,#33432,#33433,#33434,#33435,#33436,#33437,#33438,#33439,#33440,#33441,
#33442,#33443),.UNSPECIFIED.,.F.,.F.,(4,3,3,3,3,3,3,3,3,3,3,3,3,3,3,3,3,
3,3,3,3,3,3,3,3,3,3,3,3,3,3,3,3,3,3,3,3,3,3,3,3,3,3,3,3,3,3,3,3,3,3,3,3,
3,3,3,3,4),(19.9722977284267,20.0841292785655,20.1958270514293,20.3074382184884,
20.4190098076767,20.5306685538794,20.6423678179856,20.7542767869761,20.8475655304142,
20.9610447072092,21.074322199536,21.187487622554,21.3005857847419,21.4136613944765,
21.5268409608648,21.6400720440837,21.7535168319264,21.8403067461482,21.9537859227176,
22.067063414799,22.1802288375596,22.2933269994785,22.4064026089331,22.5195821750265,
22.6328132579415,22.7462580454697,22.8330479618822,22.9465271392873,23.0598046322271,
23.1729700558593,23.2860682186617,23.3991438290096,23.5123233960049,23.6255544798281,
23.7389992682632,23.8257891776162,23.9392683546151,24.0525458471412,24.1657112703555,
24.2788094327363,24.3918850426602,24.5050646092305,24.6182956926275,24.7317404806399,
24.8185303933502,24.9320095703586,25.0452870628925,25.1584524861135,25.2715506485001,
25.3846262584287,25.4978058250018,25.6110369084006,25.7244816964131,25.8112716090842,
25.9335247835262,26.0554606987231,26.1769226517213,26.2554830346759),
 .UNSPECIFIED.);
#302=B_SPLINE_CURVE_WITH_KNOTS('',3,(#33448,#33449,#33450,#33451,#33452,
#33453,#33454,#33455,#33456,#33457,#33458,#33459,#33460,#33461,#33462,#33463,
#33464,#33465,#33466,#33467,#33468,#33469,#33470,#33471,#33472,#33473,#33474,
#33475,#33476,#33477,#33478,#33479,#33480,#33481,#33482,#33483,#33484,#33485,
#33486,#33487,#33488,#33489,#33490,#33491,#33492,#33493,#33494,#33495,#33496,
#33497,#33498,#33499,#33500,#33501,#33502,#33503,#33504,#33505,#33506,#33507,
#33508,#33509,#33510,#33511,#33512,#33513,#33514,#33515,#33516,#33517,#33518,
#33519,#33520,#33521,#33522,#33523,#33524,#33525,#33526,#33527,#33528,#33529,
#33530,#33531,#33532,#33533,#33534,#33535,#33536,#33537,#33538,#33539,#33540,
#33541,#33542,#33543,#33544,#33545,#33546,#33547,#33548,#33549,#33550,#33551,
#33552,#33553,#33554,#33555,#33556,#33557,#33558,#33559,#33560,#33561,#33562,
#33563,#33564,#33565,#33566,#33567,#33568,#33569,#33570,#33571,#33572,#33573,
#33574,#33575,#33576,#33577,#33578,#33579,#33580,#33581,#33582,#33583,#33584,
#33585,#33586,#33587,#33588,#33589,#33590,#33591,#33592,#33593,#33594,#33595,
#33596,#33597,#33598,#33599,#33600,#33601,#33602,#33603,#33604,#33605,#33606,
#33607,#33608,#33609,#33610,#33611,#33612,#33613,#33614,#33615,#33616,#33617,
#33618,#33619),.UNSPECIFIED.,.F.,.F.,(4,3,3,3,3,3,3,3,3,3,3,3,3,3,3,3,3,
3,3,3,3,3,3,3,3,3,3,3,3,3,3,3,3,3,3,3,3,3,3,3,3,3,3,3,3,3,3,3,3,3,3,3,3,
3,3,3,3,4),(-35.5079500558816,-35.3961730046961,-35.2844803930079,-35.1728253066734,
-35.0610809083684,-34.9492943671217,-34.837297707012,-34.7459425506903,
-34.6324633736283,-34.5191858810389,-34.4060204577614,-34.2929222953172,
-34.1798466853304,-34.066667118698,-33.9534360352393,-33.8399912471666,
-33.7532013349563,-33.6397221578946,-33.5264446653055,-33.4132792420282,
-33.3001810795844,-33.1871054695977,-33.0739259029656,-32.9606948195071,
-32.8472500314346,-32.7604601192223,-32.6469809421594,-32.5337034495691,
-32.4205380262906,-32.3074398638457,-32.1943642538579,-32.0811846872246,
-31.9679536037652,-31.8545088156916,-31.7677189034882,-31.6542397264265,
-31.5409622338377,-31.4277968105605,-31.3146986481168,-31.2016230381304,
-31.0884434714985,-30.9752123880402,-30.8617675999679,-30.7749776877542,
-30.6614985106941,-30.5482210181067,-30.4350555948313,-30.3219574323891,
-30.2088818224045,-30.0957022557741,-29.9824711723175,-29.8690263842467,
-29.7822364720202,-29.6657715448526,-29.5495817486318,-29.4335543161685,
-29.3176737571639,-29.2247647491669),.UNSPECIFIED.);
#303=B_SPLINE_CURVE_WITH_KNOTS('',3,(#33620,#33621,#33622,#33623,#33624,
#33625,#33626,#33627,#33628,#33629,#33630,#33631,#33632,#33633,#33634,#33635,
#33636,#33637,#33638,#33639,#33640,#33641,#33642,#33643,#33644,#33645,#33646,
#33647,#33648,#33649,#33650,#33651,#33652,#33653,#33654,#33655,#33656,#33657,
#33658,#33659,#33660,#33661,#33662,#33663,#33664,#33665,#33666,#33667,#33668,
#33669,#33670,#33671,#33672,#33673,#33674,#33675,#33676,#33677,#33678,#33679,
#33680,#33681,#33682,#33683,#33684,#33685,#33686,#33687,#33688,#33689,#33690,
#33691,#33692,#33693,#33694,#33695,#33696,#33697,#33698,#33699,#33700,#33701,
#33702,#33703,#33704,#33705,#33706,#33707,#33708,#33709,#33710,#33711,#33712,
#33713,#33714,#33715,#33716,#33717,#33718,#33719,#33720,#33721,#33722,#33723,
#33724,#33725,#33726,#33727,#33728,#33729,#33730,#33731,#33732,#33733,#33734,
#33735,#33736,#33737,#33738,#33739,#33740,#33741,#33742,#33743,#33744,#33745,
#33746,#33747,#33748,#33749,#33750,#33751,#33752,#33753,#33754,#33755,#33756,
#33757,#33758,#33759,#33760,#33761,#33762,#33763,#33764,#33765,#33766,#33767,
#33768,#33769,#33770,#33771,#33772,#33773,#33774,#33775,#33776,#33777,#33778,
#33779,#33780,#33781,#33782,#33783,#33784,#33785,#33786,#33787,#33788,#33789,
#33790,#33791),.UNSPECIFIED.,.F.,.F.,(4,3,3,3,3,3,3,3,3,3,3,3,3,3,3,3,3,
3,3,3,3,3,3,3,3,3,3,3,3,3,3,3,3,3,3,3,3,3,3,3,3,3,3,3,3,3,3,3,3,3,3,3,3,
3,3,3,3,4),(26.2554830351792,26.3716311906272,26.4880031249538,26.6044911021221,
26.7212648320428,26.8040128248182,26.9174920018686,27.0307694944462,27.1439349177118,
27.2570330801439,27.3701086901187,27.4832882567393,27.5965193401862,27.7099641282473,
27.7967540405522,27.9102332176087,28.0235107101925,28.1366761334643,28.2497742959025,
28.3628499058832,28.4760294725095,28.5892605559621,28.7027053440286,28.7894952562862,
28.9029744333544,29.0162519259501,29.1294173492341,29.2425155116847,29.355591121678,
29.468770688317,29.5820017717822,29.6954465598615,29.7822364720202,29.8957156490803,
30.0089931416678,30.1221585649435,30.2352567273858,30.3483323373709,30.4615119040014,
30.5747429874581,30.688187775529,30.7749776877543,30.8884568648157,31.0017343574046,
31.1148997806817,31.2279979431252,31.3410735531117,31.4542531197435,31.5674842032017,
31.6809289912738,31.7677189034883,31.8796560322216,31.9914328602303,32.1030966456068,
32.2147356549155,32.3263521668632,32.4380819604925,32.5386683419494),
 .UNSPECIFIED.);
#304=B_SPLINE_CURVE_WITH_KNOTS('',3,(#33796,#33797,#33798,#33799,#33800,
#33801,#33802,#33803,#33804,#33805,#33806,#33807,#33808,#33809,#33810,#33811,
#33812,#33813,#33814,#33815,#33816,#33817,#33818,#33819,#33820,#33821,#33822,
#33823,#33824,#33825,#33826,#33827,#33828,#33829,#33830,#33831,#33832,#33833,
#33834,#33835,#33836,#33837,#33838,#33839,#33840,#33841,#33842,#33843,#33844,
#33845,#33846,#33847,#33848,#33849,#33850,#33851,#33852,#33853,#33854,#33855,
#33856,#33857,#33858,#33859,#33860,#33861,#33862,#33863,#33864,#33865,#33866,
#33867,#33868,#33869,#33870,#33871,#33872,#33873,#33874,#33875,#33876,#33877,
#33878,#33879,#33880,#33881,#33882,#33883,#33884,#33885,#33886,#33887,#33888,
#33889,#33890,#33891,#33892,#33893,#33894,#33895,#33896,#33897,#33898,#33899,
#33900,#33901,#33902,#33903,#33904,#33905,#33906,#33907,#33908,#33909,#33910,
#33911,#33912,#33913,#33914,#33915,#33916,#33917,#33918,#33919,#33920,#33921,
#33922,#33923,#33924,#33925,#33926,#33927,#33928,#33929,#33930,#33931,#33932,
#33933,#33934,#33935,#33936,#33937,#33938,#33939,#33940,#33941,#33942,#33943,
#33944,#33945,#33946,#33947,#33948,#33949,#33950,#33951,#33952,#33953,#33954,
#33955,#33956,#33957,#33958,#33959,#33960,#33961,#33962,#33963,#33964,#33965,
#33966,#33967),.UNSPECIFIED.,.F.,.F.,(4,3,3,3,3,3,3,3,3,3,3,3,3,3,3,3,3,
3,3,3,3,3,3,3,3,3,3,3,3,3,3,3,3,3,3,3,3,3,3,3,3,3,3,3,3,3,3,3,3,3,3,3,3,
3,3,3,3,4),(-41.791135363526,-41.6951310608283,-41.5816518837661,-41.4683743911766,
-41.355208967899,-41.2421108054547,-41.1290351954678,-41.0158556288353,
-40.9026245453764,-40.7891797573035,-40.7023898450943,-40.5889106680321,
-40.4756331754426,-40.3624677521649,-40.2493695897207,-40.1362939797336,
-40.0231144131011,-39.9098833296422,-39.7964385415693,-39.7096486293603,
-39.5961694522984,-39.482891959709,-39.3697265364315,-39.2566283739875,
-39.1435527640006,-39.0303731973683,-38.9171421139096,-38.8036973258369,
-38.7169074136263,-38.6034282365642,-38.4901507439748,-38.3769853206972,
-38.263887158253,-38.1508115482661,-38.0376319816337,-37.9244008981749,
-37.8109561101021,-37.7241661978923,-37.6106870208302,-37.4974095282408,
-37.3842441049631,-37.271145942519,-37.158070332532,-37.0448907658995,-36.9316596824407,
-36.8182148943679,-36.7314249821583,-36.6179458050963,-36.5046683125069,
-36.3915028892294,-36.2784047267853,-36.1653291167985,-36.0521495501662,
-35.9389184667075,-35.8254736786347,-35.7386837664243,-35.5878041738866,
-35.5079500563465),.UNSPECIFIED.);
#305=B_SPLINE_CURVE_WITH_KNOTS('',3,(#33968,#33969,#33970,#33971,#33972,
#33973,#33974,#33975,#33976,#33977,#33978,#33979,#33980,#33981,#33982,#33983,
#33984,#33985,#33986,#33987,#33988,#33989,#33990,#33991,#33992,#33993,#33994,
#33995,#33996,#33997,#33998,#33999,#34000,#34001,#34002,#34003,#34004,#34005,
#34006,#34007,#34008,#34009,#34010,#34011,#34012,#34013,#34014,#34015,#34016,
#34017,#34018,#34019,#34020,#34021,#34022,#34023,#34024,#34025,#34026,#34027,
#34028,#34029,#34030,#34031,#34032,#34033,#34034,#34035,#34036,#34037,#34038,
#34039,#34040,#34041,#34042,#34043,#34044,#34045,#34046,#34047,#34048,#34049,
#34050,#34051,#34052,#34053,#34054,#34055,#34056,#34057,#34058,#34059,#34060,
#34061,#34062,#34063,#34064,#34065,#34066,#34067,#34068,#34069,#34070,#34071,
#34072,#34073,#34074,#34075,#34076,#34077,#34078,#34079,#34080,#34081,#34082,
#34083,#34084,#34085,#34086,#34087,#34088,#34089,#34090,#34091,#34092,#34093,
#34094,#34095,#34096,#34097,#34098,#34099,#34100,#34101,#34102,#34103,#34104,
#34105,#34106,#34107,#34108,#34109,#34110,#34111,#34112,#34113,#34114,#34115,
#34116,#34117,#34118,#34119,#34120,#34121,#34122,#34123,#34124,#34125,#34126,
#34127,#34128,#34129,#34130,#34131,#34132,#34133,#34134,#34135,#34136,#34137,
#34138,#34139),.UNSPECIFIED.,.F.,.F.,(4,3,3,3,3,3,3,3,3,3,3,3,3,3,3,3,3,
3,3,3,3,3,3,3,3,3,3,3,3,3,3,3,3,3,3,3,3,3,3,3,3,3,3,3,3,3,3,3,3,3,3,3,3,
3,3,3,3,4),(32.5386683423588,32.692149172839,32.7604601192223,32.873939296284,
32.9872167888731,33.1003822121503,33.2134803745941,33.3265559845806,33.4397355512127,
33.5529666346711,33.6664114227435,33.7532013349563,33.8666805120184,33.9799580046078,
34.0931234278855,34.2062215903296,34.3192972003165,34.4324767669489,34.5457078504077,
34.6591526384805,34.7459425506903,34.8594217277524,34.9726992203419,35.0858646436196,
35.1989628060638,35.3120384160508,35.4252179826833,35.5384490661421,35.651893854215,
35.7386837664243,35.8521629434862,35.9654404360756,36.0786058593531,36.1917040217971,
36.3047796317839,36.4179591984163,36.5311902818749,36.6446350699476,36.7314249821583,
36.8449041592204,36.95818165181,37.0713470750876,37.1844452375319,37.2975208475188,
37.4107004141514,37.5239314976102,37.6373762856831,37.7241661978923,37.8376453749543,
37.9509228675437,38.0640882908212,38.1771864532653,38.2902620632522,38.4034416298846,
38.5166727133433,38.630117501416,38.7169074136263,38.8218536495384),
 .UNSPECIFIED.);
#306=B_SPLINE_CURVE_WITH_KNOTS('',3,(#34144,#34145,#34146,#34147,#34148,
#34149,#34150,#34151,#34152,#34153,#34154,#34155,#34156,#34157,#34158,#34159,
#34160,#34161,#34162,#34163,#34164,#34165,#34166,#34167,#34168,#34169,#34170,
#34171,#34172,#34173,#34174,#34175,#34176,#34177,#34178,#34179,#34180,#34181,
#34182,#34183,#34184,#34185,#34186,#34187,#34188,#34189,#34190,#34191,#34192,
#34193,#34194,#34195,#34196,#34197,#34198,#34199,#34200,#34201,#34202,#34203,
#34204,#34205,#34206,#34207,#34208,#34209,#34210,#34211,#34212,#34213,#34214,
#34215,#34216,#34217,#34218,#34219,#34220,#34221,#34222,#34223,#34224,#34225,
#34226,#34227,#34228,#34229,#34230,#34231,#34232,#34233,#34234,#34235,#34236,
#34237,#34238,#34239,#34240,#34241,#34242,#34243,#34244,#34245,#34246,#34247,
#34248,#34249,#34250,#34251,#34252,#34253,#34254,#34255,#34256,#34257,#34258,
#34259,#34260,#34261,#34262,#34263,#34264,#34265,#34266,#34267,#34268,#34269,
#34270,#34271,#34272,#34273,#34274,#34275,#34276,#34277,#34278,#34279,#34280,
#34281,#34282,#34283,#34284,#34285,#34286,#34287,#34288,#34289,#34290,#34291,
#34292,#34293,#34294,#34295,#34296,#34297,#34298,#34299,#34300,#34301,#34302,
#34303,#34304,#34305,#34306,#34307,#34308,#34309,#34310,#34311,#34312,#34313,
#34314,#34315),.UNSPECIFIED.,.F.,.F.,(4,3,3,3,3,3,3,3,3,3,3,3,3,3,3,3,3,
3,3,3,3,3,3,3,3,3,3,3,3,3,3,3,3,3,3,3,3,3,3,3,3,3,3,3,3,3,3,3,3,3,3,3,3,
3,3,3,3,4),(-48.0743206700366,-47.9513559785244,-47.8280201492357,-47.7041583150349,
-47.6515783552324,-47.5380991781703,-47.4248216855807,-47.311656262303,
-47.1985580998588,-47.0854824898718,-46.9723029232392,-46.8590718397803,
-46.7456270517074,-46.6588371394984,-46.5453579624364,-46.4320804698471,
-46.3189150465696,-46.2058168841256,-46.0927412741388,-45.9795617075064,
-45.8663306240477,-45.752885835975,-45.6660959237644,-45.5526167467024,
-45.4393392541129,-45.3261738308353,-45.2130756683912,-45.1000000584043,
-44.9868204917719,-44.8735894083131,-44.7601446202403,-44.6733547080304,
-44.5598755309683,-44.4465980383788,-44.3334326151011,-44.2203344526569,
-44.10725884267,-43.9940792760374,-43.8808481925786,-43.7674034045057,-43.6806134922963,
-43.5671343152343,-43.4538568226449,-43.3406913993673,-43.2275932369232,
-43.1145176269363,-43.0013380603039,-42.8881069768452,-42.7746621887724,
-42.6878722765623,-42.5757801624873,-42.4638771065973,-42.3520829464153,
-42.2403507816478,-42.1280469272264,-42.0162357830346,-41.9036855734984,
-41.7911353639623),.UNSPECIFIED.);
#307=B_SPLINE_CURVE_WITH_KNOTS('',3,(#34316,#34317,#34318,#34319,#34320,
#34321,#34322,#34323,#34324,#34325,#34326,#34327,#34328,#34329,#34330,#34331,
#34332,#34333,#34334,#34335,#34336,#34337,#34338,#34339,#34340,#34341,#34342,
#34343,#34344,#34345,#34346,#34347,#34348,#34349,#34350,#34351,#34352,#34353,
#34354,#34355,#34356,#34357,#34358,#34359,#34360,#34361,#34362,#34363,#34364,
#34365,#34366,#34367,#34368,#34369,#34370,#34371,#34372,#34373,#34374,#34375,
#34376,#34377,#34378,#34379,#34380,#34381,#34382,#34383,#34384,#34385,#34386,
#34387,#34388,#34389,#34390,#34391,#34392,#34393,#34394,#34395,#34396,#34397,
#34398,#34399,#34400,#34401,#34402,#34403,#34404,#34405,#34406,#34407,#34408,
#34409,#34410,#34411,#34412,#34413,#34414,#34415,#34416,#34417,#34418,#34419,
#34420,#34421,#34422,#34423,#34424,#34425,#34426,#34427,#34428,#34429,#34430,
#34431,#34432,#34433,#34434,#34435,#34436,#34437,#34438,#34439,#34440,#34441,
#34442,#34443,#34444,#34445,#34446,#34447,#34448,#34449,#34450,#34451,#34452,
#34453,#34454,#34455,#34456,#34457,#34458,#34459,#34460,#34461,#34462,#34463,
#34464,#34465,#34466,#34467,#34468,#34469,#34470,#34471,#34472,#34473,#34474,
#34475,#34476,#34477,#34478,#34479,#34480,#34481,#34482,#34483,#34484,#34485,
#34486,#34487),.UNSPECIFIED.,.F.,.F.,(4,3,3,3,3,3,3,3,3,3,3,3,3,3,3,3,3,
3,3,3,3,3,3,3,3,3,3,3,3,3,3,3,3,3,3,3,3,3,3,3,3,3,3,3,3,3,3,3,3,3,3,3,3,
3,3,3,3,4),(38.8218536499721,38.9337807794537,39.0455700846174,39.1572686518251,
39.2689234195309,39.3806624113781,39.492437953731,39.6044275384758,39.7096486293603,
39.8231278064224,39.9364052990119,40.0495707222895,40.1626688847336,40.2757444947206,
40.3889240613531,40.5021551448117,40.6155999328846,40.7023898450943,40.8158690221563,
40.9291465147457,41.0423119380234,41.1554101004674,41.2684857104543,41.3816652770868,
41.4948963605456,41.6083411486183,41.6951310608283,41.8086102378904,41.9218877304798,
42.0350531537575,42.1481513162016,42.2612269261883,42.3744064928207,42.4876375762795,
42.6010823643522,42.6878722765623,42.8013514536243,42.9146289462137,43.0277943694912,
43.1408925319353,43.2539681419222,43.3671477085544,43.480378792013,43.5938235800858,
43.6806134922963,43.7940926693582,43.9073701619477,44.0205355852253,44.1336337476695,
44.2467093576567,44.3598889242893,44.4731200077481,44.5865647958209,44.6733547080304,
44.7964919316645,44.919285870672,45.0415576677713,45.1050389561137),
 .UNSPECIFIED.);
#308=B_SPLINE_CURVE_WITH_KNOTS('',3,(#34492,#34493,#34494,#34495,#34496,
#34497,#34498,#34499,#34500,#34501,#34502,#34503,#34504,#34505,#34506,#34507,
#34508,#34509,#34510,#34511,#34512,#34513,#34514,#34515,#34516,#34517,#34518,
#34519,#34520,#34521,#34522,#34523,#34524,#34525,#34526,#34527,#34528,#34529,
#34530,#34531,#34532,#34533,#34534,#34535,#34536,#34537,#34538,#34539,#34540,
#34541,#34542,#34543,#34544,#34545,#34546,#34547,#34548,#34549,#34550,#34551,
#34552,#34553,#34554,#34555,#34556,#34557,#34558,#34559,#34560,#34561,#34562,
#34563,#34564,#34565,#34566,#34567,#34568,#34569,#34570,#34571,#34572,#34573,
#34574,#34575,#34576,#34577,#34578,#34579,#34580,#34581,#34582,#34583,#34584,
#34585,#34586,#34587,#34588,#34589,#34590,#34591,#34592,#34593,#34594,#34595,
#34596,#34597,#34598,#34599,#34600,#34601,#34602,#34603,#34604,#34605,#34606,
#34607,#34608,#34609,#34610,#34611,#34612,#34613,#34614,#34615,#34616,#34617,
#34618,#34619,#34620,#34621,#34622,#34623,#34624,#34625,#34626,#34627,#34628,
#34629,#34630,#34631,#34632,#34633,#34634,#34635,#34636,#34637,#34638,#34639,
#34640,#34641,#34642,#34643,#34644,#34645,#34646,#34647,#34648,#34649,#34650,
#34651,#34652,#34653,#34654,#34655,#34656,#34657,#34658,#34659,#34660,#34661,
#34662,#34663),.UNSPECIFIED.,.F.,.F.,(4,3,3,3,3,3,3,3,3,3,3,3,3,3,3,3,3,
3,3,3,3,3,3,3,3,3,3,3,3,3,3,3,3,3,3,3,3,3,3,3,3,3,3,3,3,3,3,3,3,3,3,3,3,
3,3,3,3,4),(-54.3575059778852,-54.2456434060343,-54.1338583683125,-54.0221040958961,
-53.9102549193038,-53.7983577896496,-53.6862537502742,-53.6080256496364,
-53.4945464725744,-53.3812689799849,-53.2681035567074,-53.1550053942634,
-53.0419297842766,-52.9287502176442,-52.8155191341854,-52.7020743461126,
-52.6152844339024,-52.5018052568402,-52.3885277642508,-52.2753623409732,
-52.162264178529,-52.0491885685422,-51.9360090019097,-51.8227779184509,
-51.7093331303781,-51.6225432181684,-51.5090640411063,-51.3957865485169,
-51.2826211252393,-51.1695229627951,-51.0564473528081,-50.9432677861756,
-50.8300367027168,-50.716591914644,-50.6298020024344,-50.5163228253723,
-50.4030453327828,-50.2898799095051,-50.1767817470609,-50.063706137074,
-49.9505265704415,-49.8372954869827,-49.7238506989099,-49.6370607867004,
-49.5235816096383,-49.410304117049,-49.2971386937714,-49.1840405313274,
-49.0709649213402,-48.9577853547078,-48.8445542712491,-48.7311094831763,
-48.6443195709664,-48.5283239378195,-48.4125900933358,-48.2970107053752,
-48.1815581061127,-48.0743206707056),.UNSPECIFIED.);
#309=B_SPLINE_CURVE_WITH_KNOTS('',3,(#34664,#34665,#34666,#34667,#34668,
#34669,#34670,#34671,#34672,#34673,#34674,#34675,#34676,#34677,#34678,#34679,
#34680,#34681,#34682,#34683,#34684,#34685,#34686,#34687,#34688,#34689,#34690,
#34691,#34692,#34693,#34694,#34695,#34696,#34697,#34698,#34699,#34700,#34701,
#34702,#34703,#34704,#34705,#34706,#34707,#34708,#34709,#34710,#34711,#34712,
#34713,#34714,#34715,#34716,#34717,#34718,#34719,#34720,#34721,#34722,#34723,
#34724,#34725,#34726,#34727,#34728,#34729,#34730,#34731,#34732,#34733,#34734,
#34735,#34736,#34737,#34738,#34739,#34740,#34741,#34742,#34743,#34744,#34745,
#34746,#34747,#34748,#34749,#34750,#34751,#34752,#34753,#34754,#34755,#34756,
#34757,#34758,#34759,#34760,#34761,#34762,#34763,#34764,#34765,#34766,#34767,
#34768,#34769,#34770,#34771,#34772,#34773,#34774,#34775,#34776,#34777,#34778,
#34779,#34780,#34781,#34782,#34783,#34784,#34785,#34786,#34787,#34788,#34789,
#34790,#34791,#34792,#34793,#34794,#34795,#34796,#34797,#34798,#34799,#34800,
#34801,#34802,#34803,#34804,#34805,#34806,#34807,#34808,#34809,#34810,#34811,
#34812,#34813,#34814,#34815,#34816,#34817,#34818,#34819,#34820,#34821,#34822,
#34823,#34824,#34825,#34826,#34827,#34828,#34829,#34830,#34831,#34832,#34833,
#34834,#34835),.UNSPECIFIED.,.F.,.F.,(4,3,3,3,3,3,3,3,3,3,3,3,3,3,3,3,3,
3,3,3,3,3,3,3,3,3,3,3,3,3,3,3,3,3,3,3,3,3,3,3,3,3,3,3,3,3,3,3,3,3,3,3,3,
3,3,3,3,4),(45.105038956718,45.2207328062171,45.3366289382953,45.4526267946966,
45.5689058923966,45.6660959237644,45.7795751008264,45.8928525934158,46.0060180166932,
46.1191161791372,46.232191789124,46.3453713557563,46.4586024392149,46.5720472272876,
46.6588371394984,46.7723163165606,46.8855938091501,46.9987592324278,47.1118573948719,
47.2249330048587,47.3381125714912,47.4513436549501,47.564788443023,47.6515783552324,
47.7650575322944,47.8783350248838,47.9915004481613,48.1045986106053,48.2176742205921,
48.3308537872245,48.4440848706832,48.557529658756,48.6443195709664,48.7577987480284,
48.8710762406179,48.9842416638955,49.0973398263396,49.2104154363265,49.323595002959,
49.4368260864178,49.5502708744906,49.6370607867004,49.7505399637626,49.863817456352,
49.9769828796296,50.0900810420738,50.2031566520604,50.3163362186928,50.4295673021514,
50.5430120902243,50.6298020024344,50.7418301681541,50.8536969762416,50.9654495759481,
51.0771721138825,51.1888712037852,51.300671980135,51.3882242638976),
 .UNSPECIFIED.);
#310=B_SPLINE_CURVE_WITH_KNOTS('',3,(#34840,#34841,#34842,#34843,#34844,
#34845,#34846,#34847,#34848,#34849,#34850,#34851,#34852,#34853,#34854,#34855,
#34856,#34857,#34858,#34859,#34860,#34861,#34862,#34863,#34864,#34865,#34866,
#34867,#34868,#34869,#34870,#34871,#34872,#34873,#34874,#34875,#34876,#34877,
#34878,#34879,#34880,#34881,#34882,#34883,#34884,#34885,#34886,#34887,#34888,
#34889,#34890,#34891,#34892,#34893,#34894,#34895,#34896,#34897,#34898,#34899,
#34900,#34901,#34902,#34903,#34904,#34905,#34906,#34907,#34908,#34909,#34910,
#34911,#34912,#34913,#34914,#34915,#34916,#34917,#34918,#34919,#34920,#34921,
#34922,#34923,#34924,#34925,#34926,#34927,#34928,#34929,#34930,#34931,#34932,
#34933,#34934,#34935,#34936,#34937,#34938,#34939,#34940,#34941,#34942,#34943,
#34944,#34945,#34946,#34947,#34948,#34949,#34950,#34951,#34952,#34953,#34954,
#34955,#34956,#34957,#34958,#34959,#34960,#34961,#34962,#34963,#34964,#34965,
#34966,#34967,#34968,#34969,#34970,#34971,#34972,#34973,#34974,#34975,#34976,
#34977,#34978,#34979,#34980,#34981,#34982,#34983,#34984,#34985,#34986,#34987,
#34988,#34989,#34990,#34991,#34992,#34993,#34994,#34995,#34996,#34997,#34998,
#34999,#35000,#35001,#35002,#35003,#35004,#35005,#35006,#35007,#35008,#35009,
#35010,#35011),.UNSPECIFIED.,.F.,.F.,(4,3,3,3,3,3,3,3,3,3,3,3,3,3,3,3,3,
3,3,3,3,3,3,3,3,3,3,3,3,3,3,3,3,3,3,3,3,3,3,3,3,3,3,3,3,3,3,3,3,3,3,3,3,
3,3,3,3,4),(-60.6406912850648,-60.5572141597745,-60.4437349827122,-60.3304574901225,
-60.2172920668446,-60.1041939044002,-59.9911182944131,-59.8779387277803,
-59.7647076443212,-59.6512628562482,-59.5644729440405,-59.4509937669785,
-59.3377162743891,-59.2245508511116,-59.1114526886675,-58.9983770786806,
-58.8851975120482,-58.7719664285894,-58.6585216405167,-58.5717317283065,
-58.4582525512445,-58.3449750586551,-58.2318096353775,-58.1187114729334,
-58.0056358629466,-57.8924562963142,-57.7792252128554,-57.6657804247827,
-57.5789905125725,-57.4655113355104,-57.3522338429209,-57.2390684196433,
-57.1259702571991,-57.0128946472122,-56.8997150805797,-56.7864839971209,
-56.673039209048,-56.5862492968384,-56.4727701197763,-56.3594926271869,
-56.2463272039093,-56.1332290414652,-56.0201534314783,-55.9069738648458,
-55.793742781387,-55.6802979933142,-55.5935080811044,-55.4800289040424,
-55.366751411453,-55.2535859881754,-55.1404878257313,-55.0274122157444,
-54.914232649112,-54.8010015656532,-54.6875567775805,-54.6007668653704,
-54.4531582068316,-54.3575059783892),.UNSPECIFIED.);
#311=B_SPLINE_CURVE_WITH_KNOTS('',3,(#35012,#35013,#35014,#35015,#35016,
#35017,#35018,#35019,#35020,#35021,#35022,#35023,#35024,#35025,#35026,#35027,
#35028,#35029,#35030,#35031,#35032,#35033,#35034,#35035,#35036,#35037,#35038,
#35039,#35040,#35041,#35042,#35043,#35044,#35045,#35046,#35047,#35048,#35049,
#35050,#35051,#35052,#35053,#35054,#35055,#35056,#35057,#35058,#35059,#35060,
#35061,#35062,#35063,#35064,#35065,#35066,#35067,#35068,#35069,#35070,#35071,
#35072,#35073,#35074,#35075,#35076,#35077,#35078,#35079,#35080,#35081,#35082,
#35083,#35084,#35085,#35086,#35087,#35088,#35089,#35090,#35091,#35092,#35093,
#35094,#35095,#35096,#35097,#35098,#35099,#35100,#35101,#35102,#35103,#35104,
#35105,#35106,#35107,#35108,#35109,#35110,#35111,#35112,#35113,#35114,#35115,
#35116,#35117,#35118,#35119,#35120,#35121,#35122,#35123,#35124,#35125,#35126,
#35127,#35128,#35129,#35130,#35131,#35132,#35133,#35134,#35135,#35136,#35137,
#35138,#35139,#35140,#35141,#35142,#35143,#35144,#35145,#35146,#35147,#35148,
#35149,#35150,#35151,#35152,#35153,#35154,#35155,#35156,#35157,#35158,#35159,
#35160,#35161,#35162,#35163,#35164,#35165,#35166,#35167,#35168,#35169,#35170,
#35171,#35172,#35173,#35174,#35175,#35176,#35177,#35178,#35179,#35180,#35181,
#35182,#35183),.UNSPECIFIED.,.F.,.F.,(4,3,3,3,3,3,3,3,3,3,3,3,3,3,3,3,3,
3,3,3,3,3,3,3,3,3,3,3,3,3,3,3,3,3,3,3,3,3,3,3,3,3,3,3,3,3,3,3,3,3,3,3,3,
3,3,3,3,4),(51.3882242642754,51.5381262078476,51.6225432181684,51.7360223952304,
51.8492998878198,51.9624653110973,52.0755634735413,52.1886390835281,52.3018186501605,
52.4150497336192,52.528494521692,52.6152844339024,52.7287636109646,52.8420411035543,
52.9552065268321,53.0683046892764,53.1813802992635,53.2945598658962,53.4077909493552,
53.5212357374281,53.6080256496364,53.7215048266983,53.8347823192877,53.9479477425652,
54.0610459050092,54.174121514996,54.2873010816284,54.400532165087,54.5139769531597,
54.6007668653704,54.7142460424324,54.8275235350218,54.9406889582994,55.0537871207435,
55.1668627307304,55.2800422973628,55.3932733808216,55.5067181688944,55.5935080811044,
55.7069872581665,55.820264750756,55.9334301740336,56.0465283364778,56.1596039464647,
56.2727835130972,56.386014596556,56.4994593846288,56.5862492968384,56.6997284739004,
56.8130059664899,56.9261713897674,57.0392695522115,57.1523451621984,57.2655247288308,
57.3787558122896,57.4922006003623,57.5789905125724,57.6714095710771),
 .UNSPECIFIED.);
#312=B_SPLINE_CURVE_WITH_KNOTS('',3,(#35188,#35189,#35190,#35191,#35192,
#35193,#35194,#35195,#35196,#35197,#35198,#35199,#35200,#35201,#35202,#35203,
#35204,#35205,#35206,#35207,#35208,#35209,#35210,#35211,#35212,#35213,#35214,
#35215,#35216,#35217,#35218,#35219,#35220,#35221,#35222,#35223,#35224,#35225,
#35226,#35227,#35228,#35229,#35230,#35231,#35232,#35233,#35234,#35235,#35236,
#35237,#35238,#35239,#35240,#35241,#35242,#35243,#35244,#35245,#35246,#35247,
#35248,#35249,#35250,#35251,#35252,#35253,#35254,#35255,#35256,#35257,#35258,
#35259,#35260,#35261,#35262,#35263,#35264,#35265,#35266,#35267,#35268,#35269,
#35270,#35271,#35272,#35273,#35274,#35275,#35276,#35277,#35278,#35279,#35280,
#35281,#35282,#35283,#35284,#35285,#35286,#35287,#35288,#35289,#35290,#35291,
#35292,#35293,#35294,#35295,#35296,#35297,#35298,#35299,#35300,#35301,#35302,
#35303,#35304,#35305,#35306,#35307,#35308,#35309,#35310,#35311,#35312,#35313,
#35314,#35315,#35316,#35317,#35318,#35319,#35320,#35321,#35322,#35323,#35324,
#35325,#35326,#35327,#35328,#35329,#35330,#35331,#35332,#35333,#35334,#35335,
#35336,#35337,#35338,#35339,#35340,#35341,#35342,#35343,#35344,#35345,#35346,
#35347,#35348,#35349,#35350,#35351,#35352,#35353,#35354,#35355,#35356,#35357,
#35358,#35359),.UNSPECIFIED.,.F.,.F.,(4,3,3,3,3,3,3,3,3,3,3,3,3,3,3,3,3,
3,3,3,3,3,3,3,3,3,3,3,3,3,3,3,3,3,3,3,3,3,3,3,3,3,3,3,3,3,3,3,3,3,3,3,3,
3,3,3,3,4),(-66.9238765918734,-66.7999837454187,-66.6756687169425,-66.5507949918877,
-66.5136614541785,-66.4001822771164,-66.2869047845269,-66.1737393612492,
-66.060641198805,-65.9475655888181,-65.8343860221856,-65.7211549387267,
-65.6077101506539,-65.5209202384445,-65.4074410613825,-65.2941635687931,
-65.1809981455155,-65.0678999830714,-64.9548243730845,-64.8416448064521,
-64.7284137229934,-64.6149689349206,-64.5281790227105,-64.4146998456485,
-64.3014223530591,-64.1882569297815,-64.0751587673374,-63.9620831573505,
-63.8489035907181,-63.7356725072594,-63.6222277191866,-63.5354378069765,
-63.4219586299144,-63.3086811373249,-63.1955157140473,-63.0824175516031,
-62.9693419416161,-62.8561623749836,-62.7429312915248,-62.629486503452,
-62.5426965912425,-62.4292174141805,-62.3159399215912,-62.2027744983137,
-62.0896763358696,-61.9766007258828,-61.8634211592504,-61.7501900757918,
-61.6367452877191,-61.5499553755085,-61.4362973642558,-61.3242814200128,
-61.212373921956,-61.1005281162358,-60.9855689085486,-60.8736400732645,
-60.7571656793757,-60.6406912854869),.UNSPECIFIED.);
#313=B_SPLINE_CURVE_WITH_KNOTS('',3,(#35360,#35361,#35362,#35363,#35364,
#35365,#35366,#35367,#35368,#35369,#35370,#35371,#35372,#35373,#35374,#35375,
#35376,#35377,#35378,#35379,#35380,#35381,#35382,#35383,#35384,#35385,#35386,
#35387,#35388,#35389,#35390,#35391,#35392,#35393,#35394,#35395,#35396,#35397,
#35398,#35399,#35400,#35401,#35402,#35403,#35404,#35405,#35406,#35407,#35408,
#35409,#35410,#35411,#35412,#35413,#35414,#35415,#35416,#35417,#35418,#35419,
#35420,#35421,#35422,#35423,#35424,#35425,#35426,#35427,#35428,#35429,#35430,
#35431,#35432,#35433,#35434,#35435,#35436,#35437,#35438,#35439,#35440,#35441,
#35442,#35443,#35444,#35445,#35446,#35447,#35448,#35449,#35450,#35451,#35452,
#35453,#35454,#35455,#35456,#35457,#35458,#35459,#35460,#35461,#35462,#35463,
#35464,#35465,#35466,#35467,#35468,#35469,#35470,#35471,#35472,#35473,#35474,
#35475,#35476,#35477,#35478,#35479,#35480,#35481,#35482,#35483,#35484,#35485,
#35486,#35487,#35488,#35489,#35490,#35491,#35492,#35493,#35494,#35495,#35496,
#35497,#35498,#35499,#35500,#35501,#35502,#35503,#35504,#35505,#35506,#35507,
#35508,#35509,#35510,#35511,#35512,#35513,#35514,#35515,#35516,#35517,#35518,
#35519,#35520,#35521,#35522,#35523,#35524,#35525,#35526,#35527,#35528,#35529,
#35530,#35531),.UNSPECIFIED.,.F.,.F.,(4,3,3,3,3,3,3,3,3,3,3,3,3,3,3,3,3,
3,3,3,3,3,3,3,3,3,3,3,3,3,3,3,3,3,3,3,3,3,3,3,3,3,3,3,3,3,3,3,3,3,3,3,3,
3,3,3,3,4),(57.6714095715052,57.7839498411054,57.8958482199626,58.0076522192365,
58.1194086614283,58.2324894281479,58.3443610886813,58.4580464084939,58.5717317283065,
58.6852109053686,58.7984883979581,58.9116538212357,59.0247519836799,59.1378275936667,
59.2510071602992,59.364238243758,59.4776830318308,59.5644729440405,59.6779521211025,
59.7912296136919,59.9043950369695,60.0174931994135,60.1305688094003,60.2437483760328,
60.3569794594915,60.4704242475643,60.5572141597745,60.6706933368366,60.783970829426,
60.8971362527035,61.0102344151474,61.1233100251344,61.2364895917668,61.3497206752254,
61.4631654632981,61.5499553755085,61.6634345525706,61.7767120451602,61.8898774684378,
62.0029756308821,62.1160512408688,62.2292308075014,62.3424618909603,62.4559066790332,
62.5426965912425,62.6561757683046,62.7694532608939,62.8826186841714,62.9957168466155,
63.1087924566022,63.2219720232345,63.3352031066934,63.4486478947661,63.5354378069765,
63.6595194390276,63.7832273544188,63.9063594692549,63.9545948779129),
 .UNSPECIFIED.);
#314=B_SPLINE_CURVE_WITH_KNOTS('',3,(#35536,#35537,#35538,#35539,#35540,
#35541,#35542,#35543,#35544,#35545,#35546,#35547,#35548,#35549,#35550,#35551,
#35552,#35553,#35554,#35555,#35556,#35557,#35558,#35559,#35560,#35561,#35562,
#35563,#35564,#35565,#35566,#35567,#35568,#35569,#35570,#35571,#35572,#35573,
#35574,#35575,#35576,#35577,#35578,#35579,#35580,#35581,#35582,#35583,#35584,
#35585,#35586,#35587,#35588,#35589,#35590,#35591,#35592,#35593,#35594,#35595,
#35596,#35597,#35598,#35599,#35600,#35601,#35602,#35603,#35604,#35605,#35606,
#35607,#35608,#35609,#35610,#35611,#35612,#35613,#35614,#35615,#35616,#35617,
#35618,#35619,#35620,#35621,#35622,#35623,#35624,#35625,#35626,#35627,#35628,
#35629,#35630,#35631,#35632,#35633,#35634,#35635,#35636,#35637,#35638,#35639,
#35640,#35641,#35642,#35643,#35644,#35645,#35646,#35647,#35648,#35649,#35650,
#35651,#35652,#35653,#35654,#35655,#35656,#35657,#35658,#35659,#35660,#35661,
#35662,#35663,#35664,#35665,#35666,#35667,#35668,#35669,#35670,#35671,#35672,
#35673,#35674,#35675,#35676,#35677,#35678,#35679,#35680,#35681,#35682,#35683,
#35684,#35685,#35686,#35687,#35688,#35689,#35690,#35691,#35692,#35693,#35694,
#35695,#35696,#35697,#35698,#35699,#35700,#35701,#35702,#35703,#35704,#35705,
#35706,#35707),.UNSPECIFIED.,.F.,.F.,(4,3,3,3,3,3,3,3,3,3,3,3,3,3,3,3,3,
3,3,3,3,3,3,3,3,3,3,3,3,3,3,3,3,3,3,3,3,3,3,3,3,3,3,3,3,3,3,3,3,3,3,3,3,
3,3,3,3,4),(-73.207061899424,-73.0950948311733,-72.9831980604612,-72.8713249933925,
-72.7593511740308,-72.6473233814793,-72.5350916115429,-72.4701087485826,
-72.3566295715205,-72.2433520789311,-72.1301866556534,-72.0170884932091,
-71.9040128832222,-71.7908333165897,-71.6776022331308,-71.5641574450579,
-71.4773675328486,-71.3638883557865,-71.2506108631971,-71.1374454399195,
-71.0243472774754,-70.9112716674883,-70.7980921008558,-70.6848610173971,
-70.5714162293243,-70.4846263171145,-70.3711471400524,-70.257869647463,
-70.1447042241854,-70.0316060617412,-69.9185304517543,-69.8053508851218,
-69.692119801663,-69.5786750135902,-69.4918851013805,-69.3784059243185,
-69.265128431729,-69.1519630084514,-69.0388648460073,-68.9257892360203,
-68.8126096693879,-68.6993785859291,-68.5859337978563,-68.4991438856465,
-68.3856647085844,-68.2723872159949,-68.1592217927173,-68.046123630273,
-67.9330480202861,-67.8198684536536,-67.7066373701949,-67.5931925821221,
-67.5064026699125,-67.3908458947147,-67.2741035690971,-67.1589453653598,
-67.0414109788021,-66.9238765922444),.UNSPECIFIED.);
#315=B_SPLINE_CURVE_WITH_KNOTS('',3,(#35708,#35709,#35710,#35711,#35712,
#35713,#35714,#35715,#35716,#35717,#35718,#35719,#35720,#35721,#35722,#35723,
#35724,#35725,#35726,#35727,#35728,#35729,#35730,#35731,#35732,#35733,#35734,
#35735,#35736,#35737,#35738,#35739,#35740,#35741,#35742,#35743,#35744,#35745,
#35746,#35747,#35748,#35749,#35750,#35751,#35752,#35753,#35754,#35755,#35756,
#35757,#35758,#35759,#35760,#35761,#35762,#35763,#35764,#35765,#35766,#35767,
#35768,#35769,#35770,#35771,#35772,#35773,#35774,#35775,#35776,#35777,#35778,
#35779,#35780,#35781,#35782,#35783,#35784,#35785,#35786,#35787,#35788,#35789,
#35790,#35791,#35792,#35793,#35794,#35795,#35796,#35797,#35798,#35799,#35800,
#35801,#35802,#35803,#35804,#35805,#35806,#35807,#35808,#35809,#35810,#35811,
#35812,#35813,#35814,#35815,#35816,#35817,#35818,#35819,#35820,#35821,#35822,
#35823,#35824,#35825,#35826,#35827,#35828,#35829,#35830,#35831,#35832,#35833,
#35834,#35835,#35836,#35837,#35838,#35839,#35840,#35841,#35842,#35843,#35844,
#35845,#35846,#35847,#35848,#35849,#35850,#35851,#35852,#35853,#35854,#35855,
#35856,#35857,#35858,#35859,#35860,#35861,#35862,#35863,#35864,#35865,#35866,
#35867,#35868,#35869,#35870,#35871,#35872,#35873,#35874,#35875,#35876,#35877,
#35878,#35879),.UNSPECIFIED.,.F.,.F.,(4,3,3,3,3,3,3,3,3,3,3,3,3,3,3,3,3,
3,3,3,3,3,3,3,3,3,3,3,3,3,3,3,3,3,3,3,3,3,3,3,3,3,3,3,3,3,3,3,3,3,3,3,3,
3,3,3,3,4),(63.9545948782567,64.0698636722456,64.1853150539345,64.3008548231995,
64.4166721465947,64.5281790227105,64.6416581997726,64.7549356923621,64.8681011156398,
64.9811992780839,65.0942748880708,65.2074544547033,65.3206855381621,65.434130326235,
65.5209202384445,65.6343994155065,65.747676908096,65.8608423313735,65.9739404938176,
66.0870161038044,66.2001956704368,66.3134267538955,66.4268715419683,66.5136614541785,
66.6271406312406,66.74041812383,66.8535835471076,66.9666817095518,67.0797573195385,
67.1929368861709,67.3061679696297,67.4196127577025,67.5064026699125,67.6198818469746,
67.7331593395642,67.8463247628417,67.959422925286,68.0724985352728,68.1856781019053,
68.298909185364,68.4123539734368,68.4991438856465,68.6126230627086,68.725900555298,
68.8390659785756,68.9521641410198,69.0652397510065,69.1784193176389,69.2916504010977,
69.4050951891705,69.4918851013805,69.6040236394296,69.7159996034553,69.8278600055178,
69.9396848486517,70.051485086998,70.1633755926539,70.2377801854363),
 .UNSPECIFIED.);
#316=B_SPLINE_CURVE_WITH_KNOTS('',3,(#35884,#35885,#35886,#35887,#35888,
#35889,#35890,#35891,#35892,#35893,#35894,#35895,#35896,#35897,#35898,#35899,
#35900,#35901,#35902,#35903,#35904,#35905,#35906,#35907,#35908,#35909,#35910,
#35911,#35912,#35913,#35914,#35915,#35916,#35917,#35918,#35919,#35920,#35921,
#35922,#35923,#35924,#35925,#35926,#35927,#35928,#35929,#35930,#35931,#35932,
#35933,#35934,#35935,#35936,#35937,#35938,#35939,#35940,#35941,#35942,#35943,
#35944,#35945,#35946,#35947,#35948,#35949,#35950,#35951,#35952,#35953,#35954,
#35955,#35956,#35957,#35958,#35959,#35960,#35961,#35962,#35963,#35964,#35965,
#35966,#35967,#35968,#35969,#35970,#35971,#35972,#35973,#35974,#35975,#35976,
#35977,#35978,#35979,#35980,#35981,#35982,#35983,#35984,#35985,#35986,#35987,
#35988,#35989,#35990,#35991,#35992,#35993,#35994,#35995,#35996,#35997,#35998,
#35999,#36000,#36001,#36002,#36003,#36004,#36005,#36006,#36007,#36008,#36009,
#36010,#36011,#36012,#36013,#36014,#36015,#36016,#36017,#36018,#36019,#36020,
#36021,#36022,#36023,#36024,#36025,#36026,#36027,#36028,#36029,#36030,#36031,
#36032,#36033,#36034,#36035,#36036,#36037,#36038,#36039,#36040,#36041,#36042,
#36043,#36044,#36045,#36046,#36047,#36048,#36049,#36050,#36051,#36052,#36053,
#36054,#36055),.UNSPECIFIED.,.F.,.F.,(4,3,3,3,3,3,3,3,3,3,3,3,3,3,3,3,3,
3,3,3,3,3,3,3,3,3,3,3,3,3,3,3,3,3,3,3,3,3,3,3,3,3,3,3,3,3,3,3,3,3,3,3,3,
3,3,3,3,4),(-79.4902472066036,-79.4192972587206,-79.3058180816587,-79.1925405890693,
-79.0793751657918,-78.9662770033477,-78.853201393361,-78.7400218267286,
-78.6267907432699,-78.5133459551973,-78.4265560429866,-78.3130768659242,
-78.1997993733345,-78.0866339500565,-77.9735357876121,-77.8604601776248,
-77.747280610992,-77.6340495275329,-77.5206047394597,-77.4338148272526,
-77.3203356501907,-77.2070581576014,-77.093892734324,-76.98079457188,-76.8677189618932,
-76.7545393952609,-76.6413083118023,-76.5278635237296,-76.4410736115186,
-76.3275944344566,-76.2143169418672,-76.1011515185896,-75.9880533561455,
-75.8749777461586,-75.7617981795262,-75.6485670960674,-75.5351223079947,
-75.4483323957846,-75.3348532187225,-75.221575726133,-75.1084103028553,
-74.9953121404112,-74.8822365304243,-74.7690569637918,-74.655825880333,
-74.5423810922601,-74.4555911800506,-74.3421120029886,-74.2288345103991,
-74.1156690871216,-74.0025709246775,-73.8894953146906,-73.7763157480582,
-73.6630846645994,-73.5496398765266,-73.4628499643166,-73.3181473348919,
-73.2070618999507),.UNSPECIFIED.);
#317=B_SPLINE_CURVE_WITH_KNOTS('',3,(#36056,#36057,#36058,#36059,#36060,
#36061,#36062,#36063,#36064,#36065,#36066,#36067,#36068,#36069,#36070,#36071,
#36072,#36073,#36074,#36075,#36076,#36077,#36078,#36079,#36080,#36081,#36082,
#36083,#36084,#36085,#36086,#36087,#36088,#36089,#36090,#36091,#36092,#36093,
#36094,#36095,#36096,#36097,#36098,#36099,#36100,#36101,#36102,#36103,#36104,
#36105,#36106,#36107,#36108,#36109,#36110,#36111,#36112,#36113,#36114,#36115,
#36116,#36117,#36118,#36119,#36120,#36121,#36122,#36123,#36124,#36125,#36126,
#36127,#36128,#36129,#36130,#36131,#36132,#36133,#36134,#36135,#36136,#36137,
#36138,#36139,#36140,#36141,#36142,#36143,#36144,#36145,#36146,#36147,#36148,
#36149,#36150,#36151,#36152,#36153,#36154,#36155,#36156,#36157,#36158,#36159,
#36160,#36161,#36162,#36163,#36164,#36165,#36166,#36167,#36168,#36169,#36170,
#36171,#36172,#36173,#36174,#36175,#36176,#36177,#36178,#36179,#36180,#36181,
#36182,#36183,#36184,#36185,#36186,#36187,#36188,#36189,#36190,#36191,#36192,
#36193,#36194,#36195,#36196,#36197,#36198,#36199,#36200,#36201,#36202,#36203,
#36204,#36205,#36206,#36207,#36208,#36209,#36210,#36211,#36212,#36213,#36214,
#36215,#36216,#36217,#36218,#36219,#36220,#36221,#36222,#36223,#36224,#36225,
#36226,#36227),.UNSPECIFIED.,.F.,.F.,(4,3,3,3,3,3,3,3,3,3,3,3,3,3,3,3,3,
3,3,3,3,3,3,3,3,3,3,3,3,3,3,3,3,3,3,3,3,3,3,3,3,3,3,3,3,3,3,3,3,3,3,3,3,
3,3,3,3,4),(70.2377801861003,70.3845228516675,70.4846263171145,70.5981054941765,
70.7113829867659,70.8245484100434,70.9376465724876,71.0507221824744,71.1639017491068,
71.2771328325656,71.3905776206383,71.4773675328486,71.5908467099108,71.7041242025004,
71.8172896257782,71.9303877882225,72.0434633982096,72.1566429648422,72.2698740483012,
72.3833188363742,72.4701087485826,72.5835879256446,72.6968654182339,72.8100308415114,
72.9231290039555,73.0362046139423,73.1493841805746,73.2626152640333,73.376060052106,
73.4628499643166,73.5763291413786,73.689606633968,73.8027720572456,73.9158702196897,
74.0289458296766,74.142125396309,74.2553564797677,74.3688012678405,74.4555911800506,
74.5690703571127,74.6823478497023,74.7955132729799,74.9086114354242,75.0216870454112,
75.1348666120437,75.2480976955025,75.3615424835754,75.4483323957846,75.5618115728466,
75.675089065436,75.7882544887136,75.9013526511576,76.0144282611445,76.1276078277769,
76.2408389112356,76.3542836993083,76.4410736115186,76.5209654926159),
 .UNSPECIFIED.);
#318=B_SPLINE_CURVE_WITH_KNOTS('',3,(#36232,#36233,#36234,#36235,#36236,
#36237,#36238,#36239,#36240,#36241,#36242,#36243,#36244,#36245,#36246,#36247,
#36248,#36249,#36250,#36251,#36252,#36253,#36254,#36255,#36256,#36257,#36258,
#36259,#36260,#36261,#36262,#36263,#36264,#36265,#36266,#36267,#36268,#36269,
#36270,#36271,#36272,#36273,#36274,#36275,#36276,#36277,#36278,#36279,#36280,
#36281,#36282,#36283,#36284,#36285,#36286,#36287,#36288,#36289,#36290,#36291,
#36292,#36293,#36294,#36295,#36296,#36297,#36298,#36299,#36300,#36301,#36302,
#36303,#36304,#36305,#36306,#36307,#36308,#36309,#36310,#36311,#36312,#36313,
#36314,#36315,#36316,#36317,#36318,#36319,#36320,#36321,#36322,#36323,#36324,
#36325,#36326,#36327,#36328,#36329,#36330,#36331,#36332,#36333,#36334,#36335,
#36336,#36337,#36338,#36339,#36340,#36341,#36342,#36343,#36344,#36345,#36346,
#36347,#36348,#36349,#36350,#36351,#36352,#36353,#36354,#36355,#36356,#36357,
#36358,#36359,#36360,#36361,#36362,#36363,#36364,#36365,#36366,#36367,#36368,
#36369,#36370,#36371,#36372,#36373,#36374,#36375,#36376,#36377,#36378,#36379,
#36380,#36381,#36382,#36383,#36384,#36385,#36386,#36387,#36388,#36389,#36390,
#36391,#36392,#36393,#36394,#36395,#36396,#36397,#36398,#36399,#36400,#36401,
#36402,#36403,#36404,#36405,#36406),.UNSPECIFIED.,.F.,.F.,(4,3,3,3,3,3,
3,3,3,3,3,3,3,3,3,3,3,3,3,3,3,3,3,3,3,3,3,3,3,3,3,3,3,3,3,3,3,3,3,3,3,3,
3,3,3,3,3,3,3,3,3,3,3,3,3,3,3,3,4),(-85.7734325133808,-85.6485487228822,
-85.5231844388738,-85.3972249658836,-85.3757445531247,-85.2622653760628,
-85.1489878834734,-85.035822460196,-84.9227242977519,-84.8096486877652,
-84.6964691211328,-84.5832380376741,-84.4697932496014,-84.3830033373907,
-84.2695241603285,-84.1562466677389,-84.0430812444612,-83.9299830820169,
-83.8169074720299,-83.7037279053972,-83.5904968219383,-83.4770520338654,
-83.3902621216566,-83.2767829445946,-83.1635054520052,-83.0503400287277,
-82.9372418662836,-82.8241662562967,-82.7109866896643,-82.5977556062056,
-82.4843108181328,-82.3975209059226,-82.2840417288606,-82.1707642362712,
-82.0575988129937,-81.9445006505496,-81.8314250405627,-81.7182454739304,
-81.6050143904716,-81.4915696023989,-81.4047796901886,-81.2913005131265,
-81.178023020537,-81.0648575972594,-80.9517594348152,-80.8386838248283,
-80.7255042581958,-80.6122731747369,-80.4988283866641,-80.4120384744546,
-80.2968145660226,-80.1846668139561,-80.0726271544152,-79.9606490097494,
-79.8430485590616,-79.730983798647,-79.6188550029826,-79.5065475500105,
-79.4902472069982),.UNSPECIFIED.);
#319=B_SPLINE_CURVE_WITH_KNOTS('',3,(#36407,#36408,#36409,#36410,#36411,
#36412,#36413,#36414,#36415,#36416,#36417,#36418,#36419,#36420,#36421,#36422,
#36423,#36424,#36425,#36426,#36427,#36428,#36429,#36430,#36431,#36432,#36433,
#36434,#36435,#36436,#36437,#36438,#36439,#36440,#36441,#36442,#36443,#36444,
#36445,#36446,#36447,#36448,#36449,#36450,#36451,#36452,#36453,#36454,#36455,
#36456,#36457,#36458,#36459,#36460,#36461,#36462,#36463,#36464,#36465,#36466,
#36467,#36468,#36469,#36470,#36471,#36472,#36473,#36474,#36475,#36476,#36477,
#36478,#36479,#36480,#36481,#36482,#36483,#36484,#36485,#36486,#36487,#36488,
#36489,#36490,#36491,#36492,#36493,#36494,#36495,#36496,#36497,#36498,#36499,
#36500,#36501,#36502,#36503,#36504,#36505,#36506,#36507,#36508,#36509,#36510,
#36511,#36512,#36513,#36514,#36515,#36516,#36517,#36518,#36519,#36520,#36521,
#36522,#36523,#36524,#36525,#36526,#36527,#36528,#36529,#36530,#36531,#36532,
#36533,#36534,#36535,#36536,#36537,#36538,#36539,#36540,#36541,#36542,#36543,
#36544,#36545,#36546,#36547,#36548,#36549,#36550,#36551,#36552,#36553,#36554,
#36555,#36556,#36557,#36558,#36559,#36560,#36561,#36562,#36563,#36564,#36565,
#36566,#36567,#36568,#36569,#36570,#36571,#36572,#36573,#36574,#36575,#36576,
#36577,#36578),.UNSPECIFIED.,.F.,.F.,(4,3,3,3,3,3,3,3,3,3,3,3,3,3,3,3,3,
3,3,3,3,3,3,3,3,3,3,3,3,3,3,3,3,3,3,3,3,3,3,3,3,3,3,3,3,3,3,3,3,3,3,3,3,
3,3,3,3,4),(76.5209654930255,76.6350716598039,76.7470962172469,76.8590234384047,
76.9709000002762,77.0866287070203,77.1986165292358,77.3162156782442,77.4338148272526,
77.5472940043146,77.660571496904,77.7737369201816,77.8868350826257,77.9999106926124,
78.1130902592448,78.2263213427036,78.3397661307763,78.4265560429866,78.5400352200487,
78.6533127126381,78.7664781359158,78.8795762983599,78.9926519083468,79.1058314749793,
79.2190625584381,79.3325073465109,79.4192972587206,79.5327764357826,79.646053928372,
79.7592193516496,79.8723175140938,79.9853931240806,80.098572690713,80.2118037741718,
80.3252485622446,80.4120384744546,80.5255176515167,80.6387951441061,80.7519605673837,
80.8650587298277,80.9781343398147,81.0913139064472,81.204544989906,81.3179897779787,
81.4047796901886,81.5182588672508,81.6315363598402,81.7447017831178,81.857799945562,
81.9708755555491,82.0840551221816,82.1972862056402,82.310730993713,82.3975209059226,
82.5226125308546,82.6472946873853,82.7713407864416,82.8041507994147),
 .UNSPECIFIED.);
#320=B_SPLINE_CURVE_WITH_KNOTS('',3,(#36583,#36584,#36585,#36586,#36587,
#36588,#36589,#36590,#36591,#36592,#36593,#36594,#36595,#36596,#36597,#36598,
#36599,#36600,#36601,#36602,#36603,#36604,#36605,#36606,#36607,#36608,#36609,
#36610,#36611,#36612,#36613,#36614,#36615,#36616,#36617,#36618,#36619,#36620,
#36621,#36622,#36623,#36624,#36625,#36626,#36627,#36628,#36629,#36630,#36631,
#36632,#36633,#36634,#36635,#36636,#36637,#36638,#36639,#36640,#36641,#36642,
#36643,#36644,#36645,#36646,#36647,#36648,#36649,#36650,#36651,#36652,#36653,
#36654,#36655,#36656,#36657,#36658,#36659,#36660,#36661,#36662,#36663,#36664,
#36665,#36666,#36667,#36668,#36669,#36670,#36671,#36672,#36673,#36674,#36675,
#36676,#36677,#36678,#36679,#36680,#36681,#36682,#36683,#36684,#36685,#36686,
#36687,#36688,#36689,#36690,#36691,#36692,#36693,#36694,#36695,#36696,#36697,
#36698,#36699,#36700,#36701,#36702,#36703,#36704,#36705,#36706,#36707,#36708,
#36709,#36710,#36711,#36712,#36713,#36714,#36715,#36716,#36717,#36718,#36719,
#36720,#36721,#36722,#36723,#36724,#36725,#36726,#36727,#36728,#36729,#36730,
#36731,#36732,#36733,#36734,#36735,#36736,#36737,#36738,#36739,#36740,#36741,
#36742,#36743,#36744,#36745,#36746,#36747,#36748,#36749,#36750,#36751,#36752,
#36753,#36754,#36755,#36756,#36757),.UNSPECIFIED.,.F.,.F.,(4,3,3,3,3,3,
3,3,3,3,3,3,3,3,3,3,3,3,3,3,3,3,3,3,3,3,3,3,3,3,3,3,3,3,3,3,3,3,3,3,3,3,
3,3,3,3,3,3,3,3,3,3,3,3,3,3,3,3,4),(-92.0566178209628,-91.9445269762773,
-91.8324988389338,-91.7204870233133,-91.6083683376705,-91.4961894402909,
-91.3838092159556,-91.3321918475287,-91.2187126704667,-91.1054351778774,
-90.9922697545999,-90.8791715921557,-90.7660959821688,-90.6529164155364,
-90.5396853320778,-90.426240544005,-90.3394506317947,-90.2259714547327,
-90.1126939621431,-89.9995285388655,-89.8864303764212,-89.7733547664343,
-89.6601751998018,-89.5469441163429,-89.4334993282701,-89.3467094160607,
-89.2332302389987,-89.1199527464093,-89.0067873231316,-88.8936891606874,
-88.7806135507007,-88.6674339840682,-88.5542029006094,-88.4407581125366,
-88.3539682003267,-88.2404890232647,-88.1272115306754,-88.0140461073978,
-87.9009479449537,-87.7878723349669,-87.6746927683346,-87.561461684876,
-87.4480168968032,-87.3612269845927,-87.2477478075305,-87.1344703149409,
-87.0213048916631,-86.9082067292188,-86.7951311192316,-86.681951552599,
-86.5687204691401,-86.4552756810672,-86.3684857688587,-86.253338783512,
-86.1333622160798,-86.0186000153121,-85.9039411269373,-85.789345853808,
-85.7734325137832),.UNSPECIFIED.);
#321=B_SPLINE_CURVE_WITH_KNOTS('',3,(#36758,#36759,#36760,#36761,#36762,
#36763,#36764,#36765,#36766,#36767,#36768,#36769,#36770,#36771,#36772,#36773,
#36774,#36775,#36776,#36777,#36778,#36779,#36780,#36781,#36782,#36783,#36784,
#36785,#36786,#36787,#36788,#36789,#36790,#36791,#36792,#36793,#36794,#36795,
#36796,#36797,#36798,#36799,#36800,#36801,#36802,#36803,#36804,#36805,#36806,
#36807,#36808,#36809,#36810,#36811,#36812,#36813,#36814,#36815,#36816,#36817,
#36818,#36819,#36820,#36821,#36822,#36823,#36824,#36825,#36826,#36827,#36828,
#36829,#36830,#36831,#36832,#36833,#36834,#36835,#36836,#36837,#36838,#36839,
#36840,#36841,#36842,#36843,#36844,#36845,#36846,#36847,#36848,#36849,#36850,
#36851,#36852,#36853,#36854,#36855,#36856,#36857,#36858,#36859,#36860,#36861,
#36862,#36863,#36864,#36865,#36866,#36867,#36868,#36869,#36870,#36871,#36872,
#36873,#36874,#36875,#36876,#36877,#36878,#36879,#36880,#36881,#36882,#36883,
#36884,#36885,#36886,#36887,#36888,#36889,#36890,#36891,#36892,#36893,#36894,
#36895,#36896,#36897,#36898,#36899,#36900,#36901,#36902,#36903,#36904,#36905,
#36906,#36907,#36908,#36909,#36910,#36911,#36912,#36913,#36914,#36915,#36916,
#36917,#36918,#36919,#36920,#36921,#36922,#36923,#36924,#36925,#36926,#36927,
#36928,#36929),.UNSPECIFIED.,.F.,.F.,(4,3,3,3,3,3,3,3,3,3,3,3,3,3,3,3,3,
3,3,3,3,3,3,3,3,3,3,3,3,3,3,3,3,3,3,3,3,3,3,3,3,3,3,3,3,3,3,3,3,3,3,3,3,
3,3,3,3,4),(82.8041507997955,82.9190225628795,83.0368324525738,83.1519469049721,
83.2711045133144,83.3902621216566,83.5037412987186,83.6170187913081,83.7301842145858,
83.8432823770299,83.9563579870169,84.0695375536494,84.1827686371082,84.296213425181,
84.3830033373907,84.4964825144528,84.6097600070423,84.7229254303199,84.836023592764,
84.9490992027509,85.0622787693834,85.1755098528421,85.288954640915,85.3757445531247,
85.4892237301867,85.6025012227762,85.7156666460537,85.8287648084979,85.9418404184848,
86.0550199851173,86.168251068576,86.2816958566487,86.3684857688587,86.4819649459208,
86.5952424385102,86.7084078617878,86.821506024232,86.9345816342187,87.0477612008512,
87.1609922843101,87.2744370723829,87.3612269845927,87.4747061616547,87.5879836542441,
87.7011490775217,87.8142472399658,87.9273228499528,88.0405024165853,88.153733500044,
88.2671782881169,88.3539682003267,88.4662367419806,88.5783413179199,88.6903287715846,
88.802274943831,88.9141951257727,89.0261943465735,89.0873361069751),
 .UNSPECIFIED.);
#322=B_SPLINE_CURVE_WITH_KNOTS('',3,(#36934,#36935,#36936,#36937,#36938,
#36939,#36940,#36941,#36942,#36943,#36944,#36945,#36946,#36947,#36948,#36949,
#36950,#36951,#36952,#36953,#36954,#36955,#36956,#36957,#36958,#36959,#36960,
#36961,#36962,#36963,#36964,#36965,#36966,#36967,#36968,#36969,#36970,#36971,
#36972,#36973,#36974,#36975,#36976,#36977,#36978,#36979,#36980,#36981,#36982,
#36983,#36984,#36985,#36986,#36987,#36988,#36989,#36990,#36991,#36992,#36993,
#36994,#36995,#36996,#36997,#36998,#36999,#37000,#37001,#37002,#37003,#37004,
#37005,#37006,#37007,#37008,#37009,#37010,#37011,#37012,#37013,#37014,#37015,
#37016,#37017,#37018,#37019,#37020,#37021,#37022,#37023,#37024,#37025,#37026,
#37027,#37028,#37029,#37030,#37031,#37032,#37033,#37034,#37035,#37036,#37037,
#37038,#37039,#37040,#37041,#37042,#37043,#37044,#37045,#37046,#37047,#37048,
#37049,#37050,#37051,#37052,#37053,#37054,#37055,#37056,#37057,#37058,#37059,
#37060,#37061,#37062,#37063,#37064,#37065,#37066,#37067,#37068,#37069,#37070,
#37071,#37072,#37073,#37074,#37075,#37076,#37077,#37078,#37079,#37080,#37081,
#37082,#37083,#37084,#37085,#37086,#37087,#37088,#37089,#37090,#37091,#37092,
#37093,#37094,#37095,#37096,#37097,#37098,#37099,#37100,#37101,#37102,#37103,
#37104,#37105),.UNSPECIFIED.,.F.,.F.,(4,3,3,3,3,3,3,3,3,3,3,3,3,3,3,3,3,
3,3,3,3,3,3,3,3,3,3,3,3,3,3,3,3,3,3,3,3,3,3,3,3,3,3,3,3,3,3,3,3,3,3,3,3,
3,3,3,3,4),(-98.3398031281424,-98.2813803576668,-98.1679011806047,-98.054623688015,
-97.9414582647372,-97.828360102293,-97.7152844923059,-97.6021049256733,
-97.4888738422143,-97.3754290541414,-97.2886391419328,-97.1751599648709,
-97.0618824722816,-96.9487170490041,-96.8356188865602,-96.7225432765735,
-96.6093637099411,-96.4961326264825,-96.3826878384099,-96.2958979261987,
-96.1824187491366,-96.0691412565472,-95.9559758332695,-95.8428776708253,
-95.7298020608384,-95.6166224942059,-95.5033914107471,-95.3899466226742,
-95.3031567104647,-95.1896775334027,-95.0764000408132,-94.9632346175356,
-94.8501364550915,-94.7370608451046,-94.6238812784722,-94.5106501950134,
-94.3972054069406,-94.3104154947307,-94.1969363176687,-94.0836588250792,
-93.9704934018016,-93.8573952393575,-93.7443196293706,-93.6311400627381,
-93.5179089792793,-93.4044641912065,-93.3176742789967,-93.2041951019347,
-93.0909176093452,-92.9777521860676,-92.8646540236235,-92.7515784136366,
-92.6383988470042,-92.5251677635455,-92.4117229754727,-92.3249330632627,
-92.1828327203833,-92.0566178213547),.UNSPECIFIED.);
#323=B_SPLINE_CURVE_WITH_KNOTS('',3,(#37106,#37107,#37108,#37109,#37110,
#37111,#37112,#37113,#37114,#37115,#37116,#37117,#37118,#37119,#37120,#37121,
#37122,#37123,#37124,#37125,#37126,#37127,#37128,#37129,#37130,#37131,#37132,
#37133,#37134,#37135,#37136,#37137,#37138,#37139,#37140,#37141,#37142,#37143,
#37144,#37145,#37146,#37147,#37148,#37149,#37150,#37151,#37152,#37153,#37154,
#37155,#37156,#37157,#37158,#37159,#37160,#37161,#37162,#37163,#37164,#37165,
#37166,#37167,#37168,#37169,#37170,#37171,#37172,#37173,#37174,#37175,#37176,
#37177,#37178,#37179,#37180,#37181,#37182,#37183,#37184,#37185,#37186,#37187,
#37188,#37189,#37190,#37191,#37192,#37193,#37194,#37195,#37196,#37197,#37198,
#37199,#37200,#37201,#37202,#37203,#37204,#37205,#37206,#37207,#37208,#37209,
#37210,#37211,#37212,#37213,#37214,#37215,#37216,#37217,#37218,#37219,#37220,
#37221,#37222,#37223,#37224,#37225,#37226,#37227,#37228,#37229,#37230,#37231,
#37232,#37233,#37234,#37235,#37236,#37237,#37238,#37239,#37240,#37241,#37242,
#37243,#37244,#37245,#37246,#37247,#37248,#37249,#37250,#37251,#37252,#37253,
#37254,#37255,#37256,#37257,#37258,#37259,#37260,#37261,#37262,#37263,#37264,
#37265,#37266,#37267,#37268,#37269,#37270,#37271,#37272,#37273,#37274,#37275,
#37276,#37277),.UNSPECIFIED.,.F.,.F.,(4,3,3,3,3,3,3,3,3,3,3,3,3,3,3,3,3,
3,3,3,3,3,3,3,3,3,3,3,3,3,3,3,3,3,3,3,3,3,3,3,3,3,3,3,3,3,3,3,3,3,3,3,3,
3,3,3,3,4),(89.0873361075773,89.2312652478138,89.3467094160607,89.4601885931227,
89.5734660857121,89.6866315089897,89.7997296714338,89.9128052814208,90.0259848480532,
90.1392159315119,90.2526607195847,90.3394506317947,90.4529298088567,90.5662073014462,
90.6793727247237,90.7924708871679,90.9055464971547,91.0187260637872,91.131957147246,
91.2454019353187,91.3321918475287,91.4456710245907,91.5589485171802,91.6721139404578,
91.7852121029019,91.8982877128888,92.0114672795213,92.1246983629801,92.2381431510529,
92.3249330632627,92.4384122403247,92.5516897329142,92.6648551561918,92.777953318636,
92.8910289286229,93.0042084952553,93.1174395787141,93.2308843667869,93.3176742789967,
93.4311534560588,93.5444309486482,93.6575963719257,93.7706945343698,93.8837701443567,
93.9969497109891,94.1101807944479,94.2236255825206,94.3104154947307,94.4238946717927,
94.5371721643822,94.6503375876598,94.7634357501039,94.8765113600907,94.9896909267232,
95.1029220101819,95.2163667982547,95.3031567104647,95.3705214141547),
 .UNSPECIFIED.);
#324=B_SPLINE_CURVE_WITH_KNOTS('',3,(#37282,#37283,#37284,#37285,#37286,
#37287,#37288,#37289,#37290,#37291,#37292,#37293,#37294,#37295,#37296,#37297,
#37298,#37299,#37300,#37301,#37302,#37303,#37304,#37305,#37306,#37307,#37308,
#37309,#37310,#37311,#37312,#37313,#37314,#37315,#37316,#37317,#37318,#37319,
#37320,#37321,#37322,#37323,#37324,#37325,#37326,#37327,#37328,#37329,#37330,
#37331,#37332,#37333,#37334,#37335,#37336,#37337,#37338,#37339,#37340,#37341,
#37342,#37343,#37344,#37345,#37346,#37347,#37348,#37349,#37350,#37351,#37352,
#37353,#37354,#37355,#37356,#37357,#37358,#37359,#37360,#37361,#37362,#37363,
#37364,#37365,#37366,#37367,#37368,#37369,#37370,#37371,#37372,#37373,#37374,
#37375,#37376,#37377,#37378,#37379,#37380,#37381,#37382,#37383,#37384,#37385,
#37386,#37387,#37388,#37389,#37390,#37391,#37392,#37393,#37394,#37395,#37396,
#37397,#37398,#37399,#37400,#37401,#37402,#37403,#37404,#37405,#37406,#37407,
#37408,#37409,#37410,#37411,#37412,#37413,#37414,#37415,#37416,#37417,#37418,
#37419,#37420,#37421,#37422,#37423,#37424,#37425,#37426,#37427,#37428,#37429,
#37430,#37431,#37432,#37433,#37434,#37435,#37436,#37437,#37438,#37439,#37440,
#37441,#37442,#37443,#37444,#37445,#37446,#37447,#37448,#37449,#37450,#37451,
#37452,#37453),.UNSPECIFIED.,.F.,.F.,(4,3,3,3,3,3,3,3,3,3,3,3,3,3,3,3,3,
3,3,3,3,3,3,3,3,3,3,3,3,3,3,3,3,3,3,3,3,3,3,3,3,3,3,3,3,3,3,3,3,3,3,3,3,
3,3,3,3,4),(-104.622988434897,-104.497045431599,-104.367436541835,-104.237827652071,
-104.124348475011,-104.011070982423,-103.897905559147,-103.784807396705,
-103.67173178672,-103.55855222009,-103.445321136633,-103.331876348562,-103.245086436337,
-103.131607259276,-103.018329766687,-102.90516434341,-102.792066180966,
-102.67899057098,-102.565811004348,-102.45257992089,-102.339135132818,-102.252345220603,
-102.13886604354,-102.02558855095,-101.912423127672,-101.799324965227,-101.686249355239,
-101.573069788606,-101.459838705146,-101.346393917072,-101.259604004869,
-101.146124827807,-101.032847335218,-100.919681911941,-100.806583749497,
-100.69350813951,-100.580328572878,-100.46709748942,-100.353652701347,-100.266862789135,
-100.153383612073,-100.040106119484,-99.9269406962061,-99.813842533762,
-99.7007669237751,-99.5875873571428,-99.4743562736841,-99.3609114856114,
-99.2741215734008,-99.1573317677877,-99.045033056258,-98.9328421780367,
-98.8207127649638,-98.7085985481294,-98.5963824897407,-98.4841051256357,
-98.3716413638913,-98.3398031284962),.UNSPECIFIED.);
#325=B_SPLINE_CURVE_WITH_KNOTS('',3,(#37454,#37455,#37456,#37457,#37458,
#37459,#37460,#37461,#37462,#37463,#37464,#37465,#37466,#37467,#37468,#37469,
#37470,#37471,#37472,#37473,#37474,#37475,#37476,#37477,#37478,#37479,#37480,
#37481,#37482,#37483,#37484,#37485,#37486,#37487,#37488,#37489,#37490,#37491,
#37492,#37493,#37494,#37495,#37496,#37497,#37498,#37499,#37500,#37501,#37502,
#37503,#37504,#37505,#37506,#37507,#37508,#37509,#37510,#37511,#37512,#37513,
#37514,#37515,#37516,#37517,#37518,#37519,#37520,#37521,#37522,#37523,#37524,
#37525,#37526,#37527,#37528,#37529,#37530,#37531,#37532,#37533,#37534,#37535,
#37536,#37537,#37538,#37539,#37540,#37541,#37542,#37543,#37544,#37545,#37546,
#37547,#37548,#37549,#37550,#37551,#37552,#37553,#37554,#37555,#37556,#37557,
#37558,#37559,#37560,#37561,#37562,#37563,#37564,#37565,#37566,#37567,#37568,
#37569,#37570,#37571,#37572,#37573,#37574,#37575,#37576,#37577,#37578,#37579,
#37580,#37581,#37582,#37583,#37584,#37585,#37586,#37587,#37588,#37589,#37590,
#37591,#37592,#37593,#37594,#37595,#37596,#37597,#37598,#37599,#37600,#37601,
#37602,#37603,#37604,#37605,#37606,#37607,#37608,#37609,#37610,#37611,#37612,
#37613,#37614,#37615,#37616,#37617,#37618,#37619,#37620,#37621,#37622,#37623,
#37624,#37625,#37626,#37627,#37628),.UNSPECIFIED.,.F.,.F.,(4,3,3,3,3,3,
3,3,3,3,3,3,3,3,3,3,3,3,3,3,3,3,3,3,3,3,3,3,3,3,3,3,3,3,3,3,3,3,3,3,3,3,
3,3,3,3,3,3,3,3,3,3,3,3,3,3,3,3,4),(95.3705214145325,95.4861934784908,95.5983624149504,
95.7104313611073,95.8224468167166,95.934455192268,96.0465754703724,96.1587643887504,
96.2711448642132,96.2958979261987,96.4093771032606,96.52265459585,96.6358200191276,
96.7489181815718,96.8619937915587,96.9751733581911,97.0884044416497,97.2018492297225,
97.2886391419327,97.4021183189946,97.515395811584,97.6285612348617,97.7416593973056,
97.8547350072924,97.9679145739248,98.0811456573836,98.1945904454564,98.2813803576667,
98.3948595347287,98.5081370273182,98.6213024505959,98.73440061304,98.847476223027,
98.9606557896595,99.0738868731184,99.1873316611913,99.2741215734008,99.3876007504629,
99.5008782430525,99.6140436663302,99.7271418287744,99.8402174387616,99.9533970053941,
100.066628088853,100.180072876926,100.266862789135,100.380341966197,100.493619458786,
100.606784882064,100.719883044508,100.832958654494,100.946138221127,101.059369304585,
101.172814092658,101.259604004869,101.385777191572,101.511498690172,101.636515904144,
101.653706720924),.UNSPECIFIED.);
#326=B_SPLINE_CURVE_WITH_KNOTS('',3,(#37633,#37634,#37635,#37636,#37637,
#37638,#37639,#37640,#37641,#37642,#37643,#37644,#37645,#37646,#37647,#37648,
#37649,#37650,#37651,#37652,#37653,#37654,#37655,#37656,#37657,#37658,#37659,
#37660,#37661,#37662,#37663,#37664,#37665,#37666,#37667,#37668,#37669,#37670,
#37671,#37672,#37673,#37674,#37675,#37676,#37677,#37678,#37679,#37680,#37681,
#37682,#37683,#37684,#37685,#37686,#37687,#37688,#37689,#37690,#37691,#37692,
#37693,#37694,#37695,#37696,#37697,#37698,#37699,#37700,#37701,#37702,#37703,
#37704,#37705,#37706,#37707,#37708,#37709,#37710,#37711,#37712,#37713,#37714,
#37715,#37716,#37717,#37718,#37719,#37720,#37721,#37722,#37723,#37724,#37725,
#37726,#37727,#37728,#37729,#37730,#37731,#37732,#37733,#37734,#37735,#37736,
#37737,#37738,#37739,#37740,#37741,#37742,#37743,#37744,#37745,#37746,#37747,
#37748,#37749,#37750,#37751,#37752,#37753,#37754,#37755,#37756,#37757,#37758,
#37759,#37760,#37761,#37762,#37763,#37764,#37765,#37766,#37767,#37768,#37769,
#37770,#37771,#37772,#37773,#37774,#37775,#37776,#37777,#37778,#37779,#37780,
#37781,#37782,#37783,#37784,#37785,#37786,#37787,#37788,#37789,#37790,#37791,
#37792,#37793,#37794,#37795,#37796,#37797,#37798,#37799,#37800,#37801,#37802,
#37803,#37804,#37805,#37806,#37807),.UNSPECIFIED.,.F.,.F.,(4,3,3,3,3,3,
3,3,3,3,3,3,3,3,3,3,3,3,3,3,3,3,3,3,3,3,3,3,3,3,3,3,3,3,3,3,3,3,3,3,3,3,
3,3,3,3,3,3,3,3,3,3,3,3,3,3,3,3,4),(-110.906173742502,-110.793939498286,
-110.681759990839,-110.569589080838,-110.457304897499,-110.344954035642,
-110.232404211857,-110.194274946475,-110.080795769476,-109.967518276951,
-109.854352853737,-109.741254691356,-109.628179081433,-109.514999514863,
-109.401768431466,-109.288323643454,-109.201533730741,-109.088054553733,
-108.974777061199,-108.861611637978,-108.748513475592,-108.635437865664,
-108.522258299091,-108.409027215692,-108.295582427679,-108.208792515007,
-108.095313337899,-107.982035845262,-107.868870421936,-107.755772259443,
-107.642696649408,-107.529517082726,-107.416285999217,-107.302841211095,
-107.216051299273,-107.102572122223,-106.989294629645,-106.87612920638,
-106.763031043948,-106.649955433973,-106.536775867352,-106.423544783906,
-106.310099995844,-106.223310083539,-106.109830906482,-105.996553413898,
-105.883387990627,-105.770289828188,-105.657214218208,-105.544034651581,
-105.430803568129,-105.317358780062,-105.230568867805,-105.115803842946,
-105.001231835846,-104.886830152399,-104.772527199561,-104.658275035006,
-104.622988435322),.UNSPECIFIED.);
#327=B_SPLINE_CURVE_WITH_KNOTS('',3,(#37808,#37809,#37810,#37811,#37812,
#37813,#37814,#37815,#37816,#37817,#37818,#37819,#37820,#37821,#37822,#37823,
#37824,#37825,#37826,#37827,#37828,#37829,#37830,#37831,#37832,#37833,#37834,
#37835,#37836,#37837,#37838,#37839,#37840,#37841,#37842,#37843,#37844,#37845,
#37846,#37847,#37848,#37849,#37850,#37851,#37852,#37853,#37854,#37855,#37856,
#37857,#37858,#37859,#37860,#37861,#37862,#37863,#37864,#37865,#37866,#37867,
#37868,#37869,#37870,#37871,#37872,#37873,#37874,#37875,#37876,#37877,#37878,
#37879,#37880,#37881,#37882,#37883,#37884,#37885,#37886,#37887,#37888,#37889,
#37890,#37891,#37892,#37893,#37894,#37895,#37896,#37897,#37898,#37899,#37900,
#37901,#37902,#37903,#37904,#37905,#37906,#37907,#37908,#37909,#37910,#37911,
#37912,#37913,#37914,#37915,#37916,#37917,#37918,#37919,#37920,#37921,#37922,
#37923,#37924,#37925,#37926,#37927,#37928,#37929,#37930,#37931,#37932,#37933,
#37934,#37935,#37936,#37937,#37938,#37939,#37940,#37941,#37942,#37943,#37944,
#37945,#37946,#37947,#37948,#37949,#37950,#37951,#37952,#37953,#37954,#37955,
#37956,#37957,#37958,#37959,#37960,#37961,#37962,#37963,#37964,#37965,#37966,
#37967,#37968,#37969,#37970,#37971,#37972,#37973,#37974,#37975,#37976,#37977,
#37978,#37979,#37980,#37981,#37982),.UNSPECIFIED.,.F.,.F.,(4,3,3,3,3,3,
3,3,3,3,3,3,3,3,3,3,3,3,3,3,3,3,3,3,3,3,3,3,3,3,3,3,3,3,3,3,3,3,3,3,3,3,
3,3,3,3,3,3,3,3,3,3,3,3,3,3,3,3,4),(101.653706721334,101.768208363524,101.882752096176,
101.997465726927,102.112280389874,102.227321629928,102.252345220603,102.365824397664,
102.479101890253,102.59226731353,102.705365475974,102.81844108596,102.931620652592,
103.04485173605,103.158296524122,103.245086436337,103.358565613397,103.471843105984,
103.58500852926,103.698106691702,103.811182301686,103.924361868317,104.037592951773,
104.151037739844,104.237827652071,104.35130682914,104.464584321736,104.57774974502,
104.69084790747,104.803923517464,104.917103084102,105.030334167568,105.143778955646,
105.230568867805,105.344048044861,105.457325537444,105.570490960716,105.683589123154,
105.796664733135,105.909844299762,106.023075383215,106.136520171283,106.223310083539,
106.336789260589,106.450066753167,106.563232176432,106.676330338865,106.789405948839,
106.902585515459,107.015816598906,107.129261386967,107.216051299273,107.328469817482,
107.440722785259,107.552856842165,107.664943651989,107.777002830859,107.889130021498,
107.936892028514),.UNSPECIFIED.);
#328=B_SPLINE_CURVE_WITH_KNOTS('',3,(#37987,#37988,#37989,#37990,#37991,
#37992,#37993,#37994,#37995,#37996,#37997,#37998,#37999,#38000,#38001,#38002,
#38003,#38004,#38005,#38006,#38007,#38008,#38009,#38010,#38011,#38012,#38013,
#38014,#38015,#38016,#38017,#38018,#38019,#38020,#38021,#38022,#38023,#38024,
#38025,#38026,#38027,#38028,#38029,#38030,#38031,#38032,#38033,#38034,#38035,
#38036,#38037,#38038,#38039,#38040,#38041,#38042,#38043,#38044,#38045,#38046,
#38047,#38048,#38049,#38050,#38051,#38052,#38053,#38054,#38055,#38056,#38057,
#38058,#38059,#38060,#38061,#38062,#38063,#38064,#38065,#38066,#38067,#38068,
#38069,#38070,#38071,#38072,#38073,#38074,#38075,#38076,#38077,#38078,#38079,
#38080,#38081,#38082,#38083,#38084,#38085,#38086,#38087,#38088,#38089,#38090,
#38091,#38092,#38093,#38094,#38095,#38096,#38097,#38098,#38099,#38100,#38101,
#38102,#38103,#38104,#38105,#38106,#38107,#38108,#38109,#38110,#38111,#38112,
#38113,#38114,#38115,#38116,#38117,#38118,#38119,#38120,#38121,#38122,#38123,
#38124,#38125,#38126,#38127,#38128,#38129,#38130,#38131,#38132,#38133,#38134,
#38135,#38136,#38137,#38138,#38139,#38140,#38141,#38142,#38143,#38144,#38145,
#38146,#38147,#38148,#38149,#38150,#38151,#38152,#38153,#38154,#38155,#38156,
#38157,#38158),.UNSPECIFIED.,.F.,.F.,(4,3,3,3,3,3,3,3,3,3,3,3,3,3,3,3,3,
3,3,3,3,3,3,3,3,3,3,3,3,3,3,3,3,3,3,3,3,3,3,3,3,3,3,3,3,3,3,3,3,3,3,3,3,
3,3,3,3,4),(-117.189359049681,-117.143463456613,-117.029984262168,-116.916706751875,
-116.803541310712,-116.690443130233,-116.577367502095,-116.464187917276,
-116.350956815583,-116.237512009426,-116.150722240879,-116.037243064179,
-115.923965571878,-115.810800148842,-115.697701986594,-115.584626376755,
-115.471446810197,-115.35821572677,-115.244770938662,-115.157981025145,
-115.044501852382,-114.931224364215,-114.818058945434,-114.70496078755,
-114.59188518218,-114.478705620214,-114.365474541458,-114.252029758087,
-114.165239809411,-114.051760629865,-113.938483134742,-113.825317708902,
-113.712219543871,-113.599143931279,-113.485964362032,-113.37273327595,
-113.259288485273,-113.172498593677,-113.059019416883,-112.945741924558,
-112.832576501541,-112.719478339354,-112.606402729621,-112.493223163233,
-112.379992080016,-112.266547292174,-112.179757377943,-112.066278201375,
-111.953000709295,-111.839835286535,-111.726737124618,-111.613661515164,
-111.500481949072,-111.387250866159,-111.273806078632,-111.187016162209,
-111.04659495261,-110.906173743011),.UNSPECIFIED.);
#329=B_SPLINE_CURVE_WITH_KNOTS('',3,(#38159,#38160,#38161,#38162,#38163,
#38164,#38165,#38166,#38167,#38168,#38169,#38170,#38171,#38172,#38173,#38174,
#38175,#38176,#38177,#38178,#38179,#38180,#38181,#38182,#38183,#38184,#38185,
#38186,#38187,#38188,#38189,#38190,#38191,#38192,#38193,#38194,#38195,#38196,
#38197,#38198,#38199,#38200,#38201,#38202,#38203,#38204,#38205,#38206,#38207,
#38208,#38209,#38210,#38211,#38212,#38213,#38214,#38215,#38216,#38217,#38218,
#38219,#38220,#38221,#38222,#38223,#38224,#38225,#38226,#38227,#38228,#38229,
#38230,#38231,#38232,#38233,#38234,#38235,#38236,#38237,#38238,#38239,#38240,
#38241,#38242,#38243,#38244,#38245,#38246,#38247,#38248,#38249,#38250,#38251,
#38252,#38253,#38254,#38255,#38256,#38257,#38258,#38259,#38260,#38261,#38262,
#38263,#38264,#38265,#38266,#38267,#38268,#38269,#38270,#38271,#38272,#38273,
#38274,#38275,#38276,#38277,#38278,#38279,#38280,#38281,#38282,#38283,#38284,
#38285,#38286,#38287,#38288,#38289,#38290,#38291,#38292,#38293,#38294,#38295,
#38296,#38297,#38298,#38299,#38300,#38301,#38302,#38303,#38304,#38305,#38306,
#38307,#38308,#38309,#38310,#38311,#38312,#38313,#38314,#38315,#38316,#38317,
#38318,#38319,#38320,#38321,#38322,#38323,#38324,#38325,#38326,#38327,#38328,
#38329,#38330),.UNSPECIFIED.,.F.,.F.,(4,3,3,3,3,3,3,3,3,3,3,3,3,3,3,3,3,
3,3,3,3,3,3,3,3,3,3,3,3,3,3,3,3,3,3,3,3,3,3,3,3,3,3,3,3,3,3,3,3,3,3,3,3,
3,3,3,3,4),(107.936892028941,108.078296556603,108.208792515007,108.322271692009,
108.435549184539,108.548714607757,108.661812770142,108.774888380071,108.888067946647,
109.00129903005,109.114743818068,109.201533730741,109.315012907743,109.428290400271,
109.541455823486,109.654553985868,109.767629595792,109.88080916236,109.994040245755,
110.107485033765,110.194274946475,110.307754123899,110.42103161685,110.53419704049,
110.647295203295,110.760370813642,110.87355038063,110.986781464442,111.10022625286,
111.187016162209,111.300495338727,111.413772830776,111.526938253515,111.640036415426,
111.753112024883,111.866291590997,111.979522673944,112.092967461519,112.179757377943,
112.293236554778,112.40651404713,112.519679470164,112.632777632358,112.745853242091,
112.859032808463,112.972263891657,113.085708679464,113.172498593677,113.285977773331,
113.399255268519,113.512420694398,113.625518859441,113.73859447202,113.851774041214,
113.96500512722,114.078449917787,114.165239809411,114.220077335693),
 .UNSPECIFIED.);
#330=B_SPLINE_CURVE_WITH_KNOTS('',3,(#38335,#38336,#38337,#38338,#38339,
#38340,#38341,#38342,#38343,#38344,#38345,#38346,#38347,#38348,#38349,#38350,
#38351,#38352,#38353,#38354,#38355,#38356,#38357,#38358,#38359,#38360,#38361,
#38362,#38363,#38364,#38365,#38366,#38367,#38368,#38369,#38370,#38371,#38372,
#38373,#38374,#38375,#38376,#38377,#38378,#38379,#38380,#38381,#38382,#38383,
#38384,#38385,#38386,#38387,#38388,#38389,#38390,#38391,#38392,#38393,#38394,
#38395,#38396,#38397,#38398,#38399,#38400,#38401,#38402,#38403,#38404,#38405,
#38406,#38407,#38408,#38409,#38410,#38411,#38412,#38413,#38414,#38415,#38416,
#38417,#38418,#38419,#38420,#38421,#38422,#38423,#38424,#38425,#38426,#38427,
#38428,#38429,#38430,#38431,#38432,#38433,#38434,#38435,#38436,#38437,#38438,
#38439,#38440,#38441,#38442,#38443,#38444,#38445,#38446,#38447,#38448,#38449,
#38450,#38451,#38452,#38453,#38454,#38455,#38456,#38457,#38458,#38459,#38460,
#38461,#38462,#38463,#38464,#38465,#38466,#38467,#38468,#38469,#38470,#38471,
#38472,#38473,#38474,#38475,#38476,#38477,#38478,#38479,#38480,#38481,#38482,
#38483,#38484,#38485,#38486,#38487,#38488,#38489,#38490,#38491,#38492,#38493,
#38494,#38495,#38496,#38497,#38498,#38499,#38500,#38501,#38502,#38503,#38504,
#38505,#38506),.UNSPECIFIED.,.F.,.F.,(4,3,3,3,3,3,3,3,3,3,3,3,3,3,3,3,3,
3,3,3,3,3,3,3,3,3,3,3,3,3,3,3,3,3,3,3,3,3,3,3,3,3,3,3,3,3,3,3,3,3,3,3,3,
3,3,3,3,4),(-123.472544356421,-123.345470616914,-123.217416259133,-123.099910751017,
-122.986430819344,-122.873152561787,-122.759986367799,-122.646887430315,
-122.533811042367,-122.420630699507,-122.30739883959,-122.193953284424,
-122.107169535283,-121.993690187015,-121.880412514652,-121.767246906492,
-121.654148554392,-121.541072750307,-121.427892984211,-121.314661698002,
-121.201216704285,-121.114428319549,-121.000949433042,-120.887672238451,
-120.774507117501,-120.661409261157,-120.548333960498,-120.435154705727,
-120.321923936018,-120.208479460878,-120.121687103815,-120.008207809519,
-119.894930197774,-119.781764654257,-119.668666370711,-119.555590638977,
-119.442410950579,-119.329179745155,-119.21573483632,-119.128945888081,
-119.015466700982,-118.902189197496,-118.789023762804,-118.675925588448,
-118.562849966072,-118.449670386406,-118.336439289535,-118.222994487593,
-118.136204672347,-118.017848969589,-117.905379905631,-117.793018509986,
-117.680718661559,-117.568434336959,-117.456046233179,-117.34359766165,
-117.23095665154,-117.189359050281),.UNSPECIFIED.);
#331=B_SPLINE_CURVE_WITH_KNOTS('',3,(#38507,#38508,#38509,#38510,#38511,
#38512,#38513,#38514,#38515,#38516,#38517,#38518,#38519,#38520,#38521,#38522,
#38523,#38524,#38525,#38526,#38527,#38528,#38529,#38530,#38531,#38532,#38533,
#38534,#38535,#38536,#38537,#38538,#38539,#38540,#38541,#38542,#38543,#38544,
#38545,#38546,#38547,#38548,#38549,#38550,#38551,#38552,#38553,#38554,#38555,
#38556,#38557,#38558,#38559,#38560,#38561,#38562,#38563,#38564,#38565,#38566,
#38567,#38568,#38569,#38570,#38571,#38572,#38573,#38574,#38575,#38576,#38577,
#38578,#38579,#38580,#38581,#38582,#38583,#38584,#38585,#38586,#38587,#38588,
#38589,#38590,#38591,#38592,#38593,#38594,#38595,#38596,#38597,#38598,#38599,
#38600,#38601,#38602,#38603,#38604,#38605,#38606,#38607,#38608,#38609,#38610,
#38611,#38612,#38613,#38614,#38615,#38616,#38617,#38618,#38619,#38620,#38621,
#38622,#38623,#38624,#38625,#38626,#38627,#38628,#38629,#38630,#38631,#38632,
#38633,#38634,#38635,#38636,#38637,#38638,#38639,#38640,#38641,#38642,#38643,
#38644,#38645,#38646,#38647,#38648,#38649,#38650,#38651,#38652,#38653,#38654,
#38655,#38656,#38657,#38658,#38659,#38660,#38661,#38662,#38663,#38664,#38665,
#38666,#38667,#38668,#38669,#38670,#38671,#38672,#38673,#38674,#38675,#38676,
#38677,#38678),.UNSPECIFIED.,.F.,.F.,(4,3,3,3,3,3,3,3,3,3,3,3,3,3,3,3,3,
3,3,3,3,3,3,3,3,3,3,3,3,3,3,3,3,3,3,3,3,3,3,3,3,3,3,3,3,3,3,3,3,3,3,3,3,
3,3,3,3,4),(114.220077336359,114.337315297457,114.449646959165,114.561876301729,
114.674049612068,114.786213085774,114.898487007242,115.010826687181,115.1233612464,
115.157981025145,115.271460202267,115.384737694835,115.497903118042,115.611001280366,
115.724076890186,115.83725645658,115.950487539759,116.063932327492,116.150722240879,
116.264201435928,116.377478946583,116.49064438796,116.603742568506,116.716818196563,
116.829997781074,116.943228882334,117.056673687856,117.143463456613,117.256942594808,
117.370220048676,117.483385433349,117.596483557373,117.709559129191,117.822738658342,
117.935969704643,118.04941445655,118.136204672347,118.2496838634,118.362961369367,
118.476126805638,118.589224980674,118.702300602833,118.815480180898,118.928711275397,
119.042156073739,119.128945888081,119.242425185255,119.355702798712,119.468868343228,
119.581966627062,119.695042358373,119.808222045258,119.921453248561,120.034898154307,
120.121687103815,120.249019832346,120.376141237394,120.503262642443),
 .UNSPECIFIED.);
#332=B_SPLINE_CURVE_WITH_KNOTS('',3,(#38683,#38684,#38685,#38686,#38687,
#38688,#38689,#38690,#38691,#38692,#38693,#38694,#38695,#38696,#38697,#38698,
#38699,#38700,#38701,#38702,#38703,#38704,#38705,#38706,#38707,#38708,#38709,
#38710,#38711,#38712,#38713,#38714,#38715,#38716,#38717,#38718,#38719,#38720,
#38721,#38722,#38723,#38724,#38725,#38726,#38727,#38728,#38729,#38730,#38731,
#38732,#38733,#38734,#38735,#38736,#38737,#38738,#38739,#38740,#38741,#38742,
#38743,#38744,#38745,#38746,#38747,#38748,#38749,#38750,#38751,#38752,#38753,
#38754,#38755,#38756,#38757,#38758,#38759,#38760,#38761,#38762,#38763,#38764,
#38765,#38766,#38767,#38768,#38769,#38770,#38771,#38772,#38773,#38774,#38775,
#38776,#38777,#38778,#38779,#38780,#38781,#38782,#38783,#38784,#38785,#38786,
#38787,#38788,#38789,#38790,#38791,#38792,#38793,#38794,#38795,#38796,#38797,
#38798,#38799,#38800,#38801,#38802,#38803,#38804,#38805,#38806,#38807,#38808,
#38809,#38810,#38811,#38812,#38813,#38814,#38815,#38816,#38817,#38818,#38819,
#38820,#38821,#38822,#38823,#38824,#38825,#38826,#38827,#38828,#38829,#38830,
#38831,#38832,#38833,#38834,#38835,#38836,#38837,#38838,#38839,#38840,#38841,
#38842,#38843,#38844,#38845,#38846,#38847,#38848,#38849,#38850,#38851,#38852,
#38853,#38854,#38855,#38856,#38857),.UNSPECIFIED.,.F.,.F.,(4,3,3,3,3,3,
3,3,3,3,3,3,3,3,3,3,3,3,3,3,3,3,3,3,3,3,3,3,3,3,3,3,3,3,3,3,3,3,3,3,3,3,
3,3,3,3,3,3,3,3,3,3,3,3,3,3,3,3,4),(-129.75572966404,-129.643438869128,
-129.531194980693,-129.418952001974,-129.306589037397,-129.19415280237,
-129.081519012781,-129.056358045421,-128.94285419673,-128.829551963253,
-128.716361776385,-128.603238873322,-128.49013859133,-128.376934659812,
-128.263679344804,-128.150210849827,-128.063616829687,-127.950117757225,
-127.836819680326,-127.723633266823,-127.610513746718,-127.497416449608,
-127.384214857179,-127.270961525952,-127.157494402443,-127.070875613953,
-126.957413872304,-126.844154214211,-126.731006856018,-126.617926956249,
-126.504869773821,-126.391708743247,-126.278496284715,-126.165070034802,
-126.078134398219,-125.964650672452,-125.851368586728,-125.738198546723,
-125.625095752438,-125.512015503945,-125.398831325955,-125.285595639135,
-125.17214631871,-125.085393182485,-124.971912019062,-124.85863246125,-124.745464926045,
-124.632364608826,-124.519286805016,-124.406105001344,-124.292871653395,
-124.17942458386,-124.092651966751,-123.978244662877,-123.864025778459,
-123.74996712899,-123.636001849746,-123.522073439414,-123.472544356861),
 .UNSPECIFIED.);
#333=B_SPLINE_CURVE_WITH_KNOTS('',3,(#38858,#38859,#38860,#38861,#38862,
#38863,#38864,#38865,#38866,#38867,#38868,#38869,#38870,#38871,#38872,#38873,
#38874,#38875,#38876,#38877,#38878,#38879,#38880,#38881,#38882,#38883,#38884,
#38885,#38886,#38887,#38888,#38889,#38890,#38891,#38892,#38893,#38894,#38895,
#38896,#38897,#38898,#38899,#38900,#38901,#38902,#38903,#38904,#38905,#38906,
#38907,#38908,#38909,#38910,#38911,#38912,#38913,#38914,#38915,#38916,#38917,
#38918,#38919,#38920,#38921,#38922,#38923,#38924,#38925,#38926,#38927,#38928,
#38929,#38930,#38931,#38932,#38933,#38934,#38935,#38936,#38937,#38938,#38939,
#38940,#38941,#38942,#38943,#38944,#38945,#38946,#38947,#38948,#38949,#38950,
#38951,#38952,#38953,#38954,#38955,#38956,#38957,#38958,#38959,#38960,#38961,
#38962,#38963,#38964,#38965,#38966,#38967,#38968,#38969,#38970,#38971,#38972,
#38973,#38974,#38975,#38976,#38977,#38978,#38979,#38980,#38981,#38982,#38983,
#38984,#38985,#38986,#38987,#38988,#38989,#38990,#38991,#38992,#38993,#38994,
#38995,#38996,#38997,#38998,#38999,#39000,#39001,#39002,#39003,#39004,#39005,
#39006,#39007,#39008,#39009,#39010,#39011,#39012,#39013,#39014,#39015,#39016,
#39017,#39018,#39019,#39020,#39021,#39022,#39023,#39024,#39025,#39026,#39027,
#39028,#39029,#39030,#39031,#39032),.UNSPECIFIED.,.F.,.F.,(4,3,3,3,3,3,
3,3,3,3,3,3,3,3,3,3,3,3,3,3,3,3,3,3,3,3,3,3,3,3,3,3,3,3,3,3,3,3,3,3,3,3,
3,3,3,3,3,3,3,3,3,3,3,3,3,3,3,3,4),(120.503262642873,120.617419761429,120.731605283755,
120.845948024917,120.960381712593,121.075041343255,121.114428319549,121.227907702834,
121.341185397125,121.454351019198,121.567449377216,121.680525179237,121.793704930971,
121.906936195968,122.020381157543,122.107169535283,122.220649475003,122.333927737086,
122.447093933443,122.560192871148,122.673269257177,122.786449594829,122.899681447703,
123.013126992918,123.099910751017,123.213387493319,123.326662553936,123.439825548767,
123.552921290523,123.665994491818,123.77917168732,123.892400416852,124.005842908394,
124.092651966751,124.206133427493,124.319413171372,124.432580824504,124.545681191699,
124.658758977639,124.771940658917,124.88517382624,124.998620622273,125.085393182485,
125.198876862092,125.312158916064,125.425328933151,125.538431713338,125.651511956554,
125.764696142916,125.877931845702,125.991381194297,126.078134398219,126.19070721261,
126.303112647737,126.415397121371,126.527628178912,126.639829704837,126.752088559023,
126.786447950053),.UNSPECIFIED.);
#334=B_SPLINE_CURVE_WITH_KNOTS('',3,(#39035,#39036,#39037,#39038,#39039,
#39040,#39041,#39042,#39043),.UNSPECIFIED.,.F.,.F.,(4,1,1,1,1,1,4),(126.786452265782,
127.070875613953,128.063616829687,129.056358045421,130.049099261155,131.041840476889,
131.946420123781),.UNSPECIFIED.);
#335=B_SPLINE_CURVE_WITH_KNOTS('',3,(#39046,#39047,#39048,#39049,#39050,
#39051,#39052,#39053),.UNSPECIFIED.,.F.,.F.,(4,1,1,1,1,4),(-134.020064124091,
-133.027322908357,-132.034581692623,-131.041840476889,-130.049099261155,
-129.755734755382),.UNSPECIFIED.);
#336=B_SPLINE_CURVE_WITH_KNOTS('',3,(#39056,#39057,#39058,#39059,#39060,
#39061,#39062,#39063,#39064,#39065,#39066,#39067,#39068,#39069,#39070,#39071,
#39072,#39073,#39074,#39075,#39076,#39077,#39078,#39079,#39080,#39081,#39082,
#39083,#39084,#39085,#39086,#39087,#39088,#39089,#39090,#39091,#39092,#39093,
#39094,#39095,#39096,#39097,#39098,#39099,#39100,#39101,#39102,#39103,#39104,
#39105,#39106,#39107,#39108,#39109,#39110,#39111,#39112,#39113,#39114,#39115,
#39116,#39117,#39118,#39119,#39120,#39121,#39122,#39123,#39124,#39125,#39126,
#39127,#39128,#39129,#39130,#39131,#39132,#39133,#39134,#39135,#39136,#39137,
#39138,#39139,#39140,#39141,#39142,#39143,#39144,#39145,#39146,#39147,#39148,
#39149,#39150,#39151,#39152,#39153,#39154,#39155,#39156,#39157,#39158,#39159,
#39160,#39161,#39162,#39163,#39164,#39165,#39166,#39167,#39168,#39169,#39170,
#39171,#39172,#39173,#39174,#39175,#39176,#39177,#39178,#39179,#39180,#39181,
#39182,#39183,#39184,#39185,#39186,#39187,#39188,#39189,#39190,#39191),
 .UNSPECIFIED.,.F.,.F.,(4,2,2,2,2,2,2,2,2,2,2,2,2,2,2,2,2,2,2,2,2,2,2,2,
2,2,2,2,2,2,2,2,2,2,2,2,2,2,2,2,2,2,2,2,2,2,2,2,2,2,2,2,2,2,2,2,2,2,2,2,
2,2,2,2,2,2,2,4),(0.00176209102869683,0.0264792159075929,0.0438495035001408,
0.047196853344516,0.0491041638455065,0.0507593654656551,0.0527996174980107,
0.055933703762744,0.0773887891690063,0.0930730615746935,0.103703602775703,
0.105131654621243,0.106358820473087,0.107289652483095,0.108188731290211,
0.109716721408549,0.114294010565008,0.137364792206793,0.157768387434864,
0.162258303445078,0.164385196431052,0.166035036296661,0.16785737095035,
0.170863338665144,0.181256475004044,0.211502491183297,0.217990192922471,
0.222064946029316,0.223500893938311,0.224460509340364,0.225312359598861,
0.226476848011434,0.229387236392034,0.251300068517605,0.268671918259035,
0.274974946524858,0.279649189219162,0.281795639089747,0.283432322865378,
0.285211897940308,0.288082858824996,0.297378534974733,0.325457406778818,
0.334233111192271,0.33925061420772,0.340792180490021,0.341768645259298,
0.342704925578973,0.343859916723438,0.34670315133294,0.369996538171123,
0.393583849234611,0.397538297291555,0.39955751987109,0.401192543613393,
0.403072688240712,0.406275811733863,0.419846162533761,0.443546581920891,
0.455527205378817,0.457527376635214,0.458611298838436,0.459529650948841,
0.460708441669346,0.462624208690482,0.4766383722512,0.500757185256959,0.500786432389318),
 .UNSPECIFIED.);
#337=B_SPLINE_CURVE_WITH_KNOTS('',3,(#39195,#39196,#39197,#39198,#39199,
#39200,#39201,#39202,#39203,#39204,#39205,#39206,#39207,#39208,#39209,#39210,
#39211,#39212,#39213,#39214,#39215,#39216,#39217,#39218,#39219),
 .UNSPECIFIED.,.F.,.F.,(4,3,3,3,3,3,3,3,4),(141.371669412108,141.493689526562,
141.615502007272,141.737153936073,141.858692142336,141.980203542838,142.101690110534,
142.223281060979,142.322100278399),.UNSPECIFIED.);
#338=B_SPLINE_CURVE_WITH_KNOTS('',3,(#39220,#39221,#39222,#39223,#39224,
#39225,#39226,#39227,#39228,#39229,#39230,#39231,#39232,#39233,#39234,#39235,
#39236,#39237,#39238,#39239,#39240,#39241,#39242,#39243,#39244,#39245,#39246,
#39247,#39248,#39249,#39250,#39251,#39252,#39253,#39254,#39255,#39256,#39257,
#39258,#39259,#39260,#39261,#39262,#39263,#39264,#39265,#39266,#39267,#39268,
#39269,#39270,#39271,#39272,#39273,#39274,#39275,#39276,#39277,#39278,#39279,
#39280),.UNSPECIFIED.,.F.,.F.,(4,3,3,3,3,3,3,3,3,3,3,3,3,3,3,3,3,3,3,3,
4),(139.325788760491,139.343876631197,139.467969283164,139.587674259952,
139.707262751196,139.826787199013,139.946299934308,140.065935202646,140.185644425912,
140.30556889234,140.336617846931,140.460710498898,140.57912419592,140.697422046221,
140.815658774885,140.933888993062,141.052258648101,141.17071039991,141.289402107531,
141.329359062665,141.371669411541),.UNSPECIFIED.);
#339=B_SPLINE_CURVE_WITH_KNOTS('',3,(#39833,#39834,#39835,#39836,#39837,
#39838,#39839,#39840,#39841,#39842,#39843,#39844,#39845,#39846,#39847,#39848,
#39849,#39850,#39851,#39852,#39853,#39854,#39855,#39856,#39857,#39858,#39859,
#39860,#39861,#39862,#39863,#39864,#39865,#39866,#39867,#39868,#39869,#39870,
#39871,#39872,#39873,#39874,#39875,#39876,#39877,#39878,#39879,#39880,#39881,
#39882,#39883,#39884,#39885,#39886,#39887,#39888,#39889,#39890,#39891,#39892,
#39893,#39894,#39895,#39896,#39897,#39898,#39899,#39900,#39901,#39902,#39903,
#39904,#39905,#39906,#39907,#39908),.UNSPECIFIED.,.F.,.F.,(4,3,3,3,3,3,
3,3,3,3,3,3,3,3,3,3,3,3,3,3,3,3,3,3,3,4),(0.,0.0128630913698734,0.0303244724323763,
0.0454691953909234,0.0523699336523886,0.0555723769695474,0.058851428328098,
0.0758814661698019,0.0926327693964218,0.107460583641014,0.112206797292344,
0.128373668063903,0.144022366178101,0.151482256100753,0.160181126345686,
0.16370248329297,0.179587174239128,0.195601783608132,0.20580545806969,0.211151145077996,
0.214604522909917,0.230111340110616,0.242198051144648,0.246866712384057,
0.261749252048383,0.27663179171271),.UNSPECIFIED.);
#340=B_SPLINE_CURVE_WITH_KNOTS('',3,(#39910,#39911,#39912,#39913,#39914,
#39915,#39916,#39917,#39918,#39919,#39920,#39921,#39922,#39923,#39924,#39925,
#39926,#39927,#39928,#39929,#39930,#39931,#39932,#39933,#39934,#39935,#39936,
#39937,#39938,#39939,#39940,#39941,#39942,#39943,#39944,#39945,#39946,#39947,
#39948,#39949,#39950,#39951,#39952,#39953,#39954,#39955,#39956,#39957,#39958,
#39959,#39960,#39961,#39962,#39963,#39964,#39965,#39966,#39967,#39968,#39969,
#39970,#39971,#39972,#39973,#39974,#39975,#39976,#39977,#39978,#39979,#39980,
#39981,#39982,#39983,#39984,#39985,#39986,#39987,#39988),.UNSPECIFIED.,
 .F.,.F.,(4,3,3,3,3,3,3,3,3,3,3,3,3,3,3,3,3,3,3,3,3,3,3,3,3,3,4),(0.,0.0104682740580808,
0.0249726762435748,0.0388983633715248,0.0464392559381417,0.0494484513162411,
0.0648276131926065,0.0805461214315321,0.0952812770765815,0.0982282573713909,
0.114463949458838,0.130606063061321,0.136378173267175,0.141969567767405,
0.145793041159068,0.148766316560102,0.165124152230842,0.181481987901583,
0.193217024208496,0.197997620770074,0.201207739543446,0.218247298082551,
0.232526043151136,0.236419268721192,0.240186973323727,0.257774625840308,
0.275362278356888),.UNSPECIFIED.);
#341=B_SPLINE_CURVE_WITH_KNOTS('',3,(#39989,#39990,#39991,#39992),
 .UNSPECIFIED.,.F.,.F.,(4,4),(-0.0118538709981997,0.),.UNSPECIFIED.);
#342=B_SPLINE_CURVE_WITH_KNOTS('',3,(#40546,#40547,#40548,#40549,#40550,
#40551,#40552,#40553,#40554,#40555,#40556,#40557,#40558,#40559,#40560,#40561,
#40562,#40563,#40564,#40565,#40566,#40567,#40568,#40569,#40570,#40571,#40572,
#40573,#40574,#40575,#40576,#40577,#40578,#40579,#40580,#40581,#40582,#40583,
#40584,#40585,#40586,#40587,#40588,#40589,#40590,#40591,#40592,#40593,#40594,
#40595,#40596,#40597,#40598,#40599,#40600,#40601,#40602,#40603,#40604,#40605,
#40606,#40607,#40608,#40609,#40610,#40611,#40612,#40613,#40614,#40615,#40616,
#40617,#40618,#40619,#40620,#40621,#40622,#40623,#40624),.UNSPECIFIED.,
 .F.,.F.,(4,3,3,3,3,3,3,3,3,3,3,3,3,3,3,3,3,3,3,3,3,3,3,3,3,3,4),(0.,0.0104682740580829,
0.024972670333206,0.0388983581999524,0.0464392448908457,0.0494484486674944,
0.0648276069840781,0.0806079623489334,0.0952812647645025,0.0982282543159663,
0.114463946169951,0.130606059492799,0.136378173267178,0.141969568696793,
0.145793045570947,0.148766323848641,0.164775566334638,0.181332445677576,
0.193217026624088,0.197997633296994,0.201207746865786,0.218247303068156,
0.23252604689034,0.236419276828848,0.240186974613934,0.257774626485413,
0.275362278356893),.UNSPECIFIED.);
#343=B_SPLINE_CURVE_WITH_KNOTS('',3,(#40625,#40626,#40627,#40628),
 .UNSPECIFIED.,.F.,.F.,(4,4),(0.,0.012085325422919),.UNSPECIFIED.);
#344=B_SPLINE_CURVE_WITH_KNOTS('',3,(#40629,#40630,#40631,#40632,#40633,
#40634,#40635,#40636,#40637,#40638,#40639,#40640,#40641,#40642,#40643,#40644,
#40645,#40646,#40647,#40648,#40649,#40650,#40651,#40652,#40653,#40654,#40655,
#40656,#40657,#40658,#40659,#40660,#40661,#40662,#40663,#40664,#40665,#40666,
#40667,#40668,#40669,#40670,#40671,#40672,#40673,#40674,#40675,#40676,#40677,
#40678,#40679,#40680,#40681,#40682,#40683,#40684,#40685,#40686,#40687,#40688,
#40689,#40690,#40691,#40692,#40693,#40694,#40695,#40696,#40697,#40698,#40699,
#40700,#40701,#40702,#40703,#40704),.UNSPECIFIED.,.F.,.F.,(4,3,3,3,3,3,
3,3,3,3,3,3,3,3,3,3,3,3,3,3,3,3,3,3,3,4),(0.,0.0128630913698816,0.0303093412047053,
0.0454691954866925,0.0523699326729681,0.055572374082829,0.0588514270956641,
0.0758800910821112,0.0927866891993117,0.107460580924677,0.111898501539777,
0.128069590135318,0.144022356052112,0.151482256100771,0.160181127295678,
0.163702483665548,0.179663555189427,0.195687409679772,0.205805457433891,
0.211151145252578,0.214604523387748,0.230111340468992,0.242198051854846,
0.246866712599024,0.261749252155874,0.276631791712723),.UNSPECIFIED.);
#352=SHAPE_REPRESENTATION_RELATIONSHIP('SRR','None',#40773,#360);
#360=ADVANCED_BREP_SHAPE_REPRESENTATION('',(#378),#40733);
#369=STYLED_ITEM('',(#40815),#378);
#378=MANIFOLD_SOLID_BREP('Body1',#3174);
#425=PLANE('',#3472);
#426=PLANE('',#3473);
#539=FACE_OUTER_BOUND('',#709,.T.);
#540=FACE_OUTER_BOUND('',#710,.T.);
#541=FACE_OUTER_BOUND('',#711,.T.);
#542=FACE_OUTER_BOUND('',#712,.T.);
#543=FACE_OUTER_BOUND('',#713,.T.);
#544=FACE_OUTER_BOUND('',#714,.T.);
#545=FACE_OUTER_BOUND('',#715,.T.);
#546=FACE_OUTER_BOUND('',#716,.T.);
#547=FACE_OUTER_BOUND('',#717,.T.);
#548=FACE_OUTER_BOUND('',#718,.T.);
#549=FACE_OUTER_BOUND('',#719,.T.);
#550=FACE_OUTER_BOUND('',#720,.T.);
#551=FACE_OUTER_BOUND('',#721,.T.);
#552=FACE_OUTER_BOUND('',#722,.T.);
#553=FACE_OUTER_BOUND('',#723,.T.);
#554=FACE_OUTER_BOUND('',#724,.T.);
#555=FACE_OUTER_BOUND('',#725,.T.);
#556=FACE_OUTER_BOUND('',#726,.T.);
#557=FACE_OUTER_BOUND('',#727,.T.);
#558=FACE_OUTER_BOUND('',#728,.T.);
#559=FACE_OUTER_BOUND('',#729,.T.);
#560=FACE_OUTER_BOUND('',#730,.T.);
#561=FACE_OUTER_BOUND('',#731,.T.);
#562=FACE_OUTER_BOUND('',#732,.T.);
#563=FACE_OUTER_BOUND('',#733,.T.);
#564=FACE_OUTER_BOUND('',#734,.T.);
#565=FACE_OUTER_BOUND('',#735,.T.);
#566=FACE_OUTER_BOUND('',#736,.T.);
#567=FACE_OUTER_BOUND('',#737,.T.);
#568=FACE_OUTER_BOUND('',#738,.T.);
#569=FACE_OUTER_BOUND('',#739,.T.);
#570=FACE_OUTER_BOUND('',#740,.T.);
#571=FACE_OUTER_BOUND('',#741,.T.);
#572=FACE_OUTER_BOUND('',#742,.T.);
#573=FACE_OUTER_BOUND('',#743,.T.);
#574=FACE_OUTER_BOUND('',#744,.T.);
#575=FACE_OUTER_BOUND('',#745,.T.);
#576=FACE_OUTER_BOUND('',#746,.T.);
#577=FACE_OUTER_BOUND('',#747,.T.);
#578=FACE_OUTER_BOUND('',#748,.T.);
#579=FACE_OUTER_BOUND('',#749,.T.);
#580=FACE_OUTER_BOUND('',#750,.T.);
#581=FACE_OUTER_BOUND('',#751,.T.);
#582=FACE_OUTER_BOUND('',#752,.T.);
#583=FACE_OUTER_BOUND('',#753,.T.);
#584=FACE_OUTER_BOUND('',#754,.T.);
#585=FACE_OUTER_BOUND('',#755,.T.);
#586=FACE_OUTER_BOUND('',#756,.T.);
#709=EDGE_LOOP('',(#2568,#2569,#2570,#2571));
#710=EDGE_LOOP('',(#2572,#2573,#2574,#2575,#2576));
#711=EDGE_LOOP('',(#2577,#2578,#2579,#2580,#2581));
#712=EDGE_LOOP('',(#2582,#2583,#2584,#2585,#2586));
#713=EDGE_LOOP('',(#2587,#2588,#2589,#2590,#2591));
#714=EDGE_LOOP('',(#2592,#2593,#2594,#2595,#2596));
#715=EDGE_LOOP('',(#2597,#2598,#2599,#2600,#2601));
#716=EDGE_LOOP('',(#2602,#2603,#2604,#2605,#2606));
#717=EDGE_LOOP('',(#2607,#2608,#2609,#2610,#2611));
#718=EDGE_LOOP('',(#2612,#2613,#2614,#2615,#2616));
#719=EDGE_LOOP('',(#2617,#2618,#2619,#2620,#2621));
#720=EDGE_LOOP('',(#2622,#2623,#2624,#2625,#2626));
#721=EDGE_LOOP('',(#2627,#2628,#2629,#2630,#2631));
#722=EDGE_LOOP('',(#2632,#2633,#2634,#2635,#2636));
#723=EDGE_LOOP('',(#2637,#2638,#2639,#2640,#2641));
#724=EDGE_LOOP('',(#2642,#2643,#2644,#2645,#2646));
#725=EDGE_LOOP('',(#2647,#2648,#2649,#2650,#2651));
#726=EDGE_LOOP('',(#2652,#2653,#2654,#2655,#2656));
#727=EDGE_LOOP('',(#2657,#2658,#2659,#2660,#2661));
#728=EDGE_LOOP('',(#2662,#2663,#2664,#2665,#2666));
#729=EDGE_LOOP('',(#2667,#2668,#2669,#2670,#2671,#2672));
#730=EDGE_LOOP('',(#2673,#2674,#2675,#2676));
#731=EDGE_LOOP('',(#2677,#2678,#2679,#2680));
#732=EDGE_LOOP('',(#2681,#2682,#2683,#2684));
#733=EDGE_LOOP('',(#2685,#2686,#2687,#2688));
#734=EDGE_LOOP('',(#2689,#2690,#2691,#2692));
#735=EDGE_LOOP('',(#2693,#2694,#2695,#2696));
#736=EDGE_LOOP('',(#2697,#2698,#2699,#2700));
#737=EDGE_LOOP('',(#2701,#2702,#2703,#2704));
#738=EDGE_LOOP('',(#2705,#2706,#2707,#2708));
#739=EDGE_LOOP('',(#2709,#2710,#2711,#2712));
#740=EDGE_LOOP('',(#2713,#2714,#2715,#2716));
#741=EDGE_LOOP('',(#2717,#2718,#2719,#2720));
#742=EDGE_LOOP('',(#2721,#2722,#2723,#2724));
#743=EDGE_LOOP('',(#2725,#2726,#2727,#2728));
#744=EDGE_LOOP('',(#2729,#2730,#2731,#2732));
#745=EDGE_LOOP('',(#2733,#2734,#2735,#2736));
#746=EDGE_LOOP('',(#2737,#2738,#2739,#2740));
#747=EDGE_LOOP('',(#2741,#2742,#2743,#2744));
#748=EDGE_LOOP('',(#2745,#2746,#2747,#2748));
#749=EDGE_LOOP('',(#2749,#2750,#2751,#2752));
#750=EDGE_LOOP('',(#2753,#2754,#2755,#2756));
#751=EDGE_LOOP('',(#2757,#2758,#2759,#2760));
#752=EDGE_LOOP('',(#2761,#2762,#2763,#2764,#2765));
#753=EDGE_LOOP('',(#2766,#2767,#2768,#2769,#2770,#2771,#2772,#2773,#2774,
#2775,#2776,#2777,#2778,#2779,#2780,#2781,#2782,#2783,#2784,#2785,#2786,
#2787,#2788,#2789,#2790,#2791,#2792,#2793,#2794,#2795,#2796,#2797,#2798,
#2799,#2800,#2801,#2802,#2803,#2804,#2805,#2806,#2807,#2808,#2809,#2810,
#2811,#2812,#2813,#2814,#2815,#2816,#2817,#2818,#2819,#2820,#2821,#2822,
#2823));
#754=EDGE_LOOP('',(#2824,#2825,#2826,#2827,#2828,#2829,#2830,#2831,#2832,
#2833,#2834,#2835,#2836,#2837,#2838,#2839,#2840,#2841,#2842,#2843,#2844,
#2845,#2846,#2847,#2848,#2849,#2850,#2851,#2852,#2853,#2854,#2855,#2856,
#2857,#2858,#2859,#2860,#2861,#2862,#2863,#2864,#2865,#2866,#2867,#2868,
#2869,#2870,#2871,#2872,#2873,#2874,#2875,#2876,#2877,#2878,#2879,#2880,
#2881));
#755=EDGE_LOOP('',(#2882,#2883,#2884,#2885,#2886));
#756=EDGE_LOOP('',(#2887,#2888,#2889,#2890,#2891));
#857=LINE('',#22895,#999);
#858=LINE('',#23067,#1000);
#859=LINE('',#23487,#1001);
#860=LINE('',#23934,#1002);
#861=LINE('',#24387,#1003);
#862=LINE('',#24838,#1004);
#863=LINE('',#25321,#1005);
#864=LINE('',#25876,#1006);
#865=LINE('',#26325,#1007);
#866=LINE('',#26776,#1008);
#867=LINE('',#27215,#1009);
#868=LINE('',#27656,#1010);
#869=LINE('',#28135,#1011);
#870=LINE('',#28610,#1012);
#871=LINE('',#29133,#1013);
#872=LINE('',#29586,#1014);
#873=LINE('',#30023,#1015);
#874=LINE('',#30482,#1016);
#875=LINE('',#30943,#1017);
#876=LINE('',#31370,#1018);
#877=LINE('',#31798,#1019);
#878=LINE('',#32199,#1020);
#879=LINE('',#32217,#1021);
#880=LINE('',#32403,#1022);
#881=LINE('',#32751,#1023);
#882=LINE('',#33099,#1024);
#883=LINE('',#33447,#1025);
#884=LINE('',#33795,#1026);
#885=LINE('',#34143,#1027);
#886=LINE('',#34491,#1028);
#887=LINE('',#34839,#1029);
#888=LINE('',#35187,#1030);
#889=LINE('',#35535,#1031);
#890=LINE('',#35883,#1032);
#891=LINE('',#36231,#1033);
#892=LINE('',#36582,#1034);
#893=LINE('',#36933,#1035);
#894=LINE('',#37281,#1036);
#895=LINE('',#37632,#1037);
#896=LINE('',#37986,#1038);
#897=LINE('',#38334,#1039);
#898=LINE('',#38682,#1040);
#999=VECTOR('',#3904,1.17775);
#1000=VECTOR('',#3909,1.17775);
#1001=VECTOR('',#3912,1.17775);
#1002=VECTOR('',#3915,1.17775);
#1003=VECTOR('',#3918,1.17775);
#1004=VECTOR('',#3921,1.17775);
#1005=VECTOR('',#3924,1.17775);
#1006=VECTOR('',#3927,1.17775);
#1007=VECTOR('',#3930,1.17775);
#1008=VECTOR('',#3933,1.17775);
#1009=VECTOR('',#3936,1.17775);
#1010=VECTOR('',#3939,1.17775);
#1011=VECTOR('',#3942,1.17775);
#1012=VECTOR('',#3945,1.17775);
#1013=VECTOR('',#3948,1.17775);
#1014=VECTOR('',#3951,1.17775);
#1015=VECTOR('',#3954,1.17775);
#1016=VECTOR('',#3957,1.17775);
#1017=VECTOR('',#3960,1.17775);
#1018=VECTOR('',#3963,1.17775);
#1019=VECTOR('',#3966,1.17775);
#1020=VECTOR('',#3969,1.4635);
#1021=VECTOR('',#3974,1.4635);
#1022=VECTOR('',#3977,1.4635);
#1023=VECTOR('',#3980,1.4635);
#1024=VECTOR('',#3983,1.4635);
#1025=VECTOR('',#3986,1.4635);
#1026=VECTOR('',#3989,1.4635);
#1027=VECTOR('',#3992,1.4635);
#1028=VECTOR('',#3995,1.4635);
#1029=VECTOR('',#3998,1.4635);
#1030=VECTOR('',#4001,1.4635);
#1031=VECTOR('',#4004,1.4635);
#1032=VECTOR('',#4007,1.4635);
#1033=VECTOR('',#4010,1.4635);
#1034=VECTOR('',#4013,1.4635);
#1035=VECTOR('',#4016,1.4635);
#1036=VECTOR('',#4019,1.4635);
#1037=VECTOR('',#4022,1.4635);
#1038=VECTOR('',#4025,1.4635);
#1039=VECTOR('',#4028,1.4635);
#1040=VECTOR('',#4031,1.4635);
#1086=CIRCLE('',#3425,1.17775);
#1087=CIRCLE('',#3447,1.4635);
#1088=CIRCLE('',#3469,1.4635);
#1089=CIRCLE('',#3471,1.17775);
#1321=VERTEX_POINT('',#22893);
#1322=VERTEX_POINT('',#22894);
#1323=VERTEX_POINT('',#22896);
#1324=VERTEX_POINT('',#23007);
#1325=VERTEX_POINT('',#23065);
#1326=VERTEX_POINT('',#23066);
#1327=VERTEX_POINT('',#23288);
#1328=VERTEX_POINT('',#23485);
#1329=VERTEX_POINT('',#23486);
#1330=VERTEX_POINT('',#23488);
#1331=VERTEX_POINT('',#23932);
#1332=VERTEX_POINT('',#23933);
#1333=VERTEX_POINT('',#24153);
#1334=VERTEX_POINT('',#24385);
#1335=VERTEX_POINT('',#24386);
#1336=VERTEX_POINT('',#24388);
#1337=VERTEX_POINT('',#24836);
#1338=VERTEX_POINT('',#24837);
#1339=VERTEX_POINT('',#25059);
#1340=VERTEX_POINT('',#25319);
#1341=VERTEX_POINT('',#25320);
#1342=VERTEX_POINT('',#25322);
#1343=VERTEX_POINT('',#25874);
#1344=VERTEX_POINT('',#25875);
#1345=VERTEX_POINT('',#26097);
#1346=VERTEX_POINT('',#26323);
#1347=VERTEX_POINT('',#26324);
#1348=VERTEX_POINT('',#26326);
#1349=VERTEX_POINT('',#26774);
#1350=VERTEX_POINT('',#26775);
#1351=VERTEX_POINT('',#26985);
#1352=VERTEX_POINT('',#27213);
#1353=VERTEX_POINT('',#27214);
#1354=VERTEX_POINT('',#27216);
#1355=VERTEX_POINT('',#27654);
#1356=VERTEX_POINT('',#27655);
#1357=VERTEX_POINT('',#27877);
#1358=VERTEX_POINT('',#28133);
#1359=VERTEX_POINT('',#28134);
#1360=VERTEX_POINT('',#28136);
#1361=VERTEX_POINT('',#28608);
#1362=VERTEX_POINT('',#28609);
#1363=VERTEX_POINT('',#28835);
#1364=VERTEX_POINT('',#29131);
#1365=VERTEX_POINT('',#29132);
#1366=VERTEX_POINT('',#29134);
#1367=VERTEX_POINT('',#29584);
#1368=VERTEX_POINT('',#29585);
#1369=VERTEX_POINT('',#29799);
#1370=VERTEX_POINT('',#30021);
#1371=VERTEX_POINT('',#30022);
#1372=VERTEX_POINT('',#30024);
#1373=VERTEX_POINT('',#30480);
#1374=VERTEX_POINT('',#30481);
#1375=VERTEX_POINT('',#30695);
#1376=VERTEX_POINT('',#30941);
#1377=VERTEX_POINT('',#30942);
#1378=VERTEX_POINT('',#30944);
#1379=VERTEX_POINT('',#31368);
#1380=VERTEX_POINT('',#31369);
#1381=VERTEX_POINT('',#31591);
#1382=VERTEX_POINT('',#31796);
#1383=VERTEX_POINT('',#31797);
#1384=VERTEX_POINT('',#31799);
#1385=VERTEX_POINT('',#31986);
#1386=VERTEX_POINT('',#32197);
#1387=VERTEX_POINT('',#32198);
#1388=VERTEX_POINT('',#32200);
#1389=VERTEX_POINT('',#32207);
#1390=VERTEX_POINT('',#32215);
#1391=VERTEX_POINT('',#32216);
#1392=VERTEX_POINT('',#32401);
#1393=VERTEX_POINT('',#32402);
#1394=VERTEX_POINT('',#32749);
#1395=VERTEX_POINT('',#32750);
#1396=VERTEX_POINT('',#33097);
#1397=VERTEX_POINT('',#33098);
#1398=VERTEX_POINT('',#33445);
#1399=VERTEX_POINT('',#33446);
#1400=VERTEX_POINT('',#33793);
#1401=VERTEX_POINT('',#33794);
#1402=VERTEX_POINT('',#34141);
#1403=VERTEX_POINT('',#34142);
#1404=VERTEX_POINT('',#34489);
#1405=VERTEX_POINT('',#34490);
#1406=VERTEX_POINT('',#34837);
#1407=VERTEX_POINT('',#34838);
#1408=VERTEX_POINT('',#35185);
#1409=VERTEX_POINT('',#35186);
#1410=VERTEX_POINT('',#35533);
#1411=VERTEX_POINT('',#35534);
#1412=VERTEX_POINT('',#35881);
#1413=VERTEX_POINT('',#35882);
#1414=VERTEX_POINT('',#36229);
#1415=VERTEX_POINT('',#36230);
#1416=VERTEX_POINT('',#36580);
#1417=VERTEX_POINT('',#36581);
#1418=VERTEX_POINT('',#36931);
#1419=VERTEX_POINT('',#36932);
#1420=VERTEX_POINT('',#37279);
#1421=VERTEX_POINT('',#37280);
#1422=VERTEX_POINT('',#37630);
#1423=VERTEX_POINT('',#37631);
#1424=VERTEX_POINT('',#37984);
#1425=VERTEX_POINT('',#37985);
#1426=VERTEX_POINT('',#38332);
#1427=VERTEX_POINT('',#38333);
#1428=VERTEX_POINT('',#38680);
#1429=VERTEX_POINT('',#38681);
#1430=VERTEX_POINT('',#39034);
#1431=VERTEX_POINT('',#39044);
#1432=VERTEX_POINT('',#39055);
#1433=VERTEX_POINT('',#39192);
#1434=VERTEX_POINT('',#39194);
#1435=VERTEX_POINT('',#39909);
#1436=VERTEX_POINT('',#40545);
#1760=EDGE_CURVE('',#1321,#1322,#857,.T.);
#1761=EDGE_CURVE('',#1323,#1321,#229,.F.);
#1762=EDGE_CURVE('',#1324,#1323,#1086,.T.);
#1763=EDGE_CURVE('',#1324,#1322,#230,.T.);
#1764=EDGE_CURVE('',#1325,#1326,#858,.T.);
#1765=EDGE_CURVE('',#1321,#1325,#231,.F.);
#1766=EDGE_CURVE('',#1322,#1327,#232,.T.);
#1767=EDGE_CURVE('',#1327,#1326,#233,.T.);
#1768=EDGE_CURVE('',#1328,#1329,#859,.T.);
#1769=EDGE_CURVE('',#1330,#1328,#234,.F.);
#1770=EDGE_CURVE('',#1325,#1330,#235,.F.);
#1771=EDGE_CURVE('',#1326,#1329,#236,.T.);
#1772=EDGE_CURVE('',#1331,#1332,#860,.T.);
#1773=EDGE_CURVE('',#1328,#1331,#237,.F.);
#1774=EDGE_CURVE('',#1329,#1333,#238,.T.);
#1775=EDGE_CURVE('',#1333,#1332,#239,.T.);
#1776=EDGE_CURVE('',#1334,#1335,#861,.T.);
#1777=EDGE_CURVE('',#1336,#1334,#240,.F.);
#1778=EDGE_CURVE('',#1331,#1336,#241,.F.);
#1779=EDGE_CURVE('',#1332,#1335,#242,.T.);
#1780=EDGE_CURVE('',#1337,#1338,#862,.T.);
#1781=EDGE_CURVE('',#1334,#1337,#243,.F.);
#1782=EDGE_CURVE('',#1335,#1339,#244,.T.);
#1783=EDGE_CURVE('',#1339,#1338,#245,.T.);
#1784=EDGE_CURVE('',#1340,#1341,#863,.T.);
#1785=EDGE_CURVE('',#1342,#1340,#246,.F.);
#1786=EDGE_CURVE('',#1337,#1342,#247,.F.);
#1787=EDGE_CURVE('',#1338,#1341,#248,.T.);
#1788=EDGE_CURVE('',#1343,#1344,#864,.T.);
#1789=EDGE_CURVE('',#1340,#1343,#249,.F.);
#1790=EDGE_CURVE('',#1341,#1345,#250,.T.);
#1791=EDGE_CURVE('',#1345,#1344,#251,.T.);
#1792=EDGE_CURVE('',#1346,#1347,#865,.T.);
#1793=EDGE_CURVE('',#1348,#1346,#252,.F.);
#1794=EDGE_CURVE('',#1343,#1348,#253,.F.);
#1795=EDGE_CURVE('',#1344,#1347,#254,.T.);
#1796=EDGE_CURVE('',#1349,#1350,#866,.T.);
#1797=EDGE_CURVE('',#1346,#1349,#255,.F.);
#1798=EDGE_CURVE('',#1347,#1351,#256,.T.);
#1799=EDGE_CURVE('',#1351,#1350,#257,.T.);
#1800=EDGE_CURVE('',#1352,#1353,#867,.T.);
#1801=EDGE_CURVE('',#1354,#1352,#258,.F.);
#1802=EDGE_CURVE('',#1349,#1354,#259,.F.);
#1803=EDGE_CURVE('',#1350,#1353,#260,.T.);
#1804=EDGE_CURVE('',#1355,#1356,#868,.T.);
#1805=EDGE_CURVE('',#1352,#1355,#261,.F.);
#1806=EDGE_CURVE('',#1353,#1357,#262,.T.);
#1807=EDGE_CURVE('',#1357,#1356,#263,.T.);
#1808=EDGE_CURVE('',#1358,#1359,#869,.T.);
#1809=EDGE_CURVE('',#1360,#1358,#264,.F.);
#1810=EDGE_CURVE('',#1355,#1360,#265,.F.);
#1811=EDGE_CURVE('',#1356,#1359,#266,.T.);
#1812=EDGE_CURVE('',#1361,#1362,#870,.T.);
#1813=EDGE_CURVE('',#1358,#1361,#267,.F.);
#1814=EDGE_CURVE('',#1359,#1363,#268,.T.);
#1815=EDGE_CURVE('',#1363,#1362,#269,.T.);
#1816=EDGE_CURVE('',#1364,#1365,#871,.T.);
#1817=EDGE_CURVE('',#1366,#1364,#270,.F.);
#1818=EDGE_CURVE('',#1361,#1366,#271,.F.);
#1819=EDGE_CURVE('',#1362,#1365,#272,.T.);
#1820=EDGE_CURVE('',#1367,#1368,#872,.T.);
#1821=EDGE_CURVE('',#1364,#1367,#273,.F.);
#1822=EDGE_CURVE('',#1365,#1369,#274,.T.);
#1823=EDGE_CURVE('',#1369,#1368,#275,.T.);
#1824=EDGE_CURVE('',#1370,#1371,#873,.T.);
#1825=EDGE_CURVE('',#1372,#1370,#276,.F.);
#1826=EDGE_CURVE('',#1367,#1372,#277,.F.);
#1827=EDGE_CURVE('',#1368,#1371,#278,.T.);
#1828=EDGE_CURVE('',#1373,#1374,#874,.T.);
#1829=EDGE_CURVE('',#1370,#1373,#279,.F.);
#1830=EDGE_CURVE('',#1371,#1375,#280,.T.);
#1831=EDGE_CURVE('',#1375,#1374,#281,.T.);
#1832=EDGE_CURVE('',#1376,#1377,#875,.T.);
#1833=EDGE_CURVE('',#1378,#1376,#282,.F.);
#1834=EDGE_CURVE('',#1373,#1378,#283,.F.);
#1835=EDGE_CURVE('',#1374,#1377,#284,.T.);
#1836=EDGE_CURVE('',#1379,#1380,#876,.T.);
#1837=EDGE_CURVE('',#1376,#1379,#285,.F.);
#1838=EDGE_CURVE('',#1377,#1381,#286,.T.);
#1839=EDGE_CURVE('',#1381,#1380,#287,.T.);
#1840=EDGE_CURVE('',#1382,#1383,#877,.T.);
#1841=EDGE_CURVE('',#1384,#1382,#288,.T.);
#1842=EDGE_CURVE('',#1379,#1384,#289,.F.);
#1843=EDGE_CURVE('',#1380,#1385,#290,.T.);
#1844=EDGE_CURVE('',#1385,#1383,#291,.F.);
#1845=EDGE_CURVE('',#1386,#1387,#878,.T.);
#1846=EDGE_CURVE('',#1386,#1388,#292,.T.);
#1847=EDGE_CURVE('',#1389,#1388,#1087,.F.);
#1848=EDGE_CURVE('',#1389,#1387,#293,.T.);
#1849=EDGE_CURVE('',#1390,#1391,#879,.T.);
#1850=EDGE_CURVE('',#1390,#1386,#294,.T.);
#1851=EDGE_CURVE('',#1387,#1391,#295,.T.);
#1852=EDGE_CURVE('',#1392,#1393,#880,.T.);
#1853=EDGE_CURVE('',#1392,#1390,#296,.T.);
#1854=EDGE_CURVE('',#1391,#1393,#297,.T.);
#1855=EDGE_CURVE('',#1394,#1395,#881,.T.);
#1856=EDGE_CURVE('',#1394,#1392,#298,.T.);
#1857=EDGE_CURVE('',#1393,#1395,#299,.T.);
#1858=EDGE_CURVE('',#1396,#1397,#882,.T.);
#1859=EDGE_CURVE('',#1396,#1394,#300,.T.);
#1860=EDGE_CURVE('',#1395,#1397,#301,.T.);
#1861=EDGE_CURVE('',#1398,#1399,#883,.T.);
#1862=EDGE_CURVE('',#1398,#1396,#302,.T.);
#1863=EDGE_CURVE('',#1397,#1399,#303,.T.);
#1864=EDGE_CURVE('',#1400,#1401,#884,.T.);
#1865=EDGE_CURVE('',#1400,#1398,#304,.T.);
#1866=EDGE_CURVE('',#1399,#1401,#305,.T.);
#1867=EDGE_CURVE('',#1402,#1403,#885,.T.);
#1868=EDGE_CURVE('',#1402,#1400,#306,.T.);
#1869=EDGE_CURVE('',#1401,#1403,#307,.T.);
#1870=EDGE_CURVE('',#1404,#1405,#886,.T.);
#1871=EDGE_CURVE('',#1404,#1402,#308,.T.);
#1872=EDGE_CURVE('',#1403,#1405,#309,.T.);
#1873=EDGE_CURVE('',#1406,#1407,#887,.T.);
#1874=EDGE_CURVE('',#1406,#1404,#310,.T.);
#1875=EDGE_CURVE('',#1405,#1407,#311,.T.);
#1876=EDGE_CURVE('',#1408,#1409,#888,.T.);
#1877=EDGE_CURVE('',#1408,#1406,#312,.T.);
#1878=EDGE_CURVE('',#1407,#1409,#313,.T.);
#1879=EDGE_CURVE('',#1410,#1411,#889,.T.);
#1880=EDGE_CURVE('',#1410,#1408,#314,.T.);
#1881=EDGE_CURVE('',#1409,#1411,#315,.T.);
#1882=EDGE_CURVE('',#1412,#1413,#890,.T.);
#1883=EDGE_CURVE('',#1412,#1410,#316,.T.);
#1884=EDGE_CURVE('',#1411,#1413,#317,.T.);
#1885=EDGE_CURVE('',#1414,#1415,#891,.T.);
#1886=EDGE_CURVE('',#1414,#1412,#318,.T.);
#1887=EDGE_CURVE('',#1413,#1415,#319,.T.);
#1888=EDGE_CURVE('',#1416,#1417,#892,.T.);
#1889=EDGE_CURVE('',#1416,#1414,#320,.T.);
#1890=EDGE_CURVE('',#1415,#1417,#321,.T.);
#1891=EDGE_CURVE('',#1418,#1419,#893,.T.);
#1892=EDGE_CURVE('',#1418,#1416,#322,.T.);
#1893=EDGE_CURVE('',#1417,#1419,#323,.T.);
#1894=EDGE_CURVE('',#1420,#1421,#894,.T.);
#1895=EDGE_CURVE('',#1420,#1418,#324,.T.);
#1896=EDGE_CURVE('',#1419,#1421,#325,.T.);
#1897=EDGE_CURVE('',#1422,#1423,#895,.T.);
#1898=EDGE_CURVE('',#1422,#1420,#326,.T.);
#1899=EDGE_CURVE('',#1421,#1423,#327,.T.);
#1900=EDGE_CURVE('',#1424,#1425,#896,.T.);
#1901=EDGE_CURVE('',#1424,#1422,#328,.T.);
#1902=EDGE_CURVE('',#1423,#1425,#329,.T.);
#1903=EDGE_CURVE('',#1426,#1427,#897,.T.);
#1904=EDGE_CURVE('',#1426,#1424,#330,.T.);
#1905=EDGE_CURVE('',#1425,#1427,#331,.T.);
#1906=EDGE_CURVE('',#1428,#1429,#898,.T.);
#1907=EDGE_CURVE('',#1428,#1426,#332,.T.);
#1908=EDGE_CURVE('',#1427,#1429,#333,.T.);
#1909=EDGE_CURVE('',#1429,#1430,#334,.T.);
#1910=EDGE_CURVE('',#1431,#1430,#1088,.T.);
#1911=EDGE_CURVE('',#1431,#1428,#335,.T.);
#1912=EDGE_CURVE('',#1383,#1432,#336,.F.);
#1913=EDGE_CURVE('',#1433,#1432,#1089,.T.);
#1914=EDGE_CURVE('',#1434,#1433,#337,.T.);
#1915=EDGE_CURVE('',#1382,#1434,#338,.T.);
#1916=EDGE_CURVE('',#1430,#1433,#339,.T.);
#1917=EDGE_CURVE('',#1435,#1389,#340,.T.);
#1918=EDGE_CURVE('',#1435,#1323,#341,.T.);
#1919=EDGE_CURVE('',#1436,#1431,#342,.T.);
#1920=EDGE_CURVE('',#1432,#1436,#343,.T.);
#1921=EDGE_CURVE('',#1388,#1324,#344,.T.);
#2568=ORIENTED_EDGE('',*,*,#1760,.F.);
#2569=ORIENTED_EDGE('',*,*,#1761,.F.);
#2570=ORIENTED_EDGE('',*,*,#1762,.F.);
#2571=ORIENTED_EDGE('',*,*,#1763,.T.);
#2572=ORIENTED_EDGE('',*,*,#1764,.F.);
#2573=ORIENTED_EDGE('',*,*,#1765,.F.);
#2574=ORIENTED_EDGE('',*,*,#1760,.T.);
#2575=ORIENTED_EDGE('',*,*,#1766,.T.);
#2576=ORIENTED_EDGE('',*,*,#1767,.T.);
#2577=ORIENTED_EDGE('',*,*,#1768,.F.);
#2578=ORIENTED_EDGE('',*,*,#1769,.F.);
#2579=ORIENTED_EDGE('',*,*,#1770,.F.);
#2580=ORIENTED_EDGE('',*,*,#1764,.T.);
#2581=ORIENTED_EDGE('',*,*,#1771,.T.);
#2582=ORIENTED_EDGE('',*,*,#1772,.F.);
#2583=ORIENTED_EDGE('',*,*,#1773,.F.);
#2584=ORIENTED_EDGE('',*,*,#1768,.T.);
#2585=ORIENTED_EDGE('',*,*,#1774,.T.);
#2586=ORIENTED_EDGE('',*,*,#1775,.T.);
#2587=ORIENTED_EDGE('',*,*,#1776,.F.);
#2588=ORIENTED_EDGE('',*,*,#1777,.F.);
#2589=ORIENTED_EDGE('',*,*,#1778,.F.);
#2590=ORIENTED_EDGE('',*,*,#1772,.T.);
#2591=ORIENTED_EDGE('',*,*,#1779,.T.);
#2592=ORIENTED_EDGE('',*,*,#1780,.F.);
#2593=ORIENTED_EDGE('',*,*,#1781,.F.);
#2594=ORIENTED_EDGE('',*,*,#1776,.T.);
#2595=ORIENTED_EDGE('',*,*,#1782,.T.);
#2596=ORIENTED_EDGE('',*,*,#1783,.T.);
#2597=ORIENTED_EDGE('',*,*,#1784,.F.);
#2598=ORIENTED_EDGE('',*,*,#1785,.F.);
#2599=ORIENTED_EDGE('',*,*,#1786,.F.);
#2600=ORIENTED_EDGE('',*,*,#1780,.T.);
#2601=ORIENTED_EDGE('',*,*,#1787,.T.);
#2602=ORIENTED_EDGE('',*,*,#1788,.F.);
#2603=ORIENTED_EDGE('',*,*,#1789,.F.);
#2604=ORIENTED_EDGE('',*,*,#1784,.T.);
#2605=ORIENTED_EDGE('',*,*,#1790,.T.);
#2606=ORIENTED_EDGE('',*,*,#1791,.T.);
#2607=ORIENTED_EDGE('',*,*,#1792,.F.);
#2608=ORIENTED_EDGE('',*,*,#1793,.F.);
#2609=ORIENTED_EDGE('',*,*,#1794,.F.);
#2610=ORIENTED_EDGE('',*,*,#1788,.T.);
#2611=ORIENTED_EDGE('',*,*,#1795,.T.);
#2612=ORIENTED_EDGE('',*,*,#1796,.F.);
#2613=ORIENTED_EDGE('',*,*,#1797,.F.);
#2614=ORIENTED_EDGE('',*,*,#1792,.T.);
#2615=ORIENTED_EDGE('',*,*,#1798,.T.);
#2616=ORIENTED_EDGE('',*,*,#1799,.T.);
#2617=ORIENTED_EDGE('',*,*,#1800,.F.);
#2618=ORIENTED_EDGE('',*,*,#1801,.F.);
#2619=ORIENTED_EDGE('',*,*,#1802,.F.);
#2620=ORIENTED_EDGE('',*,*,#1796,.T.);
#2621=ORIENTED_EDGE('',*,*,#1803,.T.);
#2622=ORIENTED_EDGE('',*,*,#1804,.F.);
#2623=ORIENTED_EDGE('',*,*,#1805,.F.);
#2624=ORIENTED_EDGE('',*,*,#1800,.T.);
#2625=ORIENTED_EDGE('',*,*,#1806,.T.);
#2626=ORIENTED_EDGE('',*,*,#1807,.T.);
#2627=ORIENTED_EDGE('',*,*,#1808,.F.);
#2628=ORIENTED_EDGE('',*,*,#1809,.F.);
#2629=ORIENTED_EDGE('',*,*,#1810,.F.);
#2630=ORIENTED_EDGE('',*,*,#1804,.T.);
#2631=ORIENTED_EDGE('',*,*,#1811,.T.);
#2632=ORIENTED_EDGE('',*,*,#1812,.F.);
#2633=ORIENTED_EDGE('',*,*,#1813,.F.);
#2634=ORIENTED_EDGE('',*,*,#1808,.T.);
#2635=ORIENTED_EDGE('',*,*,#1814,.T.);
#2636=ORIENTED_EDGE('',*,*,#1815,.T.);
#2637=ORIENTED_EDGE('',*,*,#1816,.F.);
#2638=ORIENTED_EDGE('',*,*,#1817,.F.);
#2639=ORIENTED_EDGE('',*,*,#1818,.F.);
#2640=ORIENTED_EDGE('',*,*,#1812,.T.);
#2641=ORIENTED_EDGE('',*,*,#1819,.T.);
#2642=ORIENTED_EDGE('',*,*,#1820,.F.);
#2643=ORIENTED_EDGE('',*,*,#1821,.F.);
#2644=ORIENTED_EDGE('',*,*,#1816,.T.);
#2645=ORIENTED_EDGE('',*,*,#1822,.T.);
#2646=ORIENTED_EDGE('',*,*,#1823,.T.);
#2647=ORIENTED_EDGE('',*,*,#1824,.F.);
#2648=ORIENTED_EDGE('',*,*,#1825,.F.);
#2649=ORIENTED_EDGE('',*,*,#1826,.F.);
#2650=ORIENTED_EDGE('',*,*,#1820,.T.);
#2651=ORIENTED_EDGE('',*,*,#1827,.T.);
#2652=ORIENTED_EDGE('',*,*,#1828,.F.);
#2653=ORIENTED_EDGE('',*,*,#1829,.F.);
#2654=ORIENTED_EDGE('',*,*,#1824,.T.);
#2655=ORIENTED_EDGE('',*,*,#1830,.T.);
#2656=ORIENTED_EDGE('',*,*,#1831,.T.);
#2657=ORIENTED_EDGE('',*,*,#1832,.F.);
#2658=ORIENTED_EDGE('',*,*,#1833,.F.);
#2659=ORIENTED_EDGE('',*,*,#1834,.F.);
#2660=ORIENTED_EDGE('',*,*,#1828,.T.);
#2661=ORIENTED_EDGE('',*,*,#1835,.T.);
#2662=ORIENTED_EDGE('',*,*,#1836,.F.);
#2663=ORIENTED_EDGE('',*,*,#1837,.F.);
#2664=ORIENTED_EDGE('',*,*,#1832,.T.);
#2665=ORIENTED_EDGE('',*,*,#1838,.T.);
#2666=ORIENTED_EDGE('',*,*,#1839,.T.);
#2667=ORIENTED_EDGE('',*,*,#1840,.F.);
#2668=ORIENTED_EDGE('',*,*,#1841,.F.);
#2669=ORIENTED_EDGE('',*,*,#1842,.F.);
#2670=ORIENTED_EDGE('',*,*,#1836,.T.);
#2671=ORIENTED_EDGE('',*,*,#1843,.T.);
#2672=ORIENTED_EDGE('',*,*,#1844,.T.);
#2673=ORIENTED_EDGE('',*,*,#1845,.F.);
#2674=ORIENTED_EDGE('',*,*,#1846,.T.);
#2675=ORIENTED_EDGE('',*,*,#1847,.F.);
#2676=ORIENTED_EDGE('',*,*,#1848,.T.);
#2677=ORIENTED_EDGE('',*,*,#1849,.F.);
#2678=ORIENTED_EDGE('',*,*,#1850,.T.);
#2679=ORIENTED_EDGE('',*,*,#1845,.T.);
#2680=ORIENTED_EDGE('',*,*,#1851,.T.);
#2681=ORIENTED_EDGE('',*,*,#1852,.F.);
#2682=ORIENTED_EDGE('',*,*,#1853,.T.);
#2683=ORIENTED_EDGE('',*,*,#1849,.T.);
#2684=ORIENTED_EDGE('',*,*,#1854,.T.);
#2685=ORIENTED_EDGE('',*,*,#1855,.F.);
#2686=ORIENTED_EDGE('',*,*,#1856,.T.);
#2687=ORIENTED_EDGE('',*,*,#1852,.T.);
#2688=ORIENTED_EDGE('',*,*,#1857,.T.);
#2689=ORIENTED_EDGE('',*,*,#1858,.F.);
#2690=ORIENTED_EDGE('',*,*,#1859,.T.);
#2691=ORIENTED_EDGE('',*,*,#1855,.T.);
#2692=ORIENTED_EDGE('',*,*,#1860,.T.);
#2693=ORIENTED_EDGE('',*,*,#1861,.F.);
#2694=ORIENTED_EDGE('',*,*,#1862,.T.);
#2695=ORIENTED_EDGE('',*,*,#1858,.T.);
#2696=ORIENTED_EDGE('',*,*,#1863,.T.);
#2697=ORIENTED_EDGE('',*,*,#1864,.F.);
#2698=ORIENTED_EDGE('',*,*,#1865,.T.);
#2699=ORIENTED_EDGE('',*,*,#1861,.T.);
#2700=ORIENTED_EDGE('',*,*,#1866,.T.);
#2701=ORIENTED_EDGE('',*,*,#1867,.F.);
#2702=ORIENTED_EDGE('',*,*,#1868,.T.);
#2703=ORIENTED_EDGE('',*,*,#1864,.T.);
#2704=ORIENTED_EDGE('',*,*,#1869,.T.);
#2705=ORIENTED_EDGE('',*,*,#1870,.F.);
#2706=ORIENTED_EDGE('',*,*,#1871,.T.);
#2707=ORIENTED_EDGE('',*,*,#1867,.T.);
#2708=ORIENTED_EDGE('',*,*,#1872,.T.);
#2709=ORIENTED_EDGE('',*,*,#1873,.F.);
#2710=ORIENTED_EDGE('',*,*,#1874,.T.);
#2711=ORIENTED_EDGE('',*,*,#1870,.T.);
#2712=ORIENTED_EDGE('',*,*,#1875,.T.);
#2713=ORIENTED_EDGE('',*,*,#1876,.F.);
#2714=ORIENTED_EDGE('',*,*,#1877,.T.);
#2715=ORIENTED_EDGE('',*,*,#1873,.T.);
#2716=ORIENTED_EDGE('',*,*,#1878,.T.);
#2717=ORIENTED_EDGE('',*,*,#1879,.F.);
#2718=ORIENTED_EDGE('',*,*,#1880,.T.);
#2719=ORIENTED_EDGE('',*,*,#1876,.T.);
#2720=ORIENTED_EDGE('',*,*,#1881,.T.);
#2721=ORIENTED_EDGE('',*,*,#1882,.F.);
#2722=ORIENTED_EDGE('',*,*,#1883,.T.);
#2723=ORIENTED_EDGE('',*,*,#1879,.T.);
#2724=ORIENTED_EDGE('',*,*,#1884,.T.);
#2725=ORIENTED_EDGE('',*,*,#1885,.F.);
#2726=ORIENTED_EDGE('',*,*,#1886,.T.);
#2727=ORIENTED_EDGE('',*,*,#1882,.T.);
#2728=ORIENTED_EDGE('',*,*,#1887,.T.);
#2729=ORIENTED_EDGE('',*,*,#1888,.F.);
#2730=ORIENTED_EDGE('',*,*,#1889,.T.);
#2731=ORIENTED_EDGE('',*,*,#1885,.T.);
#2732=ORIENTED_EDGE('',*,*,#1890,.T.);
#2733=ORIENTED_EDGE('',*,*,#1891,.F.);
#2734=ORIENTED_EDGE('',*,*,#1892,.T.);
#2735=ORIENTED_EDGE('',*,*,#1888,.T.);
#2736=ORIENTED_EDGE('',*,*,#1893,.T.);
#2737=ORIENTED_EDGE('',*,*,#1894,.F.);
#2738=ORIENTED_EDGE('',*,*,#1895,.T.);
#2739=ORIENTED_EDGE('',*,*,#1891,.T.);
#2740=ORIENTED_EDGE('',*,*,#1896,.T.);
#2741=ORIENTED_EDGE('',*,*,#1897,.F.);
#2742=ORIENTED_EDGE('',*,*,#1898,.T.);
#2743=ORIENTED_EDGE('',*,*,#1894,.T.);
#2744=ORIENTED_EDGE('',*,*,#1899,.T.);
#2745=ORIENTED_EDGE('',*,*,#1900,.F.);
#2746=ORIENTED_EDGE('',*,*,#1901,.T.);
#2747=ORIENTED_EDGE('',*,*,#1897,.T.);
#2748=ORIENTED_EDGE('',*,*,#1902,.T.);
#2749=ORIENTED_EDGE('',*,*,#1903,.F.);
#2750=ORIENTED_EDGE('',*,*,#1904,.T.);
#2751=ORIENTED_EDGE('',*,*,#1900,.T.);
#2752=ORIENTED_EDGE('',*,*,#1905,.T.);
#2753=ORIENTED_EDGE('',*,*,#1906,.F.);
#2754=ORIENTED_EDGE('',*,*,#1907,.T.);
#2755=ORIENTED_EDGE('',*,*,#1903,.T.);
#2756=ORIENTED_EDGE('',*,*,#1908,.T.);
#2757=ORIENTED_EDGE('',*,*,#1906,.T.);
#2758=ORIENTED_EDGE('',*,*,#1909,.T.);
#2759=ORIENTED_EDGE('',*,*,#1910,.F.);
#2760=ORIENTED_EDGE('',*,*,#1911,.T.);
#2761=ORIENTED_EDGE('',*,*,#1840,.T.);
#2762=ORIENTED_EDGE('',*,*,#1912,.T.);
#2763=ORIENTED_EDGE('',*,*,#1913,.F.);
#2764=ORIENTED_EDGE('',*,*,#1914,.F.);
#2765=ORIENTED_EDGE('',*,*,#1915,.F.);
#2766=ORIENTED_EDGE('',*,*,#1916,.F.);
#2767=ORIENTED_EDGE('',*,*,#1909,.F.);
#2768=ORIENTED_EDGE('',*,*,#1908,.F.);
#2769=ORIENTED_EDGE('',*,*,#1905,.F.);
#2770=ORIENTED_EDGE('',*,*,#1902,.F.);
#2771=ORIENTED_EDGE('',*,*,#1899,.F.);
#2772=ORIENTED_EDGE('',*,*,#1896,.F.);
#2773=ORIENTED_EDGE('',*,*,#1893,.F.);
#2774=ORIENTED_EDGE('',*,*,#1890,.F.);
#2775=ORIENTED_EDGE('',*,*,#1887,.F.);
#2776=ORIENTED_EDGE('',*,*,#1884,.F.);
#2777=ORIENTED_EDGE('',*,*,#1881,.F.);
#2778=ORIENTED_EDGE('',*,*,#1878,.F.);
#2779=ORIENTED_EDGE('',*,*,#1875,.F.);
#2780=ORIENTED_EDGE('',*,*,#1872,.F.);
#2781=ORIENTED_EDGE('',*,*,#1869,.F.);
#2782=ORIENTED_EDGE('',*,*,#1866,.F.);
#2783=ORIENTED_EDGE('',*,*,#1863,.F.);
#2784=ORIENTED_EDGE('',*,*,#1860,.F.);
#2785=ORIENTED_EDGE('',*,*,#1857,.F.);
#2786=ORIENTED_EDGE('',*,*,#1854,.F.);
#2787=ORIENTED_EDGE('',*,*,#1851,.F.);
#2788=ORIENTED_EDGE('',*,*,#1848,.F.);
#2789=ORIENTED_EDGE('',*,*,#1917,.F.);
#2790=ORIENTED_EDGE('',*,*,#1918,.T.);
#2791=ORIENTED_EDGE('',*,*,#1761,.T.);
#2792=ORIENTED_EDGE('',*,*,#1765,.T.);
#2793=ORIENTED_EDGE('',*,*,#1770,.T.);
#2794=ORIENTED_EDGE('',*,*,#1769,.T.);
#2795=ORIENTED_EDGE('',*,*,#1773,.T.);
#2796=ORIENTED_EDGE('',*,*,#1778,.T.);
#2797=ORIENTED_EDGE('',*,*,#1777,.T.);
#2798=ORIENTED_EDGE('',*,*,#1781,.T.);
#2799=ORIENTED_EDGE('',*,*,#1786,.T.);
#2800=ORIENTED_EDGE('',*,*,#1785,.T.);
#2801=ORIENTED_EDGE('',*,*,#1789,.T.);
#2802=ORIENTED_EDGE('',*,*,#1794,.T.);
#2803=ORIENTED_EDGE('',*,*,#1793,.T.);
#2804=ORIENTED_EDGE('',*,*,#1797,.T.);
#2805=ORIENTED_EDGE('',*,*,#1802,.T.);
#2806=ORIENTED_EDGE('',*,*,#1801,.T.);
#2807=ORIENTED_EDGE('',*,*,#1805,.T.);
#2808=ORIENTED_EDGE('',*,*,#1810,.T.);
#2809=ORIENTED_EDGE('',*,*,#1809,.T.);
#2810=ORIENTED_EDGE('',*,*,#1813,.T.);
#2811=ORIENTED_EDGE('',*,*,#1818,.T.);
#2812=ORIENTED_EDGE('',*,*,#1817,.T.);
#2813=ORIENTED_EDGE('',*,*,#1821,.T.);
#2814=ORIENTED_EDGE('',*,*,#1826,.T.);
#2815=ORIENTED_EDGE('',*,*,#1825,.T.);
#2816=ORIENTED_EDGE('',*,*,#1829,.T.);
#2817=ORIENTED_EDGE('',*,*,#1834,.T.);
#2818=ORIENTED_EDGE('',*,*,#1833,.T.);
#2819=ORIENTED_EDGE('',*,*,#1837,.T.);
#2820=ORIENTED_EDGE('',*,*,#1842,.T.);
#2821=ORIENTED_EDGE('',*,*,#1841,.T.);
#2822=ORIENTED_EDGE('',*,*,#1915,.T.);
#2823=ORIENTED_EDGE('',*,*,#1914,.T.);
#2824=ORIENTED_EDGE('',*,*,#1919,.F.);
#2825=ORIENTED_EDGE('',*,*,#1920,.F.);
#2826=ORIENTED_EDGE('',*,*,#1912,.F.);
#2827=ORIENTED_EDGE('',*,*,#1844,.F.);
#2828=ORIENTED_EDGE('',*,*,#1843,.F.);
#2829=ORIENTED_EDGE('',*,*,#1839,.F.);
#2830=ORIENTED_EDGE('',*,*,#1838,.F.);
#2831=ORIENTED_EDGE('',*,*,#1835,.F.);
#2832=ORIENTED_EDGE('',*,*,#1831,.F.);
#2833=ORIENTED_EDGE('',*,*,#1830,.F.);
#2834=ORIENTED_EDGE('',*,*,#1827,.F.);
#2835=ORIENTED_EDGE('',*,*,#1823,.F.);
#2836=ORIENTED_EDGE('',*,*,#1822,.F.);
#2837=ORIENTED_EDGE('',*,*,#1819,.F.);
#2838=ORIENTED_EDGE('',*,*,#1815,.F.);
#2839=ORIENTED_EDGE('',*,*,#1814,.F.);
#2840=ORIENTED_EDGE('',*,*,#1811,.F.);
#2841=ORIENTED_EDGE('',*,*,#1807,.F.);
#2842=ORIENTED_EDGE('',*,*,#1806,.F.);
#2843=ORIENTED_EDGE('',*,*,#1803,.F.);
#2844=ORIENTED_EDGE('',*,*,#1799,.F.);
#2845=ORIENTED_EDGE('',*,*,#1798,.F.);
#2846=ORIENTED_EDGE('',*,*,#1795,.F.);
#2847=ORIENTED_EDGE('',*,*,#1791,.F.);
#2848=ORIENTED_EDGE('',*,*,#1790,.F.);
#2849=ORIENTED_EDGE('',*,*,#1787,.F.);
#2850=ORIENTED_EDGE('',*,*,#1783,.F.);
#2851=ORIENTED_EDGE('',*,*,#1782,.F.);
#2852=ORIENTED_EDGE('',*,*,#1779,.F.);
#2853=ORIENTED_EDGE('',*,*,#1775,.F.);
#2854=ORIENTED_EDGE('',*,*,#1774,.F.);
#2855=ORIENTED_EDGE('',*,*,#1771,.F.);
#2856=ORIENTED_EDGE('',*,*,#1767,.F.);
#2857=ORIENTED_EDGE('',*,*,#1766,.F.);
#2858=ORIENTED_EDGE('',*,*,#1763,.F.);
#2859=ORIENTED_EDGE('',*,*,#1921,.F.);
#2860=ORIENTED_EDGE('',*,*,#1846,.F.);
#2861=ORIENTED_EDGE('',*,*,#1850,.F.);
#2862=ORIENTED_EDGE('',*,*,#1853,.F.);
#2863=ORIENTED_EDGE('',*,*,#1856,.F.);
#2864=ORIENTED_EDGE('',*,*,#1859,.F.);
#2865=ORIENTED_EDGE('',*,*,#1862,.F.);
#2866=ORIENTED_EDGE('',*,*,#1865,.F.);
#2867=ORIENTED_EDGE('',*,*,#1868,.F.);
#2868=ORIENTED_EDGE('',*,*,#1871,.F.);
#2869=ORIENTED_EDGE('',*,*,#1874,.F.);
#2870=ORIENTED_EDGE('',*,*,#1877,.F.);
#2871=ORIENTED_EDGE('',*,*,#1880,.F.);
#2872=ORIENTED_EDGE('',*,*,#1883,.F.);
#2873=ORIENTED_EDGE('',*,*,#1886,.F.);
#2874=ORIENTED_EDGE('',*,*,#1889,.F.);
#2875=ORIENTED_EDGE('',*,*,#1892,.F.);
#2876=ORIENTED_EDGE('',*,*,#1895,.F.);
#2877=ORIENTED_EDGE('',*,*,#1898,.F.);
#2878=ORIENTED_EDGE('',*,*,#1901,.F.);
#2879=ORIENTED_EDGE('',*,*,#1904,.F.);
#2880=ORIENTED_EDGE('',*,*,#1907,.F.);
#2881=ORIENTED_EDGE('',*,*,#1911,.F.);
#2882=ORIENTED_EDGE('',*,*,#1916,.T.);
#2883=ORIENTED_EDGE('',*,*,#1913,.T.);
#2884=ORIENTED_EDGE('',*,*,#1920,.T.);
#2885=ORIENTED_EDGE('',*,*,#1919,.T.);
#2886=ORIENTED_EDGE('',*,*,#1910,.T.);
#2887=ORIENTED_EDGE('',*,*,#1917,.T.);
#2888=ORIENTED_EDGE('',*,*,#1847,.T.);
#2889=ORIENTED_EDGE('',*,*,#1921,.T.);
#2890=ORIENTED_EDGE('',*,*,#1762,.T.);
#2891=ORIENTED_EDGE('',*,*,#1918,.F.);
#2962=CYLINDRICAL_SURFACE('',#3424,1.17775);
#2963=CYLINDRICAL_SURFACE('',#3426,1.17775);
#2964=CYLINDRICAL_SURFACE('',#3427,1.17775);
#2965=CYLINDRICAL_SURFACE('',#3428,1.17775);
#2966=CYLINDRICAL_SURFACE('',#3429,1.17775);
#2967=CYLINDRICAL_SURFACE('',#3430,1.17775);
#2968=CYLINDRICAL_SURFACE('',#3431,1.17775);
#2969=CYLINDRICAL_SURFACE('',#3432,1.17775);
#2970=CYLINDRICAL_SURFACE('',#3433,1.17775);
#2971=CYLINDRICAL_SURFACE('',#3434,1.17775);
#2972=CYLINDRICAL_SURFACE('',#3435,1.17775);
#2973=CYLINDRICAL_SURFACE('',#3436,1.17775);
#2974=CYLINDRICAL_SURFACE('',#3437,1.17775);
#2975=CYLINDRICAL_SURFACE('',#3438,1.17775);
#2976=CYLINDRICAL_SURFACE('',#3439,1.17775);
#2977=CYLINDRICAL_SURFACE('',#3440,1.17775);
#2978=CYLINDRICAL_SURFACE('',#3441,1.17775);
#2979=CYLINDRICAL_SURFACE('',#3442,1.17775);
#2980=CYLINDRICAL_SURFACE('',#3443,1.17775);
#2981=CYLINDRICAL_SURFACE('',#3444,1.17775);
#2982=CYLINDRICAL_SURFACE('',#3445,1.17775);
#2983=CYLINDRICAL_SURFACE('',#3446,1.4635);
#2984=CYLINDRICAL_SURFACE('',#3448,1.4635);
#2985=CYLINDRICAL_SURFACE('',#3449,1.4635);
#2986=CYLINDRICAL_SURFACE('',#3450,1.4635);
#2987=CYLINDRICAL_SURFACE('',#3451,1.4635);
#2988=CYLINDRICAL_SURFACE('',#3452,1.4635);
#2989=CYLINDRICAL_SURFACE('',#3453,1.4635);
#2990=CYLINDRICAL_SURFACE('',#3454,1.4635);
#2991=CYLINDRICAL_SURFACE('',#3455,1.4635);
#2992=CYLINDRICAL_SURFACE('',#3456,1.4635);
#2993=CYLINDRICAL_SURFACE('',#3457,1.4635);
#2994=CYLINDRICAL_SURFACE('',#3458,1.4635);
#2995=CYLINDRICAL_SURFACE('',#3459,1.4635);
#2996=CYLINDRICAL_SURFACE('',#3460,1.4635);
#2997=CYLINDRICAL_SURFACE('',#3461,1.4635);
#2998=CYLINDRICAL_SURFACE('',#3462,1.4635);
#2999=CYLINDRICAL_SURFACE('',#3463,1.4635);
#3000=CYLINDRICAL_SURFACE('',#3464,1.4635);
#3001=CYLINDRICAL_SURFACE('',#3465,1.4635);
#3002=CYLINDRICAL_SURFACE('',#3466,1.4635);
#3003=CYLINDRICAL_SURFACE('',#3467,1.4635);
#3004=CYLINDRICAL_SURFACE('',#3468,1.4635);
#3005=CYLINDRICAL_SURFACE('',#3470,1.17775);
#3118=ADVANCED_FACE('',(#539),#2962,.T.);
#3119=ADVANCED_FACE('',(#540),#2963,.T.);
#3120=ADVANCED_FACE('',(#541),#2964,.T.);
#3121=ADVANCED_FACE('',(#542),#2965,.T.);
#3122=ADVANCED_FACE('',(#543),#2966,.T.);
#3123=ADVANCED_FACE('',(#544),#2967,.T.);
#3124=ADVANCED_FACE('',(#545),#2968,.T.);
#3125=ADVANCED_FACE('',(#546),#2969,.T.);
#3126=ADVANCED_FACE('',(#547),#2970,.T.);
#3127=ADVANCED_FACE('',(#548),#2971,.T.);
#3128=ADVANCED_FACE('',(#549),#2972,.T.);
#3129=ADVANCED_FACE('',(#550),#2973,.T.);
#3130=ADVANCED_FACE('',(#551),#2974,.T.);
#3131=ADVANCED_FACE('',(#552),#2975,.T.);
#3132=ADVANCED_FACE('',(#553),#2976,.T.);
#3133=ADVANCED_FACE('',(#554),#2977,.T.);
#3134=ADVANCED_FACE('',(#555),#2978,.T.);
#3135=ADVANCED_FACE('',(#556),#2979,.T.);
#3136=ADVANCED_FACE('',(#557),#2980,.T.);
#3137=ADVANCED_FACE('',(#558),#2981,.T.);
#3138=ADVANCED_FACE('',(#559),#2982,.T.);
#3139=ADVANCED_FACE('',(#560),#2983,.T.);
#3140=ADVANCED_FACE('',(#561),#2984,.T.);
#3141=ADVANCED_FACE('',(#562),#2985,.T.);
#3142=ADVANCED_FACE('',(#563),#2986,.T.);
#3143=ADVANCED_FACE('',(#564),#2987,.T.);
#3144=ADVANCED_FACE('',(#565),#2988,.T.);
#3145=ADVANCED_FACE('',(#566),#2989,.T.);
#3146=ADVANCED_FACE('',(#567),#2990,.T.);
#3147=ADVANCED_FACE('',(#568),#2991,.T.);
#3148=ADVANCED_FACE('',(#569),#2992,.T.);
#3149=ADVANCED_FACE('',(#570),#2993,.T.);
#3150=ADVANCED_FACE('',(#571),#2994,.T.);
#3151=ADVANCED_FACE('',(#572),#2995,.T.);
#3152=ADVANCED_FACE('',(#573),#2996,.T.);
#3153=ADVANCED_FACE('',(#574),#2997,.T.);
#3154=ADVANCED_FACE('',(#575),#2998,.T.);
#3155=ADVANCED_FACE('',(#576),#2999,.T.);
#3156=ADVANCED_FACE('',(#577),#3000,.T.);
#3157=ADVANCED_FACE('',(#578),#3001,.T.);
#3158=ADVANCED_FACE('',(#579),#3002,.T.);
#3159=ADVANCED_FACE('',(#580),#3003,.T.);
#3160=ADVANCED_FACE('',(#581),#3004,.T.);
#3161=ADVANCED_FACE('',(#582),#3005,.T.);
#3162=ADVANCED_FACE('',(#583),#49,.F.);
#3163=ADVANCED_FACE('',(#584),#50,.F.);
#3164=ADVANCED_FACE('',(#585),#425,.F.);
#3165=ADVANCED_FACE('',(#586),#426,.T.);
#3174=CLOSED_SHELL('',(#3118,#3119,#3120,#3121,#3122,#3123,#3124,#3125,
#3126,#3127,#3128,#3129,#3130,#3131,#3132,#3133,#3134,#3135,#3136,#3137,
#3138,#3139,#3140,#3141,#3142,#3143,#3144,#3145,#3146,#3147,#3148,#3149,
#3150,#3151,#3152,#3153,#3154,#3155,#3156,#3157,#3158,#3159,#3160,#3161,
#3162,#3163,#3164,#3165));
#3423=AXIS2_PLACEMENT_3D('',#22891,#3900,#3901);
#3424=AXIS2_PLACEMENT_3D('',#22892,#3902,#3903);
#3425=AXIS2_PLACEMENT_3D('',#23008,#3905,#3906);
#3426=AXIS2_PLACEMENT_3D('',#23064,#3907,#3908);
#3427=AXIS2_PLACEMENT_3D('',#23484,#3910,#3911);
#3428=AXIS2_PLACEMENT_3D('',#23931,#3913,#3914);
#3429=AXIS2_PLACEMENT_3D('',#24384,#3916,#3917);
#3430=AXIS2_PLACEMENT_3D('',#24835,#3919,#3920);
#3431=AXIS2_PLACEMENT_3D('',#25318,#3922,#3923);
#3432=AXIS2_PLACEMENT_3D('',#25873,#3925,#3926);
#3433=AXIS2_PLACEMENT_3D('',#26322,#3928,#3929);
#3434=AXIS2_PLACEMENT_3D('',#26773,#3931,#3932);
#3435=AXIS2_PLACEMENT_3D('',#27212,#3934,#3935);
#3436=AXIS2_PLACEMENT_3D('',#27653,#3937,#3938);
#3437=AXIS2_PLACEMENT_3D('',#28132,#3940,#3941);
#3438=AXIS2_PLACEMENT_3D('',#28607,#3943,#3944);
#3439=AXIS2_PLACEMENT_3D('',#29130,#3946,#3947);
#3440=AXIS2_PLACEMENT_3D('',#29583,#3949,#3950);
#3441=AXIS2_PLACEMENT_3D('',#30020,#3952,#3953);
#3442=AXIS2_PLACEMENT_3D('',#30479,#3955,#3956);
#3443=AXIS2_PLACEMENT_3D('',#30940,#3958,#3959);
#3444=AXIS2_PLACEMENT_3D('',#31367,#3961,#3962);
#3445=AXIS2_PLACEMENT_3D('',#31795,#3964,#3965);
#3446=AXIS2_PLACEMENT_3D('',#32196,#3967,#3968);
#3447=AXIS2_PLACEMENT_3D('',#32208,#3970,#3971);
#3448=AXIS2_PLACEMENT_3D('',#32214,#3972,#3973);
#3449=AXIS2_PLACEMENT_3D('',#32400,#3975,#3976);
#3450=AXIS2_PLACEMENT_3D('',#32748,#3978,#3979);
#3451=AXIS2_PLACEMENT_3D('',#33096,#3981,#3982);
#3452=AXIS2_PLACEMENT_3D('',#33444,#3984,#3985);
#3453=AXIS2_PLACEMENT_3D('',#33792,#3987,#3988);
#3454=AXIS2_PLACEMENT_3D('',#34140,#3990,#3991);
#3455=AXIS2_PLACEMENT_3D('',#34488,#3993,#3994);
#3456=AXIS2_PLACEMENT_3D('',#34836,#3996,#3997);
#3457=AXIS2_PLACEMENT_3D('',#35184,#3999,#4000);
#3458=AXIS2_PLACEMENT_3D('',#35532,#4002,#4003);
#3459=AXIS2_PLACEMENT_3D('',#35880,#4005,#4006);
#3460=AXIS2_PLACEMENT_3D('',#36228,#4008,#4009);
#3461=AXIS2_PLACEMENT_3D('',#36579,#4011,#4012);
#3462=AXIS2_PLACEMENT_3D('',#36930,#4014,#4015);
#3463=AXIS2_PLACEMENT_3D('',#37278,#4017,#4018);
#3464=AXIS2_PLACEMENT_3D('',#37629,#4020,#4021);
#3465=AXIS2_PLACEMENT_3D('',#37983,#4023,#4024);
#3466=AXIS2_PLACEMENT_3D('',#38331,#4026,#4027);
#3467=AXIS2_PLACEMENT_3D('',#38679,#4029,#4030);
#3468=AXIS2_PLACEMENT_3D('',#39033,#4032,#4033);
#3469=AXIS2_PLACEMENT_3D('',#39045,#4034,#4035);
#3470=AXIS2_PLACEMENT_3D('',#39054,#4036,#4037);
#3471=AXIS2_PLACEMENT_3D('',#39193,#4038,#4039);
#3472=AXIS2_PLACEMENT_3D('',#40705,#4040,#4041);
#3473=AXIS2_PLACEMENT_3D('',#40706,#4042,#4043);
#3900=DIRECTION('axis',(0.,0.,1.));
#3901=DIRECTION('refdir',(1.,0.,0.));
#3902=DIRECTION('center_axis',(1.22464679914735E-16,-1.22464679914735E-16,
-1.));
#3903=DIRECTION('ref_axis',(0.457379984296263,-0.88927135901543,1.64917225715414E-16));
#3904=DIRECTION('',(-1.22464679914735E-16,1.22464679914735E-16,1.));
#3905=DIRECTION('center_axis',(-1.22464679914735E-16,1.22464679914735E-16,
1.));
#3906=DIRECTION('ref_axis',(-1.,4.0036529262094E-14,-1.2246467991474E-16));
#3907=DIRECTION('center_axis',(1.22464679914735E-16,-1.22464679914735E-16,
-1.));
#3908=DIRECTION('ref_axis',(0.457379984296263,-0.88927135901543,1.64917225715414E-16));
#3909=DIRECTION('',(-1.22464679914735E-16,1.22464679914735E-16,1.));
#3910=DIRECTION('center_axis',(1.22464679914735E-16,-1.22464679914735E-16,
-1.));
#3911=DIRECTION('ref_axis',(0.457379984296263,-0.88927135901543,1.64917225715414E-16));
#3912=DIRECTION('',(-1.22464679914735E-16,1.22464679914735E-16,1.));
#3913=DIRECTION('center_axis',(1.22464679914735E-16,-1.22464679914735E-16,
-1.));
#3914=DIRECTION('ref_axis',(0.457379984296263,-0.88927135901543,1.64917225715414E-16));
#3915=DIRECTION('',(-1.22464679914735E-16,1.22464679914735E-16,1.));
#3916=DIRECTION('center_axis',(1.22464679914735E-16,-1.22464679914735E-16,
-1.));
#3917=DIRECTION('ref_axis',(0.457379984296263,-0.88927135901543,1.64917225715414E-16));
#3918=DIRECTION('',(-1.22464679914735E-16,1.22464679914735E-16,1.));
#3919=DIRECTION('center_axis',(1.22464679914735E-16,-1.22464679914735E-16,
-1.));
#3920=DIRECTION('ref_axis',(0.457379984296263,-0.88927135901543,1.64917225715414E-16));
#3921=DIRECTION('',(-1.22464679914735E-16,1.22464679914735E-16,1.));
#3922=DIRECTION('center_axis',(1.22464679914735E-16,-1.22464679914735E-16,
-1.));
#3923=DIRECTION('ref_axis',(0.457379984296263,-0.88927135901543,1.64917225715414E-16));
#3924=DIRECTION('',(-1.22464679914735E-16,1.22464679914735E-16,1.));
#3925=DIRECTION('center_axis',(1.22464679914735E-16,-1.22464679914735E-16,
-1.));
#3926=DIRECTION('ref_axis',(0.457379984296263,-0.88927135901543,1.64917225715414E-16));
#3927=DIRECTION('',(-1.22464679914735E-16,1.22464679914735E-16,1.));
#3928=DIRECTION('center_axis',(1.22464679914735E-16,-1.22464679914735E-16,
-1.));
#3929=DIRECTION('ref_axis',(0.457379984296263,-0.88927135901543,1.64917225715414E-16));
#3930=DIRECTION('',(-1.22464679914735E-16,1.22464679914735E-16,1.));
#3931=DIRECTION('center_axis',(1.22464679914735E-16,-1.22464679914735E-16,
-1.));
#3932=DIRECTION('ref_axis',(0.457379984296263,-0.88927135901543,1.64917225715414E-16));
#3933=DIRECTION('',(-1.22464679914735E-16,1.22464679914735E-16,1.));
#3934=DIRECTION('center_axis',(1.22464679914735E-16,-1.22464679914735E-16,
-1.));
#3935=DIRECTION('ref_axis',(0.457379984296263,-0.88927135901543,1.64917225715414E-16));
#3936=DIRECTION('',(-1.22464679914735E-16,1.22464679914735E-16,1.));
#3937=DIRECTION('center_axis',(1.22464679914735E-16,-1.22464679914735E-16,
-1.));
#3938=DIRECTION('ref_axis',(0.457379984296263,-0.88927135901543,1.64917225715414E-16));
#3939=DIRECTION('',(-1.22464679914735E-16,1.22464679914735E-16,1.));
#3940=DIRECTION('center_axis',(1.22464679914735E-16,-1.22464679914735E-16,
-1.));
#3941=DIRECTION('ref_axis',(0.457379984296263,-0.88927135901543,1.64917225715414E-16));
#3942=DIRECTION('',(-1.22464679914735E-16,1.22464679914735E-16,1.));
#3943=DIRECTION('center_axis',(1.22464679914735E-16,-1.22464679914735E-16,
-1.));
#3944=DIRECTION('ref_axis',(0.457379984296263,-0.88927135901543,1.64917225715414E-16));
#3945=DIRECTION('',(-1.22464679914735E-16,1.22464679914735E-16,1.));
#3946=DIRECTION('center_axis',(1.22464679914735E-16,-1.22464679914735E-16,
-1.));
#3947=DIRECTION('ref_axis',(0.457379984296263,-0.88927135901543,1.64917225715414E-16));
#3948=DIRECTION('',(-1.22464679914735E-16,1.22464679914735E-16,1.));
#3949=DIRECTION('center_axis',(1.22464679914735E-16,-1.22464679914735E-16,
-1.));
#3950=DIRECTION('ref_axis',(0.457379984296263,-0.88927135901543,1.64917225715414E-16));
#3951=DIRECTION('',(-1.22464679914735E-16,1.22464679914735E-16,1.));
#3952=DIRECTION('center_axis',(1.22464679914735E-16,-1.22464679914735E-16,
-1.));
#3953=DIRECTION('ref_axis',(0.457379984296263,-0.88927135901543,1.64917225715414E-16));
#3954=DIRECTION('',(-1.22464679914735E-16,1.22464679914735E-16,1.));
#3955=DIRECTION('center_axis',(1.22464679914735E-16,-1.22464679914735E-16,
-1.));
#3956=DIRECTION('ref_axis',(0.457379984296263,-0.88927135901543,1.64917225715414E-16));
#3957=DIRECTION('',(-1.22464679914735E-16,1.22464679914735E-16,1.));
#3958=DIRECTION('center_axis',(1.22464679914735E-16,-1.22464679914735E-16,
-1.));
#3959=DIRECTION('ref_axis',(0.457379984296263,-0.88927135901543,1.64917225715414E-16));
#3960=DIRECTION('',(-1.22464679914735E-16,1.22464679914735E-16,1.));
#3961=DIRECTION('center_axis',(1.22464679914735E-16,-1.22464679914735E-16,
-1.));
#3962=DIRECTION('ref_axis',(0.457379984296263,-0.88927135901543,1.64917225715414E-16));
#3963=DIRECTION('',(-1.22464679914735E-16,1.22464679914735E-16,1.));
#3964=DIRECTION('center_axis',(1.22464679914735E-16,-1.22464679914735E-16,
-1.));
#3965=DIRECTION('ref_axis',(0.457379984296263,-0.88927135901543,1.64917225715414E-16));
#3966=DIRECTION('',(-1.22464679914735E-16,1.22464679914735E-16,1.));
#3967=DIRECTION('center_axis',(1.22464679914735E-16,-1.22464679914735E-16,
-1.));
#3968=DIRECTION('ref_axis',(-1.,1.258548236767E-48,-1.22464679914735E-16));
#3969=DIRECTION('',(-1.22464679914735E-16,1.22464679914735E-16,1.));
#3970=DIRECTION('center_axis',(1.22464679914735E-16,-1.22464679914735E-16,
-1.));
#3971=DIRECTION('ref_axis',(-1.,1.258548236767E-48,-1.22464679914735E-16));
#3972=DIRECTION('center_axis',(1.22464679914735E-16,-1.22464679914735E-16,
-1.));
#3973=DIRECTION('ref_axis',(-1.,1.258548236767E-48,-1.22464679914735E-16));
#3974=DIRECTION('',(-1.22464679914735E-16,1.22464679914735E-16,1.));
#3975=DIRECTION('center_axis',(1.22464679914735E-16,-1.22464679914735E-16,
-1.));
#3976=DIRECTION('ref_axis',(-1.,1.258548236767E-48,-1.22464679914735E-16));
#3977=DIRECTION('',(-1.22464679914735E-16,1.22464679914735E-16,1.));
#3978=DIRECTION('center_axis',(1.22464679914735E-16,-1.22464679914735E-16,
-1.));
#3979=DIRECTION('ref_axis',(-1.,1.258548236767E-48,-1.22464679914735E-16));
#3980=DIRECTION('',(-1.22464679914735E-16,1.22464679914735E-16,1.));
#3981=DIRECTION('center_axis',(1.22464679914735E-16,-1.22464679914735E-16,
-1.));
#3982=DIRECTION('ref_axis',(-1.,1.258548236767E-48,-1.22464679914735E-16));
#3983=DIRECTION('',(-1.22464679914735E-16,1.22464679914735E-16,1.));
#3984=DIRECTION('center_axis',(1.22464679914735E-16,-1.22464679914735E-16,
-1.));
#3985=DIRECTION('ref_axis',(-1.,1.258548236767E-48,-1.22464679914735E-16));
#3986=DIRECTION('',(-1.22464679914735E-16,1.22464679914735E-16,1.));
#3987=DIRECTION('center_axis',(1.22464679914735E-16,-1.22464679914735E-16,
-1.));
#3988=DIRECTION('ref_axis',(-1.,1.258548236767E-48,-1.22464679914735E-16));
#3989=DIRECTION('',(-1.22464679914735E-16,1.22464679914735E-16,1.));
#3990=DIRECTION('center_axis',(1.22464679914735E-16,-1.22464679914735E-16,
-1.));
#3991=DIRECTION('ref_axis',(-1.,1.258548236767E-48,-1.22464679914735E-16));
#3992=DIRECTION('',(-1.22464679914735E-16,1.22464679914735E-16,1.));
#3993=DIRECTION('center_axis',(1.22464679914735E-16,-1.22464679914735E-16,
-1.));
#3994=DIRECTION('ref_axis',(-1.,1.258548236767E-48,-1.22464679914735E-16));
#3995=DIRECTION('',(-1.22464679914735E-16,1.22464679914735E-16,1.));
#3996=DIRECTION('center_axis',(1.22464679914735E-16,-1.22464679914735E-16,
-1.));
#3997=DIRECTION('ref_axis',(-1.,1.258548236767E-48,-1.22464679914735E-16));
#3998=DIRECTION('',(-1.22464679914735E-16,1.22464679914735E-16,1.));
#3999=DIRECTION('center_axis',(1.22464679914735E-16,-1.22464679914735E-16,
-1.));
#4000=DIRECTION('ref_axis',(-1.,1.258548236767E-48,-1.22464679914735E-16));
#4001=DIRECTION('',(-1.22464679914735E-16,1.22464679914735E-16,1.));
#4002=DIRECTION('center_axis',(1.22464679914735E-16,-1.22464679914735E-16,
-1.));
#4003=DIRECTION('ref_axis',(-1.,1.258548236767E-48,-1.22464679914735E-16));
#4004=DIRECTION('',(-1.22464679914735E-16,1.22464679914735E-16,1.));
#4005=DIRECTION('center_axis',(1.22464679914735E-16,-1.22464679914735E-16,
-1.));
#4006=DIRECTION('ref_axis',(-1.,1.258548236767E-48,-1.22464679914735E-16));
#4007=DIRECTION('',(-1.22464679914735E-16,1.22464679914735E-16,1.));
#4008=DIRECTION('center_axis',(1.22464679914735E-16,-1.22464679914735E-16,
-1.));
#4009=DIRECTION('ref_axis',(-1.,1.258548236767E-48,-1.22464679914735E-16));
#4010=DIRECTION('',(-1.22464679914735E-16,1.22464679914735E-16,1.));
#4011=DIRECTION('center_axis',(1.22464679914735E-16,-1.22464679914735E-16,
-1.));
#4012=DIRECTION('ref_axis',(-1.,1.258548236767E-48,-1.22464679914735E-16));
#4013=DIRECTION('',(-1.22464679914735E-16,1.22464679914735E-16,1.));
#4014=DIRECTION('center_axis',(1.22464679914735E-16,-1.22464679914735E-16,
-1.));
#4015=DIRECTION('ref_axis',(-1.,1.258548236767E-48,-1.22464679914735E-16));
#4016=DIRECTION('',(-1.22464679914735E-16,1.22464679914735E-16,1.));
#4017=DIRECTION('center_axis',(1.22464679914735E-16,-1.22464679914735E-16,
-1.));
#4018=DIRECTION('ref_axis',(-1.,1.258548236767E-48,-1.22464679914735E-16));
#4019=DIRECTION('',(-1.22464679914735E-16,1.22464679914735E-16,1.));
#4020=DIRECTION('center_axis',(1.22464679914735E-16,-1.22464679914735E-16,
-1.));
#4021=DIRECTION('ref_axis',(-1.,1.258548236767E-48,-1.22464679914735E-16));
#4022=DIRECTION('',(-1.22464679914735E-16,1.22464679914735E-16,1.));
#4023=DIRECTION('center_axis',(1.22464679914735E-16,-1.22464679914735E-16,
-1.));
#4024=DIRECTION('ref_axis',(-1.,1.258548236767E-48,-1.22464679914735E-16));
#4025=DIRECTION('',(-1.22464679914735E-16,1.22464679914735E-16,1.));
#4026=DIRECTION('center_axis',(1.22464679914735E-16,-1.22464679914735E-16,
-1.));
#4027=DIRECTION('ref_axis',(-1.,1.258548236767E-48,-1.22464679914735E-16));
#4028=DIRECTION('',(-1.22464679914735E-16,1.22464679914735E-16,1.));
#4029=DIRECTION('center_axis',(1.22464679914735E-16,-1.22464679914735E-16,
-1.));
#4030=DIRECTION('ref_axis',(-1.,1.258548236767E-48,-1.22464679914735E-16));
#4031=DIRECTION('',(-1.22464679914735E-16,1.22464679914735E-16,1.));
#4032=DIRECTION('center_axis',(1.22464679914735E-16,-1.22464679914735E-16,
-1.));
#4033=DIRECTION('ref_axis',(-1.,1.258548236767E-48,-1.22464679914735E-16));
#4034=DIRECTION('center_axis',(1.22464679914735E-16,-1.22464679914735E-16,
-1.));
#4035=DIRECTION('ref_axis',(-1.,1.258548236767E-48,-1.22464679914735E-16));
#4036=DIRECTION('center_axis',(1.22464679914735E-16,-1.22464679914735E-16,
-1.));
#4037=DIRECTION('ref_axis',(0.457379984296263,-0.88927135901543,1.64917225715414E-16));
#4038=DIRECTION('center_axis',(1.22464679914735E-16,-1.22464679914735E-16,
-1.));
#4039=DIRECTION('ref_axis',(-1.,4.0036529262094E-14,-1.2246467991474E-16));
#4040=DIRECTION('center_axis',(-1.22464679914735E-16,1.22464679914735E-16,
1.));
#4041=DIRECTION('ref_axis',(-1.,1.258548236767E-48,-1.22464679914735E-16));
#4042=DIRECTION('center_axis',(-1.22464679914735E-16,1.22464679914735E-16,
1.));
#4043=DIRECTION('ref_axis',(-1.,1.258548236767E-48,-1.22464679914735E-16));
#22891=CARTESIAN_POINT('',(0.,0.,0.));
#22892=CARTESIAN_POINT('Origin',(96.460480949577,-7.19464945638997E-16,
0.924367114736168));
#22893=CARTESIAN_POINT('',(95.9218016724468,1.04733934275882,-0.262495071028826));
#22894=CARTESIAN_POINT('',(95.9218016730721,1.04733934308042,-0.162850753546055));
#22895=CARTESIAN_POINT('',(95.9218016730721,1.04733934308042,0.924367114736168));
#22896=CARTESIAN_POINT('',(97.1339231275304,-0.966214621837945,-5.34765442106351E-14));
#22897=CARTESIAN_POINT('Ctrl Pts',(95.9218016724468,1.04733934275882,-0.262495071028825));
#22898=CARTESIAN_POINT('Ctrl Pts',(95.9168323908224,1.04478348629092,-0.262102466988266));
#22899=CARTESIAN_POINT('Ctrl Pts',(95.9118812731618,1.04219225000779,-0.261708746243414));
#22900=CARTESIAN_POINT('Ctrl Pts',(95.8615982372324,1.01541830112118,-0.257684079597526));
#22901=CARTESIAN_POINT('Ctrl Pts',(95.817881247505,0.988331638390339,-0.253964206255137));
#22902=CARTESIAN_POINT('Ctrl Pts',(95.7085732743141,0.910280094927417,-0.244136329072671));
#22903=CARTESIAN_POINT('Ctrl Pts',(95.6463469511429,0.855080568629144,-0.237981412999409));
#22904=CARTESIAN_POINT('Ctrl Pts',(95.5848295257772,0.787653983866887,-0.231596017471511));
#22905=CARTESIAN_POINT('Ctrl Pts',(95.5792897742812,0.781451429369945,-0.231018128933633));
#22906=CARTESIAN_POINT('Ctrl Pts',(95.5711678613817,0.772161563912934,-0.23016722728284));
#22907=CARTESIAN_POINT('Ctrl Pts',(95.5685352158595,0.769119014787333,-0.229890832536729));
#22908=CARTESIAN_POINT('Ctrl Pts',(95.5640451150508,0.763875742122085,-0.229418511236026));
#22909=CARTESIAN_POINT('Ctrl Pts',(95.5621800667519,0.761681612745837,-0.229222048236102));
#22910=CARTESIAN_POINT('Ctrl Pts',(95.5583052004454,0.757089011804468,-0.228813334904457));
#22911=CARTESIAN_POINT('Ctrl Pts',(95.5562968797751,0.754689354806667,-0.228601202842244));
#22912=CARTESIAN_POINT('Ctrl Pts',(95.5513891953363,0.748777660595372,-0.228082015489454));
#22913=CARTESIAN_POINT('Ctrl Pts',(95.5485005544082,0.745256709583808,-0.227775722724851));
#22914=CARTESIAN_POINT('Ctrl Pts',(95.5379805653814,0.732281179789277,-0.226657282874926));
#22915=CARTESIAN_POINT('Ctrl Pts',(95.5304749108787,0.72272503882737,-0.225853512167293));
#22916=CARTESIAN_POINT('Ctrl Pts',(95.5118553269796,0.698248202961025,-0.223839659051407));
#22917=CARTESIAN_POINT('Ctrl Pts',(95.5009442470649,0.683176785131831,-0.222640720972597));
#22918=CARTESIAN_POINT('Ctrl Pts',(95.4527554960439,0.613180375978137,-0.217225437062142));
#22919=CARTESIAN_POINT('Ctrl Pts',(95.4198033491736,0.555420689895478,-0.21317042092782));
#22920=CARTESIAN_POINT('Ctrl Pts',(95.3622453187482,0.431213720152704,-0.204691697395776));
#22921=CARTESIAN_POINT('Ctrl Pts',(95.3384078824534,0.364714717858227,-0.200274417096875));
#22922=CARTESIAN_POINT('Ctrl Pts',(95.3180297803759,0.286373245568453,-0.194964067220175));
#22923=CARTESIAN_POINT('Ctrl Pts',(95.3155333865259,0.276223417137716,-0.194274339566029));
#22924=CARTESIAN_POINT('Ctrl Pts',(95.3116539451387,0.259493289874712,-0.193133956989658));
#22925=CARTESIAN_POINT('Ctrl Pts',(95.3101915379279,0.252931848328484,-0.192685831511372));
#22926=CARTESIAN_POINT('Ctrl Pts',(95.3076564554833,0.241080644457487,-0.191874692369414));
#22927=CARTESIAN_POINT('Ctrl Pts',(95.3065638111565,0.235795308068159,-0.191512324206385));
#22928=CARTESIAN_POINT('Ctrl Pts',(95.3043029214912,0.22446673289002,-0.190734210525823));
#22929=CARTESIAN_POINT('Ctrl Pts',(95.3031456501842,0.218421494097882,-0.190318129003744));
#22930=CARTESIAN_POINT('Ctrl Pts',(95.3001190491258,0.201911669313706,-0.189179310361597));
#22931=CARTESIAN_POINT('Ctrl Pts',(95.2983439662919,0.191430617664011,-0.188453631496875));
#22932=CARTESIAN_POINT('Ctrl Pts',(95.2890156874044,0.131428770594929,-0.184282638221013));
#22933=CARTESIAN_POINT('Ctrl Pts',(95.2844871441334,0.0814967000799421,
-0.180743822486812));
#22934=CARTESIAN_POINT('Ctrl Pts',(95.2818161501703,-0.0185434480269267,
-0.173526918471726));
#22935=CARTESIAN_POINT('Ctrl Pts',(95.2836655013368,-0.0685522922392763,
-0.169856405756507));
#22936=CARTESIAN_POINT('Ctrl Pts',(95.2898734133365,-0.13004909239642,-0.165319055376679));
#22937=CARTESIAN_POINT('Ctrl Pts',(95.2912375276573,-0.141790670241545,
-0.164451831728975));
#22938=CARTESIAN_POINT('Ctrl Pts',(95.2995472056142,-0.204999889568257,
-0.159783082837273));
#22939=CARTESIAN_POINT('Ctrl Pts',(95.3097154142873,-0.255992341042425,
-0.156013580207507));
#22940=CARTESIAN_POINT('Ctrl Pts',(95.3248847675913,-0.312341902781773,
-0.151952114068799));
#22941=CARTESIAN_POINT('Ctrl Pts',(95.3266016223442,-0.318518176262677,
-0.151508421645522));
#22942=CARTESIAN_POINT('Ctrl Pts',(95.3294493942366,-0.328447934975755,
-0.150797795129124));
#22943=CARTESIAN_POINT('Ctrl Pts',(95.3305487434164,-0.332210228268276,
-0.150529175473158));
#22944=CARTESIAN_POINT('Ctrl Pts',(95.3325349181096,-0.338883567439533,
-0.150053920071292));
#22945=CARTESIAN_POINT('Ctrl Pts',(95.3334142571126,-0.341796713741235,
-0.14984687062544));
#22946=CARTESIAN_POINT('Ctrl Pts',(95.3353525669371,-0.348129283328287,
-0.149397692909303));
#22947=CARTESIAN_POINT('Ctrl Pts',(95.3364158395737,-0.351547300740957,
-0.14915581422261));
#22948=CARTESIAN_POINT('Ctrl Pts',(95.3394686084005,-0.361205326566207,
-0.148473820040189));
#22949=CARTESIAN_POINT('Ctrl Pts',(95.3414946324133,-0.367433781589195,
-0.148035736328086));
#22950=CARTESIAN_POINT('Ctrl Pts',(95.3553690263957,-0.408907424332733,
-0.145128237207898));
#22951=CARTESIAN_POINT('Ctrl Pts',(95.368830142273,-0.44359528065562,-0.142742616817202));
#22952=CARTESIAN_POINT('Ctrl Pts',(95.4054551811603,-0.526154102342101,
-0.137046987745201));
#22953=CARTESIAN_POINT('Ctrl Pts',(95.4302607539313,-0.573205319099704,
-0.13378385334963));
#22954=CARTESIAN_POINT('Ctrl Pts',(95.496835198365,-0.681107281832769,-0.12592896825162));
#22955=CARTESIAN_POINT('Ctrl Pts',(95.5413003738846,-0.740017028192766,
-0.121320580631259));
#22956=CARTESIAN_POINT('Ctrl Pts',(95.5980112425028,-0.802091024433251,
-0.115801343177005));
#22957=CARTESIAN_POINT('Ctrl Pts',(95.6051533128247,-0.809702803253676,
-0.115112184838288));
#22958=CARTESIAN_POINT('Ctrl Pts',(95.6170852467238,-0.822085416853332,
-0.113969799383936));
#22959=CARTESIAN_POINT('Ctrl Pts',(95.6218167913321,-0.826911827637914,
-0.113519043179907));
#22960=CARTESIAN_POINT('Ctrl Pts',(95.6304431432331,-0.835560938291993,
-0.112701108714745));
#22961=CARTESIAN_POINT('Ctrl Pts',(95.6343235027868,-0.839397827593819,
-0.112334562682231));
#22962=CARTESIAN_POINT('Ctrl Pts',(95.6427106780903,-0.847576549442378,
-0.111545150971558));
#22963=CARTESIAN_POINT('Ctrl Pts',(95.6472256985851,-0.851909689011483,
-0.11112192935171));
#22964=CARTESIAN_POINT('Ctrl Pts',(95.6596994538843,-0.863691425957646,
-0.109957264320697));
#22965=CARTESIAN_POINT('Ctrl Pts',(95.6677272361081,-0.871065680151812,
-0.109212740924639));
#22966=CARTESIAN_POINT('Ctrl Pts',(95.7162031223826,-0.91437003037409,-0.104745218885447));
#22967=CARTESIAN_POINT('Ctrl Pts',(95.7589798171695,-0.9475846564076,-0.100913910332391));
#22968=CARTESIAN_POINT('Ctrl Pts',(95.8430555670714,-1.00404561387092,-0.0935930913100962));
#22969=CARTESIAN_POINT('Ctrl Pts',(95.8837732202382,-1.0279734928091,-0.0901297649956015));
#22970=CARTESIAN_POINT('Ctrl Pts',(95.9764607364817,-1.0751978665864,-0.0825046897981003));
#22971=CARTESIAN_POINT('Ctrl Pts',(96.0289143655834,-1.09730470165327,-0.0783539314668988));
#22972=CARTESIAN_POINT('Ctrl Pts',(96.0922356957895,-1.11874505103074,-0.0736682238755853));
#22973=CARTESIAN_POINT('Ctrl Pts',(96.1017480195882,-1.12183143004247,-0.072972763418035));
#22974=CARTESIAN_POINT('Ctrl Pts',(96.1150848051069,-1.12597170499654,-0.0720104997719221));
#22975=CARTESIAN_POINT('Ctrl Pts',(96.1188767081283,-1.12712790774487,-0.071738345647365));
#22976=CARTESIAN_POINT('Ctrl Pts',(96.1256655444289,-1.12916050925448,-0.0712537444420071));
#22977=CARTESIAN_POINT('Ctrl Pts',(96.1286602441681,-1.13004417240052,-0.0710408970244024));
#22978=CARTESIAN_POINT('Ctrl Pts',(96.1347808419727,-1.13182378288448,-0.0706077883512765));
#22979=CARTESIAN_POINT('Ctrl Pts',(96.1379069616128,-1.13271870229142,-0.0703875820424255));
#22980=CARTESIAN_POINT('Ctrl Pts',(96.1456145631442,-1.13489067370124,-0.0698470345285675));
#22981=CARTESIAN_POINT('Ctrl Pts',(96.1502001987723,-1.13615295630171,-0.0695275026503178));
#22982=CARTESIAN_POINT('Ctrl Pts',(96.1603216789144,-1.13887323421163,-0.0688265171665768));
#22983=CARTESIAN_POINT('Ctrl Pts',(96.1658607941909,-1.14031872668004,-0.0684457087685313));
#22984=CARTESIAN_POINT('Ctrl Pts',(96.1818979644173,-1.14437914330862,-0.0673507041001178));
#22985=CARTESIAN_POINT('Ctrl Pts',(96.1924220619256,-1.14688994837368,-0.066641419878612));
#22986=CARTESIAN_POINT('Ctrl Pts',(96.2297049004991,-1.15524351249402,-0.0641566012865987));
#22987=CARTESIAN_POINT('Ctrl Pts',(96.256632697569,-1.1602979120863,-0.0624122995080675));
#22988=CARTESIAN_POINT('Ctrl Pts',(96.3636616471749,-1.17654580478821,-0.0555926116133099));
#22989=CARTESIAN_POINT('Ctrl Pts',(96.4446463678075,-1.18041678584323,-0.0506659079224153));
#22990=CARTESIAN_POINT('Ctrl Pts',(96.5646673606718,-1.17379198969531,-0.0430543066728464));
#22991=CARTESIAN_POINT('Ctrl Pts',(96.6038074886636,-1.16965784180789,-0.0405254741412704));
#22992=CARTESIAN_POINT('Ctrl Pts',(96.6529971820366,-1.16195608316122,-0.0372489460046783));
#22993=CARTESIAN_POINT('Ctrl Pts',(96.6633073347592,-1.16020079517852,-0.0365567300417322));
#22994=CARTESIAN_POINT('Ctrl Pts',(96.679688055867,-1.15718698609715,-0.0354475859696136));
#22995=CARTESIAN_POINT('Ctrl Pts',(96.6857745806643,-1.15601741059374,-0.035033398705134));
#22996=CARTESIAN_POINT('Ctrl Pts',(96.6967267677052,-1.15382307929414,-0.0342842442105372));
#22997=CARTESIAN_POINT('Ctrl Pts',(96.7015957413507,-1.15281544091163,-0.0339498150351981));
#22998=CARTESIAN_POINT('Ctrl Pts',(96.7130428970855,-1.15037074978377,-0.0331602278284289));
#22999=CARTESIAN_POINT('Ctrl Pts',(96.7196153678732,-1.14890806826841,-0.0327042818610877));
#23000=CARTESIAN_POINT('Ctrl Pts',(96.7388299251554,-1.14445867098202,-0.0313634986172859));
#23001=CARTESIAN_POINT('Ctrl Pts',(96.7514352267475,-1.14131914346809,-0.0304739265301974));
#23002=CARTESIAN_POINT('Ctrl Pts',(96.8282399042547,-1.12083482611298,-0.0249902212920711));
#23003=CARTESIAN_POINT('Ctrl Pts',(96.8909165022146,-1.09828954316116,-0.0202318454842622));
#23004=CARTESIAN_POINT('Ctrl Pts',(97.0152059874345,-1.04130225887301,-0.0102566782470006));
#23005=CARTESIAN_POINT('Ctrl Pts',(97.0763067357945,-1.00637268554291,-0.00504969948552843));
#23006=CARTESIAN_POINT('Ctrl Pts',(97.1339231275304,-0.966214621837945,
-5.34765442106351E-14));
#23007=CARTESIAN_POINT('',(95.7758165250375,-0.958295198918397,1.18465120291105E-14));
#23008=CARTESIAN_POINT('Origin',(96.460480949577,-8.32667268468867E-16,
1.18130019239114E-14));
#23009=CARTESIAN_POINT('Ctrl Pts',(95.7758165250375,-0.958295198918382,
1.23234755733392E-14));
#23010=CARTESIAN_POINT('Ctrl Pts',(95.7361773941706,-0.929974590868919,
-0.00329165982696945));
#23011=CARTESIAN_POINT('Ctrl Pts',(95.698263491806,-0.899166066562328,-0.0065833196539512));
#23012=CARTESIAN_POINT('Ctrl Pts',(95.6623872069498,-0.866107060633552,
-0.00987497948093297));
#23013=CARTESIAN_POINT('Ctrl Pts',(95.6269881901253,-0.833487844018334,
-0.0131228498237755));
#23014=CARTESIAN_POINT('Ctrl Pts',(95.5935732745532,-0.798678049076778,
-0.016370720166618));
#23015=CARTESIAN_POINT('Ctrl Pts',(95.5624087893347,-0.761945836328084,
-0.0196185905094606));
#23016=CARTESIAN_POINT('Ctrl Pts',(95.5312515903722,-0.725222211569948,
-0.0228657015002861));
#23017=CARTESIAN_POINT('Ctrl Pts',(95.50234411452,-0.686577458385615,-0.0261128124911119));
#23018=CARTESIAN_POINT('Ctrl Pts',(95.4759133383833,-0.646313918686786,
-0.0293599234819374));
#23019=CARTESIAN_POINT('Ctrl Pts',(95.4494795040222,-0.606045720216871,
-0.0326074101860486));
#23020=CARTESIAN_POINT('Ctrl Pts',(95.425523222863,-0.564158800022298,-0.0358548968901596));
#23021=CARTESIAN_POINT('Ctrl Pts',(95.4042276697578,-0.52098375346178,-0.0391023835942709));
#23022=CARTESIAN_POINT('Ctrl Pts',(95.3824252116664,-0.476780997206698,
-0.0424271712820442));
#23023=CARTESIAN_POINT('Ctrl Pts',(95.3634120793787,-0.431228492082274,
-0.0457519589698178));
#23024=CARTESIAN_POINT('Ctrl Pts',(95.3473332165921,-0.384704025259145,
-0.0490767466575911));
#23025=CARTESIAN_POINT('Ctrl Pts',(95.3315957313724,-0.33916734031433,-0.0523309442827269));
#23026=CARTESIAN_POINT('Ctrl Pts',(95.3186691853137,-0.292700104231772,
-0.0555851419078624));
#23027=CARTESIAN_POINT('Ctrl Pts',(95.3086384940891,-0.245670552235394,
-0.0588393395329982));
#23028=CARTESIAN_POINT('Ctrl Pts',(95.2982814241977,-0.197110752508088,
-0.0621994222520902));
#23029=CARTESIAN_POINT('Ctrl Pts',(95.2910120737039,-0.147951994733136,
-0.0655595049711821));
#23030=CARTESIAN_POINT('Ctrl Pts',(95.286866085045,-0.0986063499450008,
-0.0689195876902741));
#23031=CARTESIAN_POINT('Ctrl Pts',(95.2827200963861,-0.0492607051568646,
-0.0722796704093661));
#23032=CARTESIAN_POINT('Ctrl Pts',(95.281697415506,0.000271221556261803,
-0.0756397531284582));
#23033=CARTESIAN_POINT('Ctrl Pts',(95.2837749850334,0.04957958760985,-0.0789998358475502));
#23034=CARTESIAN_POINT('Ctrl Pts',(95.2858102480679,0.0978838649868566,
-0.082291495674532));
#23035=CARTESIAN_POINT('Ctrl Pts',(95.2908306717257,0.146196916652632,-0.0855831555015136));
#23036=CARTESIAN_POINT('Ctrl Pts',(95.2988379439023,0.194114888318772,-0.0888748153284954));
#23037=CARTESIAN_POINT('Ctrl Pts',(95.3064816880046,0.239857396533906,-0.0920170346554361));
#23038=CARTESIAN_POINT('Ctrl Pts',(95.3168468319963,0.285239281260163,-0.0951592539823768));
#23039=CARTESIAN_POINT('Ctrl Pts',(95.3298817822784,0.329909965602386,-0.0983014733093175));
#23040=CARTESIAN_POINT('Ctrl Pts',(95.3429020065228,0.37453018391514,-0.101440142761536));
#23041=CARTESIAN_POINT('Ctrl Pts',(95.3585859147225,0.418440247031338,-0.104578812213755));
#23042=CARTESIAN_POINT('Ctrl Pts',(95.376830955067,0.461300067091394,-0.107717481665974));
#23043=CARTESIAN_POINT('Ctrl Pts',(95.3950638069178,0.504131254896376,-0.110854054348206));
#23044=CARTESIAN_POINT('Ctrl Pts',(95.4158541826417,0.545913065207913,-0.113990627030438));
#23045=CARTESIAN_POINT('Ctrl Pts',(95.4390507459098,0.586323632080711,-0.11712719971267));
#23046=CARTESIAN_POINT('Ctrl Pts',(95.4622425210494,0.62672585758928,-0.120263124957927));
#23047=CARTESIAN_POINT('Ctrl Pts',(95.4878392142814,0.665756908007129,-0.123399050203184));
#23048=CARTESIAN_POINT('Ctrl Pts',(95.5156440752432,0.703120433069016,-0.126534975448441));
#23049=CARTESIAN_POINT('Ctrl Pts',(95.5434755084833,0.740519665339904,-0.129673897604133));
#23050=CARTESIAN_POINT('Ctrl Pts',(95.5735189791043,0.776247735140941,-0.132812819759825));
#23051=CARTESIAN_POINT('Ctrl Pts',(95.6055362907784,0.810039932899456,-0.135951741915517));
#23052=CARTESIAN_POINT('Ctrl Pts',(95.6375716526691,0.843851181491955,-0.139092433683393));
#23053=CARTESIAN_POINT('Ctrl Pts',(95.6715826527233,0.875723998278705,-0.142233125451269));
#23054=CARTESIAN_POINT('Ctrl Pts',(95.707295670523,0.90543193996919,-0.145373817219145));
#23055=CARTESIAN_POINT('Ctrl Pts',(95.74307434671,0.935194499713862,-0.148520283149194));
#23056=CARTESIAN_POINT('Ctrl Pts',(95.7805608209667,0.962783912497935,-0.151666749079243));
#23057=CARTESIAN_POINT('Ctrl Pts',(95.8194516823276,0.988016467995215,-0.154813215009293));
#23058=CARTESIAN_POINT('Ctrl Pts',(95.8325800669933,0.996534219545908,-0.155875367237899));
#23059=CARTESIAN_POINT('Ctrl Pts',(95.8458682817941,1.0047837881853,-0.156937519466506));
#23060=CARTESIAN_POINT('Ctrl Pts',(95.8593040846046,1.01275931964212,-0.157999671695113));
#23061=CARTESIAN_POINT('Ctrl Pts',(95.8797588359455,1.02490131927261,-0.15961669897876));
#23062=CARTESIAN_POINT('Ctrl Pts',(95.9006043517095,1.03643689984567,-0.161233726262408));
#23063=CARTESIAN_POINT('Ctrl Pts',(95.9218016730721,1.04733934308042,-0.162850753546055));
#23064=CARTESIAN_POINT('Origin',(96.460480949577,-7.19464945638997E-16,
0.924367114736168));
#23065=CARTESIAN_POINT('',(95.921801662562,1.04733933767479,-0.761747732816349));
#23066=CARTESIAN_POINT('',(95.9218016734189,1.04733934325879,-0.661999947661212));
#23067=CARTESIAN_POINT('',(95.9218016730721,1.04733934308042,0.924367114736168));
#23068=CARTESIAN_POINT('Ctrl Pts',(95.921801662562,1.04733933767479,-0.761747732816352));
#23069=CARTESIAN_POINT('Ctrl Pts',(95.883175508933,1.02747270214554,-0.759053178224855));
#23070=CARTESIAN_POINT('Ctrl Pts',(95.8456739353038,1.0054824021569,-0.756338917671403));
#23071=CARTESIAN_POINT('Ctrl Pts',(95.7930101764126,0.97055032306898,-0.752300385322997));
#23072=CARTESIAN_POINT('Ctrl Pts',(95.7768288777527,0.959221007440542,-0.751026396207034));
#23073=CARTESIAN_POINT('Ctrl Pts',(95.7489791754977,0.938659341417836,-0.748768147748057));
#23074=CARTESIAN_POINT('Ctrl Pts',(95.7371863806177,0.929602639869777,-0.747790326834797));
#23075=CARTESIAN_POINT('Ctrl Pts',(95.7200663091019,0.915931658638611,-0.746336714737209));
#23076=CARTESIAN_POINT('Ctrl Pts',(95.7146036249844,0.911488703265523,-0.745867635471517));
#23077=CARTESIAN_POINT('Ctrl Pts',(95.7049759903812,0.90351377223756,-0.745031317294701));
#23078=CARTESIAN_POINT('Ctrl Pts',(95.7007951117538,0.900001281160456,-0.744664865071834));
#23079=CARTESIAN_POINT('Ctrl Pts',(95.6920493365921,0.892549312429411,-0.743891280900056));
#23080=CARTESIAN_POINT('Ctrl Pts',(95.6874899774325,0.888603608818043,-0.743483902360617));
#23081=CARTESIAN_POINT('Ctrl Pts',(95.6754943726046,0.878060339647571,-0.742401051401197));
#23082=CARTESIAN_POINT('Ctrl Pts',(95.668111152382,0.871403454248285,-0.741723149027886));
#23083=CARTESIAN_POINT('Ctrl Pts',(95.6356286319705,0.841362282641241,-0.738688566017347));
#23084=CARTESIAN_POINT('Ctrl Pts',(95.6114760782899,0.816983569241954,-0.736290333530637));
#23085=CARTESIAN_POINT('Ctrl Pts',(95.5209915352847,0.71730074211193,-0.726720246965365));
#23086=CARTESIAN_POINT('Ctrl Pts',(95.4633315461491,0.634704031424583,-0.719240177441031));
#23087=CARTESIAN_POINT('Ctrl Pts',(95.4068753061827,0.526757118265861,-0.710431220858489));
#23088=CARTESIAN_POINT('Ctrl Pts',(95.3974283974248,0.507422207953915,-0.708889581995119));
#23089=CARTESIAN_POINT('Ctrl Pts',(95.3829184905314,0.475538458686883,-0.70641694709215));
#23090=CARTESIAN_POINT('Ctrl Pts',(95.377532812947,0.463142581971482,-0.705472286298644));
#23091=CARTESIAN_POINT('Ctrl Pts',(95.370538095951,0.446253676992116,-0.704210150104191));
#23092=CARTESIAN_POINT('Ctrl Pts',(95.3687414767789,0.441840122548483,-0.703882593050572));
#23093=CARTESIAN_POINT('Ctrl Pts',(95.3657886165976,0.434458174171859,-0.703338663209367));
#23094=CARTESIAN_POINT('Ctrl Pts',(95.3646175597465,0.431495817522591,-0.703121435561114));
#23095=CARTESIAN_POINT('Ctrl Pts',(95.3624229651439,0.425877711778397,-0.702711497325987));
#23096=CARTESIAN_POINT('Ctrl Pts',(95.3613970137209,0.423222949458762,-0.702518641099976));
#23097=CARTESIAN_POINT('Ctrl Pts',(95.3589899062457,0.41692650779497,-0.702063196056052));
#23098=CARTESIAN_POINT('Ctrl Pts',(95.3576171602591,0.413281616724026,-0.70180109689761));
#23099=CARTESIAN_POINT('Ctrl Pts',(95.3528520751442,0.400436620127926,-0.700882645218786));
#23100=CARTESIAN_POINT('Ctrl Pts',(95.3495564599009,0.391200720625591,-0.700231631579146));
#23101=CARTESIAN_POINT('Ctrl Pts',(95.3235020744241,0.315197956433535,-0.694942528266368));
#23102=CARTESIAN_POINT('Ctrl Pts',(95.3066652524538,0.246541720849499,-0.690587662731763));
#23103=CARTESIAN_POINT('Ctrl Pts',(95.2871758999191,0.11817243775893,-0.682556262573215));
#23104=CARTESIAN_POINT('Ctrl Pts',(95.2827159202301,0.0589774671510073,
-0.678893948014252));
#23105=CARTESIAN_POINT('Ctrl Pts',(95.2827364028008,-0.0216032836315505,
-0.67375862036588));
#23106=CARTESIAN_POINT('Ctrl Pts',(95.2833198525272,-0.0429020934960637,
-0.672387663883698));
#23107=CARTESIAN_POINT('Ctrl Pts',(95.2853392862911,-0.0799094805642896,
-0.669973549186979));
#23108=CARTESIAN_POINT('Ctrl Pts',(95.2865137929773,-0.095627040862744,
-0.668938174233592));
#23109=CARTESIAN_POINT('Ctrl Pts',(95.288684274623,-0.118488513312446,-0.667415339378116));
#23110=CARTESIAN_POINT('Ctrl Pts',(95.2894310573696,-0.125654770400463,
-0.666935566827369));
#23111=CARTESIAN_POINT('Ctrl Pts',(95.2908617015114,-0.138260357386943,
-0.666087172534181));
#23112=CARTESIAN_POINT('Ctrl Pts',(95.2915178809062,-0.143702659064925,
-0.665719420049251));
#23113=CARTESIAN_POINT('Ctrl Pts',(95.2929653561576,-0.155041261594513,
-0.664950079167147));
#23114=CARTESIAN_POINT('Ctrl Pts',(95.2937633811791,-0.160936531053128,
-0.664548291101586));
#23115=CARTESIAN_POINT('Ctrl Pts',(95.2959621700797,-0.176302972258673,
-0.663496211740579));
#23116=CARTESIAN_POINT('Ctrl Pts',(95.2974337976727,-0.185763394915532,
-0.6628437313546));
#23117=CARTESIAN_POINT('Ctrl Pts',(95.3041297854199,-0.225604284995654,
-0.660075124693852));
#23118=CARTESIAN_POINT('Ctrl Pts',(95.3104300855992,-0.255789007360232,
-0.657925883700481));
#23119=CARTESIAN_POINT('Ctrl Pts',(95.3380853240114,-0.366392145815569,
-0.649853020082257));
#23120=CARTESIAN_POINT('Ctrl Pts',(95.3667558691237,-0.444721502703924,
-0.643721683528358));
#23121=CARTESIAN_POINT('Ctrl Pts',(95.4264488532246,-0.566213086230039,
-0.633812571898049));
#23122=CARTESIAN_POINT('Ctrl Pts',(95.4525588129756,-0.611484998968461,
-0.630025482866978));
#23123=CARTESIAN_POINT('Ctrl Pts',(95.4854589832101,-0.660663036865783,
-0.625910146231612));
#23124=CARTESIAN_POINT('Ctrl Pts',(95.4893795043116,-0.666412388866609,
-0.625429045201617));
#23125=CARTESIAN_POINT('Ctrl Pts',(95.4954404839801,-0.675133593744484,
-0.624699693948617));
#23126=CARTESIAN_POINT('Ctrl Pts',(95.497544145083,-0.678130651946481,-0.624449129982574));
#23127=CARTESIAN_POINT('Ctrl Pts',(95.5014210988507,-0.6835996778996,-0.623992117964115));
#23128=CARTESIAN_POINT('Ctrl Pts',(95.5031899977151,-0.686074595673858,
-0.623785393930058));
#23129=CARTESIAN_POINT('Ctrl Pts',(95.5072052740297,-0.691646721034061,
-0.623320150460493));
#23130=CARTESIAN_POINT('Ctrl Pts',(95.5094571667806,-0.694739854835062,
-0.623062009242804));
#23131=CARTESIAN_POINT('Ctrl Pts',(95.5153166979157,-0.702706456626337,
-0.622397299369914));
#23132=CARTESIAN_POINT('Ctrl Pts',(95.5189470229731,-0.707563209667553,
-0.621992214828497));
#23133=CARTESIAN_POINT('Ctrl Pts',(95.5435737488713,-0.739984374202579,
-0.619287460584144));
#23134=CARTESIAN_POINT('Ctrl Pts',(95.5657424625328,-0.766641529032463,
-0.617060368082938));
#23135=CARTESIAN_POINT('Ctrl Pts',(95.608028899734,-0.813151857328128,-0.613088443996411));
#23136=CARTESIAN_POINT('Ctrl Pts',(95.6277451311158,-0.833331637360445,
-0.611332377661967));
#23137=CARTESIAN_POINT('Ctrl Pts',(95.6828814034993,-0.885851259702204,
-0.606611168969166));
#23138=CARTESIAN_POINT('Ctrl Pts',(95.7195813084104,-0.916766675901992,
-0.603662983051974));
#23139=CARTESIAN_POINT('Ctrl Pts',(95.8009142147579,-0.977198428823439,
-0.59732679130867));
#23140=CARTESIAN_POINT('Ctrl Pts',(95.8458756378212,-1.00608363014918,-0.593933277407727));
#23141=CARTESIAN_POINT('Ctrl Pts',(95.9021298814729,-1.03704221295016,-0.589713131939763));
#23142=CARTESIAN_POINT('Ctrl Pts',(95.9116939988176,-1.04213498961617,-0.588996647613429));
#23143=CARTESIAN_POINT('Ctrl Pts',(95.9268602191834,-1.04994414881689,-0.587861367674102));
#23144=CARTESIAN_POINT('Ctrl Pts',(95.9324160781207,-1.05274939494953,-0.587445663834514));
#23145=CARTESIAN_POINT('Ctrl Pts',(95.9428592077469,-1.05791883776531,-0.586664493736362));
#23146=CARTESIAN_POINT('Ctrl Pts',(95.947741116453,-1.06029354272856,-0.586299401733016));
#23147=CARTESIAN_POINT('Ctrl Pts',(95.9587072892667,-1.06553436733621,-0.585479400461564));
#23148=CARTESIAN_POINT('Ctrl Pts',(95.9647999963751,-1.06838227406905,-0.585023883402262));
#23149=CARTESIAN_POINT('Ctrl Pts',(95.9803651615633,-1.07549607833121,-0.583860170693215));
#23150=CARTESIAN_POINT('Ctrl Pts',(95.9898701192688,-1.07968903801979,-0.58314954489004));
#23151=CARTESIAN_POINT('Ctrl Pts',(96.0688174940618,-1.11327487395352,-0.577245684955331));
#23152=CARTESIAN_POINT('Ctrl Pts',(96.1408675037319,-1.13605659196619,-0.57183118287821));
#23153=CARTESIAN_POINT('Ctrl Pts',(96.271027585386,-1.1638441470624,-0.562095418288413));
#23154=CARTESIAN_POINT('Ctrl Pts',(96.3282780046136,-1.17172880972086,-0.55783301952061));
#23155=CARTESIAN_POINT('Ctrl Pts',(96.4064210712549,-1.17668873084238,-0.552178135924882));
#23156=CARTESIAN_POINT('Ctrl Pts',(96.4269975000278,-1.17745394775479,-0.550704859581647));
#23157=CARTESIAN_POINT('Ctrl Pts',(96.460676718844,-1.17782275800697,-0.548329315087066));
#23158=CARTESIAN_POINT('Ctrl Pts',(96.4737710499031,-1.17774780684484,-0.54741459827547));
#23159=CARTESIAN_POINT('Ctrl Pts',(96.4915692344859,-1.17734903472878,-0.546185715716059));
#23160=CARTESIAN_POINT('Ctrl Pts',(96.4962758268873,-1.17721534125518,-0.545862120274871));
#23161=CARTESIAN_POINT('Ctrl Pts',(96.5041535940924,-1.17694427911458,-0.545322932476015));
#23162=CARTESIAN_POINT('Ctrl Pts',(96.5073252042244,-1.17682231140232,-0.54510651590472));
#23163=CARTESIAN_POINT('Ctrl Pts',(96.5133515988379,-1.1765661579976,-0.544696607346896));
#23164=CARTESIAN_POINT('Ctrl Pts',(96.5162064393188,-1.17643440103334,-0.544502979149504));
#23165=CARTESIAN_POINT('Ctrl Pts',(96.5229931550246,-1.17609641966686,-0.544043932661879));
#23166=CARTESIAN_POINT('Ctrl Pts',(96.5269245626726,-1.17588086622953,-0.543779021649199));
#23167=CARTESIAN_POINT('Ctrl Pts',(96.5408393247403,-1.17504793105682,-0.542844725833134));
#23168=CARTESIAN_POINT('Ctrl Pts',(96.5508161520526,-1.17432307146511,-0.54218090365708));
#23169=CARTESIAN_POINT('Ctrl Pts',(96.6236928733034,-1.16809396251231,-0.537368405130885));
#23170=CARTESIAN_POINT('Ctrl Pts',(96.6860772599701,-1.15766577448211,-0.533444365229694));
#23171=CARTESIAN_POINT('Ctrl Pts',(96.8076751106828,-1.12713010411461,-0.525681964414421));
#23172=CARTESIAN_POINT('Ctrl Pts',(96.8667198121304,-1.10721971269949,-0.521853641267478));
#23173=CARTESIAN_POINT('Ctrl Pts',(96.9565764886802,-1.06875935943932,-0.515647447785411));
#23174=CARTESIAN_POINT('Ctrl Pts',(96.9885869091643,-1.05330957811765,-0.513356456117118));
#23175=CARTESIAN_POINT('Ctrl Pts',(97.0283783520863,-1.03183407812645,-0.510377300056813));
#23176=CARTESIAN_POINT('Ctrl Pts',(97.0368513147062,-1.02712521999043,-0.509735128418848));
#23177=CARTESIAN_POINT('Ctrl Pts',(97.0504529069733,-1.01934482544907,-0.508691053061727));
#23178=CARTESIAN_POINT('Ctrl Pts',(97.0556180818328,-1.0163378253653,-0.508291442175202));
#23179=CARTESIAN_POINT('Ctrl Pts',(97.065471845453,-1.01050040599915,-0.507522959230861));
#23180=CARTESIAN_POINT('Ctrl Pts',(97.0701640286481,-1.00767633492837,-0.507154322362964));
#23181=CARTESIAN_POINT('Ctrl Pts',(97.0808373589423,-1.00115056970297,-0.506309497127684));
#23182=CARTESIAN_POINT('Ctrl Pts',(97.0868053344931,-0.997427841502103,
-0.505832555579537));
#23183=CARTESIAN_POINT('Ctrl Pts',(97.1055903858657,-0.985474954680329,
-0.504316573511841));
#23184=CARTESIAN_POINT('Ctrl Pts',(97.1182808876775,-0.97704978117323,-0.503270445204628));
#23185=CARTESIAN_POINT('Ctrl Pts',(97.2014241411096,-0.919497204083365,
-0.496265631504845));
#23186=CARTESIAN_POINT('Ctrl Pts',(97.2664725388368,-0.863043601592718,
-0.490024242795726));
#23187=CARTESIAN_POINT('Ctrl Pts',(97.3584923083937,-0.763630432497412,
-0.480082845415622));
#23188=CARTESIAN_POINT('Ctrl Pts',(97.3898574909068,-0.725131442667534,
-0.47643880324814));
#23189=CARTESIAN_POINT('Ctrl Pts',(97.4277539183399,-0.672101492416839,
-0.471769616429379));
#23190=CARTESIAN_POINT('Ctrl Pts',(97.4365536782622,-0.65925677080646,-0.47066392381815));
#23191=CARTESIAN_POINT('Ctrl Pts',(97.450947588531,-0.637326135923955,-0.468822744339366));
#23192=CARTESIAN_POINT('Ctrl Pts',(97.4566774954469,-0.628332100348734,
-0.46808047217702));
#23193=CARTESIAN_POINT('Ctrl Pts',(97.4645698119503,-0.615564380396892,
-0.467045970709026));
#23194=CARTESIAN_POINT('Ctrl Pts',(97.4668344900243,-0.611854968997145,
-0.466747664461544));
#23195=CARTESIAN_POINT('Ctrl Pts',(97.4706813912681,-0.605474826087057,
-0.466238533587721));
#23196=CARTESIAN_POINT('Ctrl Pts',(97.4722736713353,-0.602810240900197,
-0.466027075008146));
#23197=CARTESIAN_POINT('Ctrl Pts',(97.4753524003984,-0.597611605487717,
-0.465616834140029));
#23198=CARTESIAN_POINT('Ctrl Pts',(97.4768399161787,-0.595078267283493,
-0.465417978232927));
#23199=CARTESIAN_POINT('Ctrl Pts',(97.4808977304109,-0.588107939547102,
-0.464873660669491));
#23200=CARTESIAN_POINT('Ctrl Pts',(97.4834485942745,-0.583659622955238,
-0.464529413745853));
#23201=CARTESIAN_POINT('Ctrl Pts',(97.4933650466222,-0.566102111953248,
-0.463182338794736));
#23202=CARTESIAN_POINT('Ctrl Pts',(97.5005087257035,-0.552868370947933,
-0.462192414695996));
#23203=CARTESIAN_POINT('Ctrl Pts',(97.5191780650158,-0.51663998773245,-0.459540628846992));
#23204=CARTESIAN_POINT('Ctrl Pts',(97.5302075893586,-0.49339796471292,-0.45790152035355));
#23205=CARTESIAN_POINT('Ctrl Pts',(97.5613029659211,-0.421917026002823,
-0.45299158517889));
#23206=CARTESIAN_POINT('Ctrl Pts',(97.5789297272181,-0.372687343470029,
-0.449783838693494));
#23207=CARTESIAN_POINT('Ctrl Pts',(97.6131931189828,-0.252321296073137,
-0.442031229795563));
#23208=CARTESIAN_POINT('Ctrl Pts',(97.6265977460064,-0.180501841042826,
-0.437469067927289));
#23209=CARTESIAN_POINT('Ctrl Pts',(97.6342318086101,-0.0975324642251496,
-0.432001344547463));
#23210=CARTESIAN_POINT('Ctrl Pts',(97.6350488238433,-0.0871433192819611,
-0.431313480616302));
#23211=CARTESIAN_POINT('Ctrl Pts',(97.6361665474715,-0.0700268708716457,
-0.430174254414681));
#23212=CARTESIAN_POINT('Ctrl Pts',(97.6365476265763,-0.0633052591097759,
-0.429725375911245));
#23213=CARTESIAN_POINT('Ctrl Pts',(97.6371316861353,-0.0511618978609094,
-0.428911541953791));
#23214=CARTESIAN_POINT('Ctrl Pts',(97.6373548722398,-0.0457412735787324,
-0.428547221717702));
#23215=CARTESIAN_POINT('Ctrl Pts',(97.6377531758196,-0.0341134384786835,
-0.42776340314737));
#23216=CARTESIAN_POINT('Ctrl Pts',(97.6379166687722,-0.0279060204894306,
-0.42734355645944));
#23217=CARTESIAN_POINT('Ctrl Pts',(97.6382297343926,-0.0109157201833946,
-0.426190385203877));
#23218=CARTESIAN_POINT('Ctrl Pts',(97.6382803052739,-0.000131842598366711,
-0.425454034069181));
#23219=CARTESIAN_POINT('Ctrl Pts',(97.6377087775588,0.0630636529869075,
-0.421111713507778));
#23220=CARTESIAN_POINT('Ctrl Pts',(97.633736564964,0.115378690850311,-0.417403533785645));
#23221=CARTESIAN_POINT('Ctrl Pts',(97.6152083901342,0.244529779270065,-0.407979584444264));
#23222=CARTESIAN_POINT('Ctrl Pts',(97.5964659729673,0.320510900434516,-0.402183935243037));
#23223=CARTESIAN_POINT('Ctrl Pts',(97.5590097426722,0.426001490579876,-0.394072370120888));
#23224=CARTESIAN_POINT('Ctrl Pts',(97.5463007056735,0.457426174424071,-0.391650022603342));
#23225=CARTESIAN_POINT('Ctrl Pts',(97.5297533990795,0.493748766075535,-0.388875976599983));
#23226=CARTESIAN_POINT('Ctrl Pts',(97.5272116481038,0.499216421901405,-0.388459118458316));
#23227=CARTESIAN_POINT('Ctrl Pts',(97.5229935109954,0.508110882160203,-0.387782459316815));
#23228=CARTESIAN_POINT('Ctrl Pts',(97.5213423057645,0.511549406920673,-0.387521227998317));
#23229=CARTESIAN_POINT('Ctrl Pts',(97.518344871286,0.517714429857221,-0.387053586461117));
#23230=CARTESIAN_POINT('Ctrl Pts',(97.5170047687458,0.520443779750109,-0.386846818113173));
#23231=CARTESIAN_POINT('Ctrl Pts',(97.5140241850062,0.526455293733115,-0.386391983380981));
#23232=CARTESIAN_POINT('Ctrl Pts',(97.5123789288335,0.529734997306368,-0.386144213239588));
#23233=CARTESIAN_POINT('Ctrl Pts',(97.5075527880926,0.539244428409664,-0.385426743344741));
#23234=CARTESIAN_POINT('Ctrl Pts',(97.504331633202,0.545453705407088,-0.384959435322203));
#23235=CARTESIAN_POINT('Ctrl Pts',(97.4756384149433,0.599579122224819,-0.38089302884618));
#23236=CARTESIAN_POINT('Ctrl Pts',(97.4469346321389,0.645717081971682,-0.37747399607917));
#23237=CARTESIAN_POINT('Ctrl Pts',(97.3632655202171,0.761527161251995,-0.368584937962893));
#23238=CARTESIAN_POINT('Ctrl Pts',(97.30345136125,0.827250687989441,-0.363193827150058));
#23239=CARTESIAN_POINT('Ctrl Pts',(97.2181118995332,0.902058947730075,-0.355903010213178));
#23240=CARTESIAN_POINT('Ctrl Pts',(97.1988740497568,0.917872807074346,-0.354283610705932));
#23241=CARTESIAN_POINT('Ctrl Pts',(97.1721265760849,0.938474384311253,-0.352054838550277));
#23242=CARTESIAN_POINT('Ctrl Pts',(97.1650418792318,0.943804829953751,-0.351466595056858));
#23243=CARTESIAN_POINT('Ctrl Pts',(97.1536924764191,0.952144987217313,-0.35052719461897));
#23244=CARTESIAN_POINT('Ctrl Pts',(97.1494666842747,0.955207283017022,-0.350178059111182));
#23245=CARTESIAN_POINT('Ctrl Pts',(97.1407573313736,0.96143080952085,-0.349459709170628));
#23246=CARTESIAN_POINT('Ctrl Pts',(97.1362717628489,0.964588996452458,-0.34909039116953));
#23247=CARTESIAN_POINT('Ctrl Pts',(97.125834319578,0.971829224757706,-0.348232436638685));
#23248=CARTESIAN_POINT('Ctrl Pts',(97.1198667125322,0.975888088187573,-0.34774294896745));
#23249=CARTESIAN_POINT('Ctrl Pts',(97.1007044791588,0.988665260234743,-0.346174257112538));
#23250=CARTESIAN_POINT('Ctrl Pts',(97.0873718739467,0.997172448222111,-0.345087369360005));
#23251=CARTESIAN_POINT('Ctrl Pts',(97.0556054106112,1.01655291574387,-0.342507111447704));
#23252=CARTESIAN_POINT('Ctrl Pts',(97.0370389756335,1.02719701058837,-0.341006191423924));
#23253=CARTESIAN_POINT('Ctrl Pts',(96.9655640134995,1.06562504371581,-0.335254427332842));
#23254=CARTESIAN_POINT('Ctrl Pts',(96.9108625239515,1.08987184139744,-0.330899911259941));
#23255=CARTESIAN_POINT('Ctrl Pts',(96.788836999403,1.13319992221958,-0.321400919226787));
#23256=CARTESIAN_POINT('Ctrl Pts',(96.7211609044422,1.15065524141902,-0.31626326058391));
#23257=CARTESIAN_POINT('Ctrl Pts',(96.6426352963192,1.1636199803381,-0.310684842131048));
#23258=CARTESIAN_POINT('Ctrl Pts',(96.6329178744116,1.16509964694966,-0.310001245297676));
#23259=CARTESIAN_POINT('Ctrl Pts',(96.619309486215,1.16699779432538,-0.309054338598213));
#23260=CARTESIAN_POINT('Ctrl Pts',(96.6154335545219,1.16751875673237,-0.308785818224782));
#23261=CARTESIAN_POINT('Ctrl Pts',(96.6087256575918,1.16838636945384,-0.308323218540102));
#23262=CARTESIAN_POINT('Ctrl Pts',(96.6058949249572,1.16874204937883,-0.308128652193352));
#23263=CARTESIAN_POINT('Ctrl Pts',(96.5998920975165,1.16947415439466,-0.307717474527367));
#23264=CARTESIAN_POINT('Ctrl Pts',(96.5967196987903,1.16984796866048,-0.307501012233984));
#23265=CARTESIAN_POINT('Ctrl Pts',(96.5888061242937,1.17074782372535,-0.306963047038128));
#23266=CARTESIAN_POINT('Ctrl Pts',(96.5840631449785,1.17125798189131,-0.306642408530999));
#23267=CARTESIAN_POINT('Ctrl Pts',(96.565910797779,1.17309896730375,-0.305421649475919));
#23268=CARTESIAN_POINT('Ctrl Pts',(96.5524814479601,1.1742285068074,-0.304531835572617));
#23269=CARTESIAN_POINT('Ctrl Pts',(96.5176686038893,1.1765556496786,-0.30225276191564));
#23270=CARTESIAN_POINT('Ctrl Pts',(96.4962659261763,1.17740102382463,-0.300878449029231));
#23271=CARTESIAN_POINT('Ctrl Pts',(96.3757729610454,1.17887128754924,-0.293233736932032));
#23272=CARTESIAN_POINT('Ctrl Pts',(96.2769370490261,1.1675729618675,-0.287280365906995));
#23273=CARTESIAN_POINT('Ctrl Pts',(96.1467186906655,1.13572469125749,-0.278766983427975));
#23274=CARTESIAN_POINT('Ctrl Pts',(96.113148245026,1.12591161353944,-0.276513013453992));
#23275=CARTESIAN_POINT('Ctrl Pts',(96.0705880123846,1.11138600820529,-0.273551977230737));
#23276=CARTESIAN_POINT('Ctrl Pts',(96.0611517740671,1.10803048747445,-0.272888829077721));
#23277=CARTESIAN_POINT('Ctrl Pts',(96.0460819976803,1.10245418113594,-0.271818520353859));
#23278=CARTESIAN_POINT('Ctrl Pts',(96.0404206616993,1.10030953148593,-0.27141385828414));
#23279=CARTESIAN_POINT('Ctrl Pts',(96.0296762839738,1.09614429731005,-0.270640833639246));
#23280=CARTESIAN_POINT('Ctrl Pts',(96.0245902780235,1.09413175676287,-0.270272745195363));
#23281=CARTESIAN_POINT('Ctrl Pts',(96.0129948036356,1.08944972795434,-0.269428488257682));
#23282=CARTESIAN_POINT('Ctrl Pts',(96.0064949190696,1.08675721343144,-0.268951564267823));
#23283=CARTESIAN_POINT('Ctrl Pts',(95.9864069298799,1.07822429434095,-0.267465959759572));
#23284=CARTESIAN_POINT('Ctrl Pts',(95.9729048845689,1.07218624849779,-0.266450717872592));
#23285=CARTESIAN_POINT('Ctrl Pts',(95.946837381003,1.05993478354444,-0.26445698429842));
#23286=CARTESIAN_POINT('Ctrl Pts',(95.9342624202848,1.05374829386364,-0.263479547321252));
#23287=CARTESIAN_POINT('Ctrl Pts',(95.9218016724468,1.04733934275882,-0.262495071028825));
#23288=CARTESIAN_POINT('',(97.6382306586311,0.000827842401244189,-0.325632885263827));
#23289=CARTESIAN_POINT('Ctrl Pts',(95.9218016730721,1.04733934308042,-0.162850753546055));
#23290=CARTESIAN_POINT('Ctrl Pts',(95.963457953322,1.06876446670931,-0.16602848249336));
#23291=CARTESIAN_POINT('Ctrl Pts',(96.0064744835986,1.08774169819866,-0.169206211440665));
#23292=CARTESIAN_POINT('Ctrl Pts',(96.0505334981692,1.10410060664064,-0.172383940387971));
#23293=CARTESIAN_POINT('Ctrl Pts',(96.0945382959645,1.12043938464457,-0.175557758984172));
#23294=CARTESIAN_POINT('Ctrl Pts',(96.139582521453,1.13416602324947,-0.178731577580373));
#23295=CARTESIAN_POINT('Ctrl Pts',(96.1853263829313,1.14515720621843,-0.181905396176574));
#23296=CARTESIAN_POINT('Ctrl Pts',(96.2310339716416,1.15613967368727,-0.185076698081309));
#23297=CARTESIAN_POINT('Ctrl Pts',(96.277439558641,1.1643908508674,-0.188247999986045));
#23298=CARTESIAN_POINT('Ctrl Pts',(96.3241886475632,1.16983736942867,-0.19141930189078));
#23299=CARTESIAN_POINT('Ctrl Pts',(96.3709211218398,1.17528195229497,-0.194589476713496));
#23300=CARTESIAN_POINT('Ctrl Pts',(96.4179963040495,1.17792378871448,-0.197759651536212));
#23301=CARTESIAN_POINT('Ctrl Pts',(96.4650526666343,1.17774112686241,-0.200929826358928));
#23302=CARTESIAN_POINT('Ctrl Pts',(96.5121475638274,1.17755831542797,-0.204102597248113));
#23303=CARTESIAN_POINT('Ctrl Pts',(96.5592230532303,1.17454638285798,-0.207275368137299));
#23304=CARTESIAN_POINT('Ctrl Pts',(96.6059176191503,1.16873574328991,-0.210448139026484));
#23305=CARTESIAN_POINT('Ctrl Pts',(96.6526303191125,1.16292284713414,-0.213622142075341));
#23306=CARTESIAN_POINT('Ctrl Pts',(96.6989612519655,1.15430917475159,-0.216796145124199));
#23307=CARTESIAN_POINT('Ctrl Pts',(96.7445576924114,1.14297658186009,-0.219970148173057));
#23308=CARTESIAN_POINT('Ctrl Pts',(96.7902419709798,1.13162215757844,-0.22315026570071));
#23309=CARTESIAN_POINT('Ctrl Pts',(96.8351883971898,1.11753851314616,-0.226330383228363));
#23310=CARTESIAN_POINT('Ctrl Pts',(96.8790595461831,1.10085740264727,-0.229510500756015));
#23311=CARTESIAN_POINT('Ctrl Pts',(96.9134976164422,1.08776302813135,-0.232006836351569));
#23312=CARTESIAN_POINT('Ctrl Pts',(96.9472733745764,1.07306913453378,-0.234503171947122));
#23313=CARTESIAN_POINT('Ctrl Pts',(96.9802341500302,1.05685934405611,-0.236999507542675));
#23314=CARTESIAN_POINT('Ctrl Pts',(97.0236961190942,1.03548516815837,-0.240291167369657));
#23315=CARTESIAN_POINT('Ctrl Pts',(97.0659334661461,1.01137835486445,-0.243582827196638));
#23316=CARTESIAN_POINT('Ctrl Pts',(97.1065838599168,0.984706094096334,-0.24687448702362));
#23317=CARTESIAN_POINT('Ctrl Pts',(97.1458237609606,0.958959310951739,-0.250051932403593));
#23318=CARTESIAN_POINT('Ctrl Pts',(97.1835845317979,0.930822543258878,-0.253229377783565));
#23319=CARTESIAN_POINT('Ctrl Pts',(97.2195635397929,0.900493577839994,-0.256406823163538));
#23320=CARTESIAN_POINT('Ctrl Pts',(97.2555079630214,0.870193766092844,-0.259581214228987));
#23321=CARTESIAN_POINT('Ctrl Pts',(97.2896735909337,0.837706284579617,-0.262755605294436));
#23322=CARTESIAN_POINT('Ctrl Pts',(97.3217887886277,0.803270732001229,-0.265929996359885));
#23323=CARTESIAN_POINT('Ctrl Pts',(97.353887119405,0.768853264991046,-0.269102720233673));
#23324=CARTESIAN_POINT('Ctrl Pts',(97.3839367753294,0.732490159590648,-0.27227544410746));
#23325=CARTESIAN_POINT('Ctrl Pts',(97.4117030748047,0.694457724398867,-0.275448167981248));
#23326=CARTESIAN_POINT('Ctrl Pts',(97.4394668978288,0.656428681285709,-0.278620608882652));
#23327=CARTESIAN_POINT('Ctrl Pts',(97.4649474433992,0.616731053807496,-0.281793049784056));
#23328=CARTESIAN_POINT('Ctrl Pts',(97.4879520809459,0.575671900220555,-0.28496549068546));
#23329=CARTESIAN_POINT('Ctrl Pts',(97.5109804732496,0.534570348651244,-0.288141207472548));
#23330=CARTESIAN_POINT('Ctrl Pts',(97.5315275861647,0.492104952068775,-0.291316924259635));
#23331=CARTESIAN_POINT('Ctrl Pts',(97.5494466716691,0.448607532937615,-0.294492641046723));
#23332=CARTESIAN_POINT('Ctrl Pts',(97.5673769246852,0.40508300539552,-0.297670337000331));
#23333=CARTESIAN_POINT('Ctrl Pts',(97.5826757106302,0.360525700835335,-0.300848032953939));
#23334=CARTESIAN_POINT('Ctrl Pts',(97.5952456640176,0.315284166047998,-0.304025728907547));
#23335=CARTESIAN_POINT('Ctrl Pts',(97.607838216946,0.269961291426521,-0.307209138046241));
#23336=CARTESIAN_POINT('Ctrl Pts',(97.6176920373088,0.223952275727347,-0.310392547184935));
#23337=CARTESIAN_POINT('Ctrl Pts',(97.6247608897451,0.177615549493993,-0.313575956323629));
#23338=CARTESIAN_POINT('Ctrl Pts',(97.6265546235301,0.16585752341037,-0.314383752012498));
#23339=CARTESIAN_POINT('Ctrl Pts',(97.6281692948468,0.154078412576249,-0.315191547701367));
#23340=CARTESIAN_POINT('Ctrl Pts',(97.6296046814756,0.142284089101716,-0.315999343390236));
#23341=CARTESIAN_POINT('Ctrl Pts',(97.6353106858459,0.095398838854968,-0.319210524014766));
#23342=CARTESIAN_POINT('Ctrl Pts',(97.6381973880941,0.0481609642844836,
-0.322421704639297));
#23343=CARTESIAN_POINT('Ctrl Pts',(97.6382306586311,0.000827842401244189,
-0.325632885263827));
#23344=CARTESIAN_POINT('Ctrl Pts',(97.638230626738,0.00087203623034647,
-0.326333448408234));
#23345=CARTESIAN_POINT('Ctrl Pts',(97.638286653864,-0.0747967573660931,
-0.331106951541581));
#23346=CARTESIAN_POINT('Ctrl Pts',(97.6310503143384,-0.150299827625081,
-0.335701552920094));
#23347=CARTESIAN_POINT('Ctrl Pts',(97.6065752538257,-0.276290640543653,
-0.343727845590335));
#23348=CARTESIAN_POINT('Ctrl Pts',(97.5930771831955,-0.327251259773279,
-0.347076331299543));
#23349=CARTESIAN_POINT('Ctrl Pts',(97.5727718465764,-0.387323797531268,
-0.351243588323239));
#23350=CARTESIAN_POINT('Ctrl Pts',(97.5691881255141,-0.397465909388993,
-0.351954786272469));
#23351=CARTESIAN_POINT('Ctrl Pts',(97.5633268243591,-0.413357298293986,
-0.353081903965348));
#23352=CARTESIAN_POINT('Ctrl Pts',(97.5611419630215,-0.419140323267442,
-0.353494761614325));
#23353=CARTESIAN_POINT('Ctrl Pts',(97.5569658010524,-0.4299361864992,-0.354270671893381));
#23354=CARTESIAN_POINT('Ctrl Pts',(97.5549853879578,-0.434953085601531,
-0.35463335385735));
#23355=CARTESIAN_POINT('Ctrl Pts',(97.5504741686503,-0.446155248917659,
-0.355448012816802));
#23356=CARTESIAN_POINT('Ctrl Pts',(97.5479250526679,-0.452332889820701,
-0.355900594056792));
#23357=CARTESIAN_POINT('Ctrl Pts',(97.54130493958,-0.467996930121249,-0.357056808364033));
#23358=CARTESIAN_POINT('Ctrl Pts',(97.5371616120618,-0.477451948542248,
-0.357762856559819));
#23359=CARTESIAN_POINT('Ctrl Pts',(97.501988241869,-0.554930277674469,-0.363617460740938));
#23360=CARTESIAN_POINT('Ctrl Pts',(97.4646753399647,-0.619899070466905,
-0.368984890550831));
#23361=CARTESIAN_POINT('Ctrl Pts',(97.3887244692412,-0.727094549333626,
-0.378598449683826));
#23362=CARTESIAN_POINT('Ctrl Pts',(97.3526921559772,-0.770883811115552,
-0.382784366829987));
#23363=CARTESIAN_POINT('Ctrl Pts',(97.2983523795545,-0.827984826870115,
-0.388492113375989));
#23364=CARTESIAN_POINT('Ctrl Pts',(97.2826037832981,-0.843624072369617,
-0.390084122301438));
#23365=CARTESIAN_POINT('Ctrl Pts',(97.2596099943568,-0.865202343965956,
-0.392311658655913));
#23366=CARTESIAN_POINT('Ctrl Pts',(97.2527221509007,-0.871513750700355,
-0.39296715274739));
#23367=CARTESIAN_POINT('Ctrl Pts',(97.2419402985011,-0.88115981102705,-0.393974232478295));
#23368=CARTESIAN_POINT('Ctrl Pts',(97.2380985494794,-0.884551975423763,
-0.394329419251078));
#23369=CARTESIAN_POINT('Ctrl Pts',(97.2309868797649,-0.890749253457098,
-0.394980046441199));
#23370=CARTESIAN_POINT('Ctrl Pts',(97.2277234941237,-0.89356169361344,-0.395275979316444));
#23371=CARTESIAN_POINT('Ctrl Pts',(97.2220939187674,-0.898359776486915,
-0.39578188883736));
#23372=CARTESIAN_POINT('Ctrl Pts',(97.2197352316942,-0.900354118570464,
-0.395992484975316));
#23373=CARTESIAN_POINT('Ctrl Pts',(97.2151804080346,-0.904174732838357,
-0.39639649511028));
#23374=CARTESIAN_POINT('Ctrl Pts',(97.2129854537589,-0.906002313312708,
-0.396590009691239));
#23375=CARTESIAN_POINT('Ctrl Pts',(97.20775142626,-0.910328168317545,-0.397048730528729));
#23376=CARTESIAN_POINT('Ctrl Pts',(97.2047064170228,-0.912819255964677,
-0.39731343043369));
#23377=CARTESIAN_POINT('Ctrl Pts',(97.1938746389186,-0.921590380420619,
-0.398247601276371));
#23378=CARTESIAN_POINT('Ctrl Pts',(97.1860201418531,-0.927786629336338,
-0.398911504529218));
#23379=CARTESIAN_POINT('Ctrl Pts',(97.1274032075592,-0.972828586360824,
-0.403775394732494));
#23380=CARTESIAN_POINT('Ctrl Pts',(97.0736255359534,-1.00758952055075,-0.407744936598658));
#23381=CARTESIAN_POINT('Ctrl Pts',(96.9628335653648,-1.06703112701297,-0.415527671305366));
#23382=CARTESIAN_POINT('Ctrl Pts',(96.9061698609204,-1.09191318868212,-0.419331122902057));
#23383=CARTESIAN_POINT('Ctrl Pts',(96.8143642675086,-1.12388455892939,-0.425504562497344));
#23384=CARTESIAN_POINT('Ctrl Pts',(96.7804053869462,-1.13401846613699,-0.427789056511789));
#23385=CARTESIAN_POINT('Ctrl Pts',(96.7366376884247,-1.14495699488098,-0.430761529832749));
#23386=CARTESIAN_POINT('Ctrl Pts',(96.727203103462,-1.14719150447881,-0.431403856280194));
#23387=CARTESIAN_POINT('Ctrl Pts',(96.7119027582329,-1.15061633250221,-0.432448575648654));
#23388=CARTESIAN_POINT('Ctrl Pts',(96.7060535000077,-1.15187889586214,-0.432848680443888));
#23389=CARTESIAN_POINT('Ctrl Pts',(96.6948225444863,-1.15421366724631,-0.433618389107223));
#23390=CARTESIAN_POINT('Ctrl Pts',(96.6894424644627,-1.15529294800911,-0.433987759314069));
#23391=CARTESIAN_POINT('Ctrl Pts',(96.6771296621551,-1.15767359506622,-0.43483467085645));
#23392=CARTESIAN_POINT('Ctrl Pts',(96.6701924524564,-1.15895034371545,-0.435312970227495));
#23393=CARTESIAN_POINT('Ctrl Pts',(96.64871663689,-1.16270369774481,-0.436797395805814));
#23394=CARTESIAN_POINT('Ctrl Pts',(96.6341431435467,-1.16496951506449,-0.43781002015643));
#23395=CARTESIAN_POINT('Ctrl Pts',(96.5304332668459,-1.17910461722937,-0.445056738645634));
#23396=CARTESIAN_POINT('Ctrl Pts',(96.4402532700717,-1.18100210103111,-0.451603848062412));
#23397=CARTESIAN_POINT('Ctrl Pts',(96.3330120482362,-1.17096725549395,-0.459504678241724));
#23398=CARTESIAN_POINT('Ctrl Pts',(96.3153088108866,-1.16890448561184,-0.460811442676354));
#23399=CARTESIAN_POINT('Ctrl Pts',(96.2534134697254,-1.16026459829467,-0.465378565572855));
#23400=CARTESIAN_POINT('Ctrl Pts',(96.2095503574649,-1.1515752416042,-0.468613282352042));
#23401=CARTESIAN_POINT('Ctrl Pts',(96.1569795149387,-1.138013295214,-0.472414445999536));
#23402=CARTESIAN_POINT('Ctrl Pts',(96.1477052079481,-1.13549933116797,-0.473082049171882));
#23403=CARTESIAN_POINT('Ctrl Pts',(96.1344440850418,-1.13172986020041,-0.47403136114128));
#23404=CARTESIAN_POINT('Ctrl Pts',(96.1304318537952,-1.13056627811609,-0.4743178830513));
#23405=CARTESIAN_POINT('Ctrl Pts',(96.1234678780811,-1.12850643199712,-0.474813879337796));
#23406=CARTESIAN_POINT('Ctrl Pts',(96.1205133335706,-1.12761988205035,-0.47502389568723));
#23407=CARTESIAN_POINT('Ctrl Pts',(96.1142659347862,-1.12571848077101,-0.475467061339255));
#23408=CARTESIAN_POINT('Ctrl Pts',(96.1109740210883,-1.12470077892736,-0.475700046185299));
#23409=CARTESIAN_POINT('Ctrl Pts',(96.1020183155644,-1.12188898681131,-0.476332559052906));
#23410=CARTESIAN_POINT('Ctrl Pts',(96.0963634630065,-1.12006643479134,-0.476730493953298));
#23411=CARTESIAN_POINT('Ctrl Pts',(96.0693878937946,-1.1111463536967,-0.478622918039608));
#23412=CARTESIAN_POINT('Ctrl Pts',(96.0482578738526,-1.10348189409222,-0.480087705162348));
#23413=CARTESIAN_POINT('Ctrl Pts',(95.9315902415259,-1.05734366709929,-0.488144435009503));
#23414=CARTESIAN_POINT('Ctrl Pts',(95.8411968708528,-1.00707107590836,-0.494305631442383));
#23415=CARTESIAN_POINT('Ctrl Pts',(95.7365015771007,-0.929353974180032,
-0.502537883011989));
#23416=CARTESIAN_POINT('Ctrl Pts',(95.7150908513257,-0.912271004488046,
-0.504285583845986));
#23417=CARTESIAN_POINT('Ctrl Pts',(95.6798282908509,-0.882065408523191,
-0.507294611658994));
#23418=CARTESIAN_POINT('Ctrl Pts',(95.6656641508287,-0.86932396088567,-0.508541594396956));
#23419=CARTESIAN_POINT('Ctrl Pts',(95.6461717376941,-0.850914707735897,
-0.510316666380331));
#23420=CARTESIAN_POINT('Ctrl Pts',(95.6405805893273,-0.845528667083554,
-0.510832934842955));
#23421=CARTESIAN_POINT('Ctrl Pts',(95.6310659143291,-0.836179916407774,
-0.511724078215793));
#23422=CARTESIAN_POINT('Ctrl Pts',(95.6271164837528,-0.832243845626137,
-0.512097797509473));
#23423=CARTESIAN_POINT('Ctrl Pts',(95.6196230058521,-0.824668891885829,
-0.512814310352976));
#23424=CARTESIAN_POINT('Ctrl Pts',(95.6160742496399,-0.821034826594318,
-0.513156887551569));
#23425=CARTESIAN_POINT('Ctrl Pts',(95.6078127972499,-0.812464558746713,
-0.513962145954227));
#23426=CARTESIAN_POINT('Ctrl Pts',(95.6031193197148,-0.807510166782562,
-0.514425633124294));
#23427=CARTESIAN_POINT('Ctrl Pts',(95.589387568834,-0.792760380530263,-0.515799745379227));
#23428=CARTESIAN_POINT('Ctrl Pts',(95.5804724683874,-0.782852314762888,
-0.516715452300022));
#23429=CARTESIAN_POINT('Ctrl Pts',(95.5111181626091,-0.703091411133919,
-0.524032195534013));
#23430=CARTESIAN_POINT('Ctrl Pts',(95.4589301588594,-0.626511645363865,
-0.530768169076817));
#23431=CARTESIAN_POINT('Ctrl Pts',(95.3870295048484,-0.488655627230942,
-0.542179085015026));
#23432=CARTESIAN_POINT('Ctrl Pts',(95.3623752128076,-0.430404306197625,
-0.54680356069869));
#23433=CARTESIAN_POINT('Ctrl Pts',(95.339936571119,-0.362687542914304,-0.551781786799588));
#23434=CARTESIAN_POINT('Ctrl Pts',(95.337444801866,-0.354896855630555,-0.552348691949884));
#23435=CARTESIAN_POINT('Ctrl Pts',(95.3338830769724,-0.343347574015294,
-0.553179880678885));
#23436=CARTESIAN_POINT('Ctrl Pts',(95.3327504023157,-0.339608799970925,
-0.553447537500628));
#23437=CARTESIAN_POINT('Ctrl Pts',(95.3307677716046,-0.332945152200068,
-0.553921979334297));
#23438=CARTESIAN_POINT('Ctrl Pts',(95.3299105364955,-0.330022545678446,
-0.554129171267704));
#23439=CARTESIAN_POINT('Ctrl Pts',(95.3280664273338,-0.323643831836692,
-0.554579420538322));
#23440=CARTESIAN_POINT('Ctrl Pts',(95.3270840304339,-0.320186515354768,
-0.554822222302329));
#23441=CARTESIAN_POINT('Ctrl Pts',(95.3243796908818,-0.310500803848293,
-0.555499118262961));
#23442=CARTESIAN_POINT('Ctrl Pts',(95.3226931261551,-0.304262539162929,
-0.55593125998588));
#23443=CARTESIAN_POINT('Ctrl Pts',(95.3131446598321,-0.267754627932298,
-0.558439681465034));
#23444=CARTESIAN_POINT('Ctrl Pts',(95.3064388270834,-0.237192469622415,
-0.560457316304132));
#23445=CARTESIAN_POINT('Ctrl Pts',(95.2828459683939,-0.104649286476163,
-0.568997223734907));
#23446=CARTESIAN_POINT('Ctrl Pts',(95.2782047698755,-0.000959642945746481,
-0.575188967530022));
#23447=CARTESIAN_POINT('Ctrl Pts',(95.2890334061612,0.123592247912445,-0.583151241255716));
#23448=CARTESIAN_POINT('Ctrl Pts',(95.2915048553716,0.145117872134375,-0.584544587217426));
#23449=CARTESIAN_POINT('Ctrl Pts',(95.2968257556906,0.182363451527379,-0.586994379173968));
#23450=CARTESIAN_POINT('Ctrl Pts',(95.2994040233507,0.198116557834131,-0.588042703817235));
#23451=CARTESIAN_POINT('Ctrl Pts',(95.3036155157851,0.220929440703581,-0.589580856496452));
#23452=CARTESIAN_POINT('Ctrl Pts',(95.3049950619999,0.228034667037812,-0.590062761988184));
#23453=CARTESIAN_POINT('Ctrl Pts',(95.3075345994478,0.240499144872412,-0.590913355505525));
#23454=CARTESIAN_POINT('Ctrl Pts',(95.30866670098,0.245863905353598,-0.591281155645434));
#23455=CARTESIAN_POINT('Ctrl Pts',(95.3109458082844,0.256302714917933,-0.592000231632617));
#23456=CARTESIAN_POINT('Ctrl Pts',(95.3120890549894,0.261377462091896,-0.592351380784895));
#23457=CARTESIAN_POINT('Ctrl Pts',(95.3152573433004,0.275018987825597,-0.593299649006156));
#23458=CARTESIAN_POINT('Ctrl Pts',(95.3173448410281,0.283570770832722,-0.593898735068732));
#23459=CARTESIAN_POINT('Ctrl Pts',(95.3256003580512,0.315817317966197,-0.59617574555046));
#23460=CARTESIAN_POINT('Ctrl Pts',(95.332410497508,0.339339706891084,-0.597873851692947));
#23461=CARTESIAN_POINT('Ctrl Pts',(95.3708228260312,0.458033991083355,-0.606639205950092));
#23462=CARTESIAN_POINT('Ctrl Pts',(95.4137522649853,0.549092584150526,-0.614066800457536));
#23463=CARTESIAN_POINT('Ctrl Pts',(95.4835850573301,0.658516218059673,-0.62353278495938));
#23464=CARTESIAN_POINT('Ctrl Pts',(95.5004244603388,0.682833044100112,-0.625671400343901));
#23465=CARTESIAN_POINT('Ctrl Pts',(95.5282687066087,0.719971697025328,-0.628966703663235));
#23466=CARTESIAN_POINT('Ctrl Pts',(95.5386638619967,0.733234096361876,-0.630149578985386));
#23467=CARTESIAN_POINT('Ctrl Pts',(95.5526134626546,0.750265530815474,-0.631671973309801));
#23468=CARTESIAN_POINT('Ctrl Pts',(95.555912591069,0.75423990069677,-0.632027475570406));
#23469=CARTESIAN_POINT('Ctrl Pts',(95.5613428018692,0.760694646566433,-0.632605066966588));
#23470=CARTESIAN_POINT('Ctrl Pts',(95.5634582123561,0.763188026341498,-0.632828237512009));
#23471=CARTESIAN_POINT('Ctrl Pts',(95.5676086356474,0.768038926166544,-0.633262471452468));
#23472=CARTESIAN_POINT('Ctrl Pts',(95.5696426537094,0.770397230046601,-0.633473598879998));
#23473=CARTESIAN_POINT('Ctrl Pts',(95.5742060871919,0.775645977829048,-0.633943612181957));
#23474=CARTESIAN_POINT('Ctrl Pts',(95.5767403593831,0.778532199006007,-0.63420214810385));
#23475=CARTESIAN_POINT('Ctrl Pts',(95.5855539895755,0.788471336881261,-0.635092951167112));
#23476=CARTESIAN_POINT('Ctrl Pts',(95.591904219335,0.795461320174383,-0.635720304095556));
#23477=CARTESIAN_POINT('Ctrl Pts',(95.6511517069113,0.85912212087262,-0.641450384559067));
#23478=CARTESIAN_POINT('Ctrl Pts',(95.7094471544897,0.91052533541087,-0.646207497355856));
#23479=CARTESIAN_POINT('Ctrl Pts',(95.8167297554877,0.987757933655887,-0.654385905932889));
#23480=CARTESIAN_POINT('Ctrl Pts',(95.8632456112907,1.01655824077084,-0.657775375548533));
#23481=CARTESIAN_POINT('Ctrl Pts',(95.9149851355834,1.04381229502683,-0.661508623022443));
#23482=CARTESIAN_POINT('Ctrl Pts',(95.9183891636579,1.0455841831001,-0.661754055889336));
#23483=CARTESIAN_POINT('Ctrl Pts',(95.9218016734189,1.0473393432588,-0.661999947661213));
#23484=CARTESIAN_POINT('Origin',(96.460480949577,-7.19464945638997E-16,
0.924367114736168));
#23485=CARTESIAN_POINT('',(95.9218016672795,1.0473393401011,-1.26059202888094));
#23486=CARTESIAN_POINT('',(95.9218016937941,1.04733935373838,-1.1624507611287));
#23487=CARTESIAN_POINT('',(95.9218016730721,1.04733934308042,0.924367114736168));
#23488=CARTESIAN_POINT('',(97.6382305348814,-0.00104073772955277,-0.924212417541179));
#23489=CARTESIAN_POINT('Ctrl Pts',(95.9218016672795,1.04733934010109,-1.26059202888093));
#23490=CARTESIAN_POINT('Ctrl Pts',(95.9124909570254,1.04255055147708,-1.25985189138548));
#23491=CARTESIAN_POINT('Ctrl Pts',(95.9032430830649,1.03763708108747,-1.2591170773026));
#23492=CARTESIAN_POINT('Ctrl Pts',(95.8885707434698,1.02958874570432,-1.25795317209041));
#23493=CARTESIAN_POINT('Ctrl Pts',(95.8831048669043,1.02653355158647,-1.25752001752847));
#23494=CARTESIAN_POINT('Ctrl Pts',(95.8742870279693,1.02151203921229,-1.25682224850314));
#23495=CARTESIAN_POINT('Ctrl Pts',(95.8709200601205,1.01957251762484,-1.25655605840964));
#23496=CARTESIAN_POINT('Ctrl Pts',(95.864931242162,1.01608310871101,-1.25608310502353));
#23497=CARTESIAN_POINT('Ctrl Pts',(95.8623057467824,1.01453968146771,-1.25587594672969));
#23498=CARTESIAN_POINT('Ctrl Pts',(95.8565779764428,1.01114258179217,-1.25542442204969));
#23499=CARTESIAN_POINT('Ctrl Pts',(95.8534782306762,1.00928480707794,-1.25518032116734));
#23500=CARTESIAN_POINT('Ctrl Pts',(95.8446303081737,1.00392646351676,-1.25448414295944));
#23501=CARTESIAN_POINT('Ctrl Pts',(95.8389034051741,1.00039078274829,-1.25403424444454));
#23502=CARTESIAN_POINT('Ctrl Pts',(95.797090520294,0.974078609272367,-1.25075228311072));
#23503=CARTESIAN_POINT('Ctrl Pts',(95.7622314401185,0.949402180134824,-1.24803114254563));
#23504=CARTESIAN_POINT('Ctrl Pts',(95.6569933917553,0.865965742160164,-1.23960744590673));
#23505=CARTESIAN_POINT('Ctrl Pts',(95.5920898069141,0.800865892348069,-1.23406931740228));
#23506=CARTESIAN_POINT('Ctrl Pts',(95.5155508720362,0.703725404878514,-1.22619237992788));
#23507=CARTESIAN_POINT('Ctrl Pts',(95.4967525246725,0.677753299100132,-1.22412116278549));
#23508=CARTESIAN_POINT('Ctrl Pts',(95.4736715895503,0.642959240143239,-1.22137030981065));
#23509=CARTESIAN_POINT('Ctrl Pts',(95.4684057498474,0.634803974735654,-1.22072722837716));
#23510=CARTESIAN_POINT('Ctrl Pts',(95.4600607763342,0.62152255143322,-1.21968212205514));
#23511=CARTESIAN_POINT('Ctrl Pts',(95.4569187454284,0.616436294475653,-1.21928240073601));
#23512=CARTESIAN_POINT('Ctrl Pts',(95.450974505995,0.606647972576106,-1.21851401131606));
#23513=CARTESIAN_POINT('Ctrl Pts',(95.4481660789842,0.601949851155458,-1.21814558058679));
#23514=CARTESIAN_POINT('Ctrl Pts',(95.4417682914031,0.591075804647422,-1.21729359409879));
#23515=CARTESIAN_POINT('Ctrl Pts',(95.4382021957157,0.584886512305568,-1.21680922302402));
#23516=CARTESIAN_POINT('Ctrl Pts',(95.4271172572576,0.565236465655884,-1.21527294699474));
#23517=CARTESIAN_POINT('Ctrl Pts',(95.419806583154,0.55166077144025,-1.21421379189066));
#23518=CARTESIAN_POINT('Ctrl Pts',(95.4033084353605,0.5195285958921,-1.21171086258152));
#23519=CARTESIAN_POINT('Ctrl Pts',(95.3943398781203,0.500866062612544,-1.21026013151297));
#23520=CARTESIAN_POINT('Ctrl Pts',(95.3627862867526,0.430514504873537,-1.20480176114072));
#23521=CARTESIAN_POINT('Ctrl Pts',(95.3434334155344,0.377465027147153,-1.20070165693744));
#23522=CARTESIAN_POINT('Ctrl Pts',(95.3074172711921,0.251276227315327,-1.19108140531528));
#23523=CARTESIAN_POINT('Ctrl Pts',(95.2937820379467,0.177513712894609,-1.1855523505221));
#23524=CARTESIAN_POINT('Ctrl Pts',(95.2864013510727,0.0934025379049221,
-1.17963729572722));
#23525=CARTESIAN_POINT('Ctrl Pts',(95.2856800443095,0.0838438150060226,
-1.17897088378348));
#23526=CARTESIAN_POINT('Ctrl Pts',(95.2848316916561,0.070418951065792,-1.178044022437));
#23527=CARTESIAN_POINT('Ctrl Pts',(95.284606884592,0.0665596775109735,-1.17777862838284));
#23528=CARTESIAN_POINT('Ctrl Pts',(95.2842349254296,0.059582666803825,-1.17730081914477));
#23529=CARTESIAN_POINT('Ctrl Pts',(95.2840811572407,0.0564653247373613,
-1.17708804899433));
#23530=CARTESIAN_POINT('Ctrl Pts',(95.2837919640534,0.0500873557338245,
-1.17665424130214));
#23531=CARTESIAN_POINT('Ctrl Pts',(95.283657695698,0.0468267193401669,-1.17643326804342));
#23532=CARTESIAN_POINT('Ctrl Pts',(95.2833473591183,0.0384428232385585,
-1.17586706160092));
#23533=CARTESIAN_POINT('Ctrl Pts',(95.2831911813203,0.0333188294994105,
-1.17552290312707));
#23534=CARTESIAN_POINT('Ctrl Pts',(95.2826742418162,0.0117307616841884,
-1.17408026397162));
#23535=CARTESIAN_POINT('Ctrl Pts',(95.2826253333605,-0.00473982236947986,
-1.17299759331857));
#23536=CARTESIAN_POINT('Ctrl Pts',(95.2834364301867,-0.0497775063634159,
-1.17007310830347));
#23537=CARTESIAN_POINT('Ctrl Pts',(95.2849906209954,-0.0783218708327382,
-1.16825913657225));
#23538=CARTESIAN_POINT('Ctrl Pts',(95.295535584052,-0.194146924935691,-1.16096066227737));
#23539=CARTESIAN_POINT('Ctrl Pts',(95.3132247607793,-0.280347081034544,
-1.15565194527878));
#23540=CARTESIAN_POINT('Ctrl Pts',(95.3513597993906,-0.397771595732273,
-1.1478200029324));
#23541=CARTESIAN_POINT('Ctrl Pts',(95.3639373760131,-0.431235174541892,
-1.14551818412745));
#23542=CARTESIAN_POINT('Ctrl Pts',(95.3820023193155,-0.473372237807435,
-1.14250042879455));
#23543=CARTESIAN_POINT('Ctrl Pts',(95.3861086134336,-0.48261941975773,-1.14183062993081));
#23544=CARTESIAN_POINT('Ctrl Pts',(95.3928673445161,-0.497325922631234,
-1.14075270757178));
#23545=CARTESIAN_POINT('Ctrl Pts',(95.395443787189,-0.502819772320877,-1.14034716341966));
#23546=CARTESIAN_POINT('Ctrl Pts',(95.4004153985107,-0.513211273847619,
-1.1395744967103));
#23547=CARTESIAN_POINT('Ctrl Pts',(95.4028023523809,-0.518112697665197,
-1.1392076632697));
#23548=CARTESIAN_POINT('Ctrl Pts',(95.4083181477115,-0.529241981979873,
-1.13836917810798));
#23549=CARTESIAN_POINT('Ctrl Pts',(95.4114683902067,-0.53545894687706,-1.13789679754734));
#23550=CARTESIAN_POINT('Ctrl Pts',(95.4213374349547,-0.554513997220439,
-1.13643638217215));
#23551=CARTESIAN_POINT('Ctrl Pts',(95.4282379070595,-0.56725592622167,-1.1354420774274));
#23552=CARTESIAN_POINT('Ctrl Pts',(95.4632361181719,-0.62912702703182,-1.13052404786013));
#23553=CARTESIAN_POINT('Ctrl Pts',(95.4946110860976,-0.676307479226715,
-1.12648582006652));
#23554=CARTESIAN_POINT('Ctrl Pts',(95.5669868263335,-0.769780827820381,
-1.11789205804334));
#23555=CARTESIAN_POINT('Ctrl Pts',(95.6084890700907,-0.815477652153749,
-1.11333495959732));
#23556=CARTESIAN_POINT('Ctrl Pts',(95.6821768532518,-0.884817369836728,
-1.10597255643867));
#23557=CARTESIAN_POINT('Ctrl Pts',(95.7123278684236,-0.910454116505678,
-1.10313099529562));
#23558=CARTESIAN_POINT('Ctrl Pts',(95.7486650249066,-0.938324075352465,
-1.09994622954635));
#23559=CARTESIAN_POINT('Ctrl Pts',(95.753645381812,-0.942081453666663,-1.09951469441509));
#23560=CARTESIAN_POINT('Ctrl Pts',(95.7617702695327,-0.948110485153555,
-1.09881901079236));
#23561=CARTESIAN_POINT('Ctrl Pts',(95.7648965016738,-0.950406430630044,
-1.09855330152303));
#23562=CARTESIAN_POINT('Ctrl Pts',(95.7704972583483,-0.954477260541574,
-1.09808086176581));
#23563=CARTESIAN_POINT('Ctrl Pts',(95.7729673764979,-0.956258031380015,
-1.09787373987894));
#23564=CARTESIAN_POINT('Ctrl Pts',(95.7783883697733,-0.960134299360713,
-1.0974218961112));
#23565=CARTESIAN_POINT('Ctrl Pts',(95.7813420108848,-0.962225785907608,
-1.09717744265485));
#23566=CARTESIAN_POINT('Ctrl Pts',(95.7898363360079,-0.968182058903928,
-1.09647923238217));
#23567=CARTESIAN_POINT('Ctrl Pts',(95.7954008035634,-0.972012912247251,
-1.09602767428959));
#23568=CARTESIAN_POINT('Ctrl Pts',(95.8370547656034,-1.00016437035739,-1.09268805648767));
#23569=CARTESIAN_POINT('Ctrl Pts',(95.8744389910636,-1.02251881222603,-1.08991540596361));
#23570=CARTESIAN_POINT('Ctrl Pts',(96.0016566312504,-1.08931485285468,-1.08090944030054));
#23571=CARTESIAN_POINT('Ctrl Pts',(96.0959065195447,-1.12437196226241,-1.07486860092377));
#23572=CARTESIAN_POINT('Ctrl Pts',(96.2173064670503,-1.15263214177568,-1.06685673614855));
#23573=CARTESIAN_POINT('Ctrl Pts',(96.2413218258221,-1.1574384765649,-1.06526352103096));
#23574=CARTESIAN_POINT('Ctrl Pts',(96.2741543962825,-1.16295101101242,-1.06306550008254));
#23575=CARTESIAN_POINT('Ctrl Pts',(96.2828564242327,-1.16431188240613,-1.06248107236912));
#23576=CARTESIAN_POINT('Ctrl Pts',(96.2967249274311,-1.16632162397627,-1.06154635589683));
#23577=CARTESIAN_POINT('Ctrl Pts',(96.3018819715535,-1.1670340732127,-1.06119805415939));
#23578=CARTESIAN_POINT('Ctrl Pts',(96.3124848960986,-1.16842729798062,-1.06048037372655));
#23579=CARTESIAN_POINT('Ctrl Pts',(96.3179311424039,-1.16910424395648,-1.06011088520195));
#23580=CARTESIAN_POINT('Ctrl Pts',(96.3305790794201,-1.17058663857696,-1.05925075190084));
#23581=CARTESIAN_POINT('Ctrl Pts',(96.3377838049122,-1.17136372699265,-1.05875923992152));
#23582=CARTESIAN_POINT('Ctrl Pts',(96.3609064790329,-1.17364203103342,-1.0571765795812));
#23583=CARTESIAN_POINT('Ctrl Pts',(96.376847411003,-1.17488556035057,-1.05607754560635));
#23584=CARTESIAN_POINT('Ctrl Pts',(96.4144788704661,-1.17705142234109,-1.05346313378178));
#23585=CARTESIAN_POINT('Ctrl Pts',(96.436178749755,-1.17769925801184,-1.05193992448423));
#23586=CARTESIAN_POINT('Ctrl Pts',(96.5617269039242,-1.17797620020088,-1.04303641956692));
#23587=CARTESIAN_POINT('Ctrl Pts',(96.6651405634321,-1.16446886721859,-1.03528776949736));
#23588=CARTESIAN_POINT('Ctrl Pts',(96.7951197415441,-1.12962714322742,-1.02556444795194));
#23589=CARTESIAN_POINT('Ctrl Pts',(96.8245006383974,-1.12050463434462,-1.02337224247196));
#23590=CARTESIAN_POINT('Ctrl Pts',(96.8595614623931,-1.10809351730552,-1.02078877066075));
#23591=CARTESIAN_POINT('Ctrl Pts',(96.8656120519584,-1.10589569731973,-1.02034413553984));
#23592=CARTESIAN_POINT('Ctrl Pts',(96.8750088372945,-1.10239493043487,-1.01965581053436));
#23593=CARTESIAN_POINT('Ctrl Pts',(96.8783674972106,-1.10112614468873,-1.01941022754282));
#23594=CARTESIAN_POINT('Ctrl Pts',(96.8845665795091,-1.09875189659968,-1.01895784271981));
#23595=CARTESIAN_POINT('Ctrl Pts',(96.8874085090051,-1.09765076921486,-1.01875080425368));
#23596=CARTESIAN_POINT('Ctrl Pts',(96.8938195606446,-1.09513809205787,-1.01828452367841));
#23597=CARTESIAN_POINT('Ctrl Pts',(96.8973860810425,-1.09372011943526,-1.01802566373096));
#23598=CARTESIAN_POINT('Ctrl Pts',(96.908187517084,-1.08936443136305,-1.01724313251011));
#23599=CARTESIAN_POINT('Ctrl Pts',(96.9154003826095,-1.08637210585536,-1.01672255399734));
#23600=CARTESIAN_POINT('Ctrl Pts',(96.932261770753,-1.07917961394909,-1.01550904237972));
#23601=CARTESIAN_POINT('Ctrl Pts',(96.9418849612362,-1.07492138170674,-1.01481913043827));
#23602=CARTESIAN_POINT('Ctrl Pts',(96.9754710792321,-1.0595180965846,-1.01241626403282));
#23603=CARTESIAN_POINT('Ctrl Pts',(96.999116082,-1.04769547718561,-1.01073359862451));
#23604=CARTESIAN_POINT('Ctrl Pts',(97.1009420444648,-0.992422492754522,
-1.00344255079753));
#23605=CARTESIAN_POINT('Ctrl Pts',(97.1744240522513,-0.940945761401129,
-0.998039341482925));
#23606=CARTESIAN_POINT('Ctrl Pts',(97.2691348069077,-0.857058496987549,
-0.990023897388688));
#23607=CARTESIAN_POINT('Ctrl Pts',(97.2957164893404,-0.831174769270511,
-0.987637552706962));
#23608=CARTESIAN_POINT('Ctrl Pts',(97.327994502585,-0.796629977571779,-0.984526096777031));
#23609=CARTESIAN_POINT('Ctrl Pts',(97.3348604807485,-0.789087771151467,
-0.983850997318281));
#23610=CARTESIAN_POINT('Ctrl Pts',(97.3456654839905,-0.776904395144889,
-0.982766560201739));
#23611=CARTESIAN_POINT('Ctrl Pts',(97.3496680841486,-0.772320099780294,
-0.98235985806375));
#23612=CARTESIAN_POINT('Ctrl Pts',(97.3571863493935,-0.763573292261414,
-0.981586278932822));
#23613=CARTESIAN_POINT('Ctrl Pts',(97.3607090205332,-0.759416990373271,
-0.981219701023391));
#23614=CARTESIAN_POINT('Ctrl Pts',(97.3686519997188,-0.74991236064334,-0.980383602493388));
#23615=CARTESIAN_POINT('Ctrl Pts',(97.3730541031154,-0.744549152735319,
-0.979913368477185));
#23616=CARTESIAN_POINT('Ctrl Pts',(97.3857719141876,-0.728772448150182,
-0.978534400550419));
#23617=CARTESIAN_POINT('Ctrl Pts',(97.3939583448664,-0.718256623781256,
-0.977620639102936));
#23618=CARTESIAN_POINT('Ctrl Pts',(97.4359300948534,-0.662412288907622,
-0.972794101565266));
#23619=CARTESIAN_POINT('Ctrl Pts',(97.4665929336296,-0.614839873319073,
-0.96876535672004));
#23620=CARTESIAN_POINT('Ctrl Pts',(97.516707567981,-0.523234832625769,-0.961180454725356));
#23621=CARTESIAN_POINT('Ctrl Pts',(97.5371109118217,-0.479851024723814,
-0.957654073463454));
#23622=CARTESIAN_POINT('Ctrl Pts',(97.5748625466004,-0.384954599822675,
-0.950172572279888));
#23623=CARTESIAN_POINT('Ctrl Pts',(97.5914075263396,-0.333230945947142,
-0.946230811720642));
#23624=CARTESIAN_POINT('Ctrl Pts',(97.6058621785013,-0.274296024846149,
-0.942008102137619));
#23625=CARTESIAN_POINT('Ctrl Pts',(97.607343771293,-0.268033844086378,-0.941562771856642));
#23626=CARTESIAN_POINT('Ctrl Pts',(97.6096490346917,-0.25792106385158,-0.940849346772095));
#23627=CARTESIAN_POINT('Ctrl Pts',(97.6105048269944,-0.254078030383814,
-0.94057956275809));
#23628=CARTESIAN_POINT('Ctrl Pts',(97.6119892382536,-0.247250930128726,
-0.940102738622853));
#23629=CARTESIAN_POINT('Ctrl Pts',(97.6126255566902,-0.244268635706022,
-0.939895276606408));
#23630=CARTESIAN_POINT('Ctrl Pts',(97.6139828345146,-0.237784038228632,
-0.939445992250417));
#23631=CARTESIAN_POINT('Ctrl Pts',(97.6146994321108,-0.234280905794114,
-0.939204414362909));
#23632=CARTESIAN_POINT('Ctrl Pts',(97.6161480392174,-0.227031300609771,
-0.938706722046309));
#23633=CARTESIAN_POINT('Ctrl Pts',(97.6168778118979,-0.223284418018694,
-0.93845073090803));
#23634=CARTESIAN_POINT('Ctrl Pts',(97.6187096775019,-0.213629115425764,
-0.937794093620395));
#23635=CARTESIAN_POINT('Ctrl Pts',(97.619784799232,-0.207715605748008,-0.937394836571943));
#23636=CARTESIAN_POINT('Ctrl Pts',(97.6323431383334,-0.135504017529939,
-0.932551945019631));
#23637=CARTESIAN_POINT('Ctrl Pts',(97.6381710435508,-0.0683401826375768,
-0.928377508108212));
#23638=CARTESIAN_POINT('Ctrl Pts',(97.6382304901167,-0.00104031656738834,
-0.924212313232804));
#23639=CARTESIAN_POINT('Ctrl Pts',(97.6382304897404,-0.00104074251348296,
-0.924212339594643));
#23640=CARTESIAN_POINT('Ctrl Pts',(97.6383086585134,0.087418444371562,-0.918737592289391));
#23641=CARTESIAN_POINT('Ctrl Pts',(97.6284213334225,0.175597665774794,-0.913292158566966));
#23642=CARTESIAN_POINT('Ctrl Pts',(97.6065569748955,0.271482309211362,-0.906868613012748));
#23643=CARTESIAN_POINT('Ctrl Pts',(97.6042365879264,0.281097723819844,-0.906219031606458));
#23644=CARTESIAN_POINT('Ctrl Pts',(97.600193161266,0.296973535564489,-0.905136898968108));
#23645=CARTESIAN_POINT('Ctrl Pts',(97.5985389424447,0.303251064941707,-0.904706498433585));
#23646=CARTESIAN_POINT('Ctrl Pts',(97.595199203206,0.315512588634975,-0.903860721769332));
#23647=CARTESIAN_POINT('Ctrl Pts',(97.5935180317108,0.321497553204364,-0.903445495359054));
#23648=CARTESIAN_POINT('Ctrl Pts',(97.5902799656531,0.332684120375035,-0.902664763176757));
#23649=CARTESIAN_POINT('Ctrl Pts',(97.5887343240487,0.337888830799272,-0.902299627870652));
#23650=CARTESIAN_POINT('Ctrl Pts',(97.5851908284601,0.349525552391896,-0.901478925396652));
#23651=CARTESIAN_POINT('Ctrl Pts',(97.5831736901027,0.355951444083561,-0.901022745579801));
#23652=CARTESIAN_POINT('Ctrl Pts',(97.5778954730715,0.372274675046682,-0.899856163598356));
#23653=CARTESIAN_POINT('Ctrl Pts',(97.574558004916,0.382146508122994,-0.899143310330824));
#23654=CARTESIAN_POINT('Ctrl Pts',(97.5483577604015,0.456381898599413,-0.893725681538761));
#23655=CARTESIAN_POINT('Ctrl Pts',(97.5200696032039,0.51868038345569,-0.888841803407394));
#23656=CARTESIAN_POINT('Ctrl Pts',(97.4578171927982,0.62915903863508,-0.879591269695259));
#23657=CARTESIAN_POINT('Ctrl Pts',(97.4253242814016,0.677936570523005,-0.875265808775647));
#23658=CARTESIAN_POINT('Ctrl Pts',(97.3742360092596,0.743471784678426,-0.869234871334851));
#23659=CARTESIAN_POINT('Ctrl Pts',(97.3585282978016,0.762371116019068,-0.867467677670331));
#23660=CARTESIAN_POINT('Ctrl Pts',(97.3324854923082,0.791782575044832,-0.864688149693622));
#23661=CARTESIAN_POINT('Ctrl Pts',(97.3225248755267,0.802615653912336,-0.863657628258942));
#23662=CARTESIAN_POINT('Ctrl Pts',(97.3090232215204,0.816758515284516,-0.862306379825623));
#23663=CARTESIAN_POINT('Ctrl Pts',(97.3056615460485,0.820236685932479,-0.861973580504424));
#23664=CARTESIAN_POINT('Ctrl Pts',(97.2999932433029,0.826029568315095,-0.861418636342975));
#23665=CARTESIAN_POINT('Ctrl Pts',(97.297698277208,0.828355531172675,-0.861195631753239));
#23666=CARTESIAN_POINT('Ctrl Pts',(97.2931943594301,0.832882442247074,-0.860761303963134));
#23667=CARTESIAN_POINT('Ctrl Pts',(97.2909863061762,0.835084210460701,-0.860549919913104));
#23668=CARTESIAN_POINT('Ctrl Pts',(97.2860290374284,0.839988260136294,-0.860078716670001));
#23669=CARTESIAN_POINT('Ctrl Pts',(97.283275220611,0.842685891132548,-0.859819253064847));
#23670=CARTESIAN_POINT('Ctrl Pts',(97.2736731780032,0.852000080448579,-0.858922262303198));
#23671=CARTESIAN_POINT('Ctrl Pts',(97.2667577717605,0.858547283259369,-0.858289739748856));
#23672=CARTESIAN_POINT('Ctrl Pts',(97.2041614266855,0.916387256190625,-0.852675312332903));
#23673=CARTESIAN_POINT('Ctrl Pts',(97.1437268687053,0.962291315162671,-0.848022311707098));
#23674=CARTESIAN_POINT('Ctrl Pts',(97.0317799325913,1.03142195284057,-0.839883340416475));
#23675=CARTESIAN_POINT('Ctrl Pts',(96.9822399099621,1.05734607375344,-0.836423171278922));
#23676=CARTESIAN_POINT('Ctrl Pts',(96.9121810818576,1.08788132197737,-0.831546596753414));
#23677=CARTESIAN_POINT('Ctrl Pts',(96.8930996430919,1.09560931547076,-0.830220522303214));
#23678=CARTESIAN_POINT('Ctrl Pts',(96.8595783497304,1.10817320368518,-0.827887145797917));
#23679=CARTESIAN_POINT('Ctrl Pts',(96.8452288074174,1.11323655871224,-0.8268871324083));
#23680=CARTESIAN_POINT('Ctrl Pts',(96.8239702546377,1.12027770391992,-0.825401969000131));
#23681=CARTESIAN_POINT('Ctrl Pts',(96.8171344230728,1.12247267442038,-0.824923858800875));
#23682=CARTESIAN_POINT('Ctrl Pts',(96.805047722053,1.1262321326089,-0.824077332517465));
#23683=CARTESIAN_POINT('Ctrl Pts',(96.7998051562549,1.12782275125519,-0.823709772586361));
#23684=CARTESIAN_POINT('Ctrl Pts',(96.7888351222316,1.13106769875277,-0.822939767869058));
#23685=CARTESIAN_POINT('Ctrl Pts',(96.7831058223476,1.13271522947239,-0.822537116264939));
#23686=CARTESIAN_POINT('Ctrl Pts',(96.7680899635722,1.13691005976559,-0.821480371550895));
#23687=CARTESIAN_POINT('Ctrl Pts',(96.7587843968713,1.13938704278695,-0.820824053929541));
#23688=CARTESIAN_POINT('Ctrl Pts',(96.719082027392,1.14943543326278,-0.818017091343524));
#23689=CARTESIAN_POINT('Ctrl Pts',(96.6884224795003,1.15590599743773,-0.815832182778312));
#23690=CARTESIAN_POINT('Ctrl Pts',(96.548635955172,1.17962973600319,-0.805786667577385));
#23691=CARTESIAN_POINT('Ctrl Pts',(96.4376919078291,1.18269689179189,-0.797517192434202));
#23692=CARTESIAN_POINT('Ctrl Pts',(96.3019824333502,1.16732883216616,-0.787699858001737));
#23693=CARTESIAN_POINT('Ctrl Pts',(96.2761108158078,1.16352321708239,-0.785845713235984));
#23694=CARTESIAN_POINT('Ctrl Pts',(96.2445158475531,1.15779519717268,-0.783619116489122));
#23695=CARTESIAN_POINT('Ctrl Pts',(96.2386545234577,1.15668651082085,-0.783207664919409));
#23696=CARTESIAN_POINT('Ctrl Pts',(96.2294182374593,1.15486664943739,-0.782562113993727));
#23697=CARTESIAN_POINT('Ctrl Pts',(96.2260376408562,1.15418511976277,-0.782326431373008));
#23698=CARTESIAN_POINT('Ctrl Pts',(96.2196498366781,1.15286811215125,-0.781882289677524));
#23699=CARTESIAN_POINT('Ctrl Pts',(96.2166421454724,1.15223571668187,-0.781673675034372));
#23700=CARTESIAN_POINT('Ctrl Pts',(96.2096518414285,1.15073734234116,-0.781189959071717));
#23701=CARTESIAN_POINT('Ctrl Pts',(96.2056712047136,1.14986245599718,-0.780915359551082));
#23702=CARTESIAN_POINT('Ctrl Pts',(96.1925946986417,1.14691718881578,-0.78001585959267));
#23703=CARTESIAN_POINT('Ctrl Pts',(96.1835186039726,1.14475934324311,-0.77939563175275));
#23704=CARTESIAN_POINT('Ctrl Pts',(96.0952879351267,1.12267165523643,-0.773397712272924));
#23705=CARTESIAN_POINT('Ctrl Pts',(96.0183700125523,1.09466867527989,-0.768406168752027));
#23706=CARTESIAN_POINT('Ctrl Pts',(95.9371961092389,1.05515049884195,-0.762817833787108));
#23707=CARTESIAN_POINT('Ctrl Pts',(95.9294766873309,1.05128684229111,-0.762283141374746));
#23708=CARTESIAN_POINT('Ctrl Pts',(95.921801662562,1.04733933767479,-0.761747732816352));
#23709=CARTESIAN_POINT('Ctrl Pts',(95.9218016734189,1.0473393432588,-0.661999947661213));
#23710=CARTESIAN_POINT('Ctrl Pts',(95.9364629898361,1.05488011537431,-0.663056383341802));
#23711=CARTESIAN_POINT('Ctrl Pts',(95.9512808635733,1.06211211395517,-0.664121325308709));
#23712=CARTESIAN_POINT('Ctrl Pts',(95.9800444240408,1.07541011441399,-0.666187360446632));
#23713=CARTESIAN_POINT('Ctrl Pts',(95.9939649700543,1.08152160207347,-0.667186733626535));
#23714=CARTESIAN_POINT('Ctrl Pts',(96.0145585472731,1.09009116398921,-0.668666374329298));
#23715=CARTESIAN_POINT('Ctrl Pts',(96.0211421273872,1.09276114970359,-0.669139574791691));
#23716=CARTESIAN_POINT('Ctrl Pts',(96.0328362727037,1.09738097680985,-0.669980601250669));
#23717=CARTESIAN_POINT('Ctrl Pts',(96.0379370663037,1.09935510319017,-0.670347609583992));
#23718=CARTESIAN_POINT('Ctrl Pts',(96.0486614798548,1.1034200388425,-0.671119683938864));
#23719=CARTESIAN_POINT('Ctrl Pts',(96.0542876817077,1.10550354346032,-0.671524978474941));
#23720=CARTESIAN_POINT('Ctrl Pts',(96.0691451814749,1.11087686846875,-0.672596059602218));
#23721=CARTESIAN_POINT('Ctrl Pts',(96.0784018846483,1.11409455540222,-0.673264181047839));
#23722=CARTESIAN_POINT('Ctrl Pts',(96.1188904782369,1.12760469767797,-0.676190742391172));
#23723=CARTESIAN_POINT('Ctrl Pts',(96.1505028425569,1.13670119768807,-0.678487153149228));
#23724=CARTESIAN_POINT('Ctrl Pts',(96.2813715526448,1.16849368462877,-0.688045630061959));
#23725=CARTESIAN_POINT('Ctrl Pts',(96.3829853628467,1.17959616510827,-0.6956353657113));
#23726=CARTESIAN_POINT('Ctrl Pts',(96.506341910909,1.17705515656634,-0.704558159220456));
#23727=CARTESIAN_POINT('Ctrl Pts',(96.5279326870397,1.17601549562344,-0.706106850385334));
#23728=CARTESIAN_POINT('Ctrl Pts',(96.5630025435627,1.17335765647055,-0.708589530377186));
#23729=CARTESIAN_POINT('Ctrl Pts',(96.576503275776,1.17209970839442,-0.709537301584107));
#23730=CARTESIAN_POINT('Ctrl Pts',(96.5947231405698,1.17008412928468,-0.710802972999195));
#23731=CARTESIAN_POINT('Ctrl Pts',(96.5994631764258,1.16953058020455,-0.711131017103561));
#23732=CARTESIAN_POINT('Ctrl Pts',(96.6073637098083,1.16855923203408,-0.711675593546746));
#23733=CARTESIAN_POINT('Ctrl Pts',(96.6105260640824,1.16815739022837,-0.711892983658442));
#23734=CARTESIAN_POINT('Ctrl Pts',(96.6165083919057,1.1673725190118,-0.712303065080476));
#23735=CARTESIAN_POINT('Ctrl Pts',(96.6193286681096,1.16699210094103,-0.712495903030268));
#23736=CARTESIAN_POINT('Ctrl Pts',(96.6260029597358,1.16606718335122,-0.712951163109775));
#23737=CARTESIAN_POINT('Ctrl Pts',(96.6298557393433,1.1655137895343,-0.713213096913204));
#23738=CARTESIAN_POINT('Ctrl Pts',(96.6433388042446,1.16350888032907,-0.714126933638863));
#23739=CARTESIAN_POINT('Ctrl Pts',(96.6529540818923,1.16195697769463,-0.714773583129072));
#23740=CARTESIAN_POINT('Ctrl Pts',(96.733275287522,1.14796871871588,-0.720141457338891));
#23741=CARTESIAN_POINT('Ctrl Pts',(96.8027372298633,1.12920877610411,-0.724568867338573));
#23742=CARTESIAN_POINT('Ctrl Pts',(96.9248360783268,1.08391970457276,-0.732624184268632));
#23743=CARTESIAN_POINT('Ctrl Pts',(96.9780156332161,1.05955877934321,-0.736235742921371));
#23744=CARTESIAN_POINT('Ctrl Pts',(97.0476663566816,1.02115359429345,-0.741306206675936));
#23745=CARTESIAN_POINT('Ctrl Pts',(97.0658875633551,1.01045738059093,-0.742666079276758));
#23746=CARTESIAN_POINT('Ctrl Pts',(97.0970967739225,0.990989690156382,-0.745062429332714));
#23747=CARTESIAN_POINT('Ctrl Pts',(97.1102159001589,0.982438155994047,-0.74609128565934));
#23748=CARTESIAN_POINT('Ctrl Pts',(97.1291014086619,0.969584135052225,-0.747606300793059));
#23749=CARTESIAN_POINT('Ctrl Pts',(97.135005412813,0.965486125182712,-0.748084887153543));
#23750=CARTESIAN_POINT('Ctrl Pts',(97.1453438961868,0.958168998467339,-0.748931938084149));
#23751=CARTESIAN_POINT('Ctrl Pts',(97.1497941485706,0.954972458883899,-0.749299542748041));
#23752=CARTESIAN_POINT('Ctrl Pts',(97.1590362122003,0.948235783044142,-0.750069324082935));
#23753=CARTESIAN_POINT('Ctrl Pts',(97.1638237799105,0.94469011636331,-0.750471705422107));
#23754=CARTESIAN_POINT('Ctrl Pts',(97.1762653599038,0.935328895676632,-0.751527024748737));
#23755=CARTESIAN_POINT('Ctrl Pts',(97.1838753052197,0.929455788017907,-0.752182176419098));
#23756=CARTESIAN_POINT('Ctrl Pts',(97.2158650944623,0.904136258982206,-0.754978289253158));
#23757=CARTESIAN_POINT('Ctrl Pts',(97.2395373590085,0.883820332112883,-0.757153190553328));
#23758=CARTESIAN_POINT('Ctrl Pts',(97.3230834137621,0.806153143673275,-0.765233831574081));
#23759=CARTESIAN_POINT('Ctrl Pts',(97.3776590029529,0.743469572574596,-0.771343906035278));
#23760=CARTESIAN_POINT('Ctrl Pts',(97.4550729439242,0.632925465513976,-0.78122276206864));
#23761=CARTESIAN_POINT('Ctrl Pts',(97.4820908520014,0.588321667040079,-0.785001348935371));
#23762=CARTESIAN_POINT('Ctrl Pts',(97.5092707763867,0.535894907652004,-0.789108667124561));
#23763=CARTESIAN_POINT('Ctrl Pts',(97.5124178080195,0.529690763148121,-0.789589615302407));
#23764=CARTESIAN_POINT('Ctrl Pts',(97.5171369422625,0.520179371647318,-0.790318776711186));
#23765=CARTESIAN_POINT('Ctrl Pts',(97.5187488345946,0.51689220348368,-0.790569302008806));
#23766=CARTESIAN_POINT('Ctrl Pts',(97.5216718952282,0.510860149295372,-0.791026257014491));
#23767=CARTESIAN_POINT('Ctrl Pts',(97.5229877632403,0.508117689749636,-0.791232962559423));
#23768=CARTESIAN_POINT('Ctrl Pts',(97.5259347077451,0.50191432424975,-0.791698181688278));
#23769=CARTESIAN_POINT('Ctrl Pts',(97.5275595555245,0.498450548644316,-0.791956316970774));
#23770=CARTESIAN_POINT('Ctrl Pts',(97.5317160450122,0.489476459223481,-0.792621059105246));
#23771=CARTESIAN_POINT('Ctrl Pts',(97.5342220983695,0.48395431916189,-0.793026181248575));
#23772=CARTESIAN_POINT('Ctrl Pts',(97.5507723214078,0.4467240865121,-0.795732877469607));
#23773=CARTESIAN_POINT('Ctrl Pts',(97.5634542240544,0.414425080495898,-0.797961747330944));
#23774=CARTESIAN_POINT('Ctrl Pts',(97.5838553061855,0.354858711720401,-0.801940071729448));
#23775=CARTESIAN_POINT('Ctrl Pts',(97.5920514688766,0.327784886331824,-0.803700672873348));
#23776=CARTESIAN_POINT('Ctrl Pts',(97.611552769411,0.253867706702854,-0.808440303346063));
#23777=CARTESIAN_POINT('Ctrl Pts',(97.6209712296247,0.206584995324231,-0.811402315078615));
#23778=CARTESIAN_POINT('Ctrl Pts',(97.6346252616797,0.106281655342046,-0.817733744051123));
#23779=CARTESIAN_POINT('Ctrl Pts',(97.6382203381726,0.053287107128603,-0.821107559137969));
#23780=CARTESIAN_POINT('Ctrl Pts',(97.6382330599325,-0.0104561322608248,
-0.825297117237775));
#23781=CARTESIAN_POINT('Ctrl Pts',(97.6380896175091,-0.0211465433735564,
-0.826004033500973));
#23782=CARTESIAN_POINT('Ctrl Pts',(97.6376316346255,-0.0380845801419116,
-0.827131542462318));
#23783=CARTESIAN_POINT('Ctrl Pts',(97.6374128209864,-0.0443343892726304,
-0.827549181359122));
#23784=CARTESIAN_POINT('Ctrl Pts',(97.6369112599392,-0.0560019347455081,
-0.828331997261579));
#23785=CARTESIAN_POINT('Ctrl Pts',(97.636640831053,-0.0614200566131054,
-0.828696783700735));
#23786=CARTESIAN_POINT('Ctrl Pts',(97.6359537790895,-0.0735074191600985,
-0.829513507860688));
#23787=CARTESIAN_POINT('Ctrl Pts',(97.6355178116109,-0.0801753283364768,
-0.829966032415147));
#23788=CARTESIAN_POINT('Ctrl Pts',(97.6340645211051,-0.0998318529038032,
-0.831306089108352));
#23789=CARTESIAN_POINT('Ctrl Pts',(97.6328884199717,-0.112807348893192,
-0.832198484732599));
#23790=CARTESIAN_POINT('Ctrl Pts',(97.6297173567158,-0.14233470580817,-0.834247829698772));
#23791=CARTESIAN_POINT('Ctrl Pts',(97.6275857481215,-0.158868768057103,
-0.835408766385599));
#23792=CARTESIAN_POINT('Ctrl Pts',(97.6191843326564,-0.214668073363343,
-0.839372994425729));
#23793=CARTESIAN_POINT('Ctrl Pts',(97.6112780392822,-0.253656121319864,
-0.842222031824925));
#23794=CARTESIAN_POINT('Ctrl Pts',(97.5798595401621,-0.376348045643641,
-0.851415911361136));
#23795=CARTESIAN_POINT('Ctrl Pts',(97.5490532383205,-0.457882691521918,
-0.857892394180007));
#23796=CARTESIAN_POINT('Ctrl Pts',(97.5008638045821,-0.552326488151946,
-0.865449411361776));
#23797=CARTESIAN_POINT('Ctrl Pts',(97.4917545400068,-0.569153686263592,
-0.866797007090072));
#23798=CARTESIAN_POINT('Ctrl Pts',(97.479445922915,-0.590624227565583,-0.868511142747838));
#23799=CARTESIAN_POINT('Ctrl Pts',(97.4766182407359,-0.59547594724229,-0.868898125823845));
#23800=CARTESIAN_POINT('Ctrl Pts',(97.4720376768403,-0.603207604083673,
-0.86951401353318));
#23801=CARTESIAN_POINT('Ctrl Pts',(97.4703069868448,-0.606100487770441,
-0.869744272550769));
#23802=CARTESIAN_POINT('Ctrl Pts',(97.4669616285834,-0.611638215781978,
-0.870184638819007));
#23803=CARTESIAN_POINT('Ctrl Pts',(97.4653489236494,-0.614284151772185,
-0.870394858972442));
#23804=CARTESIAN_POINT('Ctrl Pts',(97.4614662538408,-0.620598171260433,
-0.87089612352806));
#23805=CARTESIAN_POINT('Ctrl Pts',(97.4591865165201,-0.624260251448492,
-0.871186543030097));
#23806=CARTESIAN_POINT('Ctrl Pts',(97.4513063131519,-0.636765040740172,
-0.872177462365222));
#23807=CARTESIAN_POINT('Ctrl Pts',(97.445607923305,-0.645545879421991,-0.872871962075723));
#23808=CARTESIAN_POINT('Ctrl Pts',(97.431356556009,-0.666877995032726,-0.874558952767379));
#23809=CARTESIAN_POINT('Ctrl Pts',(97.4226762372897,-0.679342312322195,
-0.875544470109523));
#23810=CARTESIAN_POINT('Ctrl Pts',(97.3858597484775,-0.73008617064834,-0.879571334097706));
#23811=CARTESIAN_POINT('Ctrl Pts',(97.3556596198792,-0.766816525818167,
-0.882522643548181));
#23812=CARTESIAN_POINT('Ctrl Pts',(97.262815909318,-0.866750201997286,-0.890967695748882));
#23813=CARTESIAN_POINT('Ctrl Pts',(97.195139872809,-0.924808865377008,-0.896431141247991));
#23814=CARTESIAN_POINT('Ctrl Pts',(97.1091212346914,-0.983151824155626,
-0.903209272507031));
#23815=CARTESIAN_POINT('Ctrl Pts',(97.0965010015412,-0.991362793789658,
-0.904199166048572));
#23816=CARTESIAN_POINT('Ctrl Pts',(97.0777877142271,-1.00303360925367,-0.905662273844377));
#23817=CARTESIAN_POINT('Ctrl Pts',(97.0718153383039,-1.00668481889584,-0.906128536172065));
#23818=CARTESIAN_POINT('Ctrl Pts',(97.0611186071721,-1.01309396823462,-0.90696259212058));
#23819=CARTESIAN_POINT('Ctrl Pts',(97.0564068781327,-1.01587266433764,-0.907329626121802));
#23820=CARTESIAN_POINT('Ctrl Pts',(97.0464954663069,-1.02162514036508,-0.9081010588962));
#23821=CARTESIAN_POINT('Ctrl Pts',(97.0412921244421,-1.02459226920312,-0.908505681440112));
#23822=CARTESIAN_POINT('Ctrl Pts',(97.0275510820101,-1.03228958749823,-0.909573379851047));
#23823=CARTESIAN_POINT('Ctrl Pts',(97.0189769697442,-1.03695347681059,-0.910238765731383));
#23824=CARTESIAN_POINT('Ctrl Pts',(96.9782034694051,-1.0584798412583,-0.913399825408443));
#23825=CARTESIAN_POINT('Ctrl Pts',(96.9452958379927,-1.07395075137319,-0.915942825457955));
#23826=CARTESIAN_POINT('Ctrl Pts',(96.8518298193367,-1.11272022504236,-0.923146922954997));
#23827=CARTESIAN_POINT('Ctrl Pts',(96.7899868929997,-1.13257426486221,-0.927898884795009));
#23828=CARTESIAN_POINT('Ctrl Pts',(96.6687688262731,-1.16071712233671,-0.937030744841404));
#23829=CARTESIAN_POINT('Ctrl Pts',(96.6097603389875,-1.16977141667093,-0.941394804668176));
#23830=CARTESIAN_POINT('Ctrl Pts',(96.5403259504138,-1.17508306141429,-0.946278057080083));
#23831=CARTESIAN_POINT('Ctrl Pts',(96.5303272461704,-1.17571975267062,-0.946975085815661));
#23832=CARTESIAN_POINT('Ctrl Pts',(96.5163875633473,-1.17642892978298,-0.947937171859414));
#23833=CARTESIAN_POINT('Ctrl Pts',(96.5124528452229,-1.17660932321249,-0.948207664455452));
#23834=CARTESIAN_POINT('Ctrl Pts',(96.5056623400249,-1.17688651467025,-0.948672543901359));
#23835=CARTESIAN_POINT('Ctrl Pts',(96.5028070003501,-1.17699266451657,-0.948867431213877));
#23836=CARTESIAN_POINT('Ctrl Pts',(96.4967809819985,-1.17719472991313,-0.949277444915885));
#23837=CARTESIAN_POINT('Ctrl Pts',(96.4936102505795,-1.17728822908428,-0.949492430727119));
#23838=CARTESIAN_POINT('Ctrl Pts',(96.4857388045422,-1.17748851831399,-0.950024357127457));
#23839=CARTESIAN_POINT('Ctrl Pts',(96.4810376913323,-1.17757997275575,-0.950340465236844));
#23840=CARTESIAN_POINT('Ctrl Pts',(96.4632871887172,-1.17781895525767,-0.951528498930309));
#23841=CARTESIAN_POINT('Ctrl Pts',(96.4502356311274,-1.1777777526242,-0.952390754216579));
#23842=CARTESIAN_POINT('Ctrl Pts',(96.4166974383298,-1.17711428709309,-0.954583652577698));
#23843=CARTESIAN_POINT('Ctrl Pts',(96.3962209057811,-1.17617421633128,-0.955900644425788));
#23844=CARTESIAN_POINT('Ctrl Pts',(96.3181160470024,-1.17054239801406,-0.960875365005902));
#23845=CARTESIAN_POINT('Ctrl Pts',(96.260834916314,-1.16214436896601,-0.964425195209515));
#23846=CARTESIAN_POINT('Ctrl Pts',(96.1307458494782,-1.13316542289944,-0.972677657563592));
#23847=CARTESIAN_POINT('Ctrl Pts',(96.0588499218609,-1.1097204251828,-0.977390384017675));
#23848=CARTESIAN_POINT('Ctrl Pts',(95.9801727207678,-1.07541015065771,-0.983023647018109));
#23849=CARTESIAN_POINT('Ctrl Pts',(95.9707057633553,-1.07113175780031,-0.983709433781056));
#23850=CARTESIAN_POINT('Ctrl Pts',(95.9552057322682,-1.06387839726196,-0.98484609598705));
#23851=CARTESIAN_POINT('Ctrl Pts',(95.9491392174156,-1.06097592771404,-0.98529451216392));
#23852=CARTESIAN_POINT('Ctrl Pts',(95.9382215580635,-1.05563708563713,-0.986108099131242));
#23853=CARTESIAN_POINT('Ctrl Pts',(95.9333617349143,-1.05321880938616,-0.986472640373134));
#23854=CARTESIAN_POINT('Ctrl Pts',(95.9229669050034,-1.04795631540226,-0.987257597619469));
#23855=CARTESIAN_POINT('Ctrl Pts',(95.9174373965677,-1.04510166207645,-0.987678366856772));
#23856=CARTESIAN_POINT('Ctrl Pts',(95.9023448805737,-1.03715791401725,-0.988835824792488));
#23857=CARTESIAN_POINT('Ctrl Pts',(95.8928292558602,-1.03198059631003,-0.989575572150987));
#23858=CARTESIAN_POINT('Ctrl Pts',(95.8368804603039,-1.00053169979989,-0.99398591923486));
#23859=CARTESIAN_POINT('Ctrl Pts',(95.7922110089307,-0.97126467362705,-0.997762500058218));
#23860=CARTESIAN_POINT('Ctrl Pts',(95.7114429941515,-0.910130414409999,
-1.00508384332328));
#23861=CARTESIAN_POINT('Ctrl Pts',(95.6750076364499,-0.87887796122329,-1.00860611030077));
#23862=CARTESIAN_POINT('Ctrl Pts',(95.6203286827153,-0.825854152109581,
-1.01419435155083));
#23863=CARTESIAN_POINT('Ctrl Pts',(95.6007880204675,-0.805493062599604,
-1.01626050349363));
#23864=CARTESIAN_POINT('Ctrl Pts',(95.558919682293,-0.758605820046568,-1.02081808083479));
#23865=CARTESIAN_POINT('Ctrl Pts',(95.5369916386512,-0.731753713375162,
-1.02329704561381));
#23866=CARTESIAN_POINT('Ctrl Pts',(95.5126536833978,-0.699110360447521,
-1.02612715181856));
#23867=CARTESIAN_POINT('Ctrl Pts',(95.5090671600995,-0.694221598380876,
-1.0265463634253));
#23868=CARTESIAN_POINT('Ctrl Pts',(95.5032793506121,-0.686203175293688,
-1.02722614408863));
#23869=CARTESIAN_POINT('Ctrl Pts',(95.501055332221,-0.68309017314326,-1.02748816292223));
#23870=CARTESIAN_POINT('Ctrl Pts',(95.4970901992691,-0.677482530060515,
-1.02795668665863));
#23871=CARTESIAN_POINT('Ctrl Pts',(95.4953435499329,-0.674991938295483,
-1.02816355531423));
#23872=CARTESIAN_POINT('Ctrl Pts',(95.491515730881,-0.669488517307791,-1.0286179816869));
#23873=CARTESIAN_POINT('Ctrl Pts',(95.4894389510797,-0.66647273606291,-1.02886524777872));
#23874=CARTESIAN_POINT('Ctrl Pts',(95.483456303712,-0.657697747229589,-1.02957980500443));
#23875=CARTESIAN_POINT('Ctrl Pts',(95.4795872886293,-0.65191342755589,-1.03004473398207));
#23876=CARTESIAN_POINT('Ctrl Pts',(95.4471304308481,-0.602446034605347,
-1.03397239308707));
#23877=CARTESIAN_POINT('Ctrl Pts',(95.4214210890852,-0.556934978372629,
-1.03726857012283));
#23878=CARTESIAN_POINT('Ctrl Pts',(95.3627947996074,-0.434859718245381,
-1.04570414474662));
#23879=CARTESIAN_POINT('Ctrl Pts',(95.334825760757,-0.356255333865905,-1.05076727746285));
#23880=CARTESIAN_POINT('Ctrl Pts',(95.3081726300709,-0.245416176256265,
-1.0580384836508));
#23881=CARTESIAN_POINT('Ctrl Pts',(95.3021499059042,-0.215203392687433,
-1.06003091121837));
#23882=CARTESIAN_POINT('Ctrl Pts',(95.2958166060167,-0.175338632095473,
-1.06269108271575));
#23883=CARTESIAN_POINT('Ctrl Pts',(95.2944301970145,-0.165868329187757,
-1.06332528118222));
#23884=CARTESIAN_POINT('Ctrl Pts',(95.2923695648052,-0.150486673043233,
-1.0643594581132));
#23885=CARTESIAN_POINT('Ctrl Pts',(95.2916244217879,-0.144585134941193,
-1.064757221713));
#23886=CARTESIAN_POINT('Ctrl Pts',(95.2902785382022,-0.13323449455988,-1.0655242459885));
#23887=CARTESIAN_POINT('Ctrl Pts',(95.28967107375,-0.12778633358409,-1.06589328701754));
#23888=CARTESIAN_POINT('Ctrl Pts',(95.2883531287802,-0.115166695595001,
-1.0667502294786));
#23889=CARTESIAN_POINT('Ctrl Pts',(95.2876703982411,-0.107992605025229,
-1.06723897819552));
#23890=CARTESIAN_POINT('Ctrl Pts',(95.2857038142906,-0.0851022316291078,
-1.06880373721008));
#23891=CARTESIAN_POINT('Ctrl Pts',(95.2846697774355,-0.0693668014803647,
-1.06988738534283));
#23892=CARTESIAN_POINT('Ctrl Pts',(95.2829814992773,-0.0323198677853692,
-1.07245867997688));
#23893=CARTESIAN_POINT('Ctrl Pts',(95.2825894538957,-0.0110025455210621,
-1.07395381334175));
#23894=CARTESIAN_POINT('Ctrl Pts',(95.2832958240645,0.0696655465751871,
-1.07967091597221));
#23895=CARTESIAN_POINT('Ctrl Pts',(95.2883015500523,0.128888087748305,-1.0839953064675));
#23896=CARTESIAN_POINT('Ctrl Pts',(95.3089594990387,0.257010355248906,-1.09351567142917));
#23897=CARTESIAN_POINT('Ctrl Pts',(95.3263872522775,0.325406276291022,-1.09870646706054));
#23898=CARTESIAN_POINT('Ctrl Pts',(95.3530859251549,0.401082778088738,-1.10433096369587));
#23899=CARTESIAN_POINT('Ctrl Pts',(95.3564623499083,0.410285366747129,-1.10501267081146));
#23900=CARTESIAN_POINT('Ctrl Pts',(95.361341904844,0.423088197630725,-1.1059568866104));
#23901=CARTESIAN_POINT('Ctrl Pts',(95.3627485102137,0.426724448892171,-1.10622458552055));
#23902=CARTESIAN_POINT('Ctrl Pts',(95.3652134909631,0.433003882509279,-1.10668596653439));
#23903=CARTESIAN_POINT('Ctrl Pts',(95.3662634309993,0.435650307751988,-1.10688013221717));
#23904=CARTESIAN_POINT('Ctrl Pts',(95.3685078060775,0.441248062871026,-1.10729020049469));
#23905=CARTESIAN_POINT('Ctrl Pts',(95.3697046331004,0.444198409524226,-1.10750595419461));
#23906=CARTESIAN_POINT('Ctrl Pts',(95.3727200827119,0.451546236355939,-1.10804243420447));
#23907=CARTESIAN_POINT('Ctrl Pts',(95.3745534441821,0.455937673384402,-1.10836229647333));
#23908=CARTESIAN_POINT('Ctrl Pts',(95.3816772124449,0.47271443729813,-1.10958178577495));
#23909=CARTESIAN_POINT('Ctrl Pts',(95.3871535372487,0.485020356737484,-1.11047107029077));
#23910=CARTESIAN_POINT('Ctrl Pts',(95.4018801592111,0.516641006949897,-1.11274934481456));
#23911=CARTESIAN_POINT('Ctrl Pts',(95.41144852683,0.535802809709676,-1.11412330859376));
#23912=CARTESIAN_POINT('Ctrl Pts',(95.4482697276092,0.604769195517504,-1.11908177095763));
#23913=CARTESIAN_POINT('Ctrl Pts',(95.4785915650294,0.652848602089483,-1.12256750481667));
#23914=CARTESIAN_POINT('Ctrl Pts',(95.5567665849524,0.758963043773968,-1.13072926237198));
#23915=CARTESIAN_POINT('Ctrl Pts',(95.606932850112,0.814971171217068,-1.1354167201004));
#23916=CARTESIAN_POINT('Ctrl Pts',(95.6697228026192,0.872871515946718,-1.14102220016301));
#23917=CARTESIAN_POINT('Ctrl Pts',(95.6774578800606,0.87981702172781,-1.14170843478696));
#23918=CARTESIAN_POINT('Ctrl Pts',(95.6903482202763,0.891086919034153,-1.14284568830409));
#23919=CARTESIAN_POINT('Ctrl Pts',(95.6954505060365,0.895471236455041,-1.14329424347457));
#23920=CARTESIAN_POINT('Ctrl Pts',(95.7047373812196,0.903314003893071,-1.14410798187684));
#23921=CARTESIAN_POINT('Ctrl Pts',(95.7089088830186,0.906787713760465,-1.14447253452396));
#23922=CARTESIAN_POINT('Ctrl Pts',(95.7179124988047,0.914180433564817,-1.14525740417223));
#23923=CARTESIAN_POINT('Ctrl Pts',(95.7227519324678,0.918090226473729,-1.14567807361662));
#23924=CARTESIAN_POINT('Ctrl Pts',(95.7360967157749,0.928697875632763,-1.14683496313205));
#23925=CARTESIAN_POINT('Ctrl Pts',(95.744663618575,0.935316950267519,-1.1475742367799));
#23926=CARTESIAN_POINT('Ctrl Pts',(95.7958643740815,0.973760901476376,-1.151973883182));
#23927=CARTESIAN_POINT('Ctrl Pts',(95.8405177347913,1.00278095157837,-1.15573961903063));
#23928=CARTESIAN_POINT('Ctrl Pts',(95.8984801375937,1.03509598674158,-1.16053550934039));
#23929=CARTESIAN_POINT('Ctrl Pts',(95.9100911605651,1.04131626169847,-1.16149161118946));
#23930=CARTESIAN_POINT('Ctrl Pts',(95.921801693794,1.04733935373837,-1.1624507611287));
#23931=CARTESIAN_POINT('Origin',(96.460480949577,-7.19464945638997E-16,
0.924367114736168));
#23932=CARTESIAN_POINT('',(95.9218016575013,1.0473393350719,-1.76247028589786));
#23933=CARTESIAN_POINT('',(95.9218016746715,1.04733934390306,-1.66387871395933));
#23934=CARTESIAN_POINT('',(95.9218016730721,1.04733934308042,0.924367114736168));
#23935=CARTESIAN_POINT('Ctrl Pts',(95.9218016575013,1.04733933507189,-1.76247028589786));
#23936=CARTESIAN_POINT('Ctrl Pts',(95.9082726027725,1.04038092018214,-1.76139659336334));
#23937=CARTESIAN_POINT('Ctrl Pts',(95.8948780141389,1.0331601766951,-1.76031482866298));
#23938=CARTESIAN_POINT('Ctrl Pts',(95.8093131916082,0.984870631619995,-1.75328399601243));
#23939=CARTESIAN_POINT('Ctrl Pts',(95.7415231109389,0.936529175992813,-1.74712890009404));
#23940=CARTESIAN_POINT('Ctrl Pts',(95.6585733912026,0.863025380711787,-1.73905915718277));
#23941=CARTESIAN_POINT('Ctrl Pts',(95.6384167269154,0.843847829252905,-1.73705122289499));
#23942=CARTESIAN_POINT('Ctrl Pts',(95.6113422499949,0.816196661379392,-1.73430698233769));
#23943=CARTESIAN_POINT('Ctrl Pts',(95.6038355698102,0.808314439676538,-1.73354076290774));
#23944=CARTESIAN_POINT('Ctrl Pts',(95.5909225317782,0.794373413556894,-1.73221492723625));
#23945=CARTESIAN_POINT('Ctrl Pts',(95.5854676461171,0.788360761339344,-1.73165233667884));
#23946=CARTESIAN_POINT('Ctrl Pts',(95.5774879563995,0.779380271941437,-1.73082620460101));
#23947=CARTESIAN_POINT('Ctrl Pts',(95.5749151449545,0.776455691633554,-1.73055934831563));
#23948=CARTESIAN_POINT('Ctrl Pts',(95.5703561828224,0.771221266138187,-1.73008568216823));
#23949=CARTESIAN_POINT('Ctrl Pts',(95.5683644381285,0.768916427477689,-1.72987847231106));
#23950=CARTESIAN_POINT('Ctrl Pts',(95.5640341406872,0.763865948753644,-1.72942738408654));
#23951=CARTESIAN_POINT('Ctrl Pts',(95.5616992448567,0.761117282005081,-1.72918376721109));
#23952=CARTESIAN_POINT('Ctrl Pts',(95.5551857309607,0.753377726087125,-1.7285029212196));
#23953=CARTESIAN_POINT('Ctrl Pts',(95.5510357295146,0.748362764626964,-1.72806767741323));
#23954=CARTESIAN_POINT('Ctrl Pts',(95.5266580830309,0.718401940606776,-1.72550052277414));
#23955=CARTESIAN_POINT('Ctrl Pts',(95.5074141246462,0.692669138227843,-1.72343045443746));
#23956=CARTESIAN_POINT('Ctrl Pts',(95.4441108528227,0.600378005131332,-1.71633815159914));
#23957=CARTESIAN_POINT('Ctrl Pts',(95.4057791956269,0.530157979120159,-1.71150037427878));
#23958=CARTESIAN_POINT('Ctrl Pts',(95.3544497619237,0.40811351776157,-1.7032166424801));
#23959=CARTESIAN_POINT('Ctrl Pts',(95.3373313313498,0.358323202982892,-1.6998710901189));
#23960=CARTESIAN_POINT('Ctrl Pts',(95.3207784930459,0.29713628823021,-1.69570479021932));
#23961=CARTESIAN_POINT('Ctrl Pts',(95.3181022006873,0.286674806413331,-1.69499072256259));
#23962=CARTESIAN_POINT('Ctrl Pts',(95.3141126190428,0.270135798081966,-1.69385841661199));
#23963=CARTESIAN_POINT('Ctrl Pts',(95.3127029182374,0.264081970102343,-1.69344324265148));
#23964=CARTESIAN_POINT('Ctrl Pts',(95.3101517426805,0.252719722482748,-1.69266255170987));
#23965=CARTESIAN_POINT('Ctrl Pts',(95.3089989241989,0.247413996999744,-1.69229740472903));
#23966=CARTESIAN_POINT('Ctrl Pts',(95.3064981096364,0.23550805984902,-1.6914766003963));
#23967=CARTESIAN_POINT('Ctrl Pts',(95.3051699807429,0.228903916880639,-1.69102032977696));
#23968=CARTESIAN_POINT('Ctrl Pts',(95.3019310279625,0.212051450239034,-1.68985336781294));
#23969=CARTESIAN_POINT('Ctrl Pts',(95.3000995202083,0.201788663431317,-1.68914022269618));
#23970=CARTESIAN_POINT('Ctrl Pts',(95.2865479733121,0.119555398662598,-1.68340465649594));
#23971=CARTESIAN_POINT('Ctrl Pts',(95.2814007888031,0.0466752038606759,
-1.67817634337518));
#23972=CARTESIAN_POINT('Ctrl Pts',(95.2841857016304,-0.0784783313742113,
-1.66902693684432));
#23973=CARTESIAN_POINT('Ctrl Pts',(95.2888292263588,-0.130620235205284,
-1.66516808325462));
#23974=CARTESIAN_POINT('Ctrl Pts',(95.3008888164893,-0.207600457552029,
-1.65950649273449));
#23975=CARTESIAN_POINT('Ctrl Pts',(95.3056809509799,-0.232785306241036,
-1.65766067802005));
#23976=CARTESIAN_POINT('Ctrl Pts',(95.3135480325982,-0.267854877683472,
-1.65511576133304));
#23977=CARTESIAN_POINT('Ctrl Pts',(95.3159367712923,-0.2778848534677,-1.65439087583065));
#23978=CARTESIAN_POINT('Ctrl Pts',(95.320359592384,-0.295430091095904,-1.65312952485407));
#23979=CARTESIAN_POINT('Ctrl Pts',(95.322337025176,-0.302958847508151,-1.65259044851323));
#23980=CARTESIAN_POINT('Ctrl Pts',(95.3253985707482,-0.314161936595017,
-1.65179208734261));
#23981=CARTESIAN_POINT('Ctrl Pts',(95.3264261532751,-0.317851300390736,
-1.65152979293913));
#23982=CARTESIAN_POINT('Ctrl Pts',(95.3282221754511,-0.324180022176224,
-1.65108099599005));
#23983=CARTESIAN_POINT('Ctrl Pts',(95.3289818765067,-0.326821765720461,
-1.65089400504389));
#23984=CARTESIAN_POINT('Ctrl Pts',(95.330739525683,-0.332854125743456,-1.65046781716339));
#23985=CARTESIAN_POINT('Ctrl Pts',(95.3317434918459,-0.336242927397643,
-1.65022896827799));
#23986=CARTESIAN_POINT('Ctrl Pts',(95.3345477977624,-0.345554510183091,
-1.64957411211087));
#23987=CARTESIAN_POINT('Ctrl Pts',(95.3363796322809,-0.351467799997539,
-1.64915985659529));
#23988=CARTESIAN_POINT('Ctrl Pts',(95.3463556559357,-0.382795082268002,
-1.64697242188612));
#23989=CARTESIAN_POINT('Ctrl Pts',(95.3553159320286,-0.407943354416816,
-1.64524163841597));
#23990=CARTESIAN_POINT('Ctrl Pts',(95.3690877099279,-0.442800441347279,
-1.64284988405034));
#23991=CARTESIAN_POINT('Ctrl Pts',(95.3731893903721,-0.452778655434962,
-1.64216607702972));
#23992=CARTESIAN_POINT('Ctrl Pts',(95.3903670993518,-0.492986998862539,
-1.63940882894324));
#23993=CARTESIAN_POINT('Ctrl Pts',(95.4045718264469,-0.522719735397757,
-1.63736552703426));
#23994=CARTESIAN_POINT('Ctrl Pts',(95.4487989405111,-0.60611169766479,-1.63152284615702));
#23995=CARTESIAN_POINT('Ctrl Pts',(95.4817968221332,-0.658064355163386,
-1.62773934504428));
#23996=CARTESIAN_POINT('Ctrl Pts',(95.5398859289373,-0.73542173191228,-1.62159545349343));
#23997=CARTESIAN_POINT('Ctrl Pts',(95.562331071069,-0.762670792571765,-1.61931956368957));
#23998=CARTESIAN_POINT('Ctrl Pts',(95.5924415416781,-0.79605035915461,-1.6163576280381));
#23999=CARTESIAN_POINT('Ctrl Pts',(95.5990072210361,-0.80315104049503,-1.61571693189914));
#24000=CARTESIAN_POINT('Ctrl Pts',(95.6097665370224,-0.814503344261714,
-1.61467475417947));
#24001=CARTESIAN_POINT('Ctrl Pts',(95.6139064592765,-0.818805434577736,
-1.61427555216223));
#24002=CARTESIAN_POINT('Ctrl Pts',(95.6219056855958,-0.826992487444782,
-1.61350751844035));
#24003=CARTESIAN_POINT('Ctrl Pts',(95.6257597339867,-0.830882385273377,
-1.61313891935744));
#24004=CARTESIAN_POINT('Ctrl Pts',(95.6346304260632,-0.839711579875305,
-1.61229370890543));
#24005=CARTESIAN_POINT('Ctrl Pts',(95.6396644719234,-0.844633015488431,
-1.61181634042057));
#24006=CARTESIAN_POINT('Ctrl Pts',(95.6557588593057,-0.860087608395602,
-1.61029707767412));
#24007=CARTESIAN_POINT('Ctrl Pts',(95.6669797383753,-0.870450530791571,
-1.60924804774239));
#24008=CARTESIAN_POINT('Ctrl Pts',(95.7419014228874,-0.936990924926088,
-1.60230611248537));
#24009=CARTESIAN_POINT('Ctrl Pts',(95.8113073767031,-0.98634534483101,-1.59613743849432));
#24010=CARTESIAN_POINT('Ctrl Pts',(95.907465296868,-1.0401480873461,-1.5880514946744));
#24011=CARTESIAN_POINT('Ctrl Pts',(95.9299225201119,-1.05178046093339,-1.58619477140776));
#24012=CARTESIAN_POINT('Ctrl Pts',(95.9911596053007,-1.0810392498335,-1.58123812175992));
#24013=CARTESIAN_POINT('Ctrl Pts',(96.0305537898655,-1.09730204029909,-1.57815941045678));
#24014=CARTESIAN_POINT('Ctrl Pts',(96.0795967560218,-1.11450000501108,-1.57452214111982));
#24015=CARTESIAN_POINT('Ctrl Pts',(96.0884845569421,-1.11749797661593,-1.57387064391252));
#24016=CARTESIAN_POINT('Ctrl Pts',(96.1013349965504,-1.12166228940029,-1.57294059686305));
#24017=CARTESIAN_POINT('Ctrl Pts',(96.1052691674886,-1.12291437705579,-1.57265745989608));
#24018=CARTESIAN_POINT('Ctrl Pts',(96.1121408584445,-1.12506163059179,-1.57216579236993));
#24019=CARTESIAN_POINT('Ctrl Pts',(96.1150754105119,-1.12596603242809,-1.57195674075906));
#24020=CARTESIAN_POINT('Ctrl Pts',(96.121322380586,-1.12786456946756,-1.57151368939184));
#24021=CARTESIAN_POINT('Ctrl Pts',(96.1246356631346,-1.12885560030019,-1.57127986656484));
#24022=CARTESIAN_POINT('Ctrl Pts',(96.1337182303821,-1.13152874505723,-1.57064195669048));
#24023=CARTESIAN_POINT('Ctrl Pts',(96.1394961973081,-1.13318134830499,-1.57023951345349));
#24024=CARTESIAN_POINT('Ctrl Pts',(96.1677467692998,-1.14102810400831,-1.56828707838497));
#24025=CARTESIAN_POINT('Ctrl Pts',(96.1903889145981,-1.14659884052418,-1.56676916640249));
#24026=CARTESIAN_POINT('Ctrl Pts',(96.3131027410879,-1.17295316159636,-1.55871995838098));
#24027=CARTESIAN_POINT('Ctrl Pts',(96.4153960845011,-1.18131727589625,-1.55260344950045));
#24028=CARTESIAN_POINT('Ctrl Pts',(96.544786846687,-1.17504652183059,-1.54442455462622));
#24029=CARTESIAN_POINT('Ctrl Pts',(96.5720256436124,-1.17277424842285,-1.5426804801343));
#24030=CARTESIAN_POINT('Ctrl Pts',(96.6180475962657,-1.16731726317867,-1.5396770690334));
#24031=CARTESIAN_POINT('Ctrl Pts',(96.6368778088317,-1.16462050617781,-1.53843201620482));
#24032=CARTESIAN_POINT('Ctrl Pts',(96.6632835681097,-1.16018375002331,-1.5366593302508));
#24033=CARTESIAN_POINT('Ctrl Pts',(96.6709204447538,-1.1588228725649,-1.53614348475565));
#24034=CARTESIAN_POINT('Ctrl Pts',(96.6840201268697,-1.15635477280528,-1.53525294770259));
#24035=CARTESIAN_POINT('Ctrl Pts',(96.6894896066919,-1.15528401595648,-1.53487940964032));
#24036=CARTESIAN_POINT('Ctrl Pts',(96.6999278428868,-1.15316349095424,-1.53416315947789));
#24037=CARTESIAN_POINT('Ctrl Pts',(96.7048978247646,-1.15212032414988,-1.53382066310721));
#24038=CARTESIAN_POINT('Ctrl Pts',(96.716531060234,-1.14959992328384,-1.53301546668836));
#24039=CARTESIAN_POINT('Ctrl Pts',(96.7231884695421,-1.14809685930183,-1.5325519597336));
#24040=CARTESIAN_POINT('Ctrl Pts',(96.7428135652766,-1.14348640989986,-1.53117738976875));
#24041=CARTESIAN_POINT('Ctrl Pts',(96.7557415989595,-1.14021664572187,-1.53026123699735));
#24042=CARTESIAN_POINT('Ctrl Pts',(96.8574977933116,-1.11263386075306,-1.52296312473441));
#24043=CARTESIAN_POINT('Ctrl Pts',(96.9432358380313,-1.07820121045382,-1.5162483984759));
#24044=CARTESIAN_POINT('Ctrl Pts',(97.0408942486186,-1.02497928712206,-1.50808646596049));
#24045=CARTESIAN_POINT('Ctrl Pts',(97.0574913531786,-1.0154017595369,-1.50668137412397));
#24046=CARTESIAN_POINT('Ctrl Pts',(97.1007767006911,-0.988995186564692,
-1.50297876588771));
#24047=CARTESIAN_POINT('Ctrl Pts',(97.1270368029671,-0.971490448266343,
-1.50069265679511));
#24048=CARTESIAN_POINT('Ctrl Pts',(97.1667994164849,-0.94261276260187,-1.49719992070009));
#24049=CARTESIAN_POINT('Ctrl Pts',(97.180802411711,-0.931955830433972,-1.49596358878165));
#24050=CARTESIAN_POINT('Ctrl Pts',(97.1986660741304,-0.917717453954565,
-1.49438342389372));
#24051=CARTESIAN_POINT('Ctrl Pts',(97.2027481002315,-0.914418986600052,
-1.49402213507619));
#24052=CARTESIAN_POINT('Ctrl Pts',(97.2093532378976,-0.909008351560454,
-1.49343738256308));
#24053=CARTESIAN_POINT('Ctrl Pts',(97.2118897311067,-0.906912747256671,
-1.49321279052856));
#24054=CARTESIAN_POINT('Ctrl Pts',(97.2168020316673,-0.902819537657584,
-1.49277781856991));
#24055=CARTESIAN_POINT('Ctrl Pts',(97.2191787643677,-0.900823136312687,
-1.49256736238963));
#24056=CARTESIAN_POINT('Ctrl Pts',(97.2249928083513,-0.895900139433797,
-1.49205245605254));
#24057=CARTESIAN_POINT('Ctrl Pts',(97.2284212863593,-0.892963091537648,
-1.49174874993205));
#24058=CARTESIAN_POINT('Ctrl Pts',(97.2382577796243,-0.884437986132794,
-1.49087690510497));
#24059=CARTESIAN_POINT('Ctrl Pts',(97.2446224366942,-0.878800026684242,
-1.49031216970905));
#24060=CARTESIAN_POINT('Ctrl Pts',(97.310874998577,-0.818819058867857,-1.48442008640676));
#24061=CARTESIAN_POINT('Ctrl Pts',(97.3650841664702,-0.758506173936913,
-1.47947184314816));
#24062=CARTESIAN_POINT('Ctrl Pts',(97.4573567282219,-0.631739413014636,
-1.4697676914808));
#24063=CARTESIAN_POINT('Ctrl Pts',(97.4959818821612,-0.566208176884739,
-1.4650380406834));
#24064=CARTESIAN_POINT('Ctrl Pts',(97.5334061731822,-0.4858892882618,-1.45923570442599));
#24065=CARTESIAN_POINT('Ctrl Pts',(97.5385922954742,-0.474270852244039,
-1.45839668752515));
#24066=CARTESIAN_POINT('Ctrl Pts',(97.5461894595004,-0.456482125720178,
-1.45711142742656));
#24067=CARTESIAN_POINT('Ctrl Pts',(97.5487384595379,-0.45037150068393,-1.45666981226544));
#24068=CARTESIAN_POINT('Ctrl Pts',(97.553281064531,-0.439217911759139,-1.45586337669233));
#24069=CARTESIAN_POINT('Ctrl Pts',(97.5552916349992,-0.434182020192706,
-1.45549913372049));
#24070=CARTESIAN_POINT('Ctrl Pts',(97.5595642900659,-0.423261873297295,
-1.45470890712129));
#24071=CARTESIAN_POINT('Ctrl Pts',(97.56181403944,-0.417373004915716,-1.45428252798347));
#24072=CARTESIAN_POINT('Ctrl Pts',(97.5678280870048,-0.401243586871699,
-1.45311389294658));
#24073=CARTESIAN_POINT('Ctrl Pts',(97.5714974544921,-0.390968554613661,
-1.45236855317874));
#24074=CARTESIAN_POINT('Ctrl Pts',(97.5912316150979,-0.333186106953388,
-1.44817098244492));
#24075=CARTESIAN_POINT('Ctrl Pts',(97.6043898405513,-0.284747726472124,
-1.4446260171281));
#24076=CARTESIAN_POINT('Ctrl Pts',(97.6303012100591,-0.157849974318005,
-1.43528344026455));
#24077=CARTESIAN_POINT('Ctrl Pts',(97.6382775717925,-0.0786760906031083,
-1.4293903563793));
#24078=CARTESIAN_POINT('Ctrl Pts',(97.6382104892888,0.0350272723140157,
-1.4211485585674));
#24079=CARTESIAN_POINT('Ctrl Pts',(97.6366890021153,0.0693460825717339,
-1.41869282350173));
#24080=CARTESIAN_POINT('Ctrl Pts',(97.6331377382809,0.10957978262549,-1.41588559547943));
#24081=CARTESIAN_POINT('Ctrl Pts',(97.6325592875135,0.115602968991305,-1.41546725218207));
#24082=CARTESIAN_POINT('Ctrl Pts',(97.6315397229621,0.12542336749079,-1.41478857882479));
#24083=CARTESIAN_POINT('Ctrl Pts',(97.6311265059398,0.129223272826107,-1.41452680681317));
#24084=CARTESIAN_POINT('Ctrl Pts',(97.6303511924804,0.136043860613749,-1.41405852099923));
#24085=CARTESIAN_POINT('Ctrl Pts',(97.6299958862938,0.139065202956841,-1.41385164544526));
#24086=CARTESIAN_POINT('Ctrl Pts',(97.6291866674897,0.145723856763769,-1.41339696022696));
#24087=CARTESIAN_POINT('Ctrl Pts',(97.6287274802272,0.149360443390521,-1.41314944406939));
#24088=CARTESIAN_POINT('Ctrl Pts',(97.6273451445935,0.159911453309238,-1.41243350409842));
#24089=CARTESIAN_POINT('Ctrl Pts',(97.6263775158981,0.166820037671098,-1.41196745620071));
#24090=CARTESIAN_POINT('Ctrl Pts',(97.6175105570039,0.226276885297638,-1.40797696645354));
#24091=CARTESIAN_POINT('Ctrl Pts',(97.6061234777592,0.278250733213789,-1.4046251165657));
#24092=CARTESIAN_POINT('Ctrl Pts',(97.5673210615536,0.411500751045216,-1.39598481583607));
#24093=CARTESIAN_POINT('Ctrl Pts',(97.5344860528934,0.490856783442581,-1.3907739865543));
#24094=CARTESIAN_POINT('Ctrl Pts',(97.4798648457576,0.590540172471542,-1.38350037529658));
#24095=CARTESIAN_POINT('Ctrl Pts',(97.4655184772984,0.614638588035848,-1.3816820400867));
#24096=CARTESIAN_POINT('Ctrl Pts',(97.4453085703628,0.645984041414679,-1.3792223571452));
#24097=CARTESIAN_POINT('Ctrl Pts',(97.4401988256442,0.653707656122043,-1.37860838512267));
#24098=CARTESIAN_POINT('Ctrl Pts',(97.4316959333098,0.666236525985062,-1.37759898411688));
#24099=CARTESIAN_POINT('Ctrl Pts',(97.4283568643858,0.671078135981539,-1.37720557241859));
#24100=CARTESIAN_POINT('Ctrl Pts',(97.4218213238439,0.680404346325787,-1.37644114122446));
#24101=CARTESIAN_POINT('Ctrl Pts',(97.4186293793926,0.684891943571002,-1.3760702993751));
#24102=CARTESIAN_POINT('Ctrl Pts',(97.4110922690535,0.695332654548716,-1.37520033566449));
#24103=CARTESIAN_POINT('Ctrl Pts',(97.4067225023077,0.701267638501984,-1.37470028407919));
#24104=CARTESIAN_POINT('Ctrl Pts',(97.3922771249502,0.720506386248491,-1.37306090191753));
#24105=CARTESIAN_POINT('Ctrl Pts',(97.3819748008172,0.733636557004614,-1.37191287099129));
#24106=CARTESIAN_POINT('Ctrl Pts',(97.3568432121465,0.76430161304173,-1.36915984129998));
#24107=CARTESIAN_POINT('Ctrl Pts',(97.3417736822543,0.781629874074417,-1.36754584094923));
#24108=CARTESIAN_POINT('Ctrl Pts',(97.2801004289617,0.848495038659795,-1.36108127060843));
#24109=CARTESIAN_POINT('Ctrl Pts',(97.229754012008,0.894391964806232,-1.35609610884823));
#24110=CARTESIAN_POINT('Ctrl Pts',(97.155420475941,0.951213972321532,-1.34923074823891));
#24111=CARTESIAN_POINT('Ctrl Pts',(97.134603831427,0.966078344869045,-1.34735692141373));
#24112=CARTESIAN_POINT('Ctrl Pts',(97.100606094342,0.988720474715964,-1.3443877829417));
#24113=CARTESIAN_POINT('Ctrl Pts',(97.0877288751555,0.99693954141716,-1.34328313771873));
#24114=CARTESIAN_POINT('Ctrl Pts',(97.0541122957174,1.01748651272546,-1.34045638416391));
#24115=CARTESIAN_POINT('Ctrl Pts',(97.0331461634347,1.02943271954926,-1.33874775841688));
#24116=CARTESIAN_POINT('Ctrl Pts',(97.0065190053498,1.04353896709603,-1.33665750863426));
#24117=CARTESIAN_POINT('Ctrl Pts',(97.0011902137795,1.04631000646257,-1.3362430900528));
#24118=CARTESIAN_POINT('Ctrl Pts',(96.9927297841228,1.0506276390357,-1.33559153040377));
#24119=CARTESIAN_POINT('Ctrl Pts',(96.9896121540982,1.05220122932029,-1.33535279754543));
#24120=CARTESIAN_POINT('Ctrl Pts',(96.9840220081176,1.05499166628097,-1.33492722710426));
#24121=CARTESIAN_POINT('Ctrl Pts',(96.9815522284154,1.0562136992524,-1.33474007841071));
#24122=CARTESIAN_POINT('Ctrl Pts',(96.9755847900612,1.0591403280166,-1.33428996468118));
#24123=CARTESIAN_POINT('Ctrl Pts',(96.972082946296,1.06083627339469,-1.33402752985998));
#24124=CARTESIAN_POINT('Ctrl Pts',(96.9612690958165,1.06600742760915,-1.33322215745436));
#24125=CARTESIAN_POINT('Ctrl Pts',(96.9539294258324,1.06942471139089,-1.33268259090663));
#24126=CARTESIAN_POINT('Ctrl Pts',(96.9366760735207,1.07724226257554,-1.33142933201042));
#24127=CARTESIAN_POINT('Ctrl Pts',(96.926735547583,1.08158187694978,-1.33071879205294));
#24128=CARTESIAN_POINT('Ctrl Pts',(96.8912332916108,1.09650021404321,-1.32821691596611));
#24129=CARTESIAN_POINT('Ctrl Pts',(96.8653590177299,1.10631562391627,-1.32645862915693));
#24130=CARTESIAN_POINT('Ctrl Pts',(96.7612660731122,1.1416613606516,-1.31955217587822));
#24131=CARTESIAN_POINT('Ctrl Pts',(96.6808140874885,1.15987770949613,-1.31456574919788));
#24132=CARTESIAN_POINT('Ctrl Pts',(96.5576700132021,1.17447497852492,-1.30674391222853));
#24133=CARTESIAN_POINT('Ctrl Pts',(96.5159936281889,1.1771809339213,-1.30406810403586));
#24134=CARTESIAN_POINT('Ctrl Pts',(96.4637210677359,1.1777927434335,-1.3006302448838));
#24135=CARTESIAN_POINT('Ctrl Pts',(96.4531765949774,1.17777454525494,-1.29993268856936));
#24136=CARTESIAN_POINT('Ctrl Pts',(96.4364739489872,1.17752141471837,-1.29882066247037));
#24137=CARTESIAN_POINT('Ctrl Pts',(96.4303147651928,1.17737972510291,-1.29840907199176));
#24138=CARTESIAN_POINT('Ctrl Pts',(96.4192669656823,1.17703882941818,-1.29766793835094));
#24139=CARTESIAN_POINT('Ctrl Pts',(96.4143779094667,1.17685747092942,-1.29733895449875));
#24140=CARTESIAN_POINT('Ctrl Pts',(96.4029369731742,1.17636166995877,-1.29656667264818));
#24141=CARTESIAN_POINT('Ctrl Pts',(96.3963863628969,1.17602294566,-1.29612263405954));
#24142=CARTESIAN_POINT('Ctrl Pts',(96.3774387590434,1.17488441098329,-1.29483268715726));
#24143=CARTESIAN_POINT('Ctrl Pts',(96.3650514766685,1.17394317571243,-1.29398245084462));
#24144=CARTESIAN_POINT('Ctrl Pts',(96.3370586531064,1.17137019941065,-1.29204474471656));
#24145=CARTESIAN_POINT('Ctrl Pts',(96.3214664337683,1.16962221743233,-1.29095388098174));
#24146=CARTESIAN_POINT('Ctrl Pts',(96.2699753536126,1.16280562930156,-1.28731234023861));
#24147=CARTESIAN_POINT('Ctrl Pts',(96.2342783422136,1.15639148583936,-1.28472376420413));
#24148=CARTESIAN_POINT('Ctrl Pts',(96.1317538853162,1.13304070557294,-1.27711687863908));
#24149=CARTESIAN_POINT('Ctrl Pts',(96.0660445827209,1.1118731531171,-1.27201697087281));
#24150=CARTESIAN_POINT('Ctrl Pts',(95.9751778002837,1.07352677021072,-1.26483747684661));
#24151=CARTESIAN_POINT('Ctrl Pts',(95.9482364649276,1.06093558086044,-1.26269341367224));
#24152=CARTESIAN_POINT('Ctrl Pts',(95.9218016672795,1.04733934010109,-1.26059202888093));
#24153=CARTESIAN_POINT('',(97.638230523307,-0.0010337549458608,-1.3257271689311));
#24154=CARTESIAN_POINT('Ctrl Pts',(95.921801693794,1.04733935373837,-1.1624507611287));
#24155=CARTESIAN_POINT('Ctrl Pts',(95.9528161361363,1.0632910475803,-1.16499099562586));
#24156=CARTESIAN_POINT('Ctrl Pts',(95.9845285161482,1.07785965256847,-1.16755324028244));
#24157=CARTESIAN_POINT('Ctrl Pts',(96.0430244658817,1.10164594866506,-1.17218628727739));
#24158=CARTESIAN_POINT('Ctrl Pts',(96.0695787477456,1.11134570458929,-1.17425609947354));
#24159=CARTESIAN_POINT('Ctrl Pts',(96.1294093411433,1.1307905223701,-1.17881737716337));
#24160=CARTESIAN_POINT('Ctrl Pts',(96.1628218594441,1.14004174355271,-1.18129645098146));
#24161=CARTESIAN_POINT('Ctrl Pts',(96.2025058987115,1.1491652176112,-1.18412667177596));
#24162=CARTESIAN_POINT('Ctrl Pts',(96.2084254533261,1.15047809840734,-1.18454589250896));
#24163=CARTESIAN_POINT('Ctrl Pts',(96.2180963958937,1.15254476166447,-1.18522568807064));
#24164=CARTESIAN_POINT('Ctrl Pts',(96.2218416955003,1.15332606272377,-1.1854877126962));
#24165=CARTESIAN_POINT('Ctrl Pts',(96.2285717559479,1.15469582254118,-1.18595624623867));
#24166=CARTESIAN_POINT('Ctrl Pts',(96.2315550407432,1.15529097875302,-1.18616311892203));
#24167=CARTESIAN_POINT('Ctrl Pts',(96.2381343713958,1.15657704867463,-1.18661755383336));
#24168=CARTESIAN_POINT('Ctrl Pts',(96.2417313503988,1.15726275500444,-1.18686482443349));
#24169=CARTESIAN_POINT('Ctrl Pts',(96.2521732574641,1.1592029128502,-1.18757939762913));
#24170=CARTESIAN_POINT('Ctrl Pts',(96.2590263216784,1.16041351527325,-1.18804433798349));
#24171=CARTESIAN_POINT('Ctrl Pts',(96.3173837365965,1.17018984796761,-1.19197238446911));
#24172=CARTESIAN_POINT('Ctrl Pts',(96.3694014869336,1.17538380535976,-1.19526890411557));
#24173=CARTESIAN_POINT('Ctrl Pts',(96.504760152378,1.17985500349988,-1.20370504674461));
#24174=CARTESIAN_POINT('Ctrl Pts',(96.5879746719896,1.17378168149418,-1.20876842550522));
#24175=CARTESIAN_POINT('Ctrl Pts',(96.7001528274863,1.15351654926691,-1.2160394023406));
#24176=CARTESIAN_POINT('Ctrl Pts',(96.7302230259782,1.14685744323325,-1.218031295103));
#24177=CARTESIAN_POINT('Ctrl Pts',(96.7692516028882,1.13659462285538,-1.2206908571464));
#24178=CARTESIAN_POINT('Ctrl Pts',(96.7784770080952,1.13404812549228,-1.2213250014173));
#24179=CARTESIAN_POINT('Ctrl Pts',(96.7933842544064,1.12973706408474,-1.22235911472994));
#24180=CARTESIAN_POINT('Ctrl Pts',(96.799085681049,1.12804134585665,-1.2227568694905));
#24181=CARTESIAN_POINT('Ctrl Pts',(96.8100165216303,1.12469995971626,-1.22352389377642));
#24182=CARTESIAN_POINT('Ctrl Pts',(96.8152477819745,1.12306082132881,-1.22389294377697));
#24183=CARTESIAN_POINT('Ctrl Pts',(96.8273294552255,1.11918237020461,-1.22474993247296));
#24184=CARTESIAN_POINT('Ctrl Pts',(96.8341710770764,1.11691659871585,-1.22523871869568));
#24185=CARTESIAN_POINT('Ctrl Pts',(96.8555493944999,1.10961823342553,-1.22677726528749));
#24186=CARTESIAN_POINT('Ctrl Pts',(96.8700080466943,1.10436371639388,-1.2278341961928));
#24187=CARTESIAN_POINT('Ctrl Pts',(96.903827685184,1.09131762716354,-1.23034642019912));
#24188=CARTESIAN_POINT('Ctrl Pts',(96.9230921722096,1.08329186101098,-1.23180896367419));
#24189=CARTESIAN_POINT('Ctrl Pts',(96.9943087866705,1.05137625952308,-1.23733529804107));
#24190=CARTESIAN_POINT('Ctrl Pts',(97.0447077312792,1.02422749185506,-1.24149411469819));
#24191=CARTESIAN_POINT('Ctrl Pts',(97.1550813148808,0.953967122597752,-1.25108785501892));
#24192=CARTESIAN_POINT('Ctrl Pts',(97.213387325223,0.908656583792617,-1.25652746633866));
#24193=CARTESIAN_POINT('Ctrl Pts',(97.2741068951509,0.851587260583021,-1.26236588064343));
#24194=CARTESIAN_POINT('Ctrl Pts',(97.2810520667816,0.84489709324905,-1.26303635116878));
#24195=CARTESIAN_POINT('Ctrl Pts',(97.2906723862343,0.835399461024587,-1.26396788067598));
#24196=CARTESIAN_POINT('Ctrl Pts',(97.2934168081405,0.832663159724074,-1.26423394827541));
#24197=CARTESIAN_POINT('Ctrl Pts',(97.2983486914858,0.827697085595556,-1.26471259702662));
#24198=CARTESIAN_POINT('Ctrl Pts',(97.3005408791025,0.825472067384314,-1.26492553713432));
#24199=CARTESIAN_POINT('Ctrl Pts',(97.3050023873716,0.820907562370081,-1.26535923921244));
#24200=CARTESIAN_POINT('Ctrl Pts',(97.3072708903037,0.8185673349154,-1.26557993977021));
#24201=CARTESIAN_POINT('Ctrl Pts',(97.3128572014846,0.812756323308112,-1.26612396676726));
#24202=CARTESIAN_POINT('Ctrl Pts',(97.3161635922391,0.809274572018157,-1.26644643787242));
#24203=CARTESIAN_POINT('Ctrl Pts',(97.329275033217,0.795297546468507,-1.26772758310172));
#24204=CARTESIAN_POINT('Ctrl Pts',(97.3389095063395,0.784643016477904,-1.26867438407875));
#24205=CARTESIAN_POINT('Ctrl Pts',(97.3639686342907,0.755890442869172,-1.27116012739227));
#24206=CARTESIAN_POINT('Ctrl Pts',(97.3790447717457,0.737496445865733,-1.27268001000859));
#24207=CARTESIAN_POINT('Ctrl Pts',(97.4307687481324,0.670340284989563,-1.27803514766421));
#24208=CARTESIAN_POINT('Ctrl Pts',(97.464175270021,0.619203451886215,-1.28176759667203));
#24209=CARTESIAN_POINT('Ctrl Pts',(97.5256948141897,0.50686772041217,-1.28971715549704));
#24210=CARTESIAN_POINT('Ctrl Pts',(97.5528273768108,0.445390799849658,-1.29393387011441));
#24211=CARTESIAN_POINT('Ctrl Pts',(97.5779532258167,0.372100858340279,-1.29901855369894));
#24212=CARTESIAN_POINT('Ctrl Pts',(97.5811970405069,0.362213706569555,-1.29970543238965));
#24213=CARTESIAN_POINT('Ctrl Pts',(97.5863224613535,0.345863048827715,-1.3008435313082));
#24214=CARTESIAN_POINT('Ctrl Pts',(97.5882804601208,0.339423951784869,-1.30129228132681));
#24215=CARTESIAN_POINT('Ctrl Pts',(97.5917178923298,0.327761364405649,-1.30210622515762));
#24216=CARTESIAN_POINT('Ctrl Pts',(97.5932166118949,0.32254371839106,-1.30247078687717));
#24217=CARTESIAN_POINT('Ctrl Pts',(97.5963548025454,0.311326727691713,-1.30325551120589));
#24218=CARTESIAN_POINT('Ctrl Pts',(97.5979829254277,0.305324407160047,-1.30367602509131));
#24219=CARTESIAN_POINT('Ctrl Pts',(97.6012142107005,0.293027104562733,-1.30453889150354));
#24220=CARTESIAN_POINT('Ctrl Pts',(97.6028129823224,0.286731200035219,-1.30498136812705));
#24221=CARTESIAN_POINT('Ctrl Pts',(97.6067170486057,0.270806023099641,-1.30610250879798));
#24222=CARTESIAN_POINT('Ctrl Pts',(97.6089531083055,0.261160462460256,-1.30678332619533));
#24223=CARTESIAN_POINT('Ctrl Pts',(97.6292015829024,0.168521420327007,-1.31334017360846));
#24224=CARTESIAN_POINT('Ctrl Pts',(97.6383049869274,0.0838549416170599,
-1.31949861334066));
#24225=CARTESIAN_POINT('Ctrl Pts',(97.6382304961252,-0.00103349190011182,
-1.32572719717278));
#24226=CARTESIAN_POINT('Ctrl Pts',(97.6382304958974,-0.00103375145213981,
-1.32572721621709));
#24227=CARTESIAN_POINT('Ctrl Pts',(97.6381786364634,-0.0601170298897422,
-1.33006237874468));
#24228=CARTESIAN_POINT('Ctrl Pts',(97.6336808842862,-0.119118016426818,
-1.33440949445678));
#24229=CARTESIAN_POINT('Ctrl Pts',(97.6230081894834,-0.189109820144788,
-1.33944026940622));
#24230=CARTESIAN_POINT('Ctrl Pts',(97.6210709776267,-0.200656217023987,
-1.34026582966023));
#24231=CARTESIAN_POINT('Ctrl Pts',(97.6178794232858,-0.218082408309804,
-1.34150336246135));
#24232=CARTESIAN_POINT('Ctrl Pts',(97.6167517628187,-0.223984315984074,
-1.34192101841758));
#24233=CARTESIAN_POINT('Ctrl Pts',(97.6148340636484,-0.233620451222935,
-1.34260024560144));
#24234=CARTESIAN_POINT('Ctrl Pts',(97.6140709690408,-0.237359843235196,
-1.34286316229607));
#24235=CARTESIAN_POINT('Ctrl Pts',(97.6125578758646,-0.244594764189681,
-1.34337047790921));
#24236=CARTESIAN_POINT('Ctrl Pts',(97.6118101124284,-0.248090714007503,
-1.34361499324002));
#24237=CARTESIAN_POINT('Ctrl Pts',(97.6103950753012,-0.254562101861767,
-1.34406639664736));
#24238=CARTESIAN_POINT('Ctrl Pts',(97.6097321669646,-0.257538346506306,
-1.34427351298786));
#24239=CARTESIAN_POINT('Ctrl Pts',(97.6081867961326,-0.264351761467536,
-1.34474656983993));
#24240=CARTESIAN_POINT('Ctrl Pts',(97.6072966450381,-0.268187109635949,
-1.34501207479532));
#24241=CARTESIAN_POINT('Ctrl Pts',(97.6049008192955,-0.278279794426113,
-1.34570885501609));
#24242=CARTESIAN_POINT('Ctrl Pts',(97.6033630352048,-0.284529480149041,
-1.34613839903327));
#24243=CARTESIAN_POINT('Ctrl Pts',(97.5879410279131,-0.345062711105292,
-1.35028298525217));
#24244=CARTESIAN_POINT('Ctrl Pts',(97.570248914536,-0.398310566002967,-1.3538060619574));
#24245=CARTESIAN_POINT('Ctrl Pts',(97.5310509963207,-0.493091224595534,
-1.36018115368523));
#24246=CARTESIAN_POINT('Ctrl Pts',(97.5107410117661,-0.534988787641947,
-1.36303983225609));
#24247=CARTESIAN_POINT('Ctrl Pts',(97.4632903385721,-0.6196984038992,-1.36908574055397));
#24248=CARTESIAN_POINT('Ctrl Pts',(97.4357606536005,-0.662179333190469,
-1.37227423470518));
#24249=CARTESIAN_POINT('Ctrl Pts',(97.3954078520451,-0.716448072030846,
-1.37666795698601));
#24250=CARTESIAN_POINT('Ctrl Pts',(97.384931571883,-0.729915852624672,-1.37778657816324));
#24251=CARTESIAN_POINT('Ctrl Pts',(97.3693669059224,-0.749052232816067,
-1.37942034593786));
#24252=CARTESIAN_POINT('Ctrl Pts',(97.3645099762238,-0.754906910542223,
-1.37992638316302));
#24253=CARTESIAN_POINT('Ctrl Pts',(97.3560145110696,-0.764948012626519,
-1.38080529992986));
#24254=CARTESIAN_POINT('Ctrl Pts',(97.3524024475681,-0.769156590956274,
-1.38117710456824));
#24255=CARTESIAN_POINT('Ctrl Pts',(97.3454059165284,-0.777193007494497,
-1.38189377627657));
#24256=CARTESIAN_POINT('Ctrl Pts',(97.3420259929671,-0.781024649477084,
-1.38223845191753));
#24257=CARTESIAN_POINT('Ctrl Pts',(97.3330949358673,-0.791017489057584,
-1.38314529602009));
#24258=CARTESIAN_POINT('Ctrl Pts',(97.3275035528655,-0.797142168220407,
-1.38370912708849));
#24259=CARTESIAN_POINT('Ctrl Pts',(97.307538749851,-0.818552616224517,-1.38570912013949));
#24260=CARTESIAN_POINT('Ctrl Pts',(97.2928227560247,-0.833512040909031,
-1.3871596543547));
#24261=CARTESIAN_POINT('Ctrl Pts',(97.2139538062443,-0.909513414495519,
-1.39481836081925));
#24262=CARTESIAN_POINT('Ctrl Pts',(97.14347490574,-0.963561214934663,-1.40130969597968));
#24263=CARTESIAN_POINT('Ctrl Pts',(97.0324279018609,-1.03036827166546,-1.41081360125513));
#24264=CARTESIAN_POINT('Ctrl Pts',(96.9961468498718,-1.04968784255756,-1.41381413822792));
#24265=CARTESIAN_POINT('Ctrl Pts',(96.9463017429934,-1.07297131382178,-1.41774261419488));
#24266=CARTESIAN_POINT('Ctrl Pts',(96.9335707525378,-1.07864514960123,-1.4187296361128));
#24267=CARTESIAN_POINT('Ctrl Pts',(96.9117953508952,-1.08789008298886,-1.42038692295335));
#24268=CARTESIAN_POINT('Ctrl Pts',(96.902802193782,-1.09157750695109,-1.42106257706736));
#24269=CARTESIAN_POINT('Ctrl Pts',(96.8900232754545,-1.09663331914765,-1.42200926786348));
#24270=CARTESIAN_POINT('Ctrl Pts',(96.8862748588287,-1.09809416464252,-1.42228534479176));
#24271=CARTESIAN_POINT('Ctrl Pts',(96.8796138040812,-1.10065089658564,-1.42277299342649));
#24272=CARTESIAN_POINT('Ctrl Pts',(96.8767041808321,-1.10175449559545,-1.42298500975249));
#24273=CARTESIAN_POINT('Ctrl Pts',(96.8710488184689,-1.10387393202832,-1.4233951350146));
#24274=CARTESIAN_POINT('Ctrl Pts',(96.8683036414395,-1.10489107393181,-1.4235933252255));
#24275=CARTESIAN_POINT('Ctrl Pts',(96.860795808329,-1.10764107970035,-1.42413300806459));
#24276=CARTESIAN_POINT('Ctrl Pts',(96.8560256451163,-1.10935348006256,-1.42447332375885));
#24277=CARTESIAN_POINT('Ctrl Pts',(96.8435545320998,-1.1137397106476,-1.42535670886852));
#24278=CARTESIAN_POINT('Ctrl Pts',(96.8358364694029,-1.11636452610495,-1.42589714475116));
#24279=CARTESIAN_POINT('Ctrl Pts',(96.7611920487,-1.14088848339568,-1.43106935529451));
#24280=CARTESIAN_POINT('Ctrl Pts',(96.6924464063933,-1.15682690149822,-1.43541727252204));
#24281=CARTESIAN_POINT('Ctrl Pts',(96.5638863914899,-1.17470249364689,-1.44344613274062));
#24282=CARTESIAN_POINT('Ctrl Pts',(96.5045624191325,-1.17842046800066,-1.44711303053659));
#24283=CARTESIAN_POINT('Ctrl Pts',(96.4238955017707,-1.17737466057927,-1.45225418597847));
#24284=CARTESIAN_POINT('Ctrl Pts',(96.4025901999534,-1.17651951366322,-1.45362612777498));
#24285=CARTESIAN_POINT('Ctrl Pts',(96.3655870892173,-1.17402678389165,-1.45604181904048));
#24286=CARTESIAN_POINT('Ctrl Pts',(96.3498769422466,-1.17265103478291,-1.45707777184707));
#24287=CARTESIAN_POINT('Ctrl Pts',(96.3270345783134,-1.1701876195918,-1.4586013034187));
#24288=CARTESIAN_POINT('Ctrl Pts',(96.3198768029197,-1.16934916476345,-1.45908118563653));
#24289=CARTESIAN_POINT('Ctrl Pts',(96.3072885966879,-1.1677573455315,-1.45992970942614));
#24290=CARTESIAN_POINT('Ctrl Pts',(96.301854837416,-1.16703164902894,-1.46029748101796));
#24291=CARTESIAN_POINT('Ctrl Pts',(96.2905359930017,-1.16543946986313,-1.46106679832068));
#24292=CARTESIAN_POINT('Ctrl Pts',(96.2846520232026,-1.16456628518632,-1.46146854326036));
#24293=CARTESIAN_POINT('Ctrl Pts',(96.2693186064281,-1.16217194301288,-1.46252036783486));
#24294=CARTESIAN_POINT('Ctrl Pts',(96.2598808022519,-1.1605801299703,-1.46317263431387));
#24295=CARTESIAN_POINT('Ctrl Pts',(96.2201611560394,-1.15338192286718,-1.46593895809901));
#24296=CARTESIAN_POINT('Ctrl Pts',(96.1900883345962,-1.14670440636737,-1.46808605790689));
#24297=CARTESIAN_POINT('Ctrl Pts',(96.0798497808304,-1.11764897403433,-1.47615827416963));
#24298=CARTESIAN_POINT('Ctrl Pts',(96.0018679202524,-1.08797519369787,-1.48229136440521));
#24299=CARTESIAN_POINT('Ctrl Pts',(95.8811166873791,-1.02672181671144,-1.49220296594283));
#24300=CARTESIAN_POINT('Ctrl Pts',(95.836173526215,-1.00003108995239,-1.4959907504425));
#24301=CARTESIAN_POINT('Ctrl Pts',(95.7874118429878,-0.966499593404055,
-1.50010675487966));
#24302=CARTESIAN_POINT('Ctrl Pts',(95.7817128786653,-0.962505791181802,
-1.50058786974931));
#24303=CARTESIAN_POINT('Ctrl Pts',(95.7730696027791,-0.956333681544294,
-1.5013172390303));
#24304=CARTESIAN_POINT('Ctrl Pts',(95.7700996157875,-0.954191849176072,
-1.50156780715301));
#24305=CARTESIAN_POINT('Ctrl Pts',(95.7646805524564,-0.950245296786186,
-1.50202482057208));
#24306=CARTESIAN_POINT('Ctrl Pts',(95.7622284695233,-0.948444933163378,
-1.50223154189108));
#24307=CARTESIAN_POINT('Ctrl Pts',(95.7567082401577,-0.94435886866627,-1.50269677367462));
#24308=CARTESIAN_POINT('Ctrl Pts',(95.7536442370983,-0.942067705781955,
-1.50295490599978));
#24309=CARTESIAN_POINT('Ctrl Pts',(95.7457534361408,-0.936107048239926,
-1.50361959221005));
#24310=CARTESIAN_POINT('Ctrl Pts',(95.7409436404996,-0.93241508401061,-1.50402466216824));
#24311=CARTESIAN_POINT('Ctrl Pts',(95.7088402568908,-0.907376401805629,
-1.50672937877678));
#24312=CARTESIAN_POINT('Ctrl Pts',(95.682468815932,-0.884869081143158,-1.50895645400073));
#24313=CARTESIAN_POINT('Ctrl Pts',(95.636504489084,-0.841993531899366,-1.51292823667213));
#24314=CARTESIAN_POINT('Ctrl Pts',(95.6165798026714,-0.822022682303489,
-1.51468418008077));
#24315=CARTESIAN_POINT('Ctrl Pts',(95.5647670924743,-0.766218396758312,
-1.51940558532152));
#24316=CARTESIAN_POINT('Ctrl Pts',(95.5343202578391,-0.729122915702506,
-1.52235409159086));
#24317=CARTESIAN_POINT('Ctrl Pts',(95.4749438125358,-0.647038776814336,
-1.52868927915255));
#24318=CARTESIAN_POINT('Ctrl Pts',(95.4466464945641,-0.601731866680707,
-1.53208141320341));
#24319=CARTESIAN_POINT('Ctrl Pts',(95.4164179239082,-0.545109917806109,
-1.53629994721787));
#24320=CARTESIAN_POINT('Ctrl Pts',(95.411448153655,-0.535483523891176,-1.5370163018179));
#24321=CARTESIAN_POINT('Ctrl Pts',(95.4038338185561,-0.520221711805234,
-1.53815139336462));
#24322=CARTESIAN_POINT('Ctrl Pts',(95.4010998453958,-0.514631385095465,
-1.53856703979477));
#24323=CARTESIAN_POINT('Ctrl Pts',(95.396064269581,-0.504124647180466,-1.53934811221355));
#24324=CARTESIAN_POINT('Ctrl Pts',(95.3937520961522,-0.499213461487374,
-1.53971316411224));
#24325=CARTESIAN_POINT('Ctrl Pts',(95.3886516271823,-0.488182538277522,
-1.54053308832544));
#24326=CARTESIAN_POINT('Ctrl Pts',(95.3858816495482,-0.482054590434231,
-1.54098856841987));
#24327=CARTESIAN_POINT('Ctrl Pts',(95.3789667575312,-0.466401143769895,
-1.54215220981922));
#24328=CARTESIAN_POINT('Ctrl Pts',(95.374895185102,-0.456844076785939,-1.54286280127476));
#24329=CARTESIAN_POINT('Ctrl Pts',(95.3422954176212,-0.377426185720986,
-1.54877035576747));
#24330=CARTESIAN_POINT('Ctrl Pts',(95.320420827739,-0.305038435815673,-1.55418894460636));
#24331=CARTESIAN_POINT('Ctrl Pts',(95.2942797097766,-0.174387896560006,
-1.56393571869398));
#24332=CARTESIAN_POINT('Ctrl Pts',(95.2871268082519,-0.11694776599024,-1.56820505755745));
#24333=CARTESIAN_POINT('Ctrl Pts',(95.2831896174929,-0.0387369023930222,
-1.57386002803975));
#24334=CARTESIAN_POINT('Ctrl Pts',(95.2826936169924,-0.0182353273264383,
-1.57532720582229));
#24335=CARTESIAN_POINT('Ctrl Pts',(95.2827582967303,0.0153242075192261,
-1.57769401404468));
#24336=CARTESIAN_POINT('Ctrl Pts',(95.2830005001584,0.0283778963087294,
-1.57860598951886));
#24337=CARTESIAN_POINT('Ctrl Pts',(95.2836251139981,0.0461250198445256,
-1.57983177549765));
#24338=CARTESIAN_POINT('Ctrl Pts',(95.2838186617399,0.0508235915674019,
-1.58015495859122));
#24339=CARTESIAN_POINT('Ctrl Pts',(95.2841898885381,0.0586895604090173,
-1.5806936144164));
#24340=CARTESIAN_POINT('Ctrl Pts',(95.2843522301988,0.0618575865423896,
-1.58090990848106));
#24341=CARTESIAN_POINT('Ctrl Pts',(95.2846851081383,0.0678775653389548,
-1.58131963338843));
#24342=CARTESIAN_POINT('Ctrl Pts',(95.2848532245011,0.070729605518265,-1.5815131999688));
#24343=CARTESIAN_POINT('Ctrl Pts',(95.2852777492193,0.077511342003848,-1.58197223505135));
#24344=CARTESIAN_POINT('Ctrl Pts',(95.2855434940812,0.0814404509278922,
-1.58223719526481));
#24345=CARTESIAN_POINT('Ctrl Pts',(95.2865548293043,0.0953562489598012,
-1.58317233856358));
#24346=CARTESIAN_POINT('Ctrl Pts',(95.2874081042898,0.105335018066843,-1.58383694081671));
#24347=CARTESIAN_POINT('Ctrl Pts',(95.2945024366643,0.177451774578565,-1.58860464650549));
#24348=CARTESIAN_POINT('Ctrl Pts',(95.305550661497,0.239025319525307,-1.59248803843815));
#24349=CARTESIAN_POINT('Ctrl Pts',(95.3373896729268,0.360139172666509,-1.60024199521176));
#24350=CARTESIAN_POINT('Ctrl Pts',(95.3581724698459,0.419463596016934,-1.60410200588416));
#24351=CARTESIAN_POINT('Ctrl Pts',(95.393159674064,0.498477605156671,-1.60958774454999));
#24352=CARTESIAN_POINT('Ctrl Pts',(95.4033861410053,0.519812549143089,-1.61110491782931));
#24353=CARTESIAN_POINT('Ctrl Pts',(95.4220860185346,0.555987775463909,-1.6137518872214));
#24354=CARTESIAN_POINT('Ctrl Pts',(95.4302528622754,0.570978527913612,-1.61487160911008));
#24355=CARTESIAN_POINT('Ctrl Pts',(95.4424405707272,0.592236555563929,-1.61649540078107));
#24356=CARTESIAN_POINT('Ctrl Pts',(95.4461998028688,0.598651903793953,-1.61699023940071));
#24357=CARTESIAN_POINT('Ctrl Pts',(95.4528537103137,0.609764584079147,-1.61785603579512));
#24358=CARTESIAN_POINT('Ctrl Pts',(95.4557211455949,0.614478019005303,-1.61822600723145));
#24359=CARTESIAN_POINT('Ctrl Pts',(95.4617002350169,0.624152577886072,-1.61899116705584));
#24360=CARTESIAN_POINT('Ctrl Pts',(95.4648159811583,0.629110979707698,-1.61938649674319));
#24361=CARTESIAN_POINT('Ctrl Pts',(95.4728919091673,0.64175274481016,-1.62040269392431));
#24362=CARTESIAN_POINT('Ctrl Pts',(95.477904764649,0.649401825407263,-1.62102548029165));
#24363=CARTESIAN_POINT('Ctrl Pts',(95.4981121723117,0.679466493345246,-1.62350551178803));
#24364=CARTESIAN_POINT('Ctrl Pts',(95.5139877537221,0.701412006233222,-1.62538783303082));
#24365=CARTESIAN_POINT('Ctrl Pts',(95.5902907372503,0.799576625296967,-1.63415234517379));
#24366=CARTESIAN_POINT('Ctrl Pts',(95.6592533348924,0.868667149739692,-1.64135766762612));
#24367=CARTESIAN_POINT('Ctrl Pts',(95.7590107633359,0.946516656059798,-1.65058278238766));
#24368=CARTESIAN_POINT('Ctrl Pts',(95.7827850247087,0.963681828214781,-1.65270231931335));
#24369=CARTESIAN_POINT('Ctrl Pts',(95.821115308615,0.989235707126706,-1.65597216811415));
#24370=CARTESIAN_POINT('Ctrl Pts',(95.8352517222745,0.998230530375245,-1.65714818706774));
#24371=CARTESIAN_POINT('Ctrl Pts',(95.8539854918529,1.00959641523064,-1.65866339181127));
#24372=CARTESIAN_POINT('Ctrl Pts',(95.858412506144,1.01224268521555,-1.65901835712953));
#24373=CARTESIAN_POINT('Ctrl Pts',(95.8656746143812,1.01651914842308,-1.65959542884377));
#24374=CARTESIAN_POINT('Ctrl Pts',(95.8684993084213,1.01816673128626,-1.65981861040835));
#24375=CARTESIAN_POINT('Ctrl Pts',(95.8740290684058,1.02136132862835,-1.66025297676189));
#24376=CARTESIAN_POINT('Ctrl Pts',(95.8767334615111,1.0229094012002,-1.66046422430594));
#24377=CARTESIAN_POINT('Ctrl Pts',(95.88279073516,1.02634491396403,-1.66093480469614));
#24378=CARTESIAN_POINT('Ctrl Pts',(95.8861468167274,1.02822671193159,-1.6611937849441));
#24379=CARTESIAN_POINT('Ctrl Pts',(95.8978045097898,1.03468844445868,-1.6620875523738));
#24380=CARTESIAN_POINT('Ctrl Pts',(95.906152423961,1.03918470573194,-1.66271738188609));
#24381=CARTESIAN_POINT('Ctrl Pts',(95.9169657544763,1.04484147278675,-1.663521385413));
#24382=CARTESIAN_POINT('Ctrl Pts',(95.9193816458742,1.04609464764928,-1.66370026126829));
#24383=CARTESIAN_POINT('Ctrl Pts',(95.9218016746715,1.04733934390307,-1.66387871395933));
#24384=CARTESIAN_POINT('Origin',(96.460480949577,-7.19464945638997E-16,
0.924367114736168));
#24385=CARTESIAN_POINT('',(95.9218015453622,1.04733927739526,-2.26182855819541));
#24386=CARTESIAN_POINT('',(95.9218016761257,1.04733934465099,-2.16205147885552));
#24387=CARTESIAN_POINT('',(95.9218016730721,1.04733934308042,0.924367114736168));
#24388=CARTESIAN_POINT('',(97.6382305799192,0.000395899098767113,-1.92539805293419));
#24389=CARTESIAN_POINT('Ctrl Pts',(95.9218015453623,1.04733927739527,-2.26182855819541));
#24390=CARTESIAN_POINT('Ctrl Pts',(95.9005594358515,1.03641379494418,-2.26034392312565));
#24391=CARTESIAN_POINT('Ctrl Pts',(95.8796424425559,1.02483833332954,-2.25885102568976));
#24392=CARTESIAN_POINT('Ctrl Pts',(95.8233247093762,0.991391149828253,-2.25471890233259));
#24393=CARTESIAN_POINT('Ctrl Pts',(95.7887222002028,0.968278933968751,-2.25205254613741));
#24394=CARTESIAN_POINT('Ctrl Pts',(95.7470775398636,0.937154749242537,-2.24863341212708));
#24395=CARTESIAN_POINT('Ctrl Pts',(95.7388215705449,0.930812106880061,-2.24794471874761));
#24396=CARTESIAN_POINT('Ctrl Pts',(95.7257922833405,0.920524822855528,-2.24683974067127));
#24397=CARTESIAN_POINT('Ctrl Pts',(95.7209639871069,0.916650448938913,-2.24642621059659));
#24398=CARTESIAN_POINT('Ctrl Pts',(95.7119966644007,0.90933782943845,-2.24565042748322));
#24399=CARTESIAN_POINT('Ctrl Pts',(95.7078502044114,0.905908920912824,-2.24528855275363));
#24400=CARTESIAN_POINT('Ctrl Pts',(95.6985575877115,0.898116570660832,-2.24447031584675));
#24401=CARTESIAN_POINT('Ctrl Pts',(95.6934251746797,0.893737108311844,-2.24401331385242));
#24402=CARTESIAN_POINT('Ctrl Pts',(95.678251952764,0.880562900034642,-2.2426468162873));
#24403=CARTESIAN_POINT('Ctrl Pts',(95.6683230107008,0.871641554117464,-2.2417321646485));
#24404=CARTESIAN_POINT('Ctrl Pts',(95.645956617397,0.850847087847731,-2.23962346779264));
#24405=CARTESIAN_POINT('Ctrl Pts',(95.6336235012992,0.838866713085102,-2.23842509959699));
#24406=CARTESIAN_POINT('Ctrl Pts',(95.5922893391359,0.796917395141394,-2.23428343663299));
#24407=CARTESIAN_POINT('Ctrl Pts',(95.5646221749364,0.765682995937537,-2.23128976342374));
#24408=CARTESIAN_POINT('Ctrl Pts',(95.4992507602404,0.683478555557929,-2.22365264124503));
#24409=CARTESIAN_POINT('Ctrl Pts',(95.4638940352677,0.630809525430696,-2.21896744349422));
#24410=CARTESIAN_POINT('Ctrl Pts',(95.4264117929955,0.563892458077927,-2.21339450110199));
#24411=CARTESIAN_POINT('Ctrl Pts',(95.4200785450134,0.552120079552428,-2.21242771296679));
#24412=CARTESIAN_POINT('Ctrl Pts',(95.402353501441,0.517783878816849,-2.20965153540369));
#24413=CARTESIAN_POINT('Ctrl Pts',(95.3914850024866,0.494956285895658,-2.20785925717368));
#24414=CARTESIAN_POINT('Ctrl Pts',(95.3789180781401,0.46621233145495,-2.20568251341245));
#24415=CARTESIAN_POINT('Ctrl Pts',(95.3765207132462,0.46061089099608,-2.20526202261331));
#24416=CARTESIAN_POINT('Ctrl Pts',(95.3728100856315,0.451751578409685,-2.20460306201076));
#24417=CARTESIAN_POINT('Ctrl Pts',(95.3714677835833,0.448506100267409,-2.20436294159042));
#24418=CARTESIAN_POINT('Ctrl Pts',(95.3690995194883,0.442706687409642,-2.2039362060559));
#24419=CARTESIAN_POINT('Ctrl Pts',(95.3680679932508,0.440155165943464,-2.20374926875774));
#24420=CARTESIAN_POINT('Ctrl Pts',(95.3656107301693,0.434015177297052,-2.2033013401377));
#24421=CARTESIAN_POINT('Ctrl Pts',(95.3641936855554,0.430423288490405,-2.20304086445674));
#24422=CARTESIAN_POINT('Ctrl Pts',(95.3599154471199,0.419420719667989,-2.20224755909827));
#24423=CARTESIAN_POINT('Ctrl Pts',(95.357111470279,0.411987822499146,-2.20171795614181));
#24424=CARTESIAN_POINT('Ctrl Pts',(95.3507476502651,0.394587224893803,-2.20049156483722));
#24425=CARTESIAN_POINT('Ctrl Pts',(95.3472464837898,0.384598641450425,-2.19979774640875));
#24426=CARTESIAN_POINT('Ctrl Pts',(95.3354019767762,0.349289349370133,-2.19737626073909));
#24427=CARTESIAN_POINT('Ctrl Pts',(95.3277836407308,0.323732518242791,-2.19567939298498));
#24428=CARTESIAN_POINT('Ctrl Pts',(95.3012415214691,0.222223958700894,-2.18907884191828));
#24429=CARTESIAN_POINT('Ctrl Pts',(95.2890395472296,0.144724961393674,-2.18432873531507));
#24430=CARTESIAN_POINT('Ctrl Pts',(95.2819767318031,0.0200009348604612,
-2.1764817983415));
#24431=CARTESIAN_POINT('Ctrl Pts',(95.2821096897527,-0.0266951193868056,
-2.17350215372494));
#24432=CARTESIAN_POINT('Ctrl Pts',(95.2856790785276,-0.0839692340116455,
-2.16973079514788));
#24433=CARTESIAN_POINT('Ctrl Pts',(95.2864930952421,-0.0946719278948646,
-2.16902113109647));
#24434=CARTESIAN_POINT('Ctrl Pts',(95.2880136276566,-0.111600530014013,
-2.16789016987684));
#24435=CARTESIAN_POINT('Ctrl Pts',(95.2886237534646,-0.117834666523381,
-2.16747185785962));
#24436=CARTESIAN_POINT('Ctrl Pts',(95.2898550552628,-0.129458528349032,
-2.16668835411016));
#24437=CARTESIAN_POINT('Ctrl Pts',(95.2904638019322,-0.13484942540551,-2.16632355785077));
#24438=CARTESIAN_POINT('Ctrl Pts',(95.2919041485002,-0.146859904881965,
-2.16550755293036));
#24439=CARTESIAN_POINT('Ctrl Pts',(95.2927547883248,-0.153476971686341,
-2.16505576317506));
#24440=CARTESIAN_POINT('Ctrl Pts',(95.2954248036017,-0.172937879822967,
-2.16372031209844));
#24441=CARTESIAN_POINT('Ctrl Pts',(95.2974001597513,-0.185758947520191,
-2.16283183907709));
#24442=CARTESIAN_POINT('Ctrl Pts',(95.3124385354089,-0.273688736979836,
-2.15667649584193));
#24443=CARTESIAN_POINT('Ctrl Pts',(95.3325534937224,-0.347394090762805,
-2.15118695028902));
#24444=CARTESIAN_POINT('Ctrl Pts',(95.3880866840082,-0.493426418705865,
-2.1397466839498));
#24445=CARTESIAN_POINT('Ctrl Pts',(95.4240827137434,-0.565136902108412,
-2.13381739521637));
#24446=CARTESIAN_POINT('Ctrl Pts',(95.4721789399126,-0.640659385052763,
-2.12754924634726));
#24447=CARTESIAN_POINT('Ctrl Pts',(95.4773789069225,-0.648610590424305,
-2.12688922290188));
#24448=CARTESIAN_POINT('Ctrl Pts',(95.484758562989,-0.65960204850743,-2.12597762413243));
#24449=CARTESIAN_POINT('Ctrl Pts',(95.4868572101564,-0.66269589788906,-2.12572111862893));
#24450=CARTESIAN_POINT('Ctrl Pts',(95.4907165276595,-0.668327440321926,
-2.1252544565966));
#24451=CARTESIAN_POINT('Ctrl Pts',(95.4924725162134,-0.67086829953477,-2.1250439969197));
#24452=CARTESIAN_POINT('Ctrl Pts',(95.4961355750922,-0.67612430022902,-2.12460887308832));
#24453=CARTESIAN_POINT('Ctrl Pts',(95.4980441480668,-0.678838327172358,
-2.12438431187135));
#24454=CARTESIAN_POINT('Ctrl Pts',(95.5030737313303,-0.685926639747509,
-2.12379803607577));
#24455=CARTESIAN_POINT('Ctrl Pts',(95.506213297219,-0.690287756717486,-2.1234375461586));
#24456=CARTESIAN_POINT('Ctrl Pts',(95.5204915848825,-0.709837886752784,
-2.12182176509973));
#24457=CARTESIAN_POINT('Ctrl Pts',(95.5319645517462,-0.724780813459593,
-2.12058738963753));
#24458=CARTESIAN_POINT('Ctrl Pts',(95.5657811065641,-0.76670326749975,-2.11710557389248));
#24459=CARTESIAN_POINT('Ctrl Pts',(95.5889771512939,-0.792971124343236,
-2.11490053461892));
#24460=CARTESIAN_POINT('Ctrl Pts',(95.6690318115688,-0.875863529872492,
-2.10771720322605));
#24461=CARTESIAN_POINT('Ctrl Pts',(95.7304982371159,-0.927714227479524,
-2.10283547142644));
#24462=CARTESIAN_POINT('Ctrl Pts',(95.8250614602941,-0.99222534983343,-2.09556207790121));
#24463=CARTESIAN_POINT('Ctrl Pts',(95.8541929099756,-1.01028884117017,-2.09335203219231));
#24464=CARTESIAN_POINT('Ctrl Pts',(95.8927337380447,-1.03191904141595,-2.0904417659188));
#24465=CARTESIAN_POINT('Ctrl Pts',(95.9014601672429,-1.03667234902755,-2.08978374278048));
#24466=CARTESIAN_POINT('Ctrl Pts',(95.9155756555645,-1.04413103890086,-2.08872028685138));
#24467=CARTESIAN_POINT('Ctrl Pts',(95.9209272886428,-1.04690651470306,-2.08831731030366));
#24468=CARTESIAN_POINT('Ctrl Pts',(95.9311664056757,-1.05211738539997,-2.08754659256149));
#24469=CARTESIAN_POINT('Ctrl Pts',(95.9360499934765,-1.05456012138142,-2.08717911799213));
#24470=CARTESIAN_POINT('Ctrl Pts',(95.9472705941701,-1.06007537014422,-2.08633498867518));
#24471=CARTESIAN_POINT('Ctrl Pts',(95.9536184820173,-1.06312515469032,-2.0858575688254));
#24472=CARTESIAN_POINT('Ctrl Pts',(95.9734589309661,-1.07243923000943,-2.08436556910142));
#24473=CARTESIAN_POINT('Ctrl Pts',(95.9870426337823,-1.07850474024511,-2.08334432002806));
#24474=CARTESIAN_POINT('Ctrl Pts',(96.0189326617879,-1.09202599401455,-2.08094626354754));
#24475=CARTESIAN_POINT('Ctrl Pts',(96.0373186052977,-1.09928122599583,-2.07956326888352));
#24476=CARTESIAN_POINT('Ctrl Pts',(96.1048444589781,-1.12398236757368,-2.07448175662579));
#24477=CARTESIAN_POINT('Ctrl Pts',(96.1549417252228,-1.13862127031158,-2.07070424602856));
#24478=CARTESIAN_POINT('Ctrl Pts',(96.2854227773387,-1.16751612461275,-2.06092205002118));
#24479=CARTESIAN_POINT('Ctrl Pts',(96.3666263727511,-1.17683155982532,-2.05487788752936));
#24480=CARTESIAN_POINT('Ctrl Pts',(96.4575079124201,-1.17778346188621,-2.04851729712666));
#24481=CARTESIAN_POINT('Ctrl Pts',(96.4668712744328,-1.17776988394416,-2.04786696012004));
#24482=CARTESIAN_POINT('Ctrl Pts',(96.4803148424791,-1.17759005463347,-2.04694130317679));
#24483=CARTESIAN_POINT('Ctrl Pts',(96.4843956128269,-1.17751425053449,-2.04666139026731));
#24484=CARTESIAN_POINT('Ctrl Pts',(96.4915492608569,-1.17734416077578,-2.04617266734272));
#24485=CARTESIAN_POINT('Ctrl Pts',(96.4946222842756,-1.17725905519267,-2.04596336434827));
#24486=CARTESIAN_POINT('Ctrl Pts',(96.5011385281733,-1.17705305456441,-2.04552093061628));
#24487=CARTESIAN_POINT('Ctrl Pts',(96.5045815769757,-1.17692908341408,-2.04528796897155));
#24488=CARTESIAN_POINT('Ctrl Pts',(96.5139692244004,-1.17654981590141,-2.04465487882865));
#24489=CARTESIAN_POINT('Ctrl Pts',(96.519912610302,-1.17626457322564,-2.0442563528917));
#24490=CARTESIAN_POINT('Ctrl Pts',(96.5517314567133,-1.17449569331199,-2.04213381626362));
#24491=CARTESIAN_POINT('Ctrl Pts',(96.5775569439145,-1.17220315410673,-2.04045014000125));
#24492=CARTESIAN_POINT('Ctrl Pts',(96.7101369196081,-1.15600780121043,-2.03191227135534));
#24493=CARTESIAN_POINT('Ctrl Pts',(96.8146964297244,-1.12836926041473,-2.02548763647532));
#24494=CARTESIAN_POINT('Ctrl Pts',(96.9452826567516,-1.07387500567844,-2.01649285745702));
#24495=CARTESIAN_POINT('Ctrl Pts',(96.975933930004,-1.05950371251568,-2.01430935942239));
#24496=CARTESIAN_POINT('Ctrl Pts',(97.0146937859113,-1.03925028156982,-2.01142934542412));
#24497=CARTESIAN_POINT('Ctrl Pts',(97.0234072102067,-1.03455644166486,-2.01077391122977));
#24498=CARTESIAN_POINT('Ctrl Pts',(97.0373236404962,-1.02683192941039,-2.00971363541899));
#24499=CARTESIAN_POINT('Ctrl Pts',(97.0425644892387,-1.02387013429646,-2.00931122331163));
#24500=CARTESIAN_POINT('Ctrl Pts',(97.0524230002938,-1.01819857328577,-2.00854821457269));
#24501=CARTESIAN_POINT('Ctrl Pts',(97.0570453546711,-1.01549723534819,-2.00818792540718));
#24502=CARTESIAN_POINT('Ctrl Pts',(97.0671571730133,-1.00949494883088,-2.00739407998663));
#24503=CARTESIAN_POINT('Ctrl Pts',(97.0726384193169,-1.00618056095106,-2.00696004818888));
#24504=CARTESIAN_POINT('Ctrl Pts',(97.0843157588999,-0.998988796768864,
-2.00602726223556));
#24505=CARTESIAN_POINT('Ctrl Pts',(97.0905033133298,-0.995098137063567,
-2.00552803852777));
#24506=CARTESIAN_POINT('Ctrl Pts',(97.106653721477,-0.984731941841143,-2.00421171745379));
#24507=CARTESIAN_POINT('Ctrl Pts',(97.1165552786883,-0.978162923726331,
-2.00339125282272));
#24508=CARTESIAN_POINT('Ctrl Pts',(97.1462315183982,-0.957821429680231,
-2.00089055685106));
#24509=CARTESIAN_POINT('Ctrl Pts',(97.1656835017828,-0.943591519510457,
-1.99919410556129));
#24510=CARTESIAN_POINT('Ctrl Pts',(97.235910573339,-0.888832690868671,-1.99285372455286));
#24511=CARTESIAN_POINT('Ctrl Pts',(97.2837397689966,-0.844723599532997,
-1.9880932340306));
#24512=CARTESIAN_POINT('Ctrl Pts',(97.3679207513842,-0.753116368535732,
-1.97896360230924));
#24513=CARTESIAN_POINT('Ctrl Pts',(97.4047874258182,-0.706341247486207,
-1.97461025231344));
#24514=CARTESIAN_POINT('Ctrl Pts',(97.4435535785153,-0.648662946639332,
-1.96973694503724));
#24515=CARTESIAN_POINT('Ctrl Pts',(97.4490354917982,-0.640277553681871,
-1.9690399615192));
#24516=CARTESIAN_POINT('Ctrl Pts',(97.4565229461797,-0.628498939443639,
-1.96807792372593));
#24517=CARTESIAN_POINT('Ctrl Pts',(97.4586192769795,-0.625164343482821,
-1.9678074345278));
#24518=CARTESIAN_POINT('Ctrl Pts',(97.4622074447231,-0.619392650511335,
-1.96734255687311));
#24519=CARTESIAN_POINT('Ctrl Pts',(97.4637071974763,-0.61696055186336,-1.96714766795057));
#24520=CARTESIAN_POINT('Ctrl Pts',(97.4668533511026,-0.61181673366493,-1.96673763493402));
#24521=CARTESIAN_POINT('Ctrl Pts',(97.468497673958,-0.609103776011535,-1.96652263148782));
#24522=CARTESIAN_POINT('Ctrl Pts',(97.4725521360846,-0.602352959972884,
-1.96599065220529));
#24523=CARTESIAN_POINT('Ctrl Pts',(97.4749491248026,-0.598307193898127,
-1.96567450909875));
#24524=CARTESIAN_POINT('Ctrl Pts',(97.4839075824221,-0.582978004483678,
-1.96448628793706));
#24525=CARTESIAN_POINT('Ctrl Pts',(97.4903058464082,-0.571599635406815,
-1.96362388383606));
#24526=CARTESIAN_POINT('Ctrl Pts',(97.5062624156401,-0.542085191527672,
-1.96143054585596));
#24527=CARTESIAN_POINT('Ctrl Pts',(97.5155390735839,-0.523801187775625,
-1.96011326980412));
#24528=CARTESIAN_POINT('Ctrl Pts',(97.5734463777405,-0.40187973268035,-1.95153871084709));
#24529=CARTESIAN_POINT('Ctrl Pts',(97.6072219320987,-0.291868963456379,
-1.94471740784097));
#24530=CARTESIAN_POINT('Ctrl Pts',(97.6282670699309,-0.154779459729459,
-1.9357990309268));
#24531=CARTESIAN_POINT('Ctrl Pts',(97.6312015066026,-0.130745367146268,
-1.93422350831416));
#24532=CARTESIAN_POINT('Ctrl Pts',(97.6341863923211,-0.0979149514149447,
-1.93204677610304));
#24533=CARTESIAN_POINT('Ctrl Pts',(97.6348822049479,-0.0891823332805456,
-1.93146544699207));
#24534=CARTESIAN_POINT('Ctrl Pts',(97.6358354863779,-0.0752581151963874,
-1.93053444410522));
#24535=CARTESIAN_POINT('Ctrl Pts',(97.6361561246045,-0.0700710527880929,
-1.93018672841799));
#24536=CARTESIAN_POINT('Ctrl Pts',(97.6367305047784,-0.0596606488056806,
-1.92948698531686));
#24537=CARTESIAN_POINT('Ctrl Pts',(97.6369838083924,-0.054437402706353,
-1.92913495253947));
#24538=CARTESIAN_POINT('Ctrl Pts',(97.6374250731574,-0.043886355395171,
-1.9284218537882));
#24539=CARTESIAN_POINT('Ctrl Pts',(97.6376116616151,-0.0385586226547256,
-1.92806075377877));
#24540=CARTESIAN_POINT('Ctrl Pts',(97.6379190328841,-0.0276689542300539,
-1.92732052551768));
#24541=CARTESIAN_POINT('Ctrl Pts',(97.6380365901767,-0.0221070690059054,
-1.9269413067899));
#24542=CARTESIAN_POINT('Ctrl Pts',(97.6381940702366,-0.0108977695560703,
-1.92617466258363));
#24543=CARTESIAN_POINT('Ctrl Pts',(97.6382327850347,-0.00525050195161463,
-1.92578721105986));
#24544=CARTESIAN_POINT('Ctrl Pts',(97.6382308827581,0.000396726675349013,
-1.92539852201626));
#24545=CARTESIAN_POINT('Ctrl Pts',(97.6382308830244,0.000395935232192423,
-1.92539857648991));
#24546=CARTESIAN_POINT('Ctrl Pts',(97.6382265374016,0.0133224357143192,
-1.92450886793651));
#24547=CARTESIAN_POINT('Ctrl Pts',(97.6380093786908,0.0262476305489435,
-1.92361273883065));
#24548=CARTESIAN_POINT('Ctrl Pts',(97.6340026413434,0.146665539748613,-1.91520159267001));
#24549=CARTESIAN_POINT('Ctrl Pts',(97.6157159879922,0.253154930688317,-1.90723146849538));
#24550=CARTESIAN_POINT('Ctrl Pts',(97.5745577916515,0.383087365134138,-1.8972993930315));
#24551=CARTESIAN_POINT('Ctrl Pts',(97.5648648723803,0.410194480244713,-1.89521967475728));
#24552=CARTESIAN_POINT('Ctrl Pts',(97.5480497718657,0.452286294200139,-1.89200350308879));
#24553=CARTESIAN_POINT('Ctrl Pts',(97.541588004908,0.467521591985525,-1.89084226700691));
#24554=CARTESIAN_POINT('Ctrl Pts',(97.5327027430685,0.487300580287322,-1.88934302041255));
#24555=CARTESIAN_POINT('Ctrl Pts',(97.5305679007914,0.49197088253236,-1.88898962966034));
#24556=CARTESIAN_POINT('Ctrl Pts',(97.5270256584936,0.499587938464253,-1.88841445409155));
#24557=CARTESIAN_POINT('Ctrl Pts',(97.5256364561683,0.502543004942228,-1.88819160730473));
#24558=CARTESIAN_POINT('Ctrl Pts',(97.5228959461513,0.508310112603684,-1.88775733158221));
#24559=CARTESIAN_POINT('Ctrl Pts',(97.5215457298677,0.511122615330469,-1.88754584338941));
#24560=CARTESIAN_POINT('Ctrl Pts',(97.5184996252597,0.517403565974013,-1.88707414224255));
#24561=CARTESIAN_POINT('Ctrl Pts',(97.5167978095243,0.520869139621444,-1.88681428733463));
#24562=CARTESIAN_POINT('Ctrl Pts',(97.5108244764237,0.532883537244145,-1.88591463980817));
#24563=CARTESIAN_POINT('Ctrl Pts',(97.5064658387097,0.541388967961465,-1.88527989069258));
#24564=CARTESIAN_POINT('Ctrl Pts',(97.4669072691013,0.61632186985188,-1.87969848995107));
#24565=CARTESIAN_POINT('Ctrl Pts',(97.4255206016595,0.67929986111712,-1.87507585288536));
#24566=CARTESIAN_POINT('Ctrl Pts',(97.3332435553384,0.794088350413717,-1.86596539129276));
#24567=CARTESIAN_POINT('Ctrl Pts',(97.2830243565291,0.845997443456439,-1.86149606498231));
#24568=CARTESIAN_POINT('Ctrl Pts',(97.2187048511936,0.90130703189762,-1.85599591993341));
#24569=CARTESIAN_POINT('Ctrl Pts',(97.2088966591738,0.909467842644396,-1.85516306220863));
#24570=CARTESIAN_POINT('Ctrl Pts',(97.1929873035577,0.922273414766934,-1.85382000104842));
#24571=CARTESIAN_POINT('Ctrl Pts',(97.186969841719,0.927020871013304,-1.85331376463745));
#24572=CARTESIAN_POINT('Ctrl Pts',(97.1756448223154,0.935777717666839,-1.85236396946781));
#24573=CARTESIAN_POINT('Ctrl Pts',(97.1703487826643,0.939801552597389,-1.85192098935931));
#24574=CARTESIAN_POINT('Ctrl Pts',(97.1649361907103,0.943842087654171,-1.85146936149807));
#24575=CARTESIAN_POINT('Ctrl Pts',(97.1648533396377,0.94390391953186,-1.85146244864693));
#24576=CARTESIAN_POINT('Ctrl Pts',(97.164683929823,0.944030315600954,-1.85144831411957));
#24577=CARTESIAN_POINT('Ctrl Pts',(97.1645973702088,0.944094878896012,-1.85144109239429));
#24578=CARTESIAN_POINT('Ctrl Pts',(97.1644200597669,0.944227093689571,-1.85142629984869));
#24579=CARTESIAN_POINT('Ctrl Pts',(97.1643293081691,0.944294743933026,-1.85141872899212));
#24580=CARTESIAN_POINT('Ctrl Pts',(97.1600480405124,0.947485229598423,-1.85106158341241));
#24581=CARTESIAN_POINT('Ctrl Pts',(97.1558368532831,0.950580107464455,-1.85071094649116));
#24582=CARTESIAN_POINT('Ctrl Pts',(97.1468005336648,0.957128884350087,-1.84995987962198));
#24583=CARTESIAN_POINT('Ctrl Pts',(97.141969633464,0.960574538634427,-1.84955914885511));
#24584=CARTESIAN_POINT('Ctrl Pts',(97.1293353117628,0.969442726550406,-1.84851304672887));
#24585=CARTESIAN_POINT('Ctrl Pts',(97.1214920662787,0.974807494994599,-1.84786553274616));
#24586=CARTESIAN_POINT('Ctrl Pts',(97.0885082505502,0.996787268299319,-1.84514967697788));
#24587=CARTESIAN_POINT('Ctrl Pts',(97.062801588149,1.01252788335023,-1.84304979373217));
#24588=CARTESIAN_POINT('Ctrl Pts',(96.9548714637412,1.07304992323332,-1.83429476235444));
#24589=CARTESIAN_POINT('Ctrl Pts',(96.8680604937866,1.10893303302928,-1.82735888733692));
#24590=CARTESIAN_POINT('Ctrl Pts',(96.7498076825339,1.1420325681494,-1.81840722328497));
#24591=CARTESIAN_POINT('Ctrl Pts',(96.7213926840502,1.14885753705859,-1.816295139538));
#24592=CARTESIAN_POINT('Ctrl Pts',(96.6817320533384,1.15683592389939,-1.81342382391201));
#24593=CARTESIAN_POINT('Ctrl Pts',(96.6706809314123,1.15889490205243,-1.81263191720072));
#24594=CARTESIAN_POINT('Ctrl Pts',(96.6513987829117,1.16220252509426,-1.81126621562524));
#24595=CARTESIAN_POINT('Ctrl Pts',(96.643181000078,1.16352268124223,-1.81068920924578));
#24596=CARTESIAN_POINT('Ctrl Pts',(96.6310586186805,1.16533849200656,-1.80984611217004));
#24597=CARTESIAN_POINT('Ctrl Pts',(96.6271646421,1.16590183545736,-1.80957651310455));
#24598=CARTESIAN_POINT('Ctrl Pts',(96.6202479264211,1.16686711888864,-1.80909988916422));
#24599=CARTESIAN_POINT('Ctrl Pts',(96.617226371315,1.16727684528748,-1.80889244378358));
#24600=CARTESIAN_POINT('Ctrl Pts',(96.6106562409375,1.16814179060423,-1.8084430482769));
#24601=CARTESIAN_POINT('Ctrl Pts',(96.6071071649316,1.16859257866669,-1.80820134366274));
#24602=CARTESIAN_POINT('Ctrl Pts',(96.5972226145616,1.16980233054787,-1.80753095765668));
#24603=CARTESIAN_POINT('Ctrl Pts',(96.5908828287067,1.17052600565403,-1.80710416599151));
#24604=CARTESIAN_POINT('Ctrl Pts',(96.5549688957119,1.17433010277992,-1.80470285810397));
#24605=CARTESIAN_POINT('Ctrl Pts',(96.5252896045336,1.17634150528124,-1.8027812045559));
#24606=CARTESIAN_POINT('Ctrl Pts',(96.4161091922748,1.17959517452041,-1.79583885398311));
#24607=CARTESIAN_POINT('Ctrl Pts',(96.3366156143811,1.17391335454048,-1.79101798267954));
#24608=CARTESIAN_POINT('Ctrl Pts',(96.222129885758,1.15396342425084,-1.7837600418481));
#24609=CARTESIAN_POINT('Ctrl Pts',(96.1862800958604,1.14597399117042,-1.78144292815811));
#24610=CARTESIAN_POINT('Ctrl Pts',(96.1355998615186,1.1321650175806,-1.77806032880301));
#24611=CARTESIAN_POINT('Ctrl Pts',(96.1204218300319,1.12769903243303,-1.7770333684734));
#24612=CARTESIAN_POINT('Ctrl Pts',(96.0934164567984,1.11915820266238,-1.775177919535));
#24613=CARTESIAN_POINT('Ctrl Pts',(96.0815552253899,1.11519805440487,-1.77435306444595));
#24614=CARTESIAN_POINT('Ctrl Pts',(96.063555870699,1.10886824776053,-1.77308508003484));
#24615=CARTESIAN_POINT('Ctrl Pts',(96.0573705773663,1.10663468859501,-1.77264638680972));
#24616=CARTESIAN_POINT('Ctrl Pts',(96.046615419615,1.1026487822053,-1.77187824271381));
#24617=CARTESIAN_POINT('Ctrl Pts',(96.0420371270102,1.10091951563691,-1.77154955824596));
#24618=CARTESIAN_POINT('Ctrl Pts',(96.0317316808656,1.09695347657279,-1.77080580047142));
#24619=CARTESIAN_POINT('Ctrl Pts',(96.0260110346347,1.09470030406605,-1.77039019184144));
#24620=CARTESIAN_POINT('Ctrl Pts',(96.0105812905629,1.08848304426616,-1.76926162753148));
#24621=CARTESIAN_POINT('Ctrl Pts',(96.0009072628689,1.08443397908109,-1.76854586396962));
#24622=CARTESIAN_POINT('Ctrl Pts',(95.9677690356828,1.07004091986321,-1.76606499384043));
#24623=CARTESIAN_POINT('Ctrl Pts',(95.9445945127439,1.05906241155277,-1.76427917195862));
#24624=CARTESIAN_POINT('Ctrl Pts',(95.9218016575013,1.04733933507189,-1.76247028589786));
#24625=CARTESIAN_POINT('Ctrl Pts',(95.9218016746715,1.04733934390307,-1.66387871395933));
#24626=CARTESIAN_POINT('Ctrl Pts',(95.9874065823963,1.08108199314961,-1.66871641355271));
#24627=CARTESIAN_POINT('Ctrl Pts',(96.0560516960037,1.10859344400043,-1.67324998907324));
#24628=CARTESIAN_POINT('Ctrl Pts',(96.1798847932374,1.14517280797898,-1.68123788313726));
#24629=CARTESIAN_POINT('Ctrl Pts',(96.2339704036729,1.15708569258995,-1.68466684759082));
#24630=CARTESIAN_POINT('Ctrl Pts',(96.3089401753641,1.16813931648903,-1.68950332679055));
#24631=CARTESIAN_POINT('Ctrl Pts',(96.329264336922,1.17059651313738,-1.69082223599255));
#24632=CARTESIAN_POINT('Ctrl Pts',(96.3648574137405,1.17396115743478,-1.69315282719167));
#24633=CARTESIAN_POINT('Ctrl Pts',(96.3800994239755,1.17510315939306,-1.6941574650653));
#24634=CARTESIAN_POINT('Ctrl Pts',(96.4024659588175,1.17634178285479,-1.6956433513529));
#24635=CARTESIAN_POINT('Ctrl Pts',(96.4095764147224,1.17667091994869,-1.69611744143678));
#24636=CARTESIAN_POINT('Ctrl Pts',(96.4221552805284,1.17713895697171,-1.69695937082973));
#24637=CARTESIAN_POINT('Ctrl Pts',(96.4276225425088,1.17730425306818,-1.69732638473655));
#24638=CARTESIAN_POINT('Ctrl Pts',(96.4390787353004,1.17757075538391,-1.69809778303085));
#24639=CARTESIAN_POINT('Ctrl Pts',(96.4450676687329,1.1776643695043,-1.69850239123021));
#24640=CARTESIAN_POINT('Ctrl Pts',(96.4608169346172,1.17779039424939,-1.69957006866021));
#24641=CARTESIAN_POINT('Ctrl Pts',(96.4705772375064,1.1777471633159,-1.70023544804834));
#24642=CARTESIAN_POINT('Ctrl Pts',(96.5128753048144,1.17703399513266,-1.70313577864109));
#24643=CARTESIAN_POINT('Ctrl Pts',(96.5453752487215,1.17513692738986,-1.70540789179309));
#24644=CARTESIAN_POINT('Ctrl Pts',(96.5911907809928,1.17055217775959,-1.70867466683405));
#24645=CARTESIAN_POINT('Ctrl Pts',(96.6046046154995,1.16897639331651,-1.70963881378869));
#24646=CARTESIAN_POINT('Ctrl Pts',(96.697363342933,1.15645880893665,-1.71635763159815));
#24647=CARTESIAN_POINT('Ctrl Pts',(96.7754359834501,1.13767821608332,-1.72229515390929));
#24648=CARTESIAN_POINT('Ctrl Pts',(96.876669926672,1.10209925641833,-1.73010393818607));
#24649=CARTESIAN_POINT('Ctrl Pts',(96.902032010247,1.09218537439806,-1.73206796963107));
#24650=CARTESIAN_POINT('Ctrl Pts',(96.9368819535102,1.0771500779737,-1.73475840160834));
#24651=CARTESIAN_POINT('Ctrl Pts',(96.9466764950858,1.072764707066,-1.73551357681964));
#24652=CARTESIAN_POINT('Ctrl Pts',(96.9636926020061,1.06486504326818,-1.73682221424171));
#24653=CARTESIAN_POINT('Ctrl Pts',(96.9709405861838,1.06140967385204,-1.73737855158689));
#24654=CARTESIAN_POINT('Ctrl Pts',(96.9816359074506,1.0561759363987,-1.73819729657352));
#24655=CARTESIAN_POINT('Ctrl Pts',(96.9851105287744,1.0544543159644,-1.73846293664237));
#24656=CARTESIAN_POINT('Ctrl Pts',(96.9910381017498,1.05148074364423,-1.73891543248546));
#24657=CARTESIAN_POINT('Ctrl Pts',(96.9934952338924,1.05023731569194,-1.7391028006834));
#24658=CARTESIAN_POINT('Ctrl Pts',(96.9990656815541,1.04739381379419,-1.73952709955042));
#24659=CARTESIAN_POINT('Ctrl Pts',(97.0021762423927,1.04578847059808,-1.73976370091689));
#24660=CARTESIAN_POINT('Ctrl Pts',(97.0106366038505,1.04137424953121,-1.7404064571907));
#24661=CARTESIAN_POINT('Ctrl Pts',(97.0159721096619,1.03853798506619,-1.74081096439893));
#24662=CARTESIAN_POINT('Ctrl Pts',(97.0429148130358,1.02394865513482,-1.74285051377832));
#24663=CARTESIAN_POINT('Ctrl Pts',(97.0641735631732,1.01156091434871,-1.74444968237002));
#24664=CARTESIAN_POINT('Ctrl Pts',(97.1781815782754,0.940251406274959,-1.75305684475485));
#24665=CARTESIAN_POINT('Ctrl Pts',(97.2627259096116,0.869237568568173,-1.75960485505639));
#24666=CARTESIAN_POINT('Ctrl Pts',(97.3510290968172,0.771045040579024,-1.7680085092121));
#24667=CARTESIAN_POINT('Ctrl Pts',(97.3653827705877,0.754147903970396,-1.76943325672768));
#24668=CARTESIAN_POINT('Ctrl Pts',(97.3894153944185,0.724182176632936,-1.77193333585525));
#24669=CARTESIAN_POINT('Ctrl Pts',(97.3993165196055,0.711299345245394,-1.77300007966956));
#24670=CARTESIAN_POINT('Ctrl Pts',(97.4132707338397,0.692343748391156,-1.77456053789185));
#24671=CARTESIAN_POINT('Ctrl Pts',(97.4175391277476,0.686431262788284,-1.7750460077719));
#24672=CARTESIAN_POINT('Ctrl Pts',(97.4249269249468,0.675994980496577,-1.77590094643916));
#24673=CARTESIAN_POINT('Ctrl Pts',(97.4280701187247,0.671488235986576,-1.7762695020053));
#24674=CARTESIAN_POINT('Ctrl Pts',(97.4345294084826,0.662087313216371,-1.77703707545382));
#24675=CARTESIAN_POINT('Ctrl Pts',(97.4378404132863,0.657189841005155,-1.77743627005851));
#24676=CARTESIAN_POINT('Ctrl Pts',(97.4463214954682,0.64443919861429,-1.77847395690659));
#24677=CARTESIAN_POINT('Ctrl Pts',(97.451434569016,0.636548802423145,-1.77911452816184));
#24678=CARTESIAN_POINT('Ctrl Pts',(97.472069136209,0.603854720695765,-1.78176295789987));
#24679=CARTESIAN_POINT('Ctrl Pts',(97.4867569813319,0.578539912404008,-1.78380043219542));
#24680=CARTESIAN_POINT('Ctrl Pts',(97.5401676937403,0.478039140287111,-1.79184460287288));
#24681=CARTESIAN_POINT('Ctrl Pts',(97.5716883899895,0.399323475348345,-1.79807431120318));
#24682=CARTESIAN_POINT('Ctrl Pts',(97.6082085949057,0.269057959989549,-1.80797950668187));
#24683=CARTESIAN_POINT('Ctrl Pts',(97.6187374865789,0.219348781594485,-1.8116644356084));
#24684=CARTESIAN_POINT('Ctrl Pts',(97.6272038178963,0.160996968519254,-1.81577919279866));
#24685=CARTESIAN_POINT('Ctrl Pts',(97.6282962919561,0.152871222990137,-1.8163474489432));
#24686=CARTESIAN_POINT('Ctrl Pts',(97.629784415835,0.140853674689231,-1.81718023996038));
#24687=CARTESIAN_POINT('Ctrl Pts',(97.6302456477839,0.136970455985371,-1.8174481652073));
#24688=CARTESIAN_POINT('Ctrl Pts',(97.6310318523547,0.130057414186865,-1.81792296334277));
#24689=CARTESIAN_POINT('Ctrl Pts',(97.6313644169031,0.127028554451477,-1.81813024433745));
#24690=CARTESIAN_POINT('Ctrl Pts',(97.6320636612878,0.120423965173217,-1.81858059722782));
#24691=CARTESIAN_POINT('Ctrl Pts',(97.6324257295137,0.116847830151574,-1.81882341415583));
#24692=CARTESIAN_POINT('Ctrl Pts',(97.6333923449253,0.106843824659397,-1.81949993489929));
#24693=CARTESIAN_POINT('Ctrl Pts',(97.633960429977,0.100412439147494,-1.81993169298631));
#24694=CARTESIAN_POINT('Ctrl Pts',(97.6369579194472,0.0629665291762586,
-1.82242884890476));
#24695=CARTESIAN_POINT('Ctrl Pts',(97.6382108437233,0.0318672258974681,
-1.82443628325917));
#24696=CARTESIAN_POINT('Ctrl Pts',(97.6382605139807,-0.0459298935289674,
-1.82937244222079));
#24697=CARTESIAN_POINT('Ctrl Pts',(97.6355148373996,-0.0925748096218537,
-1.83225609327581));
#24698=CARTESIAN_POINT('Ctrl Pts',(97.6206686781264,-0.217546054248038,
-1.84004046210982));
#24699=CARTESIAN_POINT('Ctrl Pts',(97.6034297959604,-0.295004754101485,
-1.84494164946959));
#24700=CARTESIAN_POINT('Ctrl Pts',(97.5736905230242,-0.384836338535954,
-1.85110819682083));
#24701=CARTESIAN_POINT('Ctrl Pts',(97.5685378736786,-0.399430067267293,
-1.85212521556819));
#24702=CARTESIAN_POINT('Ctrl Pts',(97.5606123859008,-0.420542459712869,
-1.85362089413242));
#24703=CARTESIAN_POINT('Ctrl Pts',(97.5580657988696,-0.427144744270413,
-1.85409214337672));
#24704=CARTESIAN_POINT('Ctrl Pts',(97.5534415482593,-0.438819132312755,
-1.8549318828774));
#24705=CARTESIAN_POINT('Ctrl Pts',(97.5513876665051,-0.443900478019776,
-1.8552995758933));
#24706=CARTESIAN_POINT('Ctrl Pts',(97.547029319414,-0.454470168053956,-1.85606908909231));
#24707=CARTESIAN_POINT('Ctrl Pts',(97.5447185679568,-0.459955735146672,
-1.85647111091044));
#24708=CARTESIAN_POINT('Ctrl Pts',(97.5385768631842,-0.474232241061616,
-1.85752446885855));
#24709=CARTESIAN_POINT('Ctrl Pts',(97.5346800168592,-0.482994173690746,
-1.85817800364721));
#24710=CARTESIAN_POINT('Ctrl Pts',(97.5163293005834,-0.522934312399349,
-1.86119030221261));
#24711=CARTESIAN_POINT('Ctrl Pts',(97.500623440765,-0.553515327286324,-1.86359110997501));
#24712=CARTESIAN_POINT('Ctrl Pts',(97.4504137820354,-0.641574805470655,
-1.87079290214668));
#24713=CARTESIAN_POINT('Ctrl Pts',(97.4123188258956,-0.696841492116763,
-1.87570160157661));
#24714=CARTESIAN_POINT('Ctrl Pts',(97.3317802821103,-0.794669116662105,
-1.88500044629635));
#24715=CARTESIAN_POINT('Ctrl Pts',(97.2903672780105,-0.837825543313859,
-1.88937327245381));
#24716=CARTESIAN_POINT('Ctrl Pts',(97.2383605747578,-0.884363894894569,
-1.8942676152662));
#24717=CARTESIAN_POINT('Ctrl Pts',(97.2307800504178,-0.890974478804823,
-1.89496741043804));
#24718=CARTESIAN_POINT('Ctrl Pts',(97.2201091218693,-0.900042036004292,
-1.89593266403938));
#24719=CARTESIAN_POINT('Ctrl Pts',(97.2170899052438,-0.902581584145772,
-1.89620360364056));
#24720=CARTESIAN_POINT('Ctrl Pts',(97.2118609580602,-0.906935123305624,
-1.89666903385385));
#24721=CARTESIAN_POINT('Ctrl Pts',(97.2096573026681,-0.908756308064865,
-1.89686402773852));
#24722=CARTESIAN_POINT('Ctrl Pts',(97.2049960683024,-0.912580051288523,
-1.89727401811257));
#24723=CARTESIAN_POINT('Ctrl Pts',(97.202536995926,-0.914580743579433,-1.89748887538521));
#24724=CARTESIAN_POINT('Ctrl Pts',(97.1964179716491,-0.91951823334458,-1.89802004799025));
#24725=CARTESIAN_POINT('Ctrl Pts',(97.1927484399336,-0.922443172414382,
-1.89833553597576));
#24726=CARTESIAN_POINT('Ctrl Pts',(97.1788612707817,-0.933377373063629,
-1.8995184657339));
#24727=CARTESIAN_POINT('Ctrl Pts',(97.1685284767702,-0.941239788765041,
-1.90037634373999));
#24728=CARTESIAN_POINT('Ctrl Pts',(97.1416739331571,-0.960981349964681,
-1.90255552620151));
#24729=CARTESIAN_POINT('Ctrl Pts',(97.1249700737067,-0.972606465951632,
-1.90386339315204));
#24730=CARTESIAN_POINT('Ctrl Pts',(97.0593589304402,-1.01578895622613,-1.90885462969111));
#24731=CARTESIAN_POINT('Ctrl Pts',(97.0084378516857,-1.04413892500902,-1.91242766571903));
#24732=CARTESIAN_POINT('Ctrl Pts',(96.8872956799053,-1.10027080822645,-1.92069505608037));
#24733=CARTESIAN_POINT('Ctrl Pts',(96.8160951131574,-1.12530130705123,-1.92539903317699));
#24734=CARTESIAN_POINT('Ctrl Pts',(96.7329126849427,-1.14585511199141,-1.93102252777811));
#24735=CARTESIAN_POINT('Ctrl Pts',(96.7227950213598,-1.14821352746912,-1.93170831843164));
#24736=CARTESIAN_POINT('Ctrl Pts',(96.7060785763117,-1.15187763910823,-1.9328449861449));
#24737=CARTESIAN_POINT('Ctrl Pts',(96.699497318131,-1.15326122892853,-1.93329340389738));
#24738=CARTESIAN_POINT('Ctrl Pts',(96.6875831576846,-1.15565960203979,-1.9341069930619));
#24739=CARTESIAN_POINT('Ctrl Pts',(96.6822543662831,-1.15669402984175,-1.93447153491668));
#24740=CARTESIAN_POINT('Ctrl Pts',(96.670801761285,-1.15883516657506,-1.93525649277245));
#24741=CARTESIAN_POINT('Ctrl Pts',(96.6646759690419,-1.1599302472946,-1.9356772620017));
#24742=CARTESIAN_POINT('Ctrl Pts',(96.6478634735958,-1.16279843453487,-1.93683471821879));
#24743=CARTESIAN_POINT('Ctrl Pts',(96.6371607571133,-1.1644726882509,-1.93757446383531));
#24744=CARTESIAN_POINT('Ctrl Pts',(96.5736196088846,-1.17351645522519,-1.94198479108199));
#24745=CARTESIAN_POINT('Ctrl Pts',(96.5203604817114,-1.17743543172055,-1.94576135206359));
#24746=CARTESIAN_POINT('Ctrl Pts',(96.4190680711731,-1.17799831779682,-1.95308254129094));
#24747=CARTESIAN_POINT('Ctrl Pts',(96.3711411256809,-1.17533528221762,-1.9566046712098));
#24748=CARTESIAN_POINT('Ctrl Pts',(96.2954957105057,-1.16647788133756,-1.96219259277469));
#24749=CARTESIAN_POINT('Ctrl Pts',(96.2676047627264,-1.16219174298689,-1.96425856314758));
#24750=CARTESIAN_POINT('Ctrl Pts',(96.2058590884811,-1.15041872861541,-1.96881599617489));
#24751=CARTESIAN_POINT('Ctrl Pts',(96.1721235347652,-1.14242988414127,-1.97129499455205));
#24752=CARTESIAN_POINT('Ctrl Pts',(96.132953736093,-1.13130798094432,-1.97412513785748));
#24753=CARTESIAN_POINT('Ctrl Pts',(96.1271339448916,-1.12960683499036,-1.97454435338091));
#24754=CARTESIAN_POINT('Ctrl Pts',(96.1176636671205,-1.12675907364142,-1.9752241408954));
#24755=CARTESIAN_POINT('Ctrl Pts',(96.1140052593695,-1.12563950548969,-1.97548616266111));
#24756=CARTESIAN_POINT('Ctrl Pts',(96.1074477932438,-1.12359775146555,-1.97595469207535));
#24757=CARTESIAN_POINT('Ctrl Pts',(96.1045468020532,-1.12268214550473,-1.9761615634761));
#24758=CARTESIAN_POINT('Ctrl Pts',(96.0981617034755,-1.12063965404669,-1.97661599682087));
#24759=CARTESIAN_POINT('Ctrl Pts',(96.094679286976,-1.11950775560829,-1.97686326712941));
#24760=CARTESIAN_POINT('Ctrl Pts',(96.0845942405277,-1.11617770521514,-1.97757783958933));
#24761=CARTESIAN_POINT('Ctrl Pts',(96.0780056044128,-1.11393720818433,-1.9780427794997));
#24762=CARTESIAN_POINT('Ctrl Pts',(96.0221564836363,-1.09439149808431,-1.98197082297189));
#24763=CARTESIAN_POINT('Ctrl Pts',(95.9740704020626,-1.07388422725954,-1.98526734000446));
#24764=CARTESIAN_POINT('Ctrl Pts',(95.8532897133958,-1.01259029501949,-1.99370416261204));
#24765=CARTESIAN_POINT('Ctrl Pts',(95.7832845678811,-0.967173702669729,
-1.99876819556398));
#24766=CARTESIAN_POINT('Ctrl Pts',(95.6947438146386,-0.895370948082752,
-2.00603938127244));
#24767=CARTESIAN_POINT('Ctrl Pts',(95.6716077258846,-0.875055013142423,
-2.00803071755667));
#24768=CARTESIAN_POINT('Ctrl Pts',(95.6423575451058,-0.847266622960754,
-2.01068964197776));
#24769=CARTESIAN_POINT('Ctrl Pts',(95.6355006037616,-0.840591491429218,
-2.01132372590403));
#24770=CARTESIAN_POINT('Ctrl Pts',(95.6245147643332,-0.829633038820408,
-2.01235776537758));
#24771=CARTESIAN_POINT('Ctrl Pts',(95.6203355512092,-0.825400599332993,
-2.01275550724539));
#24772=CARTESIAN_POINT('Ctrl Pts',(95.6123664543246,-0.817206778744284,
-2.01352252353536));
#24773=CARTESIAN_POINT('Ctrl Pts',(95.6085718098671,-0.813250227308947,
-2.01389157855539));
#24774=CARTESIAN_POINT('Ctrl Pts',(95.5998524921288,-0.804030887944494,
-2.01474860396121));
#24775=CARTESIAN_POINT('Ctrl Pts',(95.5949482742703,-0.798749143673022,
-2.01523742210443));
#24776=CARTESIAN_POINT('Ctrl Pts',(95.5794665227027,-0.78176560013576,-2.01680261402721));
#24777=CARTESIAN_POINT('Ctrl Pts',(95.5690758420639,-0.769896594638083,
-2.01788663143811));
#24778=CARTESIAN_POINT('Ctrl Pts',(95.5452039149818,-0.741497048947946,
-2.02045895531311));
#24779=CARTESIAN_POINT('Ctrl Pts',(95.5319275382242,-0.724802309666254,
-2.02195475662898));
#24780=CARTESIAN_POINT('Ctrl Pts',(95.4834162532731,-0.660278773097111,
-2.02767581048405));
#24781=CARTESIAN_POINT('Ctrl Pts',(95.451366895428,-0.610172826389735,-2.03200363925536));
#24782=CARTESIAN_POINT('Ctrl Pts',(95.3899054552065,-0.495897761151994,
-2.04152244327016));
#24783=CARTESIAN_POINT('Ctrl Pts',(95.362192718275,-0.431058259368894,-2.0467080650873));
#24784=CARTESIAN_POINT('Ctrl Pts',(95.3373936634184,-0.354776947256575,
-2.05233001573151));
#24785=CARTESIAN_POINT('Ctrl Pts',(95.3344709065608,-0.345388380519731,
-2.05301383583765));
#24786=CARTESIAN_POINT('Ctrl Pts',(95.3305565283764,-0.332236347547889,
-2.05395945255309));
#24787=CARTESIAN_POINT('Ctrl Pts',(95.3294655539239,-0.328503217833987,
-2.05422648470844));
#24788=CARTESIAN_POINT('Ctrl Pts',(95.3276086492878,-0.322030287390161,
-2.05468703632373));
#24789=CARTESIAN_POINT('Ctrl Pts',(95.3268341245526,-0.31929301794782,-2.05488103531357));
#24790=CARTESIAN_POINT('Ctrl Pts',(95.3252129797206,-0.313483420095382,
-2.05529113359179));
#24791=CARTESIAN_POINT('Ctrl Pts',(95.3243688958972,-0.310410405840028,
-2.05550708195386));
#24792=CARTESIAN_POINT('Ctrl Pts',(95.3222918089693,-0.302726481838246,
-2.05604470500677));
#24793=CARTESIAN_POINT('Ctrl Pts',(95.3210743258583,-0.29811137244346,-2.05636550770561));
#24794=CARTESIAN_POINT('Ctrl Pts',(95.31650229571,-0.28034293330303,-2.05759299582215));
#24795=CARTESIAN_POINT('Ctrl Pts',(95.3133470291543,-0.267138780883901,
-2.05848916391478));
#24796=CARTESIAN_POINT('Ctrl Pts',(95.305753650268,-0.232741572011814,-2.06078936372328));
#24797=CARTESIAN_POINT('Ctrl Pts',(95.3016702261665,-0.211474814148675,
-2.06217800425422));
#24798=CARTESIAN_POINT('Ctrl Pts',(95.2816534953787,-0.0890929820410691,
-2.07003976284231));
#24799=CARTESIAN_POINT('Ctrl Pts',(95.2783694083926,0.0136439714255365,
-2.07617658459706));
#24800=CARTESIAN_POINT('Ctrl Pts',(95.2915904042699,0.147789031022744,-2.08475842122349));
#24801=CARTESIAN_POINT('Ctrl Pts',(95.2961024178252,0.179913992057985,-2.08685341434649));
#24802=CARTESIAN_POINT('Ctrl Pts',(95.303686783858,0.221398596969202,-2.08963160044901));
#24803=CARTESIAN_POINT('Ctrl Pts',(95.3055587718141,0.230965007125942,-2.09027730355239));
#24804=CARTESIAN_POINT('Ctrl Pts',(95.3087718284124,0.246367623958067,-2.09132560597837));
#24805=CARTESIAN_POINT('Ctrl Pts',(95.3100390646057,0.252218898923648,-2.09172587506654));
#24806=CARTESIAN_POINT('Ctrl Pts',(95.3125495019763,0.26339776159507,-2.09249460044943));
#24807=CARTESIAN_POINT('Ctrl Pts',(95.3137853221664,0.268726860490963,-2.09286281410708));
#24808=CARTESIAN_POINT('Ctrl Pts',(95.3167158035357,0.280975266883418,-2.09371325295312));
#24809=CARTESIAN_POINT('Ctrl Pts',(95.3184361926592,0.287888136673279,-2.09419628392865));
#24810=CARTESIAN_POINT('Ctrl Pts',(95.3240523328934,0.309612015123492,-2.09572409499397));
#24811=CARTESIAN_POINT('Ctrl Pts',(95.328174182506,0.32436237098646,-2.09677601280118));
#24812=CARTESIAN_POINT('Ctrl Pts',(95.3384901252528,0.35868210911169,-2.09925886757043));
#24813=CARTESIAN_POINT('Ctrl Pts',(95.3449103518647,0.378177761334242,-2.10069661058697));
#24814=CARTESIAN_POINT('Ctrl Pts',(95.3705899389253,0.449800181929712,-2.10608127203403));
#24815=CARTESIAN_POINT('Ctrl Pts',(95.3930196824107,0.500707332150847,-2.11011792912098));
#24816=CARTESIAN_POINT('Ctrl Pts',(95.4545027180122,0.617171342732483,-2.11977013420041));
#24817=CARTESIAN_POINT('Ctrl Pts',(95.4964986029307,0.68090572496438,-2.12539964852766));
#24818=CARTESIAN_POINT('Ctrl Pts',(95.5503250319758,0.747530235764814,-2.13139870292436));
#24819=CARTESIAN_POINT('Ctrl Pts',(95.5563824195848,0.754845090088789,-2.13205885514755));
#24820=CARTESIAN_POINT('Ctrl Pts',(95.5650192417168,0.765021709966009,-2.13297847466055));
#24821=CARTESIAN_POINT('Ctrl Pts',(95.5675250487094,0.767945080791811,-2.13324278901702));
#24822=CARTESIAN_POINT('Ctrl Pts',(95.5720851644442,0.773212587646627,-2.13371922149339));
#24823=CARTESIAN_POINT('Ctrl Pts',(95.5741345246612,0.775560953496885,-2.13393168838374));
#24824=CARTESIAN_POINT('Ctrl Pts',(95.578352361229,0.780355625430431,-2.13436556575212));
#24825=CARTESIAN_POINT('Ctrl Pts',(95.5805217367298,0.782801081314822,-2.13458690760109));
#24826=CARTESIAN_POINT('Ctrl Pts',(95.5861366793817,0.789077758534844,-2.13515524262775));
#24827=CARTESIAN_POINT('Ctrl Pts',(95.5895973023677,0.792895508432947,-2.13550114534366));
#24828=CARTESIAN_POINT('Ctrl Pts',(95.6043853220042,0.808995987230278,-2.1369614641421));
#24829=CARTESIAN_POINT('Ctrl Pts',(95.6159489887381,0.821060331371248,-2.13805958305258));
#24830=CARTESIAN_POINT('Ctrl Pts',(95.6484130874932,0.853518175164644,-2.14103866602832));
#24831=CARTESIAN_POINT('Ctrl Pts',(95.669821961519,0.873387709907603,-2.14289050491705));
#24832=CARTESIAN_POINT('Ctrl Pts',(95.7622086602951,0.952947103714888,-2.15053576523997));
#24833=CARTESIAN_POINT('Ctrl Pts',(95.8393593761262,1.00493669980411,-2.15613886709878));
#24834=CARTESIAN_POINT('Ctrl Pts',(95.9218016761257,1.04733934465099,-2.16205147885552));
#24835=CARTESIAN_POINT('Origin',(96.460480949577,-7.19464945638997E-16,
0.924367114736168));
#24836=CARTESIAN_POINT('',(95.9218016730065,1.04733934304672,-2.76054963702842));
#24837=CARTESIAN_POINT('',(95.9218019448245,1.0473394828511,-2.66237442964626));
#24838=CARTESIAN_POINT('',(95.9218016730721,1.04733934308042,0.924367114736168));
#24839=CARTESIAN_POINT('Ctrl Pts',(95.9218016730066,1.04733934304671,-2.76054963702842));
#24840=CARTESIAN_POINT('Ctrl Pts',(95.9132326700124,1.04293203765476,-2.75987336368931));
#24841=CARTESIAN_POINT('Ctrl Pts',(95.9047176184765,1.03841949818406,-2.75920210559037));
#24842=CARTESIAN_POINT('Ctrl Pts',(95.892070821155,1.03151720700366,-2.75820730834097));
#24843=CARTESIAN_POINT('Ctrl Pts',(95.8878970085419,1.02920622562853,-2.75787935535442));
#24844=CARTESIAN_POINT('Ctrl Pts',(95.880958974298,1.02530946377949,-2.75733495101369));
#24845=CARTESIAN_POINT('Ctrl Pts',(95.8781869792196,1.02373773455601,-2.75711764169615));
#24846=CARTESIAN_POINT('Ctrl Pts',(95.8729518840646,1.02074127761324,-2.75670766670104));
#24847=CARTESIAN_POINT('Ctrl Pts',(95.870487517152,1.01931884549374,-2.756514854594));
#24848=CARTESIAN_POINT('Ctrl Pts',(95.8646652080301,1.01593002053431,-2.7560596834621));
#24849=CARTESIAN_POINT('Ctrl Pts',(95.8613117824295,1.01395587414073,-2.75579781249062));
#24850=CARTESIAN_POINT('Ctrl Pts',(95.8495100623163,1.00692926083719,-2.75487701030639));
#24851=CARTESIAN_POINT('Ctrl Pts',(95.8411151079147,1.00178736822337,-2.75422346941753));
#24852=CARTESIAN_POINT('Ctrl Pts',(95.773446678617,0.959164740115963,-2.74895905624444));
#24853=CARTESIAN_POINT('Ctrl Pts',(95.7175563549036,0.916558161321671,-2.74462789144687));
#24854=CARTESIAN_POINT('Ctrl Pts',(95.6218308237605,0.829040268364834,-2.73660475868495));
#24855=CARTESIAN_POINT('Ctrl Pts',(95.5809914824081,0.785582216163863,-2.73292642696949));
#24856=CARTESIAN_POINT('Ctrl Pts',(95.5302086309947,0.722595810722305,-2.72777066552846));
#24857=CARTESIAN_POINT('Ctrl Pts',(95.5172576316956,0.70560681908888,-2.72639623289441));
#24858=CARTESIAN_POINT('Ctrl Pts',(95.495547289152,0.675460945201987,-2.72397653692191));
#24859=CARTESIAN_POINT('Ctrl Pts',(95.4865773762583,0.662462262333529,-2.72293910632019));
#24860=CARTESIAN_POINT('Ctrl Pts',(95.4738963523066,0.643271246522407,-2.72141377573689));
#24861=CARTESIAN_POINT('Ctrl Pts',(95.4699762599913,0.637218581191932,-2.72093359796891));
#24862=CARTESIAN_POINT('Ctrl Pts',(95.463173819102,0.626501088529011,-2.72008470958096));
#24863=CARTESIAN_POINT('Ctrl Pts',(95.4602679755132,0.621851373887671,-2.71971687105228));
#24864=CARTESIAN_POINT('Ctrl Pts',(95.4542781979452,0.61211637337145,-2.71894756972824));
#24865=CARTESIAN_POINT('Ctrl Pts',(95.4512001104402,0.607027690847516,-2.71854590871304));
#24866=CARTESIAN_POINT('Ctrl Pts',(95.4432728702976,0.593695422780612,-2.71749465214029));
#24867=CARTESIAN_POINT('Ctrl Pts',(95.4384854407034,0.585415836879434,-2.71684287444403));
#24868=CARTESIAN_POINT('Ctrl Pts',(95.4187449981887,0.550295612979295,-2.71408199030836));
#24869=CARTESIAN_POINT('Ctrl Pts',(95.4047456371014,0.522935660261184,-2.71194000590012));
#24870=CARTESIAN_POINT('Ctrl Pts',(95.3568293065428,0.419502723563992,-2.70386919794851));
#24871=CARTESIAN_POINT('Ctrl Pts',(95.3299418540142,0.340451820068217,-2.69773171614675));
#24872=CARTESIAN_POINT('Ctrl Pts',(95.3001198958196,0.208291414447175,-2.68781384935152));
#24873=CARTESIAN_POINT('Ctrl Pts',(95.2920237059147,0.15662714272836,-2.68402429129148));
#24874=CARTESIAN_POINT('Ctrl Pts',(95.2867661979487,0.0976584868549712,
-2.67990658432241));
#24875=CARTESIAN_POINT('Ctrl Pts',(95.2862095877352,0.0907208512844635,
-2.67942540920466));
#24876=CARTESIAN_POINT('Ctrl Pts',(95.285453997222,0.0801257395010773,-2.67869595457418));
#24877=CARTESIAN_POINT('Ctrl Pts',(95.2852105351485,0.0764717384222711,
-2.67844536076252));
#24878=CARTESIAN_POINT('Ctrl Pts',(95.284796017663,0.0697800774980152,-2.67798830329868));
#24879=CARTESIAN_POINT('Ctrl Pts',(95.2846196878171,0.0667428789052191,
-2.67778156355324));
#24880=CARTESIAN_POINT('Ctrl Pts',(95.2842481656671,0.0598843872547714,
-2.67731629199523));
#24881=CARTESIAN_POINT('Ctrl Pts',(95.2840598239468,0.0560628039403301,
-2.67705813837584));
#24882=CARTESIAN_POINT('Ctrl Pts',(95.283621147861,0.0461826494926399,-2.6763933993011));
#24883=CARTESIAN_POINT('Ctrl Pts',(95.2833989683099,0.0401228513938409,
-2.6759882979907));
#24884=CARTESIAN_POINT('Ctrl Pts',(95.2822214008785,-0.000577114962096968,
-2.6732833319678));
#24885=CARTESIAN_POINT('Ctrl Pts',(95.2827483543245,-0.0352467980099046,
-2.6710560519316));
#24886=CARTESIAN_POINT('Ctrl Pts',(95.2864756322027,-0.0979857646210639,
-2.66708476957346));
#24887=CARTESIAN_POINT('Ctrl Pts',(95.2891571902659,-0.12605739482188,-2.66532950534991));
#24888=CARTESIAN_POINT('Ctrl Pts',(95.2991116459099,-0.201529397122044,
-2.66060953932032));
#24889=CARTESIAN_POINT('Ctrl Pts',(95.3082749595134,-0.248624258484052,
-2.65766179375882));
#24890=CARTESIAN_POINT('Ctrl Pts',(95.3336540176208,-0.346706615069992,
-2.6513264108395));
#24891=CARTESIAN_POINT('Ctrl Pts',(95.3505217365088,-0.397408946056569,
-2.64793326244505));
#24892=CARTESIAN_POINT('Ctrl Pts',(95.3748779750875,-0.456813568012807,
-2.64371355054553));
#24893=CARTESIAN_POINT('Ctrl Pts',(95.3791262430919,-0.466780933756201,
-2.64299710562028));
#24894=CARTESIAN_POINT('Ctrl Pts',(95.3860303154601,-0.482379136910381,
-2.64186188057145));
#24895=CARTESIAN_POINT('Ctrl Pts',(95.3885943526769,-0.488050118080993,
-2.64144619183088));
#24896=CARTESIAN_POINT('Ctrl Pts',(95.3934788448068,-0.498629162894915,
-2.64066504532463));
#24897=CARTESIAN_POINT('Ctrl Pts',(95.3957885312433,-0.503542040276796,
-2.64029996176263));
#24898=CARTESIAN_POINT('Ctrl Pts',(95.4010354462312,-0.514505120431153,
-2.63947997312528));
#24899=CARTESIAN_POINT('Ctrl Pts',(95.4039906802311,-0.520546444655338,
-2.63902446021902));
#24900=CARTESIAN_POINT('Ctrl Pts',(95.4116421135927,-0.535854534768218,
-2.63786074671339));
#24901=CARTESIAN_POINT('Ctrl Pts',(95.4164093985132,-0.545084920518406,
-2.63715011576225));
#24902=CARTESIAN_POINT('Ctrl Pts',(95.4568102221068,-0.620833745483993,
-2.6312424878994));
#24903=CARTESIAN_POINT('Ctrl Pts',(95.4986325805745,-0.683837190365049,
-2.62582386383385));
#24904=CARTESIAN_POINT('Ctrl Pts',(95.5826232342057,-0.787275482515682,
-2.61607681347653));
#24905=CARTESIAN_POINT('Ctrl Pts',(95.6223178531364,-0.829409264769488,
-2.61180722784019));
#24906=CARTESIAN_POINT('Ctrl Pts',(95.6800625896936,-0.882305204673697,
-2.60615228369523));
#24907=CARTESIAN_POINT('Ctrl Pts',(95.6955385149769,-0.895755804946732,
-2.60468535183273));
#24908=CARTESIAN_POINT('Ctrl Pts',(95.7214307611859,-0.917098829506772,
-2.6023188779206));
#24909=CARTESIAN_POINT('Ctrl Pts',(95.7316408326781,-0.925233788525854,
-2.6014069955598));
#24910=CARTESIAN_POINT('Ctrl Pts',(95.7457105973547,-0.936066514414634,
-2.6001812959823));
#24911=CARTESIAN_POINT('Ctrl Pts',(95.7494538660239,-0.938913022683455,
-2.5998581083639));
#24912=CARTESIAN_POINT('Ctrl Pts',(95.7557507696648,-0.943642145952737,
-2.59931943395281));
#24913=CARTESIAN_POINT('Ctrl Pts',(95.7582951114067,-0.94553697735684,-2.59910312587095));
#24914=CARTESIAN_POINT('Ctrl Pts',(95.7631456115349,-0.949118882335257,
-2.5986933650031));
#24915=CARTESIAN_POINT('Ctrl Pts',(95.7654502949104,-0.95080787544305,-2.59849977651576));
#24916=CARTESIAN_POINT('Ctrl Pts',(95.7709464485528,-0.95480508337946,-2.5980406764789));
#24917=CARTESIAN_POINT('Ctrl Pts',(95.7741434211886,-0.957105727482686,
-2.59777567343577));
#24918=CARTESIAN_POINT('Ctrl Pts',(95.7855117915613,-0.965200517928264,
-2.59684030872439));
#24919=CARTESIAN_POINT('Ctrl Pts',(95.7937457778294,-0.970906602694444,
-2.59617553101507));
#24920=CARTESIAN_POINT('Ctrl Pts',(95.8512878314194,-1.00970545766571,-2.59160946754066));
#24921=CARTESIAN_POINT('Ctrl Pts',(95.9029707410279,-1.03913692330457,-2.58790632066354));
#24922=CARTESIAN_POINT('Ctrl Pts',(96.0078716847108,-1.08878375329629,-2.58071482083196));
#24923=CARTESIAN_POINT('Ctrl Pts',(96.0607642823805,-1.10929325087114,-2.57723288641729));
#24924=CARTESIAN_POINT('Ctrl Pts',(96.1567222586179,-1.13874367171073,-2.57090918349167));
#24925=CARTESIAN_POINT('Ctrl Pts',(96.1991955152977,-1.14923268047579,-2.5681087357492));
#24926=CARTESIAN_POINT('Ctrl Pts',(96.2522749173291,-1.15924607773393,-2.56455466162513));
#24927=CARTESIAN_POINT('Ctrl Pts',(96.2624239905387,-1.1610231050887,-2.56387278567349));
#24928=CARTESIAN_POINT('Ctrl Pts',(96.2786250135422,-1.16364117920164,-2.56278002424777));
#24929=CARTESIAN_POINT('Ctrl Pts',(96.2846626045186,-1.16456871097074,-2.56237184692209));
#24930=CARTESIAN_POINT('Ctrl Pts',(96.2960943641671,-1.16623400402922,-2.56159708921766));
#24931=CARTESIAN_POINT('Ctrl Pts',(96.3014869830829,-1.16698141310375,-2.56123082055764));
#24932=CARTESIAN_POINT('Ctrl Pts',(96.3137255388461,-1.16859125501356,-2.56039767340886));
#24933=CARTESIAN_POINT('Ctrl Pts',(96.3205742108226,-1.16943096111729,-2.55993010060691));
#24934=CARTESIAN_POINT('Ctrl Pts',(96.3414664401814,-1.1718063769318,-2.55849943774581));
#24935=CARTESIAN_POINT('Ctrl Pts',(96.3555301615037,-1.17314958145816,-2.55753044246678));
#24936=CARTESIAN_POINT('Ctrl Pts',(96.4677409338544,-1.18183284990217,-2.54974864701727));
#24937=CARTESIAN_POINT('Ctrl Pts',(96.5664149179669,-1.17709468562892,-2.54254993508713));
#24938=CARTESIAN_POINT('Ctrl Pts',(96.6737418331414,-1.15832925665328,-2.5345588502835));
#24939=CARTESIAN_POINT('Ctrl Pts',(96.6841328731772,-1.15636788774511,-2.53378402479718));
#24940=CARTESIAN_POINT('Ctrl Pts',(96.7276895862205,-1.14753723154596,-2.53053399668305));
#24941=CARTESIAN_POINT('Ctrl Pts',(96.7605796149405,-1.1393784508278,-2.52807416702513));
#24942=CARTESIAN_POINT('Ctrl Pts',(96.8107558610486,-1.12460761312354,-2.52435190151598));
#24943=CARTESIAN_POINT('Ctrl Pts',(96.8283141461546,-1.11898777010534,-2.52305536999265));
#24944=CARTESIAN_POINT('Ctrl Pts',(96.8507746358994,-1.11121300777785,-2.52141076602248));
#24945=CARTESIAN_POINT('Ctrl Pts',(96.8558030662223,-1.10943406160253,-2.52104348669315));
#24946=CARTESIAN_POINT('Ctrl Pts',(96.8639313669201,-1.10649616946514,-2.5204514680714));
#24947=CARTESIAN_POINT('Ctrl Pts',(96.8670386721522,-1.10535823658944,-2.52022554916265));
#24948=CARTESIAN_POINT('Ctrl Pts',(96.873041241769,-1.10313128670861,-2.51978995775108));
#24949=CARTESIAN_POINT('Ctrl Pts',(96.8759370572823,-1.10204394342511,-2.51958019645816));
#24950=CARTESIAN_POINT('Ctrl Pts',(96.8823408312129,-1.09961057645859,-2.51911711164722));
#24951=CARTESIAN_POINT('Ctrl Pts',(96.8858467329977,-1.09825913647596,-2.51886410315168));
#24952=CARTESIAN_POINT('Ctrl Pts',(96.8983054391025,-1.09338799969193,-2.51796664718892));
#24953=CARTESIAN_POINT('Ctrl Pts',(96.9072218125448,-1.08977530595421,-2.51732739449785));
#24954=CARTESIAN_POINT('Ctrl Pts',(96.9883047012481,-1.05576007689642,-2.5115332611692));
#24955=CARTESIAN_POINT('Ctrl Pts',(97.0573257710082,-1.01833545942506,-2.50673121529573));
#24956=CARTESIAN_POINT('Ctrl Pts',(97.1669000083131,-0.943925914991809,
-2.49853612655973));
#24957=CARTESIAN_POINT('Ctrl Pts',(97.2095209644715,-0.910473751476987,
-2.49517783287065));
#24958=CARTESIAN_POINT('Ctrl Pts',(97.2646882657054,-0.860670680325778,
-2.49043221028096));
#24959=CARTESIAN_POINT('Ctrl Pts',(97.2793364466014,-0.846746143664709,
-2.48912964590121));
#24960=CARTESIAN_POINT('Ctrl Pts',(97.3043150722962,-0.821746952825859,
-2.48682533905843));
#24961=CARTESIAN_POINT('Ctrl Pts',(97.314803824049,-0.810836896909026,-2.48583041692453));
#24962=CARTESIAN_POINT('Ctrl Pts',(97.3298937954042,-0.79452290230653,-2.48435620485798));
#24963=CARTESIAN_POINT('Ctrl Pts',(97.3346613177015,-0.789274362364304,
-2.48388390996832));
#24964=CARTESIAN_POINT('Ctrl Pts',(97.3430199499101,-0.779903749603985,
-2.48304398486726));
#24965=CARTESIAN_POINT('Ctrl Pts',(97.3466303290093,-0.775799085697534,
-2.48267716611391));
#24966=CARTESIAN_POINT('Ctrl Pts',(97.3541458291074,-0.767133752321216,
-2.48190497617916));
#24967=CARTESIAN_POINT('Ctrl Pts',(97.3580449020178,-0.762568068983827,
-2.48149937305658));
#24968=CARTESIAN_POINT('Ctrl Pts',(97.3682316772607,-0.750453329889654,
-2.48042629140322));
#24969=CARTESIAN_POINT('Ctrl Pts',(97.3744600124358,-0.742855198855763,
-2.47975646042801));
#24970=CARTESIAN_POINT('Ctrl Pts',(97.4012576065385,-0.709316792701429,
-2.47681283682992));
#24971=CARTESIAN_POINT('Ctrl Pts',(97.4208211952784,-0.682595979410996,
-2.47450051388395));
#24972=CARTESIAN_POINT('Ctrl Pts',(97.4957537622936,-0.570641210241875,
-2.46493643583014));
#24973=CARTESIAN_POINT('Ctrl Pts',(97.5411051168979,-0.479236541255961,
-2.45735951257017));
#24974=CARTESIAN_POINT('Ctrl Pts',(97.5811851486512,-0.362744745057588,
-2.44845009689676));
#24975=CARTESIAN_POINT('Ctrl Pts',(97.5876499191631,-0.342128454431495,
-2.4469020651035));
#24976=CARTESIAN_POINT('Ctrl Pts',(97.5972420268341,-0.308306638459812,
-2.44442038685505));
#24977=CARTESIAN_POINT('Ctrl Pts',(97.6007146305804,-0.295204881632774,
-2.44347295933262));
#24978=CARTESIAN_POINT('Ctrl Pts',(97.6051028414988,-0.277414026042835,
-2.44220775933716));
#24979=CARTESIAN_POINT('Ctrl Pts',(97.6062170770942,-0.272775631939352,
-2.44187984385729));
#24980=CARTESIAN_POINT('Ctrl Pts',(97.6080285496197,-0.265027774515217,
-2.44133548468442));
#24981=CARTESIAN_POINT('Ctrl Pts',(97.60874139372,-0.261922066207795,-2.44111818331832));
#24982=CARTESIAN_POINT('Ctrl Pts',(97.6100669345032,-0.256037541028123,
-2.44070821035799));
#24983=CARTESIAN_POINT('Ctrl Pts',(97.6106821782182,-0.253259339857263,
-2.44051539241732));
#24984=CARTESIAN_POINT('Ctrl Pts',(97.6121150114231,-0.246676295779057,
-2.44006019145954));
#24985=CARTESIAN_POINT('Ctrl Pts',(97.6129238295065,-0.242869547020777,
-2.4397982966511));
#24986=CARTESIAN_POINT('Ctrl Pts',(97.6157122932551,-0.229417843759671,
-2.43887732551677));
#24987=CARTESIAN_POINT('Ctrl Pts',(97.6175899138848,-0.219751825293636,
-2.43822364210268));
#24988=CARTESIAN_POINT('Ctrl Pts',(97.6318464937271,-0.141101832452653,
-2.4329619885993));
#24989=CARTESIAN_POINT('Ctrl Pts',(97.6381680957031,-0.0711524774354224,
-2.42863335731764));
#24990=CARTESIAN_POINT('Ctrl Pts',(97.6383030814189,0.0805299389287755,
-2.41925057438884));
#24991=CARTESIAN_POINT('Ctrl Pts',(97.6299002013654,0.161884590980388,-2.41420906871187));
#24992=CARTESIAN_POINT('Ctrl Pts',(97.6099982017247,0.256792756807976,-2.4078889105746));
#24993=CARTESIAN_POINT('Ctrl Pts',(97.6065407504146,0.271807524029241,-2.40687633979508));
#24994=CARTESIAN_POINT('Ctrl Pts',(97.6010699376831,0.293601305789225,-2.40538597542467));
#24995=CARTESIAN_POINT('Ctrl Pts',(97.5992884016742,0.300437264602398,-2.40491551607905));
#24996=CARTESIAN_POINT('Ctrl Pts',(97.5960160250482,0.31254628200428,-2.4040766558953));
#24997=CARTESIAN_POINT('Ctrl Pts',(97.5945496662619,0.317825785811986,-2.40370904618093));
#24998=CARTESIAN_POINT('Ctrl Pts',(97.5914118184313,0.328825091880758,-2.40293916890459));
#24999=CARTESIAN_POINT('Ctrl Pts',(97.5897336564111,0.334542811963291,-2.40253669607429));
#25000=CARTESIAN_POINT('Ctrl Pts',(97.5852337036935,0.349455009413571,-2.40148094315736));
#25001=CARTESIAN_POINT('Ctrl Pts',(97.5823425979218,0.358627932482312,-2.40082544624442));
#25002=CARTESIAN_POINT('Ctrl Pts',(97.5685107475972,0.400708932075501,-2.39778952706867));
#25003=CARTESIAN_POINT('Ctrl Pts',(97.5562332357401,0.433156071046556,-2.39536624628245));
#25004=CARTESIAN_POINT('Ctrl Pts',(97.5156337119749,0.527629438455172,-2.38805827740896));
#25005=CARTESIAN_POINT('Ctrl Pts',(97.4833419703187,0.58778704486304,-2.38306170778515));
#25006=CARTESIAN_POINT('Ctrl Pts',(97.4312999513706,0.667330430498391,-2.37608704485976));
#25007=CARTESIAN_POINT('Ctrl Pts',(97.4157965552207,0.689341429891389,-2.37411511549226));
#25008=CARTESIAN_POINT('Ctrl Pts',(97.3930575780121,0.719382860231116,-2.37137929811483));
#25009=CARTESIAN_POINT('Ctrl Pts',(97.3864454226472,0.727874077618951,-2.37060084261849));
#25010=CARTESIAN_POINT('Ctrl Pts',(97.3629914327436,0.757156353660903,-2.36790095450983));
#25011=CARTESIAN_POINT('Ctrl Pts',(97.3455569049934,0.777464933731278,-2.36600081347821));
#25012=CARTESIAN_POINT('Ctrl Pts',(97.32325121528,0.801723709791192,-2.36371342182215));
#25013=CARTESIAN_POINT('Ctrl Pts',(97.3190222087448,0.806250797645612,-2.36328577202934));
#25014=CARTESIAN_POINT('Ctrl Pts',(97.3123238844396,0.813308782407185,-2.36261809377447));
#25015=CARTESIAN_POINT('Ctrl Pts',(97.3098786293201,0.815862208765486,-2.36237634422714));
#25016=CARTESIAN_POINT('Ctrl Pts',(97.3055118452146,0.82038125477079,-2.36194820581087));
#25017=CARTESIAN_POINT('Ctrl Pts',(97.3035949341689,0.822351157964499,-2.36176148184408));
#25018=CARTESIAN_POINT('Ctrl Pts',(97.2989916447623,0.827048687976497,-2.36131596266371));
#25019=CARTESIAN_POINT('Ctrl Pts',(97.2962988455441,0.829769946454978,-2.36105766686682));
#25020=CARTESIAN_POINT('Ctrl Pts',(97.2880960785796,0.837978958071862,-2.36027766604826));
#25021=CARTESIAN_POINT('Ctrl Pts',(97.2825448512507,0.843425447468989,-2.35975903230613));
#25022=CARTESIAN_POINT('Ctrl Pts',(97.233000190216,0.891081414489478,-2.35520654296209));
#25023=CARTESIAN_POINT('Ctrl Pts',(97.1858384366024,0.929876701316887,-2.3513959652217));
#25024=CARTESIAN_POINT('Ctrl Pts',(97.0576039709581,1.01964120048432,-2.34169016205082));
#25025=CARTESIAN_POINT('Ctrl Pts',(96.9729630635093,1.06469905205022,-2.33584668920782));
#25026=CARTESIAN_POINT('Ctrl Pts',(96.8703203451406,1.10423538820051,-2.3286663653343));
#25027=CARTESIAN_POINT('Ctrl Pts',(96.856733697695,1.10918341703275,-2.32771500340941));
#25028=CARTESIAN_POINT('Ctrl Pts',(96.8364738446412,1.11614197038542,-2.3262933521774));
#25029=CARTESIAN_POINT('Ctrl Pts',(96.8298680077757,1.11834554272876,-2.32582934932997));
#25030=CARTESIAN_POINT('Ctrl Pts',(96.8180570595007,1.12216937338215,-2.32499872089301));
#25031=CARTESIAN_POINT('Ctrl Pts',(96.8128594658271,1.12381233154201,-2.32463284336382));
#25032=CARTESIAN_POINT('Ctrl Pts',(96.8018491813494,1.12720878885444,-2.32385696782679));
#25033=CARTESIAN_POINT('Ctrl Pts',(96.7960339790446,1.12895353552237,-2.32344669939144));
#25034=CARTESIAN_POINT('Ctrl Pts',(96.7804778810286,1.1334900543463,-2.32234778301256));
#25035=CARTESIAN_POINT('Ctrl Pts',(96.7707141904808,1.13620115496903,-2.32165657463997));
#25036=CARTESIAN_POINT('Ctrl Pts',(96.7210795480756,1.14929583414746,-2.31813435583294));
#25037=CARTESIAN_POINT('Ctrl Pts',(96.6807227087198,1.15770696118784,-2.31524172957488));
#25038=CARTESIAN_POINT('Ctrl Pts',(96.5397754449183,1.17944642192583,-2.30503905919362));
#25039=CARTESIAN_POINT('Ctrl Pts',(96.4379756879237,1.181893222004,-2.29745394790259));
#25040=CARTESIAN_POINT('Ctrl Pts',(96.313164369762,1.16874869978967,-2.28844981335566));
#25041=CARTESIAN_POINT('Ctrl Pts',(96.2892815642239,1.16548987999856,-2.28674311631785));
#25042=CARTESIAN_POINT('Ctrl Pts',(96.2595927263151,1.1605063680388,-2.28465487241569));
#25043=CARTESIAN_POINT('Ctrl Pts',(96.2536792589954,1.15946719362418,-2.28424060371162));
#25044=CARTESIAN_POINT('Ctrl Pts',(96.2443395767925,1.15775220203899,-2.28358922677905));
#25045=CARTESIAN_POINT('Ctrl Pts',(96.2409080758883,1.15710630812177,-2.28335052820112));
#25046=CARTESIAN_POINT('Ctrl Pts',(96.2347735876527,1.15592337253678,-2.28292498609885));
#25047=CARTESIAN_POINT('Ctrl Pts',(96.2320696207874,1.15539210725295,-2.28273783173883));
#25048=CARTESIAN_POINT('Ctrl Pts',(96.2255515543974,1.15408768560123,-2.28228766210228));
#25049=CARTESIAN_POINT('Ctrl Pts',(96.2217393923493,1.15330510998306,-2.28202517741097));
#25050=CARTESIAN_POINT('Ctrl Pts',(96.2100051333279,1.15083557970825,-2.28121949679517));
#25051=CARTESIAN_POINT('Ctrl Pts',(96.2020963033408,1.14908574509046,-2.28067967563223));
#25052=CARTESIAN_POINT('Ctrl Pts',(96.1836346210007,1.14480083181942,-2.2794257286249));
#25053=CARTESIAN_POINT('Ctrl Pts',(96.1730973553807,1.14220117420704,-2.27871475992251));
#25054=CARTESIAN_POINT('Ctrl Pts',(96.1358084948056,1.13245288460476,-2.27621080742166));
#25055=CARTESIAN_POINT('Ctrl Pts',(96.1092732684615,1.12450660921455,-2.27445093206241));
#25056=CARTESIAN_POINT('Ctrl Pts',(96.0276435188413,1.09688968634833,-2.26903711044708));
#25057=CARTESIAN_POINT('Ctrl Pts',(95.9737502177826,1.07405810720824,-2.26545930969229));
#25058=CARTESIAN_POINT('Ctrl Pts',(95.9218015453623,1.04733927739527,-2.26182855819541));
#25059=CARTESIAN_POINT('',(97.6382309079769,0.000313031882164676,-2.32461928099262));
#25060=CARTESIAN_POINT('Ctrl Pts',(95.9218016761257,1.04733934465099,-2.16205147885552));
#25061=CARTESIAN_POINT('Ctrl Pts',(95.923776767422,1.04835519567381,-2.16219312880972));
#25062=CARTESIAN_POINT('Ctrl Pts',(95.9257548970161,1.0493655444312,-2.1623349385917));
#25063=CARTESIAN_POINT('Ctrl Pts',(95.9536565712311,1.06351719527435,-2.16433444469047));
#25064=CARTESIAN_POINT('Ctrl Pts',(95.9800529867209,1.07569908887628,-2.16621756057492));
#25065=CARTESIAN_POINT('Ctrl Pts',(96.0155274916952,1.09050422435866,-2.16875199961619));
#25066=CARTESIAN_POINT('Ctrl Pts',(96.0242263090449,1.09401321896232,-2.16937372951873));
#25067=CARTESIAN_POINT('Ctrl Pts',(96.0384698571873,1.09956199970929,-2.17039261553777));
#25068=CARTESIAN_POINT('Ctrl Pts',(96.043989772075,1.10166467231015,-2.17078767933817));
#25069=CARTESIAN_POINT('Ctrl Pts',(96.0546761099257,1.10564357043754,-2.17155301889669));
#25070=CARTESIAN_POINT('Ctrl Pts',(96.0598403193523,1.10752532990896,-2.17192310061477));
#25071=CARTESIAN_POINT('Ctrl Pts',(96.0718973938471,1.11182338141111,-2.17278777173518));
#25072=CARTESIAN_POINT('Ctrl Pts',(96.0787998786354,1.11421181431584,-2.17328325752817));
#25073=CARTESIAN_POINT('Ctrl Pts',(96.1011898151476,1.12172682992846,-2.17489228176829));
#25074=CARTESIAN_POINT('Ctrl Pts',(96.1167611047304,1.12659567828579,-2.17601407992511));
#25075=CARTESIAN_POINT('Ctrl Pts',(96.1538326898989,1.13734718185568,-2.17869269852132));
#25076=CARTESIAN_POINT('Ctrl Pts',(96.1754081486719,1.14294582308083,-2.18025788142672));
#25077=CARTESIAN_POINT('Ctrl Pts',(96.2598062163596,1.16230804930326,-2.18640468460287));
#25078=CARTESIAN_POINT('Ctrl Pts',(96.3235501720313,1.17152832806506,-2.19110657832467));
#25079=CARTESIAN_POINT('Ctrl Pts',(96.4510044990657,1.17941743096837,-2.20047865283491));
#25080=CARTESIAN_POINT('Ctrl Pts',(96.5145078386278,1.17821812116155,-2.20513196611785));
#25081=CARTESIAN_POINT('Ctrl Pts',(96.587561799582,1.17091653344803,-2.21028014466323));
#25082=CARTESIAN_POINT('Ctrl Pts',(96.5974999781431,1.16979522697559,-2.21097592148257));
#25083=CARTESIAN_POINT('Ctrl Pts',(96.6113279924709,1.1680563863511,-2.21193656108579));
#25084=CARTESIAN_POINT('Ctrl Pts',(96.6152305008229,1.16754577192768,-2.21220683914772));
#25085=CARTESIAN_POINT('Ctrl Pts',(96.6219607666877,1.16663082846654,-2.21267144165468));
#25086=CARTESIAN_POINT('Ctrl Pts',(96.6247897172272,1.16623576114777,-2.21286626533859));
#25087=CARTESIAN_POINT('Ctrl Pts',(96.6307579314682,1.16538014338993,-2.21327626417096));
#25088=CARTESIAN_POINT('Ctrl Pts',(96.6338968230044,1.1649171921021,-2.21349129814852));
#25089=CARTESIAN_POINT('Ctrl Pts',(96.641686312499,1.16373614794759,-2.21402352509463));
#25090=CARTESIAN_POINT('Ctrl Pts',(96.6463346128452,1.16300284750899,-2.21433988344908));
#25091=CARTESIAN_POINT('Ctrl Pts',(96.6638841034802,1.16012639345783,-2.2155300091557));
#25092=CARTESIAN_POINT('Ctrl Pts',(96.6767542519017,1.15779617615168,-2.21639406201771));
#25093=CARTESIAN_POINT('Ctrl Pts',(96.7097449234824,1.15125366473016,-2.21859260745331));
#25094=CARTESIAN_POINT('Ctrl Pts',(96.7297993863679,1.14672804503017,-2.21991335978148));
#25095=CARTESIAN_POINT('Ctrl Pts',(96.8057058485788,1.1274970906121,-2.22488733680801));
#25096=CARTESIAN_POINT('Ctrl Pts',(96.8605698145117,1.10921576668435,-2.22843325469929));
#25097=CARTESIAN_POINT('Ctrl Pts',(96.9834563742727,1.05795835245181,-2.23667773722027));
#25098=CARTESIAN_POINT('Ctrl Pts',(97.0500815666287,1.02232484078564,-2.24138643512437));
#25099=CARTESIAN_POINT('Ctrl Pts',(97.1215043092217,0.974808428180691,-2.247016312561));
#25100=CARTESIAN_POINT('Ctrl Pts',(97.1300913924227,0.968929923798267,-2.24770324335967));
#25101=CARTESIAN_POINT('Ctrl Pts',(97.1441021119463,0.959063328402978,-2.24884141115399));
#25102=CARTESIAN_POINT('Ctrl Pts',(97.149571572297,0.955141074422934,-2.24929017742411));
#25103=CARTESIAN_POINT('Ctrl Pts',(97.1592826016369,0.948050283836848,-2.25009512827424));
#25104=CARTESIAN_POINT('Ctrl Pts',(97.1635370235418,0.944899595143934,-2.25045062451046));
#25105=CARTESIAN_POINT('Ctrl Pts',(97.1679704359065,0.941569833878451,-2.25082411290007));
#25106=CARTESIAN_POINT('Ctrl Pts',(97.1681708235175,0.941419230554903,-2.25084100088488));
#25107=CARTESIAN_POINT('Ctrl Pts',(97.1684691668083,0.941194858570143,-2.25086615397441));
#25108=CARTESIAN_POINT('Ctrl Pts',(97.1685671591592,0.941121138502763,-2.25087441719745));
#25109=CARTESIAN_POINT('Ctrl Pts',(97.1688499985442,0.940908288033998,-2.25089827219897));
#25110=CARTESIAN_POINT('Ctrl Pts',(97.1690348160209,0.940769118526424,-2.25091386549126));
#25111=CARTESIAN_POINT('Ctrl Pts',(97.1693844352018,0.940505690131086,-2.25094337387004));
#25112=CARTESIAN_POINT('Ctrl Pts',(97.1695492453095,0.940381442334309,-2.25095728852732));
#25113=CARTESIAN_POINT('Ctrl Pts',(97.1698622988547,0.940145307009476,-2.25098372758335));
#25114=CARTESIAN_POINT('Ctrl Pts',(97.1700105485751,0.94003342767192,-2.25099625166744));
#25115=CARTESIAN_POINT('Ctrl Pts',(97.1702931590239,0.939820045634109,-2.25102013336215));
#25116=CARTESIAN_POINT('Ctrl Pts',(97.1704275243918,0.939718549228576,-2.25103149072401));
#25117=CARTESIAN_POINT('Ctrl Pts',(97.1706844805693,0.939524364072526,-2.25105321585586));
#25118=CARTESIAN_POINT('Ctrl Pts',(97.1708070751032,0.939431680067642,-2.25106358344609));
#25119=CARTESIAN_POINT('Ctrl Pts',(97.1710421855001,0.939253859407281,-2.25108347102667));
#25120=CARTESIAN_POINT('Ctrl Pts',(97.171154704097,0.939168726611208,-2.25109299086033));
#25121=CARTESIAN_POINT('Ctrl Pts',(97.171371039975,0.939004983390202,-2.25111129834054));
#25122=CARTESIAN_POINT('Ctrl Pts',(97.1714748595427,0.938926375947189,-2.25112008587203));
#25123=CARTESIAN_POINT('Ctrl Pts',(97.1716749296677,0.938774839759563,-2.25113702369568));
#25124=CARTESIAN_POINT('Ctrl Pts',(97.1717711820611,0.93870191341848,-2.25114517389478));
#25125=CARTESIAN_POINT('Ctrl Pts',(97.1719570583077,0.938561037895266,-2.25116091596767));
#25126=CARTESIAN_POINT('Ctrl Pts',(97.1720466836554,0.938493090669798,-2.25116850776564));
#25127=CARTESIAN_POINT('Ctrl Pts',(97.1722200941324,0.938361584714113,-2.25118319922394));
#25128=CARTESIAN_POINT('Ctrl Pts',(97.1723038805654,0.93829802753639,-2.25119029882822));
#25129=CARTESIAN_POINT('Ctrl Pts',(97.1724662798504,0.938174803389857,-2.25120406190202));
#25130=CARTESIAN_POINT('Ctrl Pts',(97.1725448937546,0.938115137732225,-2.25121072532245));
#25131=CARTESIAN_POINT('Ctrl Pts',(97.1726975160203,0.937999271651833,-2.2512236637736));
#25132=CARTESIAN_POINT('Ctrl Pts',(97.1727715252011,0.937943072373122,-2.25122993875799));
#25133=CARTESIAN_POINT('Ctrl Pts',(97.1729154252949,0.937833774190707,-2.25124214131381));
#25134=CARTESIAN_POINT('Ctrl Pts',(97.1729853169115,0.937780676242318,-2.25124806884723));
#25135=CARTESIAN_POINT('Ctrl Pts',(97.1783526532904,0.93370206553356,-2.25170333666591));
#25136=CARTESIAN_POINT('Ctrl Pts',(97.1836158009689,0.929631816222444,-2.25215441206328));
#25137=CARTESIAN_POINT('Ctrl Pts',(97.1948067862384,0.920824739924879,-2.2531236686561));
#25138=CARTESIAN_POINT('Ctrl Pts',(97.2007238741347,0.916074802631856,-2.25364235293484));
#25139=CARTESIAN_POINT('Ctrl Pts',(97.2163195049459,0.903305660609151,-2.25502623790589));
#25140=CARTESIAN_POINT('Ctrl Pts',(97.2259160537355,0.895188314618927,-2.25589528334289));
#25141=CARTESIAN_POINT('Ctrl Pts',(97.2867901785082,0.842002709301719,-2.26152316361044));
#25142=CARTESIAN_POINT('Ctrl Pts',(97.334189277498,0.792708395767236,-2.26645253863819));
#25143=CARTESIAN_POINT('Ctrl Pts',(97.427157567031,0.677494612334315,-2.27729371065023));
#25144=CARTESIAN_POINT('Ctrl Pts',(97.4708304130329,0.610457633925246,-2.28320537883991));
#25145=CARTESIAN_POINT('Ctrl Pts',(97.5117503363909,0.531053985602217,-2.28945910929593));
#25146=CARTESIAN_POINT('Ctrl Pts',(97.5160079870279,0.522540282547612,-2.29012042956892));
#25147=CARTESIAN_POINT('Ctrl Pts',(97.5217947533331,0.510609506677832,-2.29103349392651));
#25148=CARTESIAN_POINT('Ctrl Pts',(97.5234113686458,0.507235629201593,-2.29129018879512));
#25149=CARTESIAN_POINT('Ctrl Pts',(97.5263334129011,0.501062002969849,-2.29175707317118));
#25150=CARTESIAN_POINT('Ctrl Pts',(97.5276439553577,0.498264713145047,-2.29196756701761));
#25151=CARTESIAN_POINT('Ctrl Pts',(97.5303385477354,0.492453834099509,-2.29240260844135));
#25152=CARTESIAN_POINT('Ctrl Pts',(97.5317208947603,0.489439515760631,-2.29262705408531));
#25153=CARTESIAN_POINT('Ctrl Pts',(97.5353068796261,0.48153201445163,-2.2932127437687));
#25154=CARTESIAN_POINT('Ctrl Pts',(97.5374898688845,0.476629469623854,-2.2935727674455));
#25155=CARTESIAN_POINT('Ctrl Pts',(97.5471555366222,0.454516856476531,-2.29518350425007));
#25156=CARTESIAN_POINT('Ctrl Pts',(97.5542602160511,0.437143275807816,-2.29641346038068));
#25157=CARTESIAN_POINT('Ctrl Pts',(97.5733543660441,0.38706663788295,-2.29987837637098));
#25158=CARTESIAN_POINT('Ctrl Pts',(97.584313251963,0.353990310149442,-2.30207142337862));
#25159=CARTESIAN_POINT('Ctrl Pts',(97.6059723893391,0.277396073812628,-2.30703395720238));
#25160=CARTESIAN_POINT('Ctrl Pts',(97.6156880700367,0.233657523860515,-2.30978598829603));
#25161=CARTESIAN_POINT('Ctrl Pts',(97.6330852460752,0.126925754816465,-2.31649823683831));
#25162=CARTESIAN_POINT('Ctrl Pts',(97.6382140687699,0.0636688003235982,
-2.32047834256884));
#25163=CARTESIAN_POINT('Ctrl Pts',(97.6382309079769,0.000313031882164676,
-2.32461928099262));
#25164=CARTESIAN_POINT('Ctrl Pts',(97.6382309082176,0.000312125111502949,
-2.32461934025923));
#25165=CARTESIAN_POINT('Ctrl Pts',(97.6382328579085,-0.0070446953100704,
-2.32510018283114));
#25166=CARTESIAN_POINT('Ctrl Pts',(97.6381658759582,-0.0144012708024564,
-2.32558298598406));
#25167=CARTESIAN_POINT('Ctrl Pts',(97.6379025479175,-0.0286535485738951,
-2.32652247595264));
#25168=CARTESIAN_POINT('Ctrl Pts',(97.6377145311526,-0.0355490813513412,
-2.32697889396367));
#25169=CARTESIAN_POINT('Ctrl Pts',(97.6372714975406,-0.0478349875681682,
-2.32779564503261));
#25170=CARTESIAN_POINT('Ctrl Pts',(97.6370399857497,-0.053226051780862,
-2.32815525229364));
#25171=CARTESIAN_POINT('Ctrl Pts',(97.636513796166,-0.0637856193376086,
-2.32886209862418));
#25172=CARTESIAN_POINT('Ctrl Pts',(97.6362220711656,-0.0689541517168208,
-2.32920923895953));
#25173=CARTESIAN_POINT('Ctrl Pts',(97.635530697521,-0.0799180676014652,
-2.32994817268879));
#25174=CARTESIAN_POINT('Ctrl Pts',(97.6351222277693,-0.0857127362598701,
-2.33034022983032));
#25175=CARTESIAN_POINT('Ctrl Pts',(97.6339773990083,-0.100403302701495,
-2.33133812831642));
#25176=CARTESIAN_POINT('Ctrl Pts',(97.6331827530157,-0.109294156422362,
-2.33194575564432));
#25177=CARTESIAN_POINT('Ctrl Pts',(97.6297339128789,-0.143492381775446,
-2.33429770114478));
#25178=CARTESIAN_POINT('Ctrl Pts',(97.6263610501183,-0.168718626095907,
-2.33606394816952));
#25179=CARTESIAN_POINT('Ctrl Pts',(97.605738354346,-0.292327926404079,-2.34487953628559));
#25180=CARTESIAN_POINT('Ctrl Pts',(97.5768390992368,-0.3883406980941,-2.3522810097997));
#25181=CARTESIAN_POINT('Ctrl Pts',(97.5243954119919,-0.505983868348584,
-2.36166852019092));
#25182=CARTESIAN_POINT('Ctrl Pts',(97.5116322941545,-0.531991290739224,
-2.36376180114208));
#25183=CARTESIAN_POINT('Ctrl Pts',(97.4900569622962,-0.572140194747069,
-2.36699626033148));
#25184=CARTESIAN_POINT('Ctrl Pts',(97.4818819679298,-0.586609919678346,
-2.3681625352486));
#25185=CARTESIAN_POINT('Ctrl Pts',(97.470779240575,-0.60532542534575,-2.36966721114221));
#25186=CARTESIAN_POINT('Ctrl Pts',(97.468126495448,-0.609731058494446,-2.37002112812063));
#25187=CARTESIAN_POINT('Ctrl Pts',(97.4637415386422,-0.616906738803622,
-2.37059692886359));
#25188=CARTESIAN_POINT('Ctrl Pts',(97.4620265427629,-0.619687146376543,
-2.37081987905521));
#25189=CARTESIAN_POINT('Ctrl Pts',(97.4586518996869,-0.625107623264932,
-2.37125416006126));
#25190=CARTESIAN_POINT('Ctrl Pts',(97.4569933053892,-0.627748286632585,
-2.37146555134721));
#25191=CARTESIAN_POINT('Ctrl Pts',(97.4532603752451,-0.633639442071233,
-2.37193683121053));
#25192=CARTESIAN_POINT('Ctrl Pts',(97.4511805051736,-0.636886427990322,
-2.37219636370014));
#25193=CARTESIAN_POINT('Ctrl Pts',(97.4439053656858,-0.648122124710818,
-2.37309388787792));
#25194=CARTESIAN_POINT('Ctrl Pts',(97.4386289493937,-0.656058210334721,
-2.37372686696199));
#25195=CARTESIAN_POINT('Ctrl Pts',(97.3906637980103,-0.726335728807615,
-2.37933184282137));
#25196=CARTESIAN_POINT('Ctrl Pts',(97.3421581806821,-0.784507662320379,
-2.38397629970982));
#25197=CARTESIAN_POINT('Ctrl Pts',(97.2373985954766,-0.88805270252227,-2.39308791372061));
#25198=CARTESIAN_POINT('Ctrl Pts',(97.1818984494767,-0.933699035627461,
-2.39753581569024));
#25199=CARTESIAN_POINT('Ctrl Pts',(97.1120342595478,-0.981191326117177,
-2.40301298316904));
#25200=CARTESIAN_POINT('Ctrl Pts',(97.1013576392536,-0.988197947380445,
-2.40384654789385));
#25201=CARTESIAN_POINT('Ctrl Pts',(97.084090333313,-0.999132229586126,-2.40519059967739));
#25202=CARTESIAN_POINT('Ctrl Pts',(97.0775713607598,-1.00317161821522,-2.40569711158367));
#25203=CARTESIAN_POINT('Ctrl Pts',(97.0651127805488,-1.01072401052339,-2.40666370213664));
#25204=CARTESIAN_POINT('Ctrl Pts',(97.0591808198162,-1.01424905149447,-2.40712332843813));
#25205=CARTESIAN_POINT('Ctrl Pts',(97.0485760879944,-1.02042541675402,-2.40794413195134));
#25206=CARTESIAN_POINT('Ctrl Pts',(97.0439154683067,-1.02309729924003,-2.40830456293504));
#25207=CARTESIAN_POINT('Ctrl Pts',(97.0340541162283,-1.0286614099814,-2.40906665303262));
#25208=CARTESIAN_POINT('Ctrl Pts',(97.0288494310593,-1.03154628636073,-2.40946855961641));
#25209=CARTESIAN_POINT('Ctrl Pts',(97.0152078034377,-1.03897304531625,-2.41052127933083));
#25210=CARTESIAN_POINT('Ctrl Pts',(97.0067370455216,-1.0434515511149,-2.41117428619939));
#25211=CARTESIAN_POINT('Ctrl Pts',(96.9707237959743,-1.06193312114183,-2.41394835536683));
#25212=CARTESIAN_POINT('Ctrl Pts',(96.9426927294797,-1.07495172503206,-2.41610269288748));
#25213=CARTESIAN_POINT('Ctrl Pts',(96.8181518184083,-1.12694097816416,-2.42565966814911));
#25214=CARTESIAN_POINT('Ctrl Pts',(96.7172339855009,-1.15412158665157,-2.4334200967969));
#25215=CARTESIAN_POINT('Ctrl Pts',(96.5925134182985,-1.17052804421296,-2.44251948849054));
#25216=CARTESIAN_POINT('Ctrl Pts',(96.5708653584615,-1.17276761245956,-2.44407912058409));
#25217=CARTESIAN_POINT('Ctrl Pts',(96.5355825280345,-1.17543200157612,-2.44657718529343));
#25218=CARTESIAN_POINT('Ctrl Pts',(96.5219810955612,-1.17622209186339,-2.44752961105701));
#25219=CARTESIAN_POINT('Ctrl Pts',(96.5035929673586,-1.17697037263742,-2.44880033320075));
#25220=CARTESIAN_POINT('Ctrl Pts',(96.4988163838866,-1.17713563389972,-2.44912888370799));
#25221=CARTESIAN_POINT('Ctrl Pts',(96.4908520013777,-1.17736265687577,-2.44967399475973));
#25222=CARTESIAN_POINT('Ctrl Pts',(96.4876647669246,-1.17744055789687,-2.44989141796297));
#25223=CARTESIAN_POINT('Ctrl Pts',(96.4816341644796,-1.1775634548524,-2.45030139095582));
#25224=CARTESIAN_POINT('Ctrl Pts',(96.4787908905804,-1.1776110967558,-2.45049408853775));
#25225=CARTESIAN_POINT('Ctrl Pts',(96.4720628814343,-1.17769945813993,-2.4509487200334));
#25226=CARTESIAN_POINT('Ctrl Pts',(96.4681780322624,-1.17773125577461,-2.45121016857687));
#25227=CARTESIAN_POINT('Ctrl Pts',(96.4544881023195,-1.17777556685114,-2.45212797565867));
#25228=CARTESIAN_POINT('Ctrl Pts',(96.4446827688482,-1.17768486147239,-2.45277898968393));
#25229=CARTESIAN_POINT('Ctrl Pts',(96.3638539789832,-1.17592741086032,-2.45810150107689));
#25230=CARTESIAN_POINT('Ctrl Pts',(96.2931036554623,-1.16795963376462,-2.46248557709005));
#25231=CARTESIAN_POINT('Ctrl Pts',(96.165767767085,-1.14180220629355,-2.47052650241691));
#25232=CARTESIAN_POINT('Ctrl Pts',(96.1090157398355,-1.12562857411263,-2.4741683301309));
#25233=CARTESIAN_POINT('Ctrl Pts',(96.0337888096943,-1.09794339272785,-2.47927749036081));
#25234=CARTESIAN_POINT('Ctrl Pts',(96.0140658993834,-1.09007311602649,-2.48064399574213));
#25235=CARTESIAN_POINT('Ctrl Pts',(95.980129844637,-1.0754557133577,-2.48305097963976));
#25236=CARTESIAN_POINT('Ctrl Pts',(95.9658189104747,-1.06894883161682,-2.48408374056681));
#25237=CARTESIAN_POINT('Ctrl Pts',(95.9451517104817,-1.05904799011359,-2.48560343926336));
#25238=CARTESIAN_POINT('Ctrl Pts',(95.9386891680595,-1.05587887701475,-2.48608273622605));
#25239=CARTESIAN_POINT('Ctrl Pts',(95.9273576121539,-1.05019265287333,-2.48693059109396));
#25240=CARTESIAN_POINT('Ctrl Pts',(95.9224763166676,-1.04770039338141,-2.48729828353467));
#25241=CARTESIAN_POINT('Ctrl Pts',(95.9123302760931,-1.04243049319861,-2.48806779815115));
#25242=CARTESIAN_POINT('Ctrl Pts',(95.9070688499076,-1.0396468341165,-2.48846982197968));
#25243=CARTESIAN_POINT('Ctrl Pts',(95.8933868366295,-1.03227481177002,-2.48952319108248));
#25244=CARTESIAN_POINT('Ctrl Pts',(95.8850009326934,-1.02762335546255,-2.49017673510176));
#25245=CARTESIAN_POINT('Ctrl Pts',(95.8497748040735,-1.00751787561376,-2.49295642419129));
#25246=CARTESIAN_POINT('Ctrl Pts',(95.8234950375911,-0.991111955026462,
-2.49511601383429));
#25247=CARTESIAN_POINT('Ctrl Pts',(95.7292249391886,-0.926962110574596,
-2.50319149766311));
#25248=CARTESIAN_POINT('Ctrl Pts',(95.6656985624145,-0.873104640273444,
-2.50931367745915));
#25249=CARTESIAN_POINT('Ctrl Pts',(95.5723750103773,-0.775295018995918,
-2.51920970710001));
#25250=CARTESIAN_POINT('Ctrl Pts',(95.5389169839887,-0.735211318289734,
-2.52299307191744));
#25251=CARTESIAN_POINT('Ctrl Pts',(95.5041291478889,-0.687411596383303,
-2.52710491508794));
#25252=CARTESIAN_POINT('Ctrl Pts',(95.5000847807433,-0.681749716665959,
-2.52758595499823));
#25253=CARTESIAN_POINT('Ctrl Pts',(95.4939889751718,-0.673054033451855,
-2.52831523465734));
#25254=CARTESIAN_POINT('Ctrl Pts',(95.4919011998323,-0.670046071428197,
-2.52856578726807));
#25255=CARTESIAN_POINT('Ctrl Pts',(95.4881045419205,-0.664521210047747,
-2.52902278588614));
#25256=CARTESIAN_POINT('Ctrl Pts',(95.4863913761397,-0.66200741698106,-2.5292295077953));
#25257=CARTESIAN_POINT('Ctrl Pts',(95.4825454750405,-0.656316927258143,
-2.52969475769526));
#25258=CARTESIAN_POINT('Ctrl Pts',(95.4804184666913,-0.653136457438748,
-2.52995290741091));
#25259=CARTESIAN_POINT('Ctrl Pts',(95.4749605094935,-0.644888592663324,
-2.5306176686929));
#25260=CARTESIAN_POINT('Ctrl Pts',(95.4716530806006,-0.639805661216511,
-2.53102279577577));
#25261=CARTESIAN_POINT('Ctrl Pts',(95.4497003870847,-0.605491383199052,
-2.53372899480658));
#25262=CARTESIAN_POINT('Ctrl Pts',(95.4323125595053,-0.575471483685733,
-2.53595740401788));
#25263=CARTESIAN_POINT('Ctrl Pts',(95.4031992262114,-0.519662836059172,
-2.53993469764894));
#25264=CARTESIAN_POINT('Ctrl Pts',(95.3910312076051,-0.494137102975158,
-2.54169473144999));
#25265=CARTESIAN_POINT('Ctrl Pts',(95.360659664446,-0.42403385263733,-2.54643153055104));
#25266=CARTESIAN_POINT('Ctrl Pts',(95.3442517499036,-0.378739812221549,
-2.54939129353727));
#25267=CARTESIAN_POINT('Ctrl Pts',(95.3156641840501,-0.281620848485254,
-2.55572323273594));
#25268=CARTESIAN_POINT('Ctrl Pts',(95.3041322544921,-0.229722334389208,
-2.55909997911316));
#25269=CARTESIAN_POINT('Ctrl Pts',(95.294513387777,-0.166528721727784,-2.56330124523728));
#25270=CARTESIAN_POINT('Ctrl Pts',(95.2930325292862,-0.155808676108142,
-2.56401683801274));
#25271=CARTESIAN_POINT('Ctrl Pts',(95.2909334234786,-0.138896874160968,
-2.56515099415849));
#25272=CARTESIAN_POINT('Ctrl Pts',(95.2902161383819,-0.132717845932983,
-2.56556647569134));
#25273=CARTESIAN_POINT('Ctrl Pts',(95.2889646255899,-0.121136426956502,
-2.5663474019905));
#25274=CARTESIAN_POINT('Ctrl Pts',(95.2884187339504,-0.115735441049098,
-2.56671247401288));
#25275=CARTESIAN_POINT('Ctrl Pts',(95.2872798936071,-0.10363212047389,-2.56753265851575));
#25276=CARTESIAN_POINT('Ctrl Pts',(95.2867070073179,-0.0969281349678226,
-2.56798838051139));
#25277=CARTESIAN_POINT('Ctrl Pts',(95.2853949601245,-0.0798506832053449,
-2.56915305861647));
#25278=CARTESIAN_POINT('Ctrl Pts',(95.2847357112633,-0.0694718416145498,
-2.56986445233853));
#25279=CARTESIAN_POINT('Ctrl Pts',(95.2804512557265,0.0158219819775928,
-2.57574139306761));
#25280=CARTESIAN_POINT('Ctrl Pts',(95.2838531182857,0.0909040437030932,
-2.58112567076266));
#25281=CARTESIAN_POINT('Ctrl Pts',(95.3023252624909,0.221342520139699,-2.59076127423558));
#25282=CARTESIAN_POINT('Ctrl Pts',(95.3143371025519,0.276896359071611,-2.59495309411392));
#25283=CARTESIAN_POINT('Ctrl Pts',(95.3363379791686,0.351933121332829,-2.60060695087666));
#25284=CARTESIAN_POINT('Ctrl Pts',(95.3429282397361,0.372331024498018,-2.60214245785198));
#25285=CARTESIAN_POINT('Ctrl Pts',(95.3545633279369,0.405244217262078,-2.60460638724446));
#25286=CARTESIAN_POINT('Ctrl Pts',(95.3592727510937,0.417872233818749,-2.60554836432131));
#25287=CARTESIAN_POINT('Ctrl Pts',(95.3659375997813,0.434847758131694,-2.6068075016658));
#25288=CARTESIAN_POINT('Ctrl Pts',(95.3677039495857,0.439267740196754,-2.60713468484315));
#25289=CARTESIAN_POINT('Ctrl Pts',(95.3706965497113,0.446626423539653,-2.60767814929998));
#25290=CARTESIAN_POINT('Ctrl Pts',(95.3719079920369,0.449571036920018,-2.6078952826766));
#25291=CARTESIAN_POINT('Ctrl Pts',(95.3742252043801,0.455139125218332,-2.60830518169485));
#25292=CARTESIAN_POINT('Ctrl Pts',(95.375328566857,0.45776355686469,-2.60849809210146));
#25293=CARTESIAN_POINT('Ctrl Pts',(95.3779651962993,0.463971875309042,-2.60895381151797));
#25294=CARTESIAN_POINT('Ctrl Pts',(95.3795067728294,0.467552229648226,-2.60921612950088));
#25295=CARTESIAN_POINT('Ctrl Pts',(95.3849880336732,0.480110584928407,-2.61013470541584));
#25296=CARTESIAN_POINT('Ctrl Pts',(95.3890221500025,0.489047280012529,-2.61078562895274));
#25297=CARTESIAN_POINT('Ctrl Pts',(95.4229388507302,0.561747333333516,-2.61606664403242));
#25298=CARTESIAN_POINT('Ctrl Pts',(95.458377692013,0.622772423237232,-2.62041455649931));
#25299=CARTESIAN_POINT('Ctrl Pts',(95.5333492036738,0.728728680572336,-2.62844347473014));
#25300=CARTESIAN_POINT('Ctrl Pts',(95.5712481517739,0.774521230711589,-2.63211043686631));
#25301=CARTESIAN_POINT('Ctrl Pts',(95.6272298861611,0.832611710990445,-2.63725167452129));
#25302=CARTESIAN_POINT('Ctrl Pts',(95.642437433484,0.847557856606306,-2.6386236303474));
#25303=CARTESIAN_POINT('Ctrl Pts',(95.6695843969974,0.872826661600905,-2.64103934413662));
#25304=CARTESIAN_POINT('Ctrl Pts',(95.6813413797738,0.88333755192203,-2.64207530523385));
#25305=CARTESIAN_POINT('Ctrl Pts',(95.6987734593957,0.898303233211234,-2.64359884681239));
#25306=CARTESIAN_POINT('Ctrl Pts',(95.704284376056,0.902947250802624,-2.6440787306028));
#25307=CARTESIAN_POINT('Ctrl Pts',(95.7140617548011,0.911034302726085,-2.64492725624785));
#25308=CARTESIAN_POINT('Ctrl Pts',(95.7183103254208,0.914498703105236,-2.6452950281109));
#25309=CARTESIAN_POINT('Ctrl Pts',(95.7272190317424,0.921660135802268,-2.64606434506589));
#25310=CARTESIAN_POINT('Ctrl Pts',(95.7318832895431,0.925351767507479,-2.64646608938068));
#25311=CARTESIAN_POINT('Ctrl Pts',(95.7441247993499,0.934890652292875,-2.64751791027447));
#25312=CARTESIAN_POINT('Ctrl Pts',(95.7517455881633,0.940681053183735,-2.64817017366798));
#25313=CARTESIAN_POINT('Ctrl Pts',(95.7841816981849,0.964708639548181,-2.65093646461017));
#25314=CARTESIAN_POINT('Ctrl Pts',(95.8096347580536,0.982060268160886,-2.65308353366401));
#25315=CARTESIAN_POINT('Ctrl Pts',(95.8637460938545,1.01592042387009,-2.65760328689503));
#25316=CARTESIAN_POINT('Ctrl Pts',(95.8924610368534,1.03224854876223,-2.65997758591606));
#25317=CARTESIAN_POINT('Ctrl Pts',(95.9218019448244,1.04733948285108,-2.66237442964626));
#25318=CARTESIAN_POINT('Origin',(96.460480949577,-7.19464945638997E-16,
0.924367114736168));
#25319=CARTESIAN_POINT('',(95.9218016227097,1.04733931717749,-3.26242343814143));
#25320=CARTESIAN_POINT('',(95.9218016730922,1.04733934309078,-3.1639039911222));
#25321=CARTESIAN_POINT('',(95.9218016730721,1.04733934308042,0.924367114736168));
#25322=CARTESIAN_POINT('',(97.6382307847678,0.000623063363894689,-2.92357187405869));
#25323=CARTESIAN_POINT('Ctrl Pts',(95.9218016227097,1.04733931717749,-3.26242343814143));
#25324=CARTESIAN_POINT('Ctrl Pts',(95.9009760917006,1.03662809604634,-3.26076286007084));
#25325=CARTESIAN_POINT('Ctrl Pts',(95.8804699490475,1.02529568575856,-3.25908386593059));
#25326=CARTESIAN_POINT('Ctrl Pts',(95.8190575962219,0.988923619110589,-3.25392504421716));
#25327=CARTESIAN_POINT('Ctrl Pts',(95.7793366824058,0.961995788508946,-3.25040383841714));
#25328=CARTESIAN_POINT('Ctrl Pts',(95.7190393102272,0.915507724612175,-3.24481773703771));
#25329=CARTESIAN_POINT('Ctrl Pts',(95.6973338528679,0.897494680329055,-3.2427526516122));
#25330=CARTESIAN_POINT('Ctrl Pts',(95.6504413182246,0.855646906630459,-3.2381957699274));
#25331=CARTESIAN_POINT('Ctrl Pts',(95.6256154274532,0.831442053819478,-3.23571646123758));
#25332=CARTESIAN_POINT('Ctrl Pts',(95.597740441082,0.80175472839589,-3.23288598710055));
#25333=CARTESIAN_POINT('Ctrl Pts',(95.5936239825375,0.797302221286391,-3.23246673579861));
#25334=CARTESIAN_POINT('Ctrl Pts',(95.5869663858731,0.78998861300894,-3.23178689019993));
#25335=CARTESIAN_POINT('Ctrl Pts',(95.5844045401873,0.787146636680469,-3.23152484589805));
#25336=CARTESIAN_POINT('Ctrl Pts',(95.5798305899478,0.782022545901661,-3.23105627563974));
#25337=CARTESIAN_POINT('Ctrl Pts',(95.5778134428252,0.779745081021927,-3.23084938587444));
#25338=CARTESIAN_POINT('Ctrl Pts',(95.5733876777384,0.774708977634497,-3.23039490982893));
#25339=CARTESIAN_POINT('Ctrl Pts',(95.5709830891129,0.771946908867547,-3.23014761525407));
#25340=CARTESIAN_POINT('Ctrl Pts',(95.5640461349075,0.763903215082586,-3.22943296454969));
#25341=CARTESIAN_POINT('Ctrl Pts',(95.5595475577722,0.758592465210856,-3.22896797122995));
#25342=CARTESIAN_POINT('Ctrl Pts',(95.5216904385475,0.713088816751232,-3.2250384880526));
#25343=CARTESIAN_POINT('Ctrl Pts',(95.4909881354004,0.670752141001989,-3.22174071775077));
#25344=CARTESIAN_POINT('Ctrl Pts',(95.4188978841364,0.555998318018275,-3.21329928564867));
#25345=CARTESIAN_POINT('Ctrl Pts',(95.3822055789524,0.480989855424195,-3.20823192923778));
#25346=CARTESIAN_POINT('Ctrl Pts',(95.3432271524176,0.373874971906024,-3.20096082772322));
#25347=CARTESIAN_POINT('Ctrl Pts',(95.3338575705051,0.344612898304213,-3.19897354107816));
#25348=CARTESIAN_POINT('Ctrl Pts',(95.3230849535697,0.305805270613128,-3.19631922653434));
#25349=CARTESIAN_POINT('Ctrl Pts',(95.3206394455921,0.2965600313548,-3.19568555131755));
#25350=CARTESIAN_POINT('Ctrl Pts',(95.3168562027863,0.28151885953178,-3.19465199077159));
#25351=CARTESIAN_POINT('Ctrl Pts',(95.315449281176,0.275740649721048,-3.19425431490897));
#25352=CARTESIAN_POINT('Ctrl Pts',(95.3128294174555,0.264614980481494,-3.19348729673279));
#25353=CARTESIAN_POINT('Ctrl Pts',(95.3116099371108,0.259269207671798,-3.1931181729186));
#25354=CARTESIAN_POINT('Ctrl Pts',(95.3088730659749,0.246873150826158,-3.19226079534717));
#25355=CARTESIAN_POINT('Ctrl Pts',(95.3073830282832,0.239817117983475,-3.19177169192591));
#25356=CARTESIAN_POINT('Ctrl Pts',(95.302836575262,0.217264893233611,-3.19020478121577));
#25357=CARTESIAN_POINT('Ctrl Pts',(95.3000271514698,0.201721272374442,-3.18911930717782));
#25358=CARTESIAN_POINT('Ctrl Pts',(95.2941550211021,0.16503121145522,-3.18654293645155));
#25359=CARTESIAN_POINT('Ctrl Pts',(95.2913535897483,0.143849193209018,-3.18504451335201));
#25360=CARTESIAN_POINT('Ctrl Pts',(95.2829278751971,0.0633503072499742,
-3.17930799981127));
#25361=CARTESIAN_POINT('Ctrl Pts',(95.2812315076657,0.00371783528771251,
-3.17496672243804));
#25362=CARTESIAN_POINT('Ctrl Pts',(95.2873728046181,-0.125804141840988,
-3.1654540281797));
#25363=CARTESIAN_POINT('Ctrl Pts',(95.2969385670497,-0.195397804555561,
-3.16028863476569));
#25364=CARTESIAN_POINT('Ctrl Pts',(95.3148434238025,-0.273325084522133,
-3.15468427401297));
#25365=CARTESIAN_POINT('Ctrl Pts',(95.3171677595946,-0.28289027499488,-3.15399970271783));
#25366=CARTESIAN_POINT('Ctrl Pts',(95.3205783322454,-0.296196282563135,
-3.15305310770803));
#25367=CARTESIAN_POINT('Ctrl Pts',(95.3215635368278,-0.299962235651212,
-3.15278583758001));
#25368=CARTESIAN_POINT('Ctrl Pts',(95.3233012739676,-0.30647274902815,-3.15232497839477));
#25369=CARTESIAN_POINT('Ctrl Pts',(95.3240451083059,-0.309219565406145,
-3.1521309084276));
#25370=CARTESIAN_POINT('Ctrl Pts',(95.3256428422465,-0.315036004237455,
-3.15172078276427));
#25371=CARTESIAN_POINT('Ctrl Pts',(95.3264992573036,-0.318104913374181,
-3.15150487737429));
#25372=CARTESIAN_POINT('Ctrl Pts',(95.3286685605038,-0.325758376053264,
-3.1509675695998));
#25373=CARTESIAN_POINT('Ctrl Pts',(95.3299968761097,-0.330338561496088,
-3.15064703683849));
#25374=CARTESIAN_POINT('Ctrl Pts',(95.3352037756991,-0.347893261053726,
-3.14942197537411));
#25375=CARTESIAN_POINT('Ctrl Pts',(95.3392783750749,-0.360809180432816,
-3.14852791026801));
#25376=CARTESIAN_POINT('Ctrl Pts',(95.350420467529,-0.394114631164175,-3.146234449888));
#25377=CARTESIAN_POINT('Ctrl Pts',(95.35782732335,-0.414385943885653,-3.14485033243837));
#25378=CARTESIAN_POINT('Ctrl Pts',(95.4031340343663,-0.528548008740717,
-3.13706266846482));
#25379=CARTESIAN_POINT('Ctrl Pts',(95.4524587841208,-0.617445476633413,
-3.13098955491386));
#25380=CARTESIAN_POINT('Ctrl Pts',(95.5323877839963,-0.725848230390683,
-3.12242435708074));
#25381=CARTESIAN_POINT('Ctrl Pts',(95.5533614775886,-0.751895285761422,
-3.12026664759121));
#25382=CARTESIAN_POINT('Ctrl Pts',(95.5819192766561,-0.784424440552622,
-3.11741579950001));
#25383=CARTESIAN_POINT('Ctrl Pts',(95.5885181454773,-0.791753228365624,
-3.11676267125256));
#25384=CARTESIAN_POINT('Ctrl Pts',(95.5992868105714,-0.8034151251432,-3.11570522774752));
#25385=CARTESIAN_POINT('Ctrl Pts',(95.6033992090357,-0.807800777501227,
-3.11530331828718));
#25386=CARTESIAN_POINT('Ctrl Pts',(95.6113131425393,-0.816112099201845,
-3.11453338254936));
#25387=CARTESIAN_POINT('Ctrl Pts',(95.6151087838215,-0.820043183383064,
-3.11416561340655));
#25388=CARTESIAN_POINT('Ctrl Pts',(95.6238808132659,-0.829002606611762,
-3.11331900067909));
#25389=CARTESIAN_POINT('Ctrl Pts',(95.6288753855253,-0.834012764833267,
-3.11283937609178));
#25390=CARTESIAN_POINT('Ctrl Pts',(95.6446331362918,-0.849537405856089,
-3.11133342310889));
#25391=CARTESIAN_POINT('Ctrl Pts',(95.6555524990969,-0.859890464944481,
-3.11030024511203));
#25392=CARTESIAN_POINT('Ctrl Pts',(95.6814839561895,-0.883550260810635,
-3.10786929906239));
#25393=CARTESIAN_POINT('Ctrl Pts',(95.6966432719301,-0.896687960923984,
-3.10646510787272));
#25394=CARTESIAN_POINT('Ctrl Pts',(95.7533991485074,-0.943391113113564,
-3.10126779144723));
#25395=CARTESIAN_POINT('Ctrl Pts',(95.796927756772,-0.974498589916816,-3.09739165977353));
#25396=CARTESIAN_POINT('Ctrl Pts',(95.9099798663846,-1.0441953823916,-3.08766513798926));
#25397=CARTESIAN_POINT('Ctrl Pts',(95.9815890125677,-1.07891606625807,-3.081786070867));
#25398=CARTESIAN_POINT('Ctrl Pts',(96.0651215072671,-1.10944904872095,-3.07555914180613));
#25399=CARTESIAN_POINT('Ctrl Pts',(96.0741317578964,-1.11261880127896,-3.07489552143454));
#25400=CARTESIAN_POINT('Ctrl Pts',(96.0867289098586,-1.11687891514314,-3.07397982125982));
#25401=CARTESIAN_POINT('Ctrl Pts',(96.0902836645051,-1.11806219387595,-3.0737227543308));
#25402=CARTESIAN_POINT('Ctrl Pts',(96.0967809912372,-1.12019058821716,-3.07325539434339));
#25403=CARTESIAN_POINT('Ctrl Pts',(96.0997217515134,-1.12114112203396,-3.07304479484892));
#25404=CARTESIAN_POINT('Ctrl Pts',(96.1058237138427,-1.12308694707486,-3.07260978308047));
#25405=CARTESIAN_POINT('Ctrl Pts',(96.1089854177312,-1.12408048525348,-3.07238547116343));
#25406=CARTESIAN_POINT('Ctrl Pts',(96.1172680474249,-1.12664486721356,-3.07180058536465));
#25407=CARTESIAN_POINT('Ctrl Pts',(96.1223956412252,-1.12819416769388,-3.07144122553461));
#25408=CARTESIAN_POINT('Ctrl Pts',(96.1454333886894,-1.1349838428861,-3.06983812783228));
#25409=CARTESIAN_POINT('Ctrl Pts',(96.1634571135928,-1.13983341984474,-3.06861490562632));
#25410=CARTESIAN_POINT('Ctrl Pts',(96.2151287939989,-1.15242747203118,-3.06517580293584));
#25411=CARTESIAN_POINT('Ctrl Pts',(96.249013689404,-1.15912411313574,-3.06300109130569));
#25412=CARTESIAN_POINT('Ctrl Pts',(96.3603773976328,-1.17608561559311,-3.05597617286261));
#25413=CARTESIAN_POINT('Ctrl Pts',(96.4385848592033,-1.18013496855584,-3.05122035080892));
#25414=CARTESIAN_POINT('Ctrl Pts',(96.5531933428802,-1.17466605076945,-3.04394795409462));
#25415=CARTESIAN_POINT('Ctrl Pts',(96.5896648949994,-1.17121604195322,-3.04159078765786));
#25416=CARTESIAN_POINT('Ctrl Pts',(96.6359807761467,-1.164645118841,-3.03851192044276));
#25417=CARTESIAN_POINT('Ctrl Pts',(96.6460283553419,-1.16308666554623,-3.03783887884745));
#25418=CARTESIAN_POINT('Ctrl Pts',(96.662048706251,-1.16038892380336,-3.0367569719613));
#25419=CARTESIAN_POINT('Ctrl Pts',(96.6680351646755,-1.15933311022793,-3.0363507203432));
#25420=CARTESIAN_POINT('Ctrl Pts',(96.6793723745648,-1.15724297567353,-3.03557749999468));
#25421=CARTESIAN_POINT('Ctrl Pts',(96.6847246602296,-1.15621776374552,-3.03521082649259));
#25422=CARTESIAN_POINT('Ctrl Pts',(96.696886602852,-1.15380056222418,-3.03437381595719));
#25423=CARTESIAN_POINT('Ctrl Pts',(96.703691386933,-1.15238537385207,-3.03390275960276));
#25424=CARTESIAN_POINT('Ctrl Pts',(96.7245445675324,-1.14785561899205,-3.03245057728314));
#25425=CARTESIAN_POINT('Ctrl Pts',(96.7385482870937,-1.14454385692141,-3.03146328342912));
#25426=CARTESIAN_POINT('Ctrl Pts',(96.8065414721501,-1.12714258546035,-3.02660830388785));
#25427=CARTESIAN_POINT('Ctrl Pts',(96.8595364085919,-1.10948701084169,-3.02262946222148));
#25428=CARTESIAN_POINT('Ctrl Pts',(96.9930489986196,-1.0542003806011,-3.01213027339254));
#25429=CARTESIAN_POINT('Ctrl Pts',(97.0709237652827,-1.01110184527003,-3.00551388142081));
#25430=CARTESIAN_POINT('Ctrl Pts',(97.1565820562292,-0.950161672381643,
-2.99805279667147));
#25431=CARTESIAN_POINT('Ctrl Pts',(97.1697444621521,-0.940377206693605,
-2.99690149697072));
#25432=CARTESIAN_POINT('Ctrl Pts',(97.1868891613878,-0.927067586969161,
-2.99539983345348));
#25433=CARTESIAN_POINT('Ctrl Pts',(97.1910573905014,-0.92378637554014,-2.99503458623596));
#25434=CARTESIAN_POINT('Ctrl Pts',(97.1977845902097,-0.918416741647205,
-2.99444503254865));
#25435=CARTESIAN_POINT('Ctrl Pts',(97.2003571375762,-0.916345566335308,
-2.99421956394865));
#25436=CARTESIAN_POINT('Ctrl Pts',(97.2053044524956,-0.912328032690507,
-2.99378598269923));
#25437=CARTESIAN_POINT('Ctrl Pts',(97.2076803594539,-0.910383178598652,
-2.99357777379183));
#25438=CARTESIAN_POINT('Ctrl Pts',(97.2132532037757,-0.905784884220247,
-2.99308937271893));
#25439=CARTESIAN_POINT('Ctrl Pts',(97.2164437983878,-0.903123743288702,
-2.99280972325654));
#25440=CARTESIAN_POINT('Ctrl Pts',(97.2233627712162,-0.897290560427546,
-2.99220305896326));
#25441=CARTESIAN_POINT('Ctrl Pts',(97.2270856090653,-0.894112029701201,
-2.99187648880318));
#25442=CARTESIAN_POINT('Ctrl Pts',(97.2373799774598,-0.88521121153983,-2.99097269429881));
#25443=CARTESIAN_POINT('Ctrl Pts',(97.2439081256502,-0.879438945231865,
-2.9903986787372));
#25444=CARTESIAN_POINT('Ctrl Pts',(97.2651984889004,-0.860188523820308,
-2.98852136051856));
#25445=CARTESIAN_POINT('Ctrl Pts',(97.2796823452108,-0.846406392633618,
-2.98723569488297));
#25446=CARTESIAN_POINT('Ctrl Pts',(97.3518218119252,-0.774174462494765,
-2.98074433415138));
#25447=CARTESIAN_POINT('Ctrl Pts',(97.4036049931769,-0.710178400745265,
-2.97577255524557));
#25448=CARTESIAN_POINT('Ctrl Pts',(97.4769901014258,-0.597141286668738,
-2.96734429994462));
#25449=CARTESIAN_POINT('Ctrl Pts',(97.5026686331844,-0.551101044715363,
-2.96399692254765));
#25450=CARTESIAN_POINT('Ctrl Pts',(97.5298914951449,-0.493535876865327,
-2.95981454271306));
#25451=CARTESIAN_POINT('Ctrl Pts',(97.5344638238239,-0.483505273100771,
-2.95908603617534));
#25452=CARTESIAN_POINT('Ctrl Pts',(97.5414387792638,-0.467616611415199,
-2.95793174257182));
#25453=CARTESIAN_POINT('Ctrl Pts',(97.5439361936714,-0.461800667217046,
-2.95750915460304));
#25454=CARTESIAN_POINT('Ctrl Pts',(97.548465233225,-0.451014510774662,-2.95672516987478));
#25455=CARTESIAN_POINT('Ctrl Pts',(97.5505099929958,-0.44604996722813,-2.95636422460229));
#25456=CARTESIAN_POINT('Ctrl Pts',(97.5549800576062,-0.434982631839735,
-2.95555926652657));
#25457=CARTESIAN_POINT('Ctrl Pts',(97.5573883940214,-0.428873224604644,
-2.95511470289317));
#25458=CARTESIAN_POINT('Ctrl Pts',(97.5642177120164,-0.411114900009522,
-2.95382169775168));
#25459=CARTESIAN_POINT('Ctrl Pts',(97.568504977346,-0.399415867230539,-2.9529688965145));
#25460=CARTESIAN_POINT('Ctrl Pts',(97.5777891446315,-0.372780719729976,
-2.95102443631894));
#25461=CARTESIAN_POINT('Ctrl Pts',(97.5826735839436,-0.357808214621021,
-2.94992934910239));
#25462=CARTESIAN_POINT('Ctrl Pts',(97.5978663382881,-0.307861679145551,
-2.94626871955088));
#25463=CARTESIAN_POINT('Ctrl Pts',(97.6068501517927,-0.272509735916407,
-2.94366483576044));
#25464=CARTESIAN_POINT('Ctrl Pts',(97.6302157724857,-0.15867197365401,-2.93525594847338));
#25465=CARTESIAN_POINT('Ctrl Pts',(97.6382729731053,-0.07912373339909,-2.92932917990252));
#25466=CARTESIAN_POINT('Ctrl Pts',(97.6382307847678,0.000623063363894689,
-2.92357187405869));
#25467=CARTESIAN_POINT('Ctrl Pts',(97.6382307838965,0.000624708245411292,
-2.92357175530679));
#25468=CARTESIAN_POINT('Ctrl Pts',(97.6382200576542,0.0208466762333824,
-2.92211183462094));
#25469=CARTESIAN_POINT('Ctrl Pts',(97.6376885142611,0.0410664476087709,
-2.92066502402141));
#25470=CARTESIAN_POINT('Ctrl Pts',(97.6360622140238,0.0722884927679515,
-2.91846009423071));
#25471=CARTESIAN_POINT('Ctrl Pts',(97.6353329528843,0.083305023328173,-2.91768773127109));
#25472=CARTESIAN_POINT('Ctrl Pts',(97.6341135960156,0.0984835176264949,
-2.91663277603021));
#25473=CARTESIAN_POINT('Ctrl Pts',(97.6337560713312,0.102655160580913,-2.91634379392765));
#25474=CARTESIAN_POINT('Ctrl Pts',(97.6330962775147,0.109899438030602,-2.9158437317152));
#25475=CARTESIAN_POINT('Ctrl Pts',(97.6328041614323,0.112972922786058,-2.91563212772087));
#25476=CARTESIAN_POINT('Ctrl Pts',(97.6322144695702,0.118928616547422,-2.91522320904985));
#25477=CARTESIAN_POINT('Ctrl Pts',(97.6319183355781,0.121810956513514,-2.91502581734544));
#25478=CARTESIAN_POINT('Ctrl Pts',(97.6312597418791,0.127996579577273,-2.91460333773178));
#25479=CARTESIAN_POINT('Ctrl Pts',(97.6308939354182,0.131299459838404,-2.91437843690302));
#25480=CARTESIAN_POINT('Ctrl Pts',(97.6298973709302,0.139962213275983,-2.91379026823759));
#25481=CARTESIAN_POINT('Ctrl Pts',(97.6292437343871,0.145319452578551,-2.91342823956589));
#25482=CARTESIAN_POINT('Ctrl Pts',(97.6263575133559,0.167694624255707,-2.91192261479255));
#25483=CARTESIAN_POINT('Ctrl Pts',(97.6237897611973,0.184668168497702,-2.91079603636991));
#25484=CARTESIAN_POINT('Ctrl Pts',(97.616442722953,0.226960383239004,-2.90801441228442));
#25485=CARTESIAN_POINT('Ctrl Pts',(97.6112019519173,0.252190361787846,-2.90637791061506));
#25486=CARTESIAN_POINT('Ctrl Pts',(97.5838509200275,0.365120356223873,-2.89907646267668));
#25487=CARTESIAN_POINT('Ctrl Pts',(97.552513132994,0.450265876192737,-2.89361209556491));
#25488=CARTESIAN_POINT('Ctrl Pts',(97.4957586195887,0.562629324071688,-2.88561860773344));
#25489=CARTESIAN_POINT('Ctrl Pts',(97.4783580454184,0.593529653678918,-2.88333272300151));
#25490=CARTESIAN_POINT('Ctrl Pts',(97.4544641065259,0.63181194817932,-2.88035945550087));
#25491=CARTESIAN_POINT('Ctrl Pts',(97.4492352792564,0.639963843119852,-2.87971786345913));
#25492=CARTESIAN_POINT('Ctrl Pts',(97.4406197495736,0.653038037246644,-2.8786745859055));
#25493=CARTESIAN_POINT('Ctrl Pts',(97.4372950110972,0.658000784454563,-2.87827518896341));
#25494=CARTESIAN_POINT('Ctrl Pts',(97.4308509248713,0.667463219249453,-2.87750702246368));
#25495=CARTESIAN_POINT('Ctrl Pts',(97.4277376632707,0.671966878708811,-2.87713848731499));
#25496=CARTESIAN_POINT('Ctrl Pts',(97.4205532148742,0.682206554536134,-2.87629376446147));
#25497=CARTESIAN_POINT('Ctrl Pts',(97.4164618486732,0.687928088170462,-2.87581682266126));
#25498=CARTESIAN_POINT('Ctrl Pts',(97.4036685150321,0.705484271766663,-2.8743377671868));
#25499=CARTESIAN_POINT('Ctrl Pts',(97.3947964865978,0.717192641375545,-2.8733291948492));
#25500=CARTESIAN_POINT('Ctrl Pts',(97.3292443300348,0.800420320291184,-2.86599454841086));
#25501=CARTESIAN_POINT('Ctrl Pts',(97.2646501074495,0.865290863763662,-2.85934395187622));
#25502=CARTESIAN_POINT('Ctrl Pts',(97.1776881841854,0.93439989836288,-2.85119204829202));
#25503=CARTESIAN_POINT('Ctrl Pts',(97.1618317391493,0.946359591977941,-2.84973551157088));
#25504=CARTESIAN_POINT('Ctrl Pts',(97.1371256381188,0.964031978173706,-2.84751731717873));
#25505=CARTESIAN_POINT('Ctrl Pts',(97.1284892358031,0.970036404582205,-2.8467511548269));
#25506=CARTESIAN_POINT('Ctrl Pts',(97.0994809187217,0.989633173165769,-2.84421059883275));
#25507=CARTESIAN_POINT('Ctrl Pts',(97.0787644262287,1.00270657414317,-2.8424491806011));
#25508=CARTESIAN_POINT('Ctrl Pts',(97.049034194821,1.02019613648238,-2.84000879795541));
#25509=CARTESIAN_POINT('Ctrl Pts',(97.0403497088137,1.02515721546501,-2.8393061133871));
#25510=CARTESIAN_POINT('Ctrl Pts',(97.0250094818353,1.03366311509145,-2.83808393997327));
#25511=CARTESIAN_POINT('Ctrl Pts',(97.0183810320589,1.03725570837788,-2.83756197053904));
#25512=CARTESIAN_POINT('Ctrl Pts',(97.0084126612964,1.04253532052752,-2.8367866141955));
#25513=CARTESIAN_POINT('Ctrl Pts',(97.0050986125118,1.04427039479552,-2.83653041698755));
#25514=CARTESIAN_POINT('Ctrl Pts',(97.0017635779524,1.04599626142931,-2.83627421643074));
#25515=CARTESIAN_POINT('Ctrl Pts',(97.0017508597257,1.04600284276509,-2.83627323942793));
#25516=CARTESIAN_POINT('Ctrl Pts',(97.001725305159,1.04601606596627,-2.83627127639633));
#25517=CARTESIAN_POINT('Ctrl Pts',(97.0017124688816,1.04602270779372,-2.83627029037278));
#25518=CARTESIAN_POINT('Ctrl Pts',(97.0016866770629,1.04603605255711,-2.83626830921265));
#25519=CARTESIAN_POINT('Ctrl Pts',(97.0016737211745,1.04604275566701,-2.83626731404985));
#25520=CARTESIAN_POINT('Ctrl Pts',(97.0016476881485,1.04605622400551,-2.83626531446008));
#25521=CARTESIAN_POINT('Ctrl Pts',(97.0016346116658,1.04606298888959,-2.83626431008386));
#25522=CARTESIAN_POINT('Ctrl Pts',(97.0016083361947,1.04607658140938,-2.83626229197212));
#25523=CARTESIAN_POINT('Ctrl Pts',(97.0015951370314,1.04608340912971,-2.83626127822362));
#25524=CARTESIAN_POINT('Ctrl Pts',(97.0015686146738,1.04609712809335,-2.8362592412516));
#25525=CARTESIAN_POINT('Ctrl Pts',(97.0015552917613,1.0461040191849,-2.8362582180502));
#25526=CARTESIAN_POINT('Ctrl Pts',(97.0015285204552,1.0461178656232,-2.83625616206242));
#25527=CARTESIAN_POINT('Ctrl Pts',(97.0015150720133,1.04612482098877,-2.83625512927283));
#25528=CARTESIAN_POINT('Ctrl Pts',(97.0014880481205,1.04613879674694,-2.83625305399283));
#25529=CARTESIAN_POINT('Ctrl Pts',(97.0014744727672,1.04614581708281,-2.83625201151041));
#25530=CARTESIAN_POINT('Ctrl Pts',(97.0014471937013,1.04615992346106,-2.83624991674257));
#25531=CARTESIAN_POINT('Ctrl Pts',(97.0014334896944,1.04616700964929,-2.83624886443505));
#25532=CARTESIAN_POINT('Ctrl Pts',(97.0014059515975,1.04618124860451,-2.83624674988619));
#25533=CARTESIAN_POINT('Ctrl Pts',(97.0013921176172,1.04618840130826,-2.83624568765379));
#25534=CARTESIAN_POINT('Ctrl Pts',(97.0013643179878,1.04620277409486,-2.83624355313497));
#25535=CARTESIAN_POINT('Ctrl Pts',(97.0013503522125,1.0462099942363,-2.8362424808394));
#25536=CARTESIAN_POINT('Ctrl Pts',(97.0013222872284,1.04622450279055,-2.83624032606036));
#25537=CARTESIAN_POINT('Ctrl Pts',(97.0013081882112,1.04623179109754,-2.83623924359214));
#25538=CARTESIAN_POINT('Ctrl Pts',(97.0012798552718,1.04624643672321,-2.83623706835648));
#25539=CARTESIAN_POINT('Ctrl Pts',(97.0012656211068,1.04625379416046,-2.83623597557095));
#25540=CARTESIAN_POINT('Ctrl Pts',(97.001237016241,1.04626857886861,-2.83623377957715));
#25541=CARTESIAN_POINT('Ctrl Pts',(97.0012226454426,1.04627600618291,-2.83623267636196));
#25542=CARTESIAN_POINT('Ctrl Pts',(97.0011937652452,1.04629093169102,-2.83623045935203));
#25543=CARTESIAN_POINT('Ctrl Pts',(97.0011792562182,1.04629842968538,-2.83622934558644));
#25544=CARTESIAN_POINT('Ctrl Pts',(97.0011500977151,1.04631349748702,-2.83622710733557));
#25545=CARTESIAN_POINT('Ctrl Pts',(97.0011354485582,1.046321067122,-2.83622598287539));
#25546=CARTESIAN_POINT('Ctrl Pts',(97.001106008481,1.04633627886172,-2.8362237231363));
#25547=CARTESIAN_POINT('Ctrl Pts',(97.0010912172478,1.04634392112063,-2.83622258783395));
#25548=CARTESIAN_POINT('Ctrl Pts',(97.0010614914671,1.04635927888675,-2.8362203062933));
#25549=CARTESIAN_POINT('Ctrl Pts',(97.0010465565831,1.04636699456006,-2.8362191600298));
#25550=CARTESIAN_POINT('Ctrl Pts',(97.0010165410557,1.04638250039499,-2.83621685638103));
#25551=CARTESIAN_POINT('Ctrl Pts',(97.0010014610511,1.04639029021867,-2.83621569904543));
#25552=CARTESIAN_POINT('Ctrl Pts',(97.0009711537988,1.04640594509682,-2.83621337314054));
#25553=CARTESIAN_POINT('Ctrl Pts',(97.0009559261828,1.04641381033351,-2.83621220454363));
#25554=CARTESIAN_POINT('Ctrl Pts',(97.0009253219372,1.04642961692784,-2.83620985598222));
#25555=CARTESIAN_POINT('Ctrl Pts',(97.0009099453165,1.0464375582726,-2.83620867601905));
#25556=CARTESIAN_POINT('Ctrl Pts',(97.0008790411323,1.04645351805459,-2.83620630457909));
#25557=CARTESIAN_POINT('Ctrl Pts',(97.0008635134599,1.04646153653954,-2.83620511309462));
#25558=CARTESIAN_POINT('Ctrl Pts',(97.0008323050362,1.04647765167958,-2.83620271845018));
#25559=CARTESIAN_POINT('Ctrl Pts',(97.0008166245765,1.04648574817543,-2.83620151531328));
#25560=CARTESIAN_POINT('Ctrl Pts',(97.0007851088386,1.04650202020935,-2.83619909723262));
#25561=CARTESIAN_POINT('Ctrl Pts',(97.0007692733564,1.04651019584392,-2.83619788227392));
#25562=CARTESIAN_POINT('Ctrl Pts',(97.0007374458956,1.04652662699495,-2.83619544042305));
#25563=CARTESIAN_POINT('Ctrl Pts',(97.0007214535335,1.0465348827004,-2.8361942135022));
#25564=CARTESIAN_POINT('Ctrl Pts',(97.0006893100342,1.04655147514231,-2.83619174755441));
#25565=CARTESIAN_POINT('Ctrl Pts',(97.0006731590339,1.04655981179885,-2.83619050853873));
#25566=CARTESIAN_POINT('Ctrl Pts',(97.00064069607,1.04657656724463,-2.83618801823566));
#25567=CARTESIAN_POINT('Ctrl Pts',(97.000624384237,1.04658498595701,-2.83618676695905));
#25568=CARTESIAN_POINT('Ctrl Pts',(97.00059159798,1.04660190632608,-2.83618425201158));
#25569=CARTESIAN_POINT('Ctrl Pts',(97.0005751230591,1.04661040822953,-2.83618298830338));
#25570=CARTESIAN_POINT('Ctrl Pts',(97.0005420083843,1.04662749610861,-2.8361804483231));
#25571=CARTESIAN_POINT('Ctrl Pts',(97.0005253686955,1.04663608204071,-2.83617917205681));
#25572=CARTESIAN_POINT('Ctrl Pts',(97.0004919221036,1.04665333917613,-2.8361766067801));
#25573=CARTESIAN_POINT('Ctrl Pts',(97.0004751153979,1.04666201026745,-2.83617531778564));
#25574=CARTESIAN_POINT('Ctrl Pts',(97.0004413326219,1.04667943880009,-2.83617272689014));
#25575=CARTESIAN_POINT('Ctrl Pts',(97.0004243567054,1.04668819615178,-2.83617142500173));
#25576=CARTESIAN_POINT('Ctrl Pts',(97.0003927143127,1.04670451851149,-2.83616899841504));
#25577=CARTESIAN_POINT('Ctrl Pts',(97.0003780476421,1.04671208375238,-2.83616787369118));
#25578=CARTESIAN_POINT('Ctrl Pts',(97.0003480451391,1.04672755859734,-2.83616557299255));
#25579=CARTESIAN_POINT('Ctrl Pts',(97.0003327096747,1.04673546797514,-2.83616439704895));
#25580=CARTESIAN_POINT('Ctrl Pts',(97.0003013385469,1.04675164699076,-2.83616199153978));
#25581=CARTESIAN_POINT('Ctrl Pts',(97.0002853025206,1.04675991677591,-2.8361607619496));
#25582=CARTESIAN_POINT('Ctrl Pts',(97.0002524970752,1.04677683360273,-2.8361582466119));
#25583=CARTESIAN_POINT('Ctrl Pts',(97.0002357281957,1.04678548032261,-2.83615696090925));
#25584=CARTESIAN_POINT('Ctrl Pts',(97.0002014228425,1.04680316852185,-2.83615433073501));
#25585=CARTESIAN_POINT('Ctrl Pts',(97.000183886109,1.0468122100874,-2.83615298624734));
#25586=CARTESIAN_POINT('Ctrl Pts',(97.0001480088512,1.04683070649464,-2.8361502357397));
#25587=CARTESIAN_POINT('Ctrl Pts',(97.0001296685942,1.04684016114631,-2.83614882974443));
#25588=CARTESIAN_POINT('Ctrl Pts',(97.0000921464834,1.04685950305613,-2.83614595333614));
#25589=CARTESIAN_POINT('Ctrl Pts',(97.0000729645317,1.04686939030753,-2.83614448292022));
#25590=CARTESIAN_POINT('Ctrl Pts',(97.0000337193397,1.04688961770136,-2.83614147464208));
#25591=CARTESIAN_POINT('Ctrl Pts',(97.000013656137,1.04689995776169,-2.83613993678779));
#25592=CARTESIAN_POINT('Ctrl Pts',(96.9999726070225,1.04692111192968,-2.83613679047338));
#25593=CARTESIAN_POINT('Ctrl Pts',(96.9999516207137,1.04693192617316,-2.83613518198837));
#25594=CARTESIAN_POINT('Ctrl Pts',(96.9999086816822,1.04695405101928,-2.83613189107966));
#25595=CARTESIAN_POINT('Ctrl Pts',(96.9998867287839,1.04696536163717,-2.83613020864857));
#25596=CARTESIAN_POINT('Ctrl Pts',(96.9998418103219,1.04698850283274,-2.83612676632155));
#25597=CARTESIAN_POINT('Ctrl Pts',(96.9998188450897,1.04700033315721,-2.83612500645767));
#25598=CARTESIAN_POINT('Ctrl Pts',(96.9997718541473,1.04702453814519,-2.83612140562136));
#25599=CARTESIAN_POINT('Ctrl Pts',(96.9997478281137,1.04703691288499,-2.83611956463143));
#25600=CARTESIAN_POINT('Ctrl Pts',(96.9996986651567,1.04706223239331,-2.83611579770245));
#25601=CARTESIAN_POINT('Ctrl Pts',(96.9996735282113,1.0470751770743,-2.83611387176967));
#25602=CARTESIAN_POINT('Ctrl Pts',(96.9996220903764,1.04710166348479,-2.83610993091443));
#25603=CARTESIAN_POINT('Ctrl Pts',(96.9995957895622,1.04711520506718,-2.83610791600646));
#25604=CARTESIAN_POINT('Ctrl Pts',(96.9995419683922,1.04714291357581,-2.83610379296818));
#25605=CARTESIAN_POINT('Ctrl Pts',(96.9995144482628,1.04715708026666,-2.83610168486479));
#25606=CARTESIAN_POINT('Ctrl Pts',(96.9994581305478,1.04718606844328,-2.8360973710285));
#25607=CARTESIAN_POINT('Ctrl Pts',(96.9994293327486,1.04720088990876,-2.83609516528974));
#25608=CARTESIAN_POINT('Ctrl Pts',(96.9993703988724,1.04723121854093,-2.83609065155623));
#25609=CARTESIAN_POINT('Ctrl Pts',(96.9993402625758,1.04724672567792,-2.83608834355616));
#25610=CARTESIAN_POINT('Ctrl Pts',(96.9992785876637,1.04727845817155,-2.83608362043057));
#25611=CARTESIAN_POINT('Ctrl Pts',(96.9992470490281,1.04729468338197,-2.83608120531614));
#25612=CARTESIAN_POINT('Ctrl Pts',(96.9991825024183,1.04732788602431,-2.83607626286822));
#25613=CARTESIAN_POINT('Ctrl Pts',(96.9991494943946,1.04734486331,-2.8360737355448));
#25614=CARTESIAN_POINT('Ctrl Pts',(96.9990837284374,1.04737868531904,-2.83606870036398));
#25615=CARTESIAN_POINT('Ctrl Pts',(96.9990509705815,1.04739553003247,-2.83606619251011));
#25616=CARTESIAN_POINT('Ctrl Pts',(96.9989780966347,1.04743299888128,-2.83606061382459));
#25617=CARTESIAN_POINT('Ctrl Pts',(96.9989379800671,1.04745362229097,-2.83605754303485));
#25618=CARTESIAN_POINT('Ctrl Pts',(96.998848745859,1.04749948996466,-2.8360507129767));
#25619=CARTESIAN_POINT('Ctrl Pts',(96.9987996275969,1.04752473309453,-2.83604695377813));
#25620=CARTESIAN_POINT('Ctrl Pts',(96.9986903874506,1.04758086468419,-2.83603859401873));
#25621=CARTESIAN_POINT('Ctrl Pts',(96.9986302647637,1.04761175138158,-2.83603399357222));
#25622=CARTESIAN_POINT('Ctrl Pts',(96.9984497307201,1.04770447710142,-2.83602018112));
#25623=CARTESIAN_POINT('Ctrl Pts',(96.9983293112801,1.04776630058248,-2.83601097008789));
#25624=CARTESIAN_POINT('Ctrl Pts',(96.9954582575898,1.04923967752026,-2.83579141023946));
#25625=CARTESIAN_POINT('Ctrl Pts',(96.9927020756964,1.05064042095293,-2.8355817477836));
#25626=CARTESIAN_POINT('Ctrl Pts',(96.9865897183398,1.05371661110011,-2.83511917414598));
#25627=CARTESIAN_POINT('Ctrl Pts',(96.9832309584351,1.05538692538626,-2.83486657542912));
#25628=CARTESIAN_POINT('Ctrl Pts',(96.9712658332756,1.06126605844432,-2.83397215020811));
#25629=CARTESIAN_POINT('Ctrl Pts',(96.9626158788199,1.06538601994717,-2.83333547250403));
#25630=CARTESIAN_POINT('Ctrl Pts',(96.8831011816924,1.10207515009635,-2.82756433798437));
#25631=CARTESIAN_POINT('Ctrl Pts',(96.8092048344613,1.12764033084855,-2.82278019432459));
#25632=CARTESIAN_POINT('Ctrl Pts',(96.6804084361057,1.15831114223334,-2.81458872521298));
#25633=CARTESIAN_POINT('Ctrl Pts',(96.6266964660867,1.16722944498864,-2.81121475584011));
#25634=CARTESIAN_POINT('Ctrl Pts',(96.5523893872103,1.1743332720838,-2.80644895866472));
#25635=CARTESIAN_POINT('Ctrl Pts',(96.532169359578,1.17574082844781,-2.80514273902991));
#25636=CARTESIAN_POINT('Ctrl Pts',(96.4967712652627,1.17728845969005,-2.80283254760023));
#25637=CARTESIAN_POINT('Ctrl Pts',(96.4816078220439,1.17765815305746,-2.80183544577691));
#25638=CARTESIAN_POINT('Ctrl Pts',(96.4593452629466,1.17777083418023,-2.80035860838719));
#25639=CARTESIAN_POINT('Ctrl Pts',(96.4522484681269,1.17774260778417,-2.79988590429107));
#25640=CARTESIAN_POINT('Ctrl Pts',(96.4396855788131,1.177579087464,-2.79904551672093));
#25641=CARTESIAN_POINT('Ctrl Pts',(96.4342193099253,1.17746986341124,-2.79867864784263));
#25642=CARTESIAN_POINT('Ctrl Pts',(96.4227553374457,1.1771609285487,-2.79790662175393));
#25643=CARTESIAN_POINT('Ctrl Pts',(96.4167580185672,1.17695343005497,-2.79750123441681));
#25644=CARTESIAN_POINT('Ctrl Pts',(96.4009611125814,1.17628597415192,-2.79642934713953));
#25645=CARTESIAN_POINT('Ctrl Pts',(96.3911654068634,1.1757493990743,-2.79576050420177));
#25646=CARTESIAN_POINT('Ctrl Pts',(96.3484684016645,1.17287517996881,-2.79282628438202));
#25647=CARTESIAN_POINT('Ctrl Pts',(96.3156696802063,1.16927854971727,-2.79052267527381));
#25648=CARTESIAN_POINT('Ctrl Pts',(96.1824756344831,1.1489829470998,-2.78095891734609));
#25649=CARTESIAN_POINT('Ctrl Pts',(96.0842986985664,1.12068314393935,-2.77337181593966));
#25650=CARTESIAN_POINT('Ctrl Pts',(95.9711832733422,1.07151753323898,-2.7644518492937));
#25651=CARTESIAN_POINT('Ctrl Pts',(95.9516043251507,1.06235904226172,-2.76290315540541));
#25652=CARTESIAN_POINT('Ctrl Pts',(95.9287833015,1.0509081993579,-2.76110075900233));
#25653=CARTESIAN_POINT('Ctrl Pts',(95.9252880219267,1.04913248098871,-2.76082478278657));
#25654=CARTESIAN_POINT('Ctrl Pts',(95.9218016730066,1.04733934304671,-2.76054963702842));
#25655=CARTESIAN_POINT('Ctrl Pts',(95.9218019448244,1.04733948285108,-2.66237442964626));
#25656=CARTESIAN_POINT('Ctrl Pts',(95.9663540586353,1.07025400934438,-2.66601386898332));
#25657=CARTESIAN_POINT('Ctrl Pts',(96.0123492927123,1.09031600146745,-2.66970698864775));
#25658=CARTESIAN_POINT('Ctrl Pts',(96.1086000098264,1.12516685586158,-2.67720048344083));
#25659=CARTESIAN_POINT('Ctrl Pts',(96.1588220835574,1.13965954581114,-2.68098827651821));
#25660=CARTESIAN_POINT('Ctrl Pts',(96.2166448882217,1.15225321068321,-2.68510428922803));
#25661=CARTESIAN_POINT('Ctrl Pts',(96.223457413953,1.15367384288636,-2.68558540435396));
#25662=CARTESIAN_POINT('Ctrl Pts',(96.2338733587941,1.1557497436619,-2.68631477400422));
#25663=CARTESIAN_POINT('Ctrl Pts',(96.2374677634198,1.15644869747496,-2.68656534224159));
#25664=CARTESIAN_POINT('Ctrl Pts',(96.2440542443618,1.15769762804151,-2.68702235583915));
#25665=CARTESIAN_POINT('Ctrl Pts',(96.2470452029915,1.15825277864105,-2.6872290772222));
#25666=CARTESIAN_POINT('Ctrl Pts',(96.253802636675,1.15947995857396,-2.68769430912778));
#25667=CARTESIAN_POINT('Ctrl Pts',(96.257570257238,1.16014522854953,-2.68795244151098));
#25668=CARTESIAN_POINT('Ctrl Pts',(96.2673169651254,1.16181732615593,-2.68861712787747));
#25669=CARTESIAN_POINT('Ctrl Pts',(96.2733007940795,1.16279637832727,-2.6890221979335));
#25670=CARTESIAN_POINT('Ctrl Pts',(96.3135293102752,1.16905982837264,-2.69172691573369));
#25671=CARTESIAN_POINT('Ctrl Pts',(96.3479888329969,1.17287752801496,-2.69395399200171));
#25672=CARTESIAN_POINT('Ctrl Pts',(96.4107084007409,1.17703568710873,-2.69792577585794));
#25673=CARTESIAN_POINT('Ctrl Pts',(96.438905886038,1.17789004272111,-2.69968171942755));
#25674=CARTESIAN_POINT('Ctrl Pts',(96.515053759483,1.17746157386284,-2.70440312758135));
#25675=CARTESIAN_POINT('Ctrl Pts',(96.5629376360678,1.1742642312032,-2.70735163659253));
#25676=CARTESIAN_POINT('Ctrl Pts',(96.6634207426539,1.16136043503585,-2.71368682288293));
#25677=CARTESIAN_POINT('Ctrl Pts',(96.7158191573994,1.15097520984258,-2.71707895268986));
#25678=CARTESIAN_POINT('Ctrl Pts',(96.7777881101862,1.13425243655716,-2.72129748198627));
#25679=CARTESIAN_POINT('Ctrl Pts',(96.7882075808831,1.13128584644294,-2.72201383644248));
#25680=CARTESIAN_POINT('Ctrl Pts',(96.8045454837078,1.12638953532181,-2.72314892785088));
#25681=CARTESIAN_POINT('Ctrl Pts',(96.8104922467831,1.12455585821711,-2.72356457428885));
#25682=CARTESIAN_POINT('Ctrl Pts',(96.8215985279412,1.12103462174659,-2.72434564677691));
#25683=CARTESIAN_POINT('Ctrl Pts',(96.8267614726324,1.11935834534743,-2.72471069873768));
#25684=CARTESIAN_POINT('Ctrl Pts',(96.8382943024762,1.11552559693821,-2.72553062316257));
#25685=CARTESIAN_POINT('Ctrl Pts',(96.8446576338129,1.11335015116531,-2.72598610340758));
#25686=CARTESIAN_POINT('Ctrl Pts',(96.8608022575925,1.10767586638347,-2.72714974533548));
#25687=CARTESIAN_POINT('Ctrl Pts',(96.8705563584975,1.10410195255554,-2.72786033717157));
#25688=CARTESIAN_POINT('Ctrl Pts',(96.9507797487173,1.07349831447265,-2.73376886507221));
#25689=CARTESIAN_POINT('Ctrl Pts',(97.0185355208864,1.03988593423637,-2.73918851583574));
#25690=CARTESIAN_POINT('Ctrl Pts',(97.1317055887668,0.969482927792906,-2.7489383901991));
#25691=CARTESIAN_POINT('Ctrl Pts',(97.1784951794666,0.935358477456175,-2.75320978194467));
#25692=CARTESIAN_POINT('Ctrl Pts',(97.2382010136099,0.884684046383803,-2.75886465845143));
#25693=CARTESIAN_POINT('Ctrl Pts',(97.2534655393762,0.87102807056017,-2.76032991818037));
#25694=CARTESIAN_POINT('Ctrl Pts',(97.2778572319971,0.848033713443923,-2.76269399060493));
#25695=CARTESIAN_POINT('Ctrl Pts',(97.2871986512601,0.838929701006134,-2.76360511507559));
#25696=CARTESIAN_POINT('Ctrl Pts',(97.2996988533462,0.826335567239342,-2.76482995312867));
#25697=CARTESIAN_POINT('Ctrl Pts',(97.3029903976098,0.822979338471609,-2.76515302114701));
#25698=CARTESIAN_POINT('Ctrl Pts',(97.3084690829008,0.817325668490033,-2.76569153884634));
#25699=CARTESIAN_POINT('Ctrl Pts',(97.3106671692767,0.815038965475175,-2.7659078089783));
#25700=CARTESIAN_POINT('Ctrl Pts',(97.3148277645409,0.810675487541049,-2.76631752985166));
#25701=CARTESIAN_POINT('Ctrl Pts',(97.3167919900742,0.808600413495037,-2.76651111606723));
#25702=CARTESIAN_POINT('Ctrl Pts',(97.3214462009582,0.803647569217087,-2.76697024957072));
#25703=CARTESIAN_POINT('Ctrl Pts',(97.3241293599648,0.800763388232761,-2.7672352880574));
#25704=CARTESIAN_POINT('Ctrl Pts',(97.3335871098416,0.790494229011149,-2.76817098365678));
#25705=CARTESIAN_POINT('Ctrl Pts',(97.3402820881501,0.78303605670343,-2.76883605134641));
#25706=CARTESIAN_POINT('Ctrl Pts',(97.3865749324673,0.730122629399314,-2.77346160040564));
#25707=CARTESIAN_POINT('Ctrl Pts',(97.4227319137921,0.681765414417662,-2.77721774770458));
#25708=CARTESIAN_POINT('Ctrl Pts',(97.4907129690381,0.574591118580488,-2.78508024869095));
#25709=CARTESIAN_POINT('Ctrl Pts',(97.521556597827,0.515413263641715,-2.78917140781017));
#25710=CARTESIAN_POINT('Ctrl Pts',(97.5604357680378,0.42233640917668,-2.79558464550255));
#25711=CARTESIAN_POINT('Ctrl Pts',(97.5722532905243,0.390167351712429,-2.79779597112176));
#25712=CARTESIAN_POINT('Ctrl Pts',(97.5855595177424,0.348403572046824,-2.80068461261046));
#25713=CARTESIAN_POINT('Ctrl Pts',(97.5883561006421,0.339241017950264,-2.80131937103951));
#25714=CARTESIAN_POINT('Ctrl Pts',(97.5927080155404,0.324333686034414,-2.80235423823862));
#25715=CARTESIAN_POINT('Ctrl Pts',(97.5943321596776,0.31860932182205,-2.80275212662732));
#25716=CARTESIAN_POINT('Ctrl Pts',(97.5973689863232,0.307588524332501,-2.80351923880726));
#25717=CARTESIAN_POINT('Ctrl Pts',(97.5987882099123,0.302294041824895,-2.80388824183233));
#25718=CARTESIAN_POINT('Ctrl Pts',(97.6019559624507,0.290137891386286,-2.80473665691486));
#25719=CARTESIAN_POINT('Ctrl Pts',(97.6036796578444,0.283270031346951,-2.80521684625146));
#25720=CARTESIAN_POINT('Ctrl Pts',(97.6089788784832,0.261319419631843,-2.80675456967465));
#25721=CARTESIAN_POINT('Ctrl Pts',(97.6123184926412,0.246181978433166,-2.8078194878866));
#25722=CARTESIAN_POINT('Ctrl Pts',(97.630640734358,0.154574014095299,-2.81429402187953));
#25723=CARTESIAN_POINT('Ctrl Pts',(97.6382997778215,0.0768496093721461,
-2.81993130167333));
#25724=CARTESIAN_POINT('Ctrl Pts',(97.6381647893319,-0.0748980491663311,
-2.83105779166144));
#25725=CARTESIAN_POINT('Ctrl Pts',(97.631153159679,-0.148584594388026,-2.83651100063276));
#25726=CARTESIAN_POINT('Ctrl Pts',(97.6154736991933,-0.230607544573968,
-2.84236197868445));
#25727=CARTESIAN_POINT('Ctrl Pts',(97.6135463496234,-0.240058928974523,
-2.84303263086583));
#25728=CARTESIAN_POINT('Ctrl Pts',(97.6106820058404,-0.253273793745423,
-2.84396437021411));
#25729=CARTESIAN_POINT('Ctrl Pts',(97.6098422743851,-0.257057640475069,
-2.84423046884668));
#25730=CARTESIAN_POINT('Ctrl Pts',(97.6082920835984,-0.263883345113966,
-2.84470915722954));
#25731=CARTESIAN_POINT('Ctrl Pts',(97.6075881745252,-0.266926646243,-2.84492210611287));
#25732=CARTESIAN_POINT('Ctrl Pts',(97.6061251057949,-0.273139435339931,
-2.84535580638582));
#25733=CARTESIAN_POINT('Ctrl Pts',(97.6053648848538,-0.27630863036546,-2.8455764964868));
#25734=CARTESIAN_POINT('Ctrl Pts',(97.603379534233,-0.28443623828964,-2.84614116915173));
#25735=CARTESIAN_POINT('Ctrl Pts',(97.6021352724631,-0.289389975409617,
-2.84648408801441));
#25736=CARTESIAN_POINT('Ctrl Pts',(97.5967844263749,-0.310121368041253,
-2.84791457639331));
#25737=CARTESIAN_POINT('Ctrl Pts',(97.5923824693897,-0.325821836037436,
-2.84898666491449));
#25738=CARTESIAN_POINT('Ctrl Pts',(97.5794935326046,-0.368372932170697,
-2.8518740967461));
#25739=CARTESIAN_POINT('Ctrl Pts',(97.5703671887484,-0.395019662268076,
-2.85366244816334));
#25740=CARTESIAN_POINT('Ctrl Pts',(97.5299106068564,-0.500628611504686,
-2.86076312922837));
#25741=CARTESIAN_POINT('Ctrl Pts',(97.4910376196131,-0.576422005274534,
-2.8659071441088));
#25742=CARTESIAN_POINT('Ctrl Pts',(97.4230655427561,-0.679724476674423,
-2.87372873608515));
#25743=CARTESIAN_POINT('Ctrl Pts',(97.4002007336604,-0.710999799204278,
-2.87621708737866));
#25744=CARTESIAN_POINT('Ctrl Pts',(97.369332635706,-0.749126552268779,-2.8794445748785));
#25745=CARTESIAN_POINT('Ctrl Pts',(97.3627208775857,-0.757076667090176,
-2.88012884050519));
#25746=CARTESIAN_POINT('Ctrl Pts',(97.3520331234067,-0.769588974931314,
-2.88122451552935));
#25747=CARTESIAN_POINT('Ctrl Pts',(97.3480246786715,-0.774208367016738,
-2.88163319082155));
#25748=CARTESIAN_POINT('Ctrl Pts',(97.3407416566589,-0.782470536509436,
-2.88237181146634));
#25749=CARTESIAN_POINT('Ctrl Pts',(97.3374799675646,-0.786124528395592,
-2.88270122121272));
#25750=CARTESIAN_POINT('Ctrl Pts',(97.3297562787912,-0.794669297837173,
-2.88347811188416));
#25751=CARTESIAN_POINT('Ctrl Pts',(97.3252756838025,-0.79954296661796,-2.88392636270999));
#25752=CARTESIAN_POINT('Ctrl Pts',(97.3120658345516,-0.813670745079915,
-2.88524105728996));
#25753=CARTESIAN_POINT('Ctrl Pts',(97.3032276780343,-0.822821260908672,
-2.88611208946013));
#25754=CARTESIAN_POINT('Ctrl Pts',(97.2352688202048,-0.890938275222554,
-2.89274833266928));
#25755=CARTESIAN_POINT('Ctrl Pts',(97.1701865235266,-0.943599604013672,
-2.8987854688735));
#25756=CARTESIAN_POINT('Ctrl Pts',(97.039194677788,-1.02832218890769,-2.9102263522282));
#25757=CARTESIAN_POINT('Ctrl Pts',(96.9747764345198,-1.0620066336921,-2.91557835557593));
#25758=CARTESIAN_POINT('Ctrl Pts',(96.8986688311447,-1.0932433286244,-2.92134350565761));
#25759=CARTESIAN_POINT('Ctrl Pts',(96.889628416951,-1.09682362374725,-2.92201964738021));
#25760=CARTESIAN_POINT('Ctrl Pts',(96.876911070954,-1.10167878313548,-2.92295771333596));
#25761=CARTESIAN_POINT('Ctrl Pts',(96.8732708842239,-1.1030478947576,-2.92322473600786));
#25762=CARTESIAN_POINT('Ctrl Pts',(96.8669564293806,-1.10538718957934,-2.92368527581429));
#25763=CARTESIAN_POINT('Ctrl Pts',(96.8642853325616,-1.10636575113703,-2.92387927242119));
#25764=CARTESIAN_POINT('Ctrl Pts',(96.858614393183,-1.10842003744551,-2.9242893711362));
#25765=CARTESIAN_POINT('Ctrl Pts',(96.8556136754024,-1.10949328426272,-2.92450532228908));
#25766=CARTESIAN_POINT('Ctrl Pts',(96.8481078693628,-1.11214352293168,-2.925042961671));
#25767=CARTESIAN_POINT('Ctrl Pts',(96.8435974232867,-1.11370535334296,-2.9253637777945));
#25768=CARTESIAN_POINT('Ctrl Pts',(96.826222354679,-1.11960376326395,-2.92659138036781));
#25769=CARTESIAN_POINT('Ctrl Pts',(96.8132920225567,-1.12374541057853,-2.92748764698077));
#25770=CARTESIAN_POINT('Ctrl Pts',(96.7795599872562,-1.13391026548408,-2.92978816111361));
#25771=CARTESIAN_POINT('Ctrl Pts',(96.7586580314389,-1.13958521618735,-2.93117701218273));
#25772=CARTESIAN_POINT('Ctrl Pts',(96.6380778980831,-1.16877788413901,-2.93904225063871));
#25773=CARTESIAN_POINT('Ctrl Pts',(96.5358270161162,-1.17979130246164,-2.94518206607897));
#25774=CARTESIAN_POINT('Ctrl Pts',(96.4010626873588,-1.17669584278995,-2.95376466696525));
#25775=CARTESIAN_POINT('Ctrl Pts',(96.368736550134,-1.17461751554145,-2.95585668776548));
#25776=CARTESIAN_POINT('Ctrl Pts',(96.3268506949603,-1.17018500050912,-2.95863144908712));
#25777=CARTESIAN_POINT('Ctrl Pts',(96.3171755553971,-1.16903957803086,-2.95927681726107));
#25778=CARTESIAN_POINT('Ctrl Pts',(96.3015808585473,-1.16699685241761,-2.96032470843447));
#25779=CARTESIAN_POINT('Ctrl Pts',(96.2956518520169,-1.1661741974691,-2.96072490459219));
#25780=CARTESIAN_POINT('Ctrl Pts',(96.2843164256689,-1.16451322582957,-2.96149357907426));
#25781=CARTESIAN_POINT('Ctrl Pts',(96.2789090581526,-1.16368236178441,-2.96186181542352));
#25782=CARTESIAN_POINT('Ctrl Pts',(96.2664720770932,-1.16168257301862,-2.96271243653817));
#25783=CARTESIAN_POINT('Ctrl Pts',(96.2594469508878,-1.16048747109417,-2.96319562825402));
#25784=CARTESIAN_POINT('Ctrl Pts',(96.2373469939121,-1.15652117392608,-2.96472446950394));
#25785=CARTESIAN_POINT('Ctrl Pts',(96.2223156952353,-1.1535195105332,-2.96577727045876));
#25786=CARTESIAN_POINT('Ctrl Pts',(96.187282775681,-1.14580972518998,-2.9682625765319));
#25787=CARTESIAN_POINT('Ctrl Pts',(96.1673378046631,-1.14086992127229,-2.96970190607677));
#25788=CARTESIAN_POINT('Ctrl Pts',(96.0938667562285,-1.12061946410546,-2.97509554490433));
#25789=CARTESIAN_POINT('Ctrl Pts',(96.0413222022353,-1.10204294839336,-2.97913992276067));
#25790=CARTESIAN_POINT('Ctrl Pts',(95.9206239553812,-1.04948729889846,-2.98878857495109));
#25791=CARTESIAN_POINT('Ctrl Pts',(95.8540485676708,-1.01247757070838,-2.99440618208594));
#25792=CARTESIAN_POINT('Ctrl Pts',(95.7836770678246,-0.963909694778292,
-3.00039506305378));
#25793=CARTESIAN_POINT('Ctrl Pts',(95.7759201972558,-0.958416394212479,
-3.00105575947556));
#25794=CARTESIAN_POINT('Ctrl Pts',(95.7651143461908,-0.950565717938824,
-3.00197600774841));
#25795=CARTESIAN_POINT('Ctrl Pts',(95.7620093833136,-0.948286543926136,
-3.00224041512364));
#25796=CARTESIAN_POINT('Ctrl Pts',(95.7564118710914,-0.944135324862518,
-3.00271696503446));
#25797=CARTESIAN_POINT('Ctrl Pts',(95.7539154708188,-0.942268541325628,
-3.00292945688122));
#25798=CARTESIAN_POINT('Ctrl Pts',(95.7488167377208,-0.938424101695163,
-3.00336332418986));
#25799=CARTESIAN_POINT('Ctrl Pts',(95.7462151804926,-0.936445490594071,
-3.00358463140933));
#25800=CARTESIAN_POINT('Ctrl Pts',(95.739535550762,-0.931321275969118,-3.00415277204559));
#25801=CARTESIAN_POINT('Ctrl Pts',(95.7354697603805,-0.928159665744005,
-3.00449851642664));
#25802=CARTESIAN_POINT('Ctrl Pts',(95.7183195759232,-0.914642006552505,
-3.00595723620951));
#25803=CARTESIAN_POINT('Ctrl Pts',(95.7054345827661,-0.90403460007461,-3.00705395875899));
#25804=CARTESIAN_POINT('Ctrl Pts',(95.6706800978347,-0.874161776889747,
-3.01002809155301));
#25805=CARTESIAN_POINT('Ctrl Pts',(95.6492925576752,-0.854352285993023,
-3.01187649409323));
#25806=CARTESIAN_POINT('Ctrl Pts',(95.5621362240676,-0.767399590029131,
-3.0195969995126));
#25807=CARTESIAN_POINT('Ctrl Pts',(95.5037956008233,-0.693310107047775,
-3.02527350649935));
#25808=CARTESIAN_POINT('Ctrl Pts',(95.4393059161946,-0.587530097487091,
-3.0331834717284));
#25809=CARTESIAN_POINT('Ctrl Pts',(95.4247130109355,-0.561404137414405,
-3.03512036203158));
#25810=CARTESIAN_POINT('Ctrl Pts',(95.4068270695234,-0.526306401932507,
-3.03771699555707));
#25811=CARTESIAN_POINT('Ctrl Pts',(95.4026250787456,-0.517808724892698,
-3.03834523807455));
#25812=CARTESIAN_POINT('Ctrl Pts',(95.3959627046806,-0.50391578320374,-3.03937211072911));
#25813=CARTESIAN_POINT('Ctrl Pts',(95.3934396257025,-0.498550921419669,
-3.03976858489841));
#25814=CARTESIAN_POINT('Ctrl Pts',(95.3886589138722,-0.488183071325856,
-3.04053478908916));
#25815=CARTESIAN_POINT('Ctrl Pts',(95.3863955340879,-0.483182890668872,
-3.04090431161191));
#25816=CARTESIAN_POINT('Ctrl Pts',(95.3812228525201,-0.471539622694852,
-3.04176486484143));
#25817=CARTESIAN_POINT('Ctrl Pts',(95.3783398211502,-0.464885179296589,
-3.04225676575113));
#25818=CARTESIAN_POINT('Ctrl Pts',(95.3692851437974,-0.443445010976813,
-3.04384211959519));
#25819=CARTESIAN_POINT('Ctrl Pts',(95.3633539141323,-0.428560367553834,
-3.04494349646848));
#25820=CARTESIAN_POINT('Ctrl Pts',(95.350085191382,-0.393179483143595,-3.04756452643043));
#25821=CARTESIAN_POINT('Ctrl Pts',(95.3430088981202,-0.372592211810573,
-3.04909206523416));
#25822=CARTESIAN_POINT('Ctrl Pts',(95.3052665895603,-0.252015951827739,
-3.05805299057977));
#25823=CARTESIAN_POINT('Ctrl Pts',(95.2874611621814,-0.148497143163256,
-3.06586033474288));
#25824=CARTESIAN_POINT('Ctrl Pts',(95.2824332096335,-0.0140539367339928,
-3.07557432519419));
#25825=CARTESIAN_POINT('Ctrl Pts',(95.2824571030796,0.0159420902453292,
-3.07771027253911));
#25826=CARTESIAN_POINT('Ctrl Pts',(95.2838752319896,0.0522966082595831,
-3.08023711188907));
#25827=CARTESIAN_POINT('Ctrl Pts',(95.2841765124887,0.0586841184268421,
-3.08067874738934));
#25828=CARTESIAN_POINT('Ctrl Pts',(95.2847276222602,0.0686439736991038,
-3.08136341717221));
#25829=CARTESIAN_POINT('Ctrl Pts',(95.284941739024,0.0722180526845859,-3.0816083137778));
#25830=CARTESIAN_POINT('Ctrl Pts',(95.2853683390178,0.0788334248508394,
-3.08206005821494));
#25831=CARTESIAN_POINT('Ctrl Pts',(95.285576330699,0.0818748634086122,-3.0822671373571));
#25832=CARTESIAN_POINT('Ctrl Pts',(95.2860794563372,0.0888348830761416,
-3.0827396462324));
#25833=CARTESIAN_POINT('Ctrl Pts',(95.2863823937992,0.0927528231951996,
-3.08300464433913));
#25834=CARTESIAN_POINT('Ctrl Pts',(95.2873860459821,0.10493935535317,-3.08382603842329));
#25835=CARTESIAN_POINT('Ctrl Pts',(95.2881545597509,0.113202325216241,-3.08437886655753));
#25836=CARTESIAN_POINT('Ctrl Pts',(95.2901651417045,0.13259472029244,-3.08566808898048));
#25837=CARTESIAN_POINT('Ctrl Pts',(95.2914787440969,0.143716086875455,-3.08640107685722));
#25838=CARTESIAN_POINT('Ctrl Pts',(95.2967685301269,0.183608127972321,-3.08901279200894));
#25839=CARTESIAN_POINT('Ctrl Pts',(95.3016501620551,0.212249810345654,-3.0908552693653));
#25840=CARTESIAN_POINT('Ctrl Pts',(95.3264880732794,0.331225529647054,-3.09847801851818));
#25841=CARTESIAN_POINT('Ctrl Pts',(95.3559890002146,0.419223261554849,-3.10406770305709));
#25842=CARTESIAN_POINT('Ctrl Pts',(95.4088258103388,0.531124483469788,-3.11195668464847));
#25843=CARTESIAN_POINT('Ctrl Pts',(95.4232879883082,0.558840087648294,-3.11397770336914));
#25844=CARTESIAN_POINT('Ctrl Pts',(95.4436203206812,0.594291235280489,-3.116670740302));
#25845=CARTESIAN_POINT('Ctrl Pts',(95.4485084488211,0.602577181464901,-3.11730813667241));
#25846=CARTESIAN_POINT('Ctrl Pts',(95.4565879329454,0.615897219502984,-3.1183462413799));
#25847=CARTESIAN_POINT('Ctrl Pts',(95.4597170247295,0.620968709638013,-3.11874470304889));
#25848=CARTESIAN_POINT('Ctrl Pts',(95.4657965225961,0.630656775828993,-3.1195121943089));
#25849=CARTESIAN_POINT('Ctrl Pts',(95.4687409263771,0.635276949700458,-3.11988099781594));
#25850=CARTESIAN_POINT('Ctrl Pts',(95.4756199466394,0.645906697813495,-3.1207360888178));
#25851=CARTESIAN_POINT('Ctrl Pts',(95.4795774860086,0.65190110338251,-3.12122321175409));
#25852=CARTESIAN_POINT('Ctrl Pts',(95.4923246992689,0.670830154424144,-3.12277739129527));
#25853=CARTESIAN_POINT('Ctrl Pts',(95.5013169650072,0.683625651273023,-3.12385194063286));
#25854=CARTESIAN_POINT('Ctrl Pts',(95.5230280506598,0.713247418574105,-3.12639779494679));
#25855=CARTESIAN_POINT('Ctrl Pts',(95.5359490471729,0.729918135479005,-3.12787638707241));
#25856=CARTESIAN_POINT('Ctrl Pts',(95.5862113649606,0.79128987719799,-3.13349598633765));
#25857=CARTESIAN_POINT('Ctrl Pts',(95.6264002402084,0.833543628443717,-3.13773559407867));
#25858=CARTESIAN_POINT('Ctrl Pts',(95.722952260825,0.921054912916952,-3.14729289549292));
#25859=CARTESIAN_POINT('Ctrl Pts',(95.7806959365638,0.964460927588447,-3.15261008441173));
#25860=CARTESIAN_POINT('Ctrl Pts',(95.8503237999271,1.00742136910774,-3.15834341172623));
#25861=CARTESIAN_POINT('Ctrl Pts',(95.8586600977274,1.01242344881201,-3.15901943370131));
#25862=CARTESIAN_POINT('Ctrl Pts',(95.8704167543442,1.01928133038278,-3.15995736172232));
#25863=CARTESIAN_POINT('Ctrl Pts',(95.873785548795,1.02122411484335,-3.16022436430213));
#25864=CARTESIAN_POINT('Ctrl Pts',(95.8796351478772,1.02455908019468,-3.16068487908988));
#25865=CARTESIAN_POINT('Ctrl Pts',(95.8821114619338,1.02595901007983,-3.16087887064855));
#25866=CARTESIAN_POINT('Ctrl Pts',(95.8873727962883,1.02890828723372,-3.16128897029248));
#25867=CARTESIAN_POINT('Ctrl Pts',(95.8901590838189,1.03045533084014,-3.16150492736123));
#25868=CARTESIAN_POINT('Ctrl Pts',(95.8971343673452,1.0342912921111,-3.16204260135164));
#25869=CARTESIAN_POINT('Ctrl Pts',(95.9013311178489,1.0365661176592,-3.16236344592702));
#25870=CARTESIAN_POINT('Ctrl Pts',(95.910939416062,1.04169890833297,-3.1630922433017));
#25871=CARTESIAN_POINT('Ctrl Pts',(95.9163595808209,1.04454030537047,-3.16349922992478));
#25872=CARTESIAN_POINT('Ctrl Pts',(95.9218016730922,1.04733934309078,-3.1639039911222));
#25873=CARTESIAN_POINT('Origin',(96.460480949577,-7.19464945638997E-16,
0.924367114736168));
#25874=CARTESIAN_POINT('',(95.921801595944,1.04733930341107,-3.76190742309816));
#25875=CARTESIAN_POINT('',(95.9218017102038,1.04733936217843,-3.66210953954391));
#25876=CARTESIAN_POINT('',(95.9218016730721,1.04733934308042,0.924367114736168));
#25877=CARTESIAN_POINT('Ctrl Pts',(95.921801595944,1.04733930341107,-3.76190742309816));
#25878=CARTESIAN_POINT('Ctrl Pts',(95.8962264988879,1.03418523127187,-3.76011579365399));
#25879=CARTESIAN_POINT('Ctrl Pts',(95.8711315530826,1.02009353307782,-3.75831047647257));
#25880=CARTESIAN_POINT('Ctrl Pts',(95.8274863741028,0.993434893227348,-3.75505698510355));
#25881=CARTESIAN_POINT('Ctrl Pts',(95.8087413652297,0.981239237558241,-3.75362027545444));
#25882=CARTESIAN_POINT('Ctrl Pts',(95.7769064042041,0.959212374883115,-3.75110111045232));
#25883=CARTESIAN_POINT('Ctrl Pts',(95.7636530284024,0.949628003487759,-3.75002742763029));
#25884=CARTESIAN_POINT('Ctrl Pts',(95.7447697826221,0.935364125973282,-3.74845863469301));
#25885=CARTESIAN_POINT('Ctrl Pts',(95.738976823307,0.930902956494515,-3.74797189496362));
#25886=CARTESIAN_POINT('Ctrl Pts',(95.7289013511859,0.922993272446278,-3.74711546572422));
#25887=CARTESIAN_POINT('Ctrl Pts',(95.7246007061124,0.919568135210955,-3.7467466991317));
#25888=CARTESIAN_POINT('Ctrl Pts',(95.7162901545888,0.912853778048933,-3.74602774492841));
#25889=CARTESIAN_POINT('Ctrl Pts',(95.712277676495,0.909567930454248,-3.74567769681928));
#25890=CARTESIAN_POINT('Ctrl Pts',(95.7015897637707,0.900696943966807,-3.74473732240066));
#25891=CARTESIAN_POINT('Ctrl Pts',(95.6949544280044,0.895064218078987,-3.74414509196726));
#25892=CARTESIAN_POINT('Ctrl Pts',(95.6704592311989,0.873798657840505,-3.74192665430579));
#25893=CARTESIAN_POINT('Ctrl Pts',(95.6530118441587,0.857701529376837,-3.74028160503915));
#25894=CARTESIAN_POINT('Ctrl Pts',(95.5640698078699,0.77052249533053,-3.73153996219475));
#25895=CARTESIAN_POINT('Ctrl Pts',(95.5014426631754,0.691011472349212,-3.72407534013313));
#25896=CARTESIAN_POINT('Ctrl Pts',(95.4344131552923,0.578937511781002,-3.71455120705597));
#25897=CARTESIAN_POINT('Ctrl Pts',(95.4200874088515,0.552779594576922,-3.71239441864231));
#25898=CARTESIAN_POINT('Ctrl Pts',(95.3991999679067,0.510945047567632,-3.70907446133398));
#25899=CARTESIAN_POINT('Ctrl Pts',(95.3919585338193,0.49562292557937,-3.70788471077241));
#25900=CARTESIAN_POINT('Ctrl Pts',(95.3829385801679,0.475420154483092,-3.70635466661999));
#25901=CARTESIAN_POINT('Ctrl Pts',(95.3808584845957,0.470677402008181,-3.70599821894912));
#25902=CARTESIAN_POINT('Ctrl Pts',(95.3775141468252,0.462913265513497,-3.70541933722816));
#25903=CARTESIAN_POINT('Ctrl Pts',(95.3762311314206,0.459900119314074,-3.7051958156858));
#25904=CARTESIAN_POINT('Ctrl Pts',(95.3737529118436,0.454012034748813,-3.70476128791256));
#25905=CARTESIAN_POINT('Ctrl Pts',(95.3725565172301,0.451137656956187,-3.70455021577775));
#25906=CARTESIAN_POINT('Ctrl Pts',(95.3699113050293,0.444710728563006,-3.70408054294366));
#25907=CARTESIAN_POINT('Ctrl Pts',(95.3684684060854,0.441155740741356,-3.70382229017021));
#25908=CARTESIAN_POINT('Ctrl Pts',(95.363544123011,0.428851179380597,-3.70293352696014));
#25909=CARTESIAN_POINT('Ctrl Pts',(95.3601502074514,0.42006666988485,-3.70230790123492));
#25910=CARTESIAN_POINT('Ctrl Pts',(95.3296010061518,0.338084100915692,-3.6965429068482));
#25911=CARTESIAN_POINT('Ctrl Pts',(95.3096779079478,0.262385658831466,-3.69175436383144));
#25912=CARTESIAN_POINT('Ctrl Pts',(95.2888559946576,0.131664971017972,-3.68356457278708));
#25913=CARTESIAN_POINT('Ctrl Pts',(95.2840341658322,0.0775437903394788,
-3.68019718458866));
#25914=CARTESIAN_POINT('Ctrl Pts',(95.2825609572128,0.0030483911169273,
-3.67543985621155));
#25915=CARTESIAN_POINT('Ctrl Pts',(95.2826825629583,-0.017195661879143,
-3.67413516945524));
#25916=CARTESIAN_POINT('Ctrl Pts',(95.283807263385,-0.0525710119043245,
-3.67182744559456));
#25917=CARTESIAN_POINT('Ctrl Pts',(95.2845810093655,-0.067705034108542,
-3.67083125761951));
#25918=CARTESIAN_POINT('Ctrl Pts',(95.2861453524805,-0.0898960275837626,
-3.66935552085773));
#25919=CARTESIAN_POINT('Ctrl Pts',(95.286708137701,-0.0969678957148688,
-3.66888298825782));
#25920=CARTESIAN_POINT('Ctrl Pts',(95.287817686569,-0.109479781345357,-3.66804279454567));
#25921=CARTESIAN_POINT('Ctrl Pts',(95.2883385101261,-0.11492193372713,-3.66767594671396));
#25922=CARTESIAN_POINT('Ctrl Pts',(95.2895105943463,-0.126330979195489,
-3.66690385215306));
#25923=CARTESIAN_POINT('Ctrl Pts',(95.2901696160824,-0.13229689916204,-3.6664983745375));
#25924=CARTESIAN_POINT('Ctrl Pts',(95.2920265406785,-0.14800579512436,-3.66542598756796));
#25925=CARTESIAN_POINT('Ctrl Pts',(95.2933006790065,-0.157739110368548,
-3.66475673126597));
#25926=CARTESIAN_POINT('Ctrl Pts',(95.2993932951894,-0.200154527426412,
-3.66181855588219));
#25927=CARTESIAN_POINT('Ctrl Pts',(95.3054635441935,-0.232638774721101,
-3.65951127919769));
#25928=CARTESIAN_POINT('Ctrl Pts',(95.3311628016828,-0.344004827360322,
-3.65139786216768));
#25929=CARTESIAN_POINT('Ctrl Pts',(95.3575799294867,-0.421076181429397,
-3.64540523707158));
#25930=CARTESIAN_POINT('Ctrl Pts',(95.4065519807671,-0.52685511090678,-3.63687455410522));
#25931=CARTESIAN_POINT('Ctrl Pts',(95.4228262813435,-0.558225495885777,
-3.6343060402724));
#25932=CARTESIAN_POINT('Ctrl Pts',(95.449954883054,-0.605219594611901,-3.63044159753571));
#25933=CARTESIAN_POINT('Ctrl Pts',(95.4598175707864,-0.621390852404269,
-3.62910871906064));
#25934=CARTESIAN_POINT('Ctrl Pts',(95.4729797914285,-0.641845391255723,
-3.62742538307828));
#25935=CARTESIAN_POINT('Ctrl Pts',(95.4759240040404,-0.646352587528858,
-3.62705462421256));
#25936=CARTESIAN_POINT('Ctrl Pts',(95.4807337916269,-0.653606603193718,
-3.62645838484702));
#25937=CARTESIAN_POINT('Ctrl Pts',(95.4825802158884,-0.656365935278397,
-3.62623169457153));
#25938=CARTESIAN_POINT('Ctrl Pts',(95.4861661811299,-0.661676149546743,
-3.62579571092749));
#25939=CARTESIAN_POINT('Ctrl Pts',(95.487904109929,-0.664228037739306,-3.62558632161974));
#25940=CARTESIAN_POINT('Ctrl Pts',(95.4917659109567,-0.669850862114665,
-3.62512517314593));
#25941=CARTESIAN_POINT('Ctrl Pts',(95.4938944118356,-0.672918620287419,
-3.62487371930569));
#25942=CARTESIAN_POINT('Ctrl Pts',(95.5014732419932,-0.683731652578977,
-3.62398772343226));
#25943=CARTESIAN_POINT('Ctrl Pts',(95.5070025420534,-0.691421504081438,
-3.62335820345055));
#25944=CARTESIAN_POINT('Ctrl Pts',(95.5603202558847,-0.763716732617802,
-3.6174365589991));
#25945=CARTESIAN_POINT('Ctrl Pts',(95.6145173496878,-0.823348013849373,
-3.61251740585219));
#25946=CARTESIAN_POINT('Ctrl Pts',(95.7137126148767,-0.912262644176052,
-3.60427325709178));
#25947=CARTESIAN_POINT('Ctrl Pts',(95.7553778495771,-0.944836011124048,
-3.60099125938578));
#25948=CARTESIAN_POINT('Ctrl Pts',(95.8155685444667,-0.985687509875306,
-3.59634396703402));
#25949=CARTESIAN_POINT('Ctrl Pts',(95.8323314437918,-0.996453715932912,
-3.59505939547738));
#25950=CARTESIAN_POINT('Ctrl Pts',(95.8621527900226,-1.01455531102816,-3.59278408031653));
#25951=CARTESIAN_POINT('Ctrl Pts',(95.8750933488403,-1.02207650874092,-3.59179991554965));
#25952=CARTESIAN_POINT('Ctrl Pts',(95.8943432725977,-1.03277927477638,-3.59033866677666));
#25953=CARTESIAN_POINT('Ctrl Pts',(95.9005438922124,-1.03615413325488,-3.58986839939262));
#25954=CARTESIAN_POINT('Ctrl Pts',(95.9115956012941,-1.04204115886769,-3.58903076081365));
#25955=CARTESIAN_POINT('Ctrl Pts',(95.9164345745886,-1.04457572367029,-3.58866418554441));
#25956=CARTESIAN_POINT('Ctrl Pts',(95.9266427573101,-1.04983240757999,-3.5878911598405));
#25957=CARTESIAN_POINT('Ctrl Pts',(95.9320155411572,-1.05254720051486,-3.58748446836076));
#25958=CARTESIAN_POINT('Ctrl Pts',(95.9462756734567,-1.05961593810717,-3.58640536236708));
#25959=CARTESIAN_POINT('Ctrl Pts',(95.9551973350177,-1.06389917791706,-3.58573054753544));
#25960=CARTESIAN_POINT('Ctrl Pts',(95.9948540124099,-1.08232679792293,-3.5827316185277));
#25961=CARTESIAN_POINT('Ctrl Pts',(96.0261334911932,-1.09525413997415,-3.58036715298766));
#25962=CARTESIAN_POINT('Ctrl Pts',(96.1422458488791,-1.13748508981621,-3.57158860392831));
#25963=CARTESIAN_POINT('Ctrl Pts',(96.2297909045413,-1.15841458722514,-3.56493905067645));
#25964=CARTESIAN_POINT('Ctrl Pts',(96.3474409737906,-1.17266649041917,-3.55630281782057));
#25965=CARTESIAN_POINT('Ctrl Pts',(96.3761553931163,-1.17508048918689,-3.55422103812789));
#25966=CARTESIAN_POINT('Ctrl Pts',(96.4214695994568,-1.17722016024378,-3.55100208231746));
#25967=CARTESIAN_POINT('Ctrl Pts',(96.4380236986057,-1.17765229675402,-3.54984007601831));
#25968=CARTESIAN_POINT('Ctrl Pts',(96.4597184651846,-1.17776095235082,-3.54833999634666));
#25969=CARTESIAN_POINT('Ctrl Pts',(96.4648547568724,-1.17775307875157,-3.54798652206235));
#25970=CARTESIAN_POINT('Ctrl Pts',(96.473256358879,-1.17768523596426,-3.54741124523273));
#25971=CARTESIAN_POINT('Ctrl Pts',(96.4765216948585,-1.17764528668139,-3.54718838002288));
#25972=CARTESIAN_POINT('Ctrl Pts',(96.4829060535945,-1.17754061888076,-3.5467540977208));
#25973=CARTESIAN_POINT('Ctrl Pts',(96.4860250441665,-1.17747708852005,-3.54654262118865));
#25974=CARTESIAN_POINT('Ctrl Pts',(96.4930027468704,-1.17730722229821,-3.5460709765356));
#25975=CARTESIAN_POINT('Ctrl Pts',(96.4968612991698,-1.17719430604323,-3.5458111661792));
#25976=CARTESIAN_POINT('Ctrl Pts',(96.5102662788259,-1.17673605151267,-3.54491182273778));
#25977=CARTESIAN_POINT('Ctrl Pts',(96.5198093137165,-1.17629353198926,-3.54427732868217));
#25978=CARTESIAN_POINT('Ctrl Pts',(96.6044455846745,-1.17133620334127,-3.53869274241208));
#25979=CARTESIAN_POINT('Ctrl Pts',(96.6789619343092,-1.15975153802912,-3.53406714360415));
#25980=CARTESIAN_POINT('Ctrl Pts',(96.8062777120929,-1.12724116350638,-3.52593891566542));
#25981=CARTESIAN_POINT('Ctrl Pts',(96.8596163749504,-1.10947659329195,-3.5224607679926));
#25982=CARTESIAN_POINT('Ctrl Pts',(96.930558248863,-1.08006889329543,-3.51756105189604));
#25983=CARTESIAN_POINT('Ctrl Pts',(96.9494219607149,-1.07166137117709,-3.51623088690277));
#25984=CARTESIAN_POINT('Ctrl Pts',(96.9819394448575,-1.05613109045067,-3.51388218815197));
#25985=CARTESIAN_POINT('Ctrl Pts',(96.9956929073246,-1.04922827221261,-3.51287085445709));
#25986=CARTESIAN_POINT('Ctrl Pts',(97.0156218807661,-1.03873218555018,-3.51137688655667));
#25987=CARTESIAN_POINT('Ctrl Pts',(97.0219065880417,-1.03534885690895,-3.51090152394723));
#25988=CARTESIAN_POINT('Ctrl Pts',(97.0329551301552,-1.02927077412618,-3.51005812405196));
#25989=CARTESIAN_POINT('Ctrl Pts',(97.0377317041404,-1.02659952198082,-3.50969092177131));
#25990=CARTESIAN_POINT('Ctrl Pts',(97.047689226528,-1.02093940866751,-3.50891992192117));
#25991=CARTESIAN_POINT('Ctrl Pts',(97.0528663584122,-1.0179441840367,-3.5085159058378));
#25992=CARTESIAN_POINT('Ctrl Pts',(97.0663961499154,-1.00997836820594,-3.50745160869495));
#25993=CARTESIAN_POINT('Ctrl Pts',(97.0747103381124,-1.0049436713989,-3.50678904432556));
#25994=CARTESIAN_POINT('Ctrl Pts',(97.110266067293,-0.982806660159659,-3.50391778512569));
#25995=CARTESIAN_POINT('Ctrl Pts',(97.1368607178075,-0.964696686773595,
-3.50167284305935));
#25996=CARTESIAN_POINT('Ctrl Pts',(97.2285274714655,-0.896619826873043,
-3.49357537072678));
#25997=CARTESIAN_POINT('Ctrl Pts',(97.289080930863,-0.840976518992091,-3.48752804788429));
#25998=CARTESIAN_POINT('Ctrl Pts',(97.377603802382,-0.740714807832277,-3.47773879451204));
#25999=CARTESIAN_POINT('Ctrl Pts',(97.4092632435488,-0.699704359762225,
-3.47398576019866));
#26000=CARTESIAN_POINT('Ctrl Pts',(97.4420009167106,-0.650969990066961,
-3.46990245875859));
#26001=CARTESIAN_POINT('Ctrl Pts',(97.4458257131345,-0.645165929519488,
-3.46942191133067));
#26002=CARTESIAN_POINT('Ctrl Pts',(97.4515858863273,-0.636254244431529,
-3.46869320772909));
#26003=CARTESIAN_POINT('Ctrl Pts',(97.4535584515858,-0.63317101570372,-3.46844274435539));
#26004=CARTESIAN_POINT('Ctrl Pts',(97.4571443017282,-0.627508152449101,
-3.46798581185558));
#26005=CARTESIAN_POINT('Ctrl Pts',(97.4587619710553,-0.624931453451115,
-3.46777906765202));
#26006=CARTESIAN_POINT('Ctrl Pts',(97.4623926647974,-0.619098242158763,
-3.46731364558971));
#26007=CARTESIAN_POINT('Ctrl Pts',(97.4643998082453,-0.615838164443482,
-3.46705534705968));
#26008=CARTESIAN_POINT('Ctrl Pts',(97.4695486247545,-0.607383194516477,
-3.46638998155709));
#26009=CARTESIAN_POINT('Ctrl Pts',(97.4726661385212,-0.602173617142791,
-3.46598440338801));
#26010=CARTESIAN_POINT('Ctrl Pts',(97.4933986779388,-0.566912174135319,
-3.46326702613465));
#26011=CARTESIAN_POINT('Ctrl Pts',(97.5097150960555,-0.536112548932825,
-3.46102857825812));
#26012=CARTESIAN_POINT('Ctrl Pts',(97.563716282685,-0.422235373459249,-3.45306653781826));
#26013=CARTESIAN_POINT('Ctrl Pts',(97.5930880658869,-0.335579168232345,
-3.44756652821645));
#26014=CARTESIAN_POINT('Ctrl Pts',(97.6204722495787,-0.207583335840273,
-3.43929000611338));
#26015=CARTESIAN_POINT('Ctrl Pts',(97.6268082783092,-0.168376682339155,
-3.43673920724081));
#26016=CARTESIAN_POINT('Ctrl Pts',(97.6322501521289,-0.118964187548293,
-3.43346637123012));
#26017=CARTESIAN_POINT('Ctrl Pts',(97.633220193476,-0.108987144238704,-3.4328026795988));
#26018=CARTESIAN_POINT('Ctrl Pts',(97.6345710856818,-0.092973047211535,
-3.43173226013924));
#26019=CARTESIAN_POINT('Ctrl Pts',(97.6350329985036,-0.0869431841124467,
-3.43132804750004));
#26020=CARTESIAN_POINT('Ctrl Pts',(97.6358232727898,-0.075466912115708,
-3.43055640275571));
#26021=CARTESIAN_POINT('Ctrl Pts',(97.6361602662685,-0.0700212406777715,
-3.43018924815991));
#26022=CARTESIAN_POINT('Ctrl Pts',(97.6368435681495,-0.0575773083010886,
-3.42934789167097));
#26023=CARTESIAN_POINT('Ctrl Pts',(97.6371652840934,-0.0505779600130338,
-3.42887294246872));
#26024=CARTESIAN_POINT('Ctrl Pts',(97.637967888394,-0.028900574278145,-3.4273964788855));
#26025=CARTESIAN_POINT('Ctrl Pts',(97.6382366922115,-0.014216586273703,
-3.42638849319511));
#26026=CARTESIAN_POINT('Ctrl Pts',(97.638207738034,0.0586443039133953,-3.42134582836754));
#26027=CARTESIAN_POINT('Ctrl Pts',(97.6338742324366,0.116730217766737,-3.41718986520103));
#26028=CARTESIAN_POINT('Ctrl Pts',(97.6162402326283,0.234605498196122,-3.40851686435091));
#26029=CARTESIAN_POINT('Ctrl Pts',(97.602534286478,0.294165280185552,-3.40400491838927));
#26030=CARTESIAN_POINT('Ctrl Pts',(97.5793544758938,0.368086347227076,-3.39837246677786));
#26031=CARTESIAN_POINT('Ctrl Pts',(97.5741054044671,0.383674523097038,-3.3971832509645));
#26032=CARTESIAN_POINT('Ctrl Pts',(97.5606007426072,0.421163975046063,-3.39432680599592));
#26033=CARTESIAN_POINT('Ctrl Pts',(97.5520150376988,0.442940362539929,-3.39267059675925));
#26034=CARTESIAN_POINT('Ctrl Pts',(97.5404126312541,0.46997747793587,-3.39063008814944));
#26035=CARTESIAN_POINT('Ctrl Pts',(97.5379974106486,0.475488745211111,-3.3902149957794));
#26036=CARTESIAN_POINT('Ctrl Pts',(97.5341270008379,0.484139639058019,-3.38956504402371));
#26037=CARTESIAN_POINT('Ctrl Pts',(97.5327000735977,0.487291683038719,-3.38932856603096));
#26038=CARTESIAN_POINT('Ctrl Pts',(97.5299807007787,0.493228924272358,-3.38888383528646));
#26039=CARTESIAN_POINT('Ctrl Pts',(97.5286912643782,0.496015335597813,-3.38867542018727));
#26040=CARTESIAN_POINT('Ctrl Pts',(97.5256437404625,0.502533889484588,-3.38818851158696));
#26041=CARTESIAN_POINT('Ctrl Pts',(97.5238769217997,0.50626187759933,-3.38791054987453));
#26042=CARTESIAN_POINT('Ctrl Pts',(97.5180369140199,0.518418827179166,-3.38700551875452));
#26043=CARTESIAN_POINT('Ctrl Pts',(97.5138826896912,0.526808775313851,-3.38638313543998));
#26044=CARTESIAN_POINT('Ctrl Pts',(97.4903554219877,0.572933495398094,-3.38296889380943));
#26045=CARTESIAN_POINT('Ctrl Pts',(97.469052749589,0.609653949941007,-3.38027783432291));
#26046=CARTESIAN_POINT('Ctrl Pts',(97.4338745102181,0.663381494102728,-3.3762617896122));
#26047=CARTESIAN_POINT('Ctrl Pts',(97.4214322754108,0.681280131640827,-3.37490981259047));
#26048=CARTESIAN_POINT('Ctrl Pts',(97.3557183708018,0.770427180692221,-3.36805311642911));
#26049=CARTESIAN_POINT('Ctrl Pts',(97.2950011783242,0.83581214368228,-3.36258621162187));
#26050=CARTESIAN_POINT('Ctrl Pts',(97.2160848308699,0.903539914513462,-3.35580436483116));
#26051=CARTESIAN_POINT('Ctrl Pts',(97.204476755838,0.913122012347313,-3.35481474361452));
#26052=CARTESIAN_POINT('Ctrl Pts',(97.1872063250918,0.926830234182048,-3.35335195268731));
#26053=CARTESIAN_POINT('Ctrl Pts',(97.1816854104147,0.931132738410469,-3.35288573057784));
#26054=CARTESIAN_POINT('Ctrl Pts',(97.1717820923058,0.938709576764417,-3.35205170886831));
#26055=CARTESIAN_POINT('Ctrl Pts',(97.1674145728991,0.942003097474619,-3.3516846685469));
#26056=CARTESIAN_POINT('Ctrl Pts',(97.1582162864729,0.948839474814292,-3.35091318344318));
#26057=CARTESIAN_POINT('Ctrl Pts',(97.1533811266725,0.952376129275639,-3.35050851460131));
#26058=CARTESIAN_POINT('Ctrl Pts',(97.1405956728279,0.961579085619236,-3.34944060422895));
#26059=CARTESIAN_POINT('Ctrl Pts',(97.1326016777581,0.967183587268537,-3.34877505104877));
#26060=CARTESIAN_POINT('Ctrl Pts',(97.0944990655968,0.993196402963338,-3.34561203107023));
#26061=CARTESIAN_POINT('Ctrl Pts',(97.063528181944,1.01230015869973,-3.34306716432496));
#26062=CARTESIAN_POINT('Ctrl Pts',(96.9749446917226,1.06143207068858,-3.33585510726276));
#26063=CARTESIAN_POINT('Ctrl Pts',(96.9156616083976,1.0881727534905,-3.33109677911087));
#26064=CARTESIAN_POINT('Ctrl Pts',(96.7984090821579,1.12979658947852,-3.32196642117665));
#26065=CARTESIAN_POINT('Ctrl Pts',(96.740900057033,1.14542669015451,-3.31761019633741));
#26066=CARTESIAN_POINT('Ctrl Pts',(96.6726127546298,1.15853162007676,-3.31273421598941));
#26067=CARTESIAN_POINT('Ctrl Pts',(96.6627504502367,1.16029413646768,-3.31203721367748));
#26068=CARTESIAN_POINT('Ctrl Pts',(96.6489806169948,1.16257406284862,-3.31107515432437));
#26069=CARTESIAN_POINT('Ctrl Pts',(96.6450915017148,1.1631979717049,-3.31080466205198));
#26070=CARTESIAN_POINT('Ctrl Pts',(96.6383758007135,1.16424080352314,-3.31033978055128));
#26071=CARTESIAN_POINT('Ctrl Pts',(96.6355507163483,1.16466896749941,-3.31014489083879));
#26072=CARTESIAN_POINT('Ctrl Pts',(96.6295858599768,1.1655507948362,-3.30973485786621));
#26073=CARTESIAN_POINT('Ctrl Pts',(96.6264457620266,1.16600206154691,-3.30951985524483));
#26074=CARTESIAN_POINT('Ctrl Pts',(96.6186466716879,1.16709073285635,-3.3089878808779));
#26075=CARTESIAN_POINT('Ctrl Pts',(96.6139855497869,1.16771294158852,-3.30867174182828));
#26076=CARTESIAN_POINT('Ctrl Pts',(96.5963734615488,1.16995668300139,-3.30748355424475));
#26077=CARTESIAN_POINT('Ctrl Pts',(96.5833990054547,1.17139088320151,-3.30662117896036));
#26078=CARTESIAN_POINT('Ctrl Pts',(96.5499951971362,1.17452219619262,-3.30442793140284));
#26079=CARTESIAN_POINT('Ctrl Pts',(96.52953995878,1.17590226754377,-3.30311071553934));
#26080=CARTESIAN_POINT('Ctrl Pts',(96.4512988131533,1.17913211951348,-3.29813602601166));
#26081=CARTESIAN_POINT('Ctrl Pts',(96.3934390981789,1.17726082863896,-3.29458641741194));
#26082=CARTESIAN_POINT('Ctrl Pts',(96.2609143845635,1.16316892189656,-3.28633432851085));
#26083=CARTESIAN_POINT('Ctrl Pts',(96.1868318697482,1.14799944623993,-3.28162174921314));
#26084=CARTESIAN_POINT('Ctrl Pts',(96.1047829235298,1.12280092345165,-3.27598861093874));
#26085=CARTESIAN_POINT('Ctrl Pts',(96.0948925300866,1.11961962102213,-3.27530278492724));
#26086=CARTESIAN_POINT('Ctrl Pts',(96.0786710410923,1.11416403186653,-3.27416605014586));
#26087=CARTESIAN_POINT('Ctrl Pts',(96.0723149093042,1.1119655651825,-3.27371760087763));
#26088=CARTESIAN_POINT('Ctrl Pts',(96.0608629271379,1.1078943857459,-3.27290394844389));
#26089=CARTESIAN_POINT('Ctrl Pts',(96.05576049814,1.10604063593009,-3.27253937488855));
#26090=CARTESIAN_POINT('Ctrl Pts',(96.0448364989843,1.10198615500307,-3.27175434162039));
#26091=CARTESIAN_POINT('Ctrl Pts',(96.0390192139224,1.09977443048098,-3.27133352856879));
#26092=CARTESIAN_POINT('Ctrl Pts',(96.0231237928433,1.09358637410383,-3.27017593173458));
#26093=CARTESIAN_POINT('Ctrl Pts',(96.0130827768813,1.0895170038342,-3.26943608845137));
#26094=CARTESIAN_POINT('Ctrl Pts',(95.975517817703,1.07368602990993,-3.2666348868698));
#26095=CARTESIAN_POINT('Ctrl Pts',(95.9483992295894,1.0610192972329,-3.26454426774695));
#26096=CARTESIAN_POINT('Ctrl Pts',(95.9218016227097,1.04733931717749,-3.26242343814143));
#26097=CARTESIAN_POINT('',(97.6382307499679,0.00068569618098675,-3.32647283958636));
#26098=CARTESIAN_POINT('Ctrl Pts',(95.9218016730922,1.04733934309078,-3.1639039911222));
#26099=CARTESIAN_POINT('Ctrl Pts',(95.9284350625409,1.05075110208983,-3.1643973562697));
#26100=CARTESIAN_POINT('Ctrl Pts',(95.9351010302927,1.05409992667817,-3.16488741516598));
#26101=CARTESIAN_POINT('Ctrl Pts',(95.9612454033876,1.06692460104026,-3.16678894697688));
#26102=CARTESIAN_POINT('Ctrl Pts',(95.9809527995633,1.07592616055621,-3.16817824435421));
#26103=CARTESIAN_POINT('Ctrl Pts',(96.0952895725782,1.1243844560262,-3.17605087310667));
#26104=CARTESIAN_POINT('Ctrl Pts',(96.1945005918812,1.1518948418863,-3.18219704691524));
#26105=CARTESIAN_POINT('Ctrl Pts',(96.32799003106,1.17071913262763,-3.19078126878048));
#26106=CARTESIAN_POINT('Ctrl Pts',(96.3601241296241,1.1739102812802,-3.19286697222096));
#26107=CARTESIAN_POINT('Ctrl Pts',(96.4020620541466,1.17634051244649,-3.19563445854756));
#26108=CARTESIAN_POINT('Ctrl Pts',(96.4117838164527,1.1767830507194,-3.19627911828201));
#26109=CARTESIAN_POINT('Ctrl Pts',(96.4274898788756,1.17730304227345,-3.19732613959883));
#26110=CARTESIAN_POINT('Ctrl Pts',(96.4334713720535,1.17745545333156,-3.19772618150922));
#26111=CARTESIAN_POINT('Ctrl Pts',(96.4449243089704,1.17765996400205,-3.19849474863586));
#26112=CARTESIAN_POINT('Ctrl Pts',(96.4503954766207,1.17771952577118,-3.19886303327881));
#26113=CARTESIAN_POINT('Ctrl Pts',(96.4629977142343,1.17776889896263,-3.19971404136749));
#26114=CARTESIAN_POINT('Ctrl Pts',(96.4701286133761,1.17773207147511,-3.20019757423244));
#26115=CARTESIAN_POINT('Ctrl Pts',(96.4926111628343,1.17741176347643,-3.20172860340908));
#26116=CARTESIAN_POINT('Ctrl Pts',(96.5079573128253,1.17689284463589,-3.2027832802902));
#26117=CARTESIAN_POINT('Ctrl Pts',(96.5438509897074,1.17497596908158,-3.20527379517967));
#26118=CARTESIAN_POINT('Ctrl Pts',(96.5643801686324,1.17333880670873,-3.20671649674668));
#26119=CARTESIAN_POINT('Ctrl Pts',(96.6404270569036,1.16526287136231,-3.21212925456227));
#26120=CARTESIAN_POINT('Ctrl Pts',(96.6955028727292,1.15541404314257,-3.21619008429051));
#26121=CARTESIAN_POINT('Ctrl Pts',(96.8230009295493,1.12311949178227,-3.22583061178204));
#26122=CARTESIAN_POINT('Ctrl Pts',(96.8943813540385,1.09752014226995,-3.23142230417399));
#26123=CARTESIAN_POINT('Ctrl Pts',(96.971433199885,1.06118499951821,-3.23738942722104));
#26124=CARTESIAN_POINT('Ctrl Pts',(96.9799998951076,1.05701744777285,-3.23805165093634));
#26125=CARTESIAN_POINT('Ctrl Pts',(96.9919615396042,1.05101774886761,-3.23897366347195));
#26126=CARTESIAN_POINT('Ctrl Pts',(96.9953992196052,1.04927230567082,-3.23923833158901));
#26127=CARTESIAN_POINT('Ctrl Pts',(97.0016016228565,1.04608470118273,-3.23971521078501));
#26128=CARTESIAN_POINT('Ctrl Pts',(97.0043693027853,1.04464838350147,-3.23992777268958));
#26129=CARTESIAN_POINT('Ctrl Pts',(97.009966939946,1.04171515186747,-3.24035715609558));
#26130=CARTESIAN_POINT('Ctrl Pts',(97.0127965466701,1.04021766619817,-3.24057394072053));
#26131=CARTESIAN_POINT('Ctrl Pts',(97.0199897449005,1.03637325258533,-3.24112443758274));
#26132=CARTESIAN_POINT('Ctrl Pts',(97.0243447509081,1.03401026418261,-3.2414571659441));
#26133=CARTESIAN_POINT('Ctrl Pts',(97.0338576271679,1.02877068564333,-3.24218301782307));
#26134=CARTESIAN_POINT('Ctrl Pts',(97.0390090663219,1.02588262464877,-3.24257546876886));
#26135=CARTESIAN_POINT('Ctrl Pts',(97.0540581627215,1.01729621164579,-3.24372079561052));
#26136=CARTESIAN_POINT('Ctrl Pts',(97.0638951966319,1.01149234193363,-3.24446797570809));
#26137=CARTESIAN_POINT('Ctrl Pts',(97.0992031296901,0.989962136732548,-3.24715023311478));
#26138=CARTESIAN_POINT('Ctrl Pts',(97.1241580883341,0.973408426531692,-3.24904692946635));
#26139=CARTESIAN_POINT('Ctrl Pts',(97.2305040515468,0.896871270219678,-3.25725587227644));
#26140=CARTESIAN_POINT('Ctrl Pts',(97.3046040967562,0.827508243602876,-3.26335290274558));
#26141=CARTESIAN_POINT('Ctrl Pts',(97.3838153983031,0.731501932619335,-3.27136494343075));
#26142=CARTESIAN_POINT('Ctrl Pts',(97.3981522053595,0.713031611950603,-3.27288758850829));
#26143=CARTESIAN_POINT('Ctrl Pts',(97.4170290756989,0.687157636279639,-3.27500296491219));
#26144=CARTESIAN_POINT('Ctrl Pts',(97.4220516396637,0.680111561468263,-3.27557728960866));
#26145=CARTESIAN_POINT('Ctrl Pts',(97.4299539266813,0.668763039589785,-3.27649988508025));
#26146=CARTESIAN_POINT('Ctrl Pts',(97.4328837759791,0.664495747324605,-3.27684626245233));
#26147=CARTESIAN_POINT('Ctrl Pts',(97.4388698753604,0.655652689820493,-3.27756303066356));
#26148=CARTESIAN_POINT('Ctrl Pts',(97.4419223733568,0.65107455002475,-3.27793354967336));
#26149=CARTESIAN_POINT('Ctrl Pts',(97.4489736001787,0.640336841822631,-3.2788013736127));
#26150=CARTESIAN_POINT('Ctrl Pts',(97.4529469845707,0.634160986220808,-3.27929959498285));
#26151=CARTESIAN_POINT('Ctrl Pts',(97.4656803733759,0.613956604907375,-3.28092684771773));
#26152=CARTESIAN_POINT('Ctrl Pts',(97.4742023553827,0.599781174775953,-3.28206440231029));
#26153=CARTESIAN_POINT('Ctrl Pts',(97.4937019069202,0.565742347608503,-3.28478767209151));
#26154=CARTESIAN_POINT('Ctrl Pts',(97.504409081684,0.545732433353623,-3.28638213037285));
#26155=CARTESIAN_POINT('Ctrl Pts',(97.5575232445258,0.43918098927892,-3.29483928527847));
#26156=CARTESIAN_POINT('Ctrl Pts',(97.5897643793363,0.347989026783004,-3.30200586241499));
#26157=CARTESIAN_POINT('Ctrl Pts',(97.6159473589241,0.229396241711363,-3.31082030717976));
#26158=CARTESIAN_POINT('Ctrl Pts',(97.6205746673701,0.204714412379462,-3.31262571697676));
#26159=CARTESIAN_POINT('Ctrl Pts',(97.6265695890689,0.165928512977467,-3.31540044245408));
#26160=CARTESIAN_POINT('Ctrl Pts',(97.6284777067806,0.151916443611184,-3.31639024236712));
#26161=CARTESIAN_POINT('Ctrl Pts',(97.6307193117883,0.132899634094702,-3.31771359933256));
#26162=CARTESIAN_POINT('Ctrl Pts',(97.6312737985954,0.127922805171892,-3.31805808442022));
#26163=CARTESIAN_POINT('Ctrl Pts',(97.6321008893281,0.120042825293883,-3.31860044242035));
#26164=CARTESIAN_POINT('Ctrl Pts',(97.6323944758455,0.117142010167833,-3.31879943904172));
#26165=CARTESIAN_POINT('Ctrl Pts',(97.6329584392618,0.111355286562692,-3.31919505698834));
#26166=CARTESIAN_POINT('Ctrl Pts',(97.6332289376657,0.108469444035727,-3.31939167667239));
#26167=CARTESIAN_POINT('Ctrl Pts',(97.6337653850194,0.102509589717689,-3.31979639132501));
#26168=CARTESIAN_POINT('Ctrl Pts',(97.634029914557,0.0994354552902017,-3.32000440895853));
#26169=CARTESIAN_POINT('Ctrl Pts',(97.634624539983,0.0921920951228765,-3.3204928854576));
#26170=CARTESIAN_POINT('Ctrl Pts',(97.6349445180288,0.0880220480615195,
-3.32077280977784));
#26171=CARTESIAN_POINT('Ctrl Pts',(97.6359645372441,0.0737313538625278,
-3.3217279452586));
#26172=CARTESIAN_POINT('Ctrl Pts',(97.6365560495189,0.0636030888188594,
-3.32239773610283));
#26173=CARTESIAN_POINT('Ctrl Pts',(97.6378156614166,0.0358860074512165,
-3.32421425643881));
#26174=CARTESIAN_POINT('Ctrl Pts',(97.6382205020686,0.0182874587000585,
-3.32534956677183));
#26175=CARTESIAN_POINT('Ctrl Pts',(97.6382307499679,0.00068569618098675,
-3.32647283958636));
#26176=CARTESIAN_POINT('Ctrl Pts',(97.6382307490143,0.00068733208902312,
-3.32647273518933));
#26177=CARTESIAN_POINT('Ctrl Pts',(97.6382770658552,-0.0786769969879645,
-3.33153744694585));
#26178=CARTESIAN_POINT('Ctrl Pts',(97.6303013137131,-0.157851648856124,
-3.33635344872659));
#26179=CARTESIAN_POINT('Ctrl Pts',(97.606625994462,-0.273795366228378,-3.34372958097377));
#26180=CARTESIAN_POINT('Ctrl Pts',(97.5969448075925,-0.311547596326401,
-3.34618219489677));
#26181=CARTESIAN_POINT('Ctrl Pts',(97.5805410616979,-0.364459829034245,
-3.34974490195577));
#26182=CARTESIAN_POINT('Ctrl Pts',(97.5753419607074,-0.380066451572931,
-3.35081150537214));
#26183=CARTESIAN_POINT('Ctrl Pts',(97.5654877568798,-0.407702394250402,
-3.35273215743632));
#26184=CARTESIAN_POINT('Ctrl Pts',(97.5609586217089,-0.419773937184554,
-3.35358218025397));
#26185=CARTESIAN_POINT('Ctrl Pts',(97.5537925641819,-0.437960120215368,
-3.35488083065936));
#26186=CARTESIAN_POINT('Ctrl Pts',(97.551300361422,-0.444131018076531,-3.35532467823532));
#26187=CARTESIAN_POINT('Ctrl Pts',(97.546682404585,-0.455292080922485,-3.35613342188149));
#26188=CARTESIAN_POINT('Ctrl Pts',(97.5445742090377,-0.46028934695762,-3.3564977232528));
#26189=CARTESIAN_POINT('Ctrl Pts',(97.5399524088277,-0.471036956683567,
-3.35728606074298));
#26190=CARTESIAN_POINT('Ctrl Pts',(97.5374272192485,-0.476782104852329,
-3.35771047782267));
#26191=CARTESIAN_POINT('Ctrl Pts',(97.5304372174622,-0.492346418079202,
-3.35886863859466));
#26192=CARTESIAN_POINT('Ctrl Pts',(97.5258833229054,-0.502124665865675,
-3.35960537554341));
#26193=CARTESIAN_POINT('Ctrl Pts',(97.5004951274383,-0.554738189931191,
-3.3636203822063));
#26194=CARTESIAN_POINT('Ctrl Pts',(97.4772136943327,-0.596336660290867,
-3.36698186067454));
#26195=CARTESIAN_POINT('Ctrl Pts',(97.4069844483931,-0.705696171288772,
-3.37633821556428));
#26196=CARTESIAN_POINT('Ctrl Pts',(97.3553484068043,-0.770121171285593,
-3.3824550675494));
#26197=CARTESIAN_POINT('Ctrl Pts',(97.2810301096322,-0.845184429744388,
-3.39011039238728));
#26198=CARTESIAN_POINT('Ctrl Pts',(97.2641530093495,-0.861248512835887,
-3.39178336260563));
#26199=CARTESIAN_POINT('Ctrl Pts',(97.239610992501,-0.883258136035274,-3.39411358256002));
#26200=CARTESIAN_POINT('Ctrl Pts',(97.2323329381092,-0.889625247004127,
-3.39479245762194));
#26201=CARTESIAN_POINT('Ctrl Pts',(97.2209760490338,-0.899316368382955,
-3.3958321568395));
#26202=CARTESIAN_POINT('Ctrl Pts',(97.2169521487075,-0.902703746584086,
-3.39619681288014));
#26203=CARTESIAN_POINT('Ctrl Pts',(97.2095173989548,-0.908877800736754,
-3.39686355685727));
#26204=CARTESIAN_POINT('Ctrl Pts',(97.2061133722229,-0.911672502063806,
-3.3971661672936));
#26205=CARTESIAN_POINT('Ctrl Pts',(97.2002682834563,-0.916416674323551,
-3.3976811399251));
#26206=CARTESIAN_POINT('Ctrl Pts',(97.1978350218529,-0.918375627463482,
-3.39789415855569));
#26207=CARTESIAN_POINT('Ctrl Pts',(97.193171651942,-0.922099498401751,-3.39829977418749));
#26208=CARTESIAN_POINT('Ctrl Pts',(97.1909429006942,-0.923866055601311,
-3.3984924898816));
#26209=CARTESIAN_POINT('Ctrl Pts',(97.1856536255042,-0.928027345319967,
-3.39894721421844));
#26210=CARTESIAN_POINT('Ctrl Pts',(97.1825875814772,-0.930415056198753,
-3.39920873700817));
#26211=CARTESIAN_POINT('Ctrl Pts',(97.1717394396161,-0.938777223758773,
-3.40012700831896));
#26212=CARTESIAN_POINT('Ctrl Pts',(97.1638943071926,-0.944669772577159,
-3.40077840549285));
#26213=CARTESIAN_POINT('Ctrl Pts',(97.0986505312648,-0.992411444864561,
-3.40610068574788));
#26214=CARTESIAN_POINT('Ctrl Pts',(97.0376390741064,-1.02909290466519,-3.41048425996234));
#26215=CARTESIAN_POINT('Ctrl Pts',(96.9206428502157,-1.08573435739123,-3.41852464525718));
#26216=CARTESIAN_POINT('Ctrl Pts',(96.8657508961875,-1.10739499830961,-3.42216643877416));
#26217=CARTESIAN_POINT('Ctrl Pts',(96.7891920199696,-1.13114760442962,-3.42727555534493));
#26218=CARTESIAN_POINT('Ctrl Pts',(96.7687478935929,-1.136889300453,-3.42864205328648));
#26219=CARTESIAN_POINT('Ctrl Pts',(96.7329170324958,-1.14591481097142,-3.43104902526543));
#26220=CARTESIAN_POINT('Ctrl Pts',(96.7175987105506,-1.14944882113353,-3.43208178182147));
#26221=CARTESIAN_POINT('Ctrl Pts',(96.695170325036,-1.15415240193836,-3.43360147526847));
#26222=CARTESIAN_POINT('Ctrl Pts',(96.6881125754422,-1.15556510371089,-3.43408077142885));
#26223=CARTESIAN_POINT('Ctrl Pts',(96.6756586733308,-1.15793939747957,-3.43492862538003));
#26224=CARTESIAN_POINT('Ctrl Pts',(96.6702678776649,-1.15892818764057,-3.43529631771252));
#26225=CARTESIAN_POINT('Ctrl Pts',(96.6590083321617,-1.16091230177867,-3.43606583260128));
#26226=CARTESIAN_POINT('Ctrl Pts',(96.6531385585539,-1.16190082946785,-3.43646785681354));
#26227=CARTESIAN_POINT('Ctrl Pts',(96.6377935259728,-1.16436560868705,-3.43752122804168));
#26228=CARTESIAN_POINT('Ctrl Pts',(96.6283074470817,-1.16577067974211,-3.43817477381897));
#26229=CARTESIAN_POINT('Ctrl Pts',(96.5881153794085,-1.17122317816419,-3.44095448130407));
#26230=CARTESIAN_POINT('Ctrl Pts',(96.5572756728521,-1.17417407394072,-3.44311408813969));
#26231=CARTESIAN_POINT('Ctrl Pts',(96.4434276068684,-1.18055209797416,-3.45118957647388));
#26232=CARTESIAN_POINT('Ctrl Pts',(96.3602467950593,-1.1764114227093,-3.45731174126188));
#26233=CARTESIAN_POINT('Ctrl Pts',(96.226687130472,-1.15548905986495,-3.46720774948426));
#26234=CARTESIAN_POINT('Ctrl Pts',(96.1757534784659,-1.14400440733427,-3.47099110822223));
#26235=CARTESIAN_POINT('Ctrl Pts',(96.1190730342821,-1.12720189264742,-3.47510294566811));
#26236=CARTESIAN_POINT('Ctrl Pts',(96.112419768381,-1.12516527293042,-3.47558398547491));
#26237=CARTESIAN_POINT('Ctrl Pts',(96.1022933105377,-1.12196706002121,-3.47631326501021));
#26238=CARTESIAN_POINT('Ctrl Pts',(96.0988069783108,-1.12084807532427,-3.47656381759944));
#26239=CARTESIAN_POINT('Ctrl Pts',(96.0924336865831,-1.11876964964784,-3.47702081619737));
#26240=CARTESIAN_POINT('Ctrl Pts',(96.0895452148008,-1.117815278963,-3.47722753810698));
#26241=CARTESIAN_POINT('Ctrl Pts',(96.083032130833,-1.11563528565298,-3.47769278803118));
#26242=CARTESIAN_POINT('Ctrl Pts',(96.0794097718269,-1.11440318551529,-3.47795093777042));
#26243=CARTESIAN_POINT('Ctrl Pts',(96.0700619978902,-1.11117274847258,-3.47861569915611));
#26244=CARTESIAN_POINT('Ctrl Pts',(96.0643458118303,-1.10914777700991,-3.47902082631766));
#26245=CARTESIAN_POINT('Ctrl Pts',(96.0260545216806,-1.09524921430965,-3.48172702739036));
#26246=CARTESIAN_POINT('Ctrl Pts',(95.9939983918163,-1.08198507025018,-3.4839554384391));
#26247=CARTESIAN_POINT('Ctrl Pts',(95.9369542069627,-1.05537379973302,-3.48793273566414));
#26248=CARTESIAN_POINT('Ctrl Pts',(95.9117747074287,-1.04250452690599,-3.48969277121955));
#26249=CARTESIAN_POINT('Ctrl Pts',(95.8450410465118,-1.00530856258729,-3.49442958033675));
#26250=CARTESIAN_POINT('Ctrl Pts',(95.8044769525897,-0.979321316211375,
-3.49738935153617));
#26251=CARTESIAN_POINT('Ctrl Pts',(95.7227357275263,-0.919591048871131,
-3.50372128862714));
#26252=CARTESIAN_POINT('Ctrl Pts',(95.6820281079373,-0.885395849201364,
-3.5070980240436));
#26253=CARTESIAN_POINT('Ctrl Pts',(95.6359725484629,-0.841069596787787,
-3.51129927786758));
#26254=CARTESIAN_POINT('Ctrl Pts',(95.6282795382827,-0.833458438344985,
-3.51201487009788));
#26255=CARTESIAN_POINT('Ctrl Pts',(95.6163313781962,-0.821307042810172,
-3.51314902557432));
#26256=CARTESIAN_POINT('Ctrl Pts',(95.6120053329248,-0.816837121386389,
-3.51356450698912));
#26257=CARTESIAN_POINT('Ctrl Pts',(95.603970740741,-0.808402618418435,-3.51434543318382));
#26258=CARTESIAN_POINT('Ctrl Pts',(95.6002537870404,-0.804446243356598,
-3.5147105052207));
#26259=CARTESIAN_POINT('Ctrl Pts',(95.5919913610126,-0.79552886101755,-3.51553068990995));
#26260=CARTESIAN_POINT('Ctrl Pts',(95.587460814149,-0.790554346041938,-3.51598641207894));
#26261=CARTESIAN_POINT('Ctrl Pts',(95.5760368381114,-0.777792921079663,
-3.51715109092701));
#26262=CARTESIAN_POINT('Ctrl Pts',(95.5692035893285,-0.769953160572135,
-3.51786248522407));
#26263=CARTESIAN_POINT('Ctrl Pts',(95.5139475611787,-0.704836813987481,
-3.52373941571972));
#26264=CARTESIAN_POINT('Ctrl Pts',(95.4710025016443,-0.64315548341963,-3.52912368160108));
#26265=CARTESIAN_POINT('Ctrl Pts',(95.4063689084888,-0.528360586635435,
-3.53875927167759));
#26266=CARTESIAN_POINT('Ctrl Pts',(95.3821320477432,-0.476949636307013,
-3.5429510902622));
#26267=CARTESIAN_POINT('Ctrl Pts',(95.3539815457502,-0.403996798857289,
-3.54860495379084));
#26268=CARTESIAN_POINT('Ctrl Pts',(95.3468131063683,-0.383794724334684,
-3.55014046823892));
#26269=CARTESIAN_POINT('Ctrl Pts',(95.3360414552827,-0.350588771039507,
-3.55260440821723));
#26270=CARTESIAN_POINT('Ctrl Pts',(95.3321034046053,-0.337699300320329,
-3.55354638854198));
#26271=CARTESIAN_POINT('Ctrl Pts',(95.3270748461233,-0.320169208460801,
-3.55480552949018));
#26272=CARTESIAN_POINT('Ctrl Pts',(95.3257901546734,-0.315585993521177,
-3.55513271309447));
#26273=CARTESIAN_POINT('Ctrl Pts',(95.3236924921297,-0.307924022149816,
-3.55567617806474));
#26274=CARTESIAN_POINT('Ctrl Pts',(95.3228641695256,-0.304849574181654,
-3.55589331153192));
#26275=CARTESIAN_POINT('Ctrl Pts',(95.3213188598415,-0.299019899975307,
-3.55630321057245));
#26276=CARTESIAN_POINT('Ctrl Pts',(95.3205993795728,-0.29626537778691,-3.55649612091172));
#26277=CARTESIAN_POINT('Ctrl Pts',(95.3189184526351,-0.289733192291764,
-3.55695183998417));
#26278=CARTESIAN_POINT('Ctrl Pts',(95.3179657510791,-0.285953281871582,
-3.55721415769265));
#26279=CARTESIAN_POINT('Ctrl Pts',(95.3146828833548,-0.272649917649177,
-3.55813273414725));
#26280=CARTESIAN_POINT('Ctrl Pts',(95.3124528061022,-0.263101849663352,
-3.55878365847946));
#26281=CARTESIAN_POINT('Ctrl Pts',(95.2951838363263,-0.184760141228891,
-3.56406467365795));
#26282=CARTESIAN_POINT('Ctrl Pts',(95.2862212028043,-0.114762692647277,
-3.56841258552827));
#26283=CARTESIAN_POINT('Ctrl Pts',(95.2813306304502,0.0149428872917502,
-3.57644150355668));
#26284=CARTESIAN_POINT('Ctrl Pts',(95.2835818817306,0.0743417140062381,
-3.58010846610203));
#26285=CARTESIAN_POINT('Ctrl Pts',(95.2927138946204,0.154498224522783,-3.58524970427908));
#26286=CARTESIAN_POINT('Ctrl Pts',(95.29570180392,0.175610524798074,-3.58662166019366));
#26287=CARTESIAN_POINT('Ctrl Pts',(95.3018936552606,0.212177330451747,-3.58903737412449));
#26288=CARTESIAN_POINT('Ctrl Pts',(95.3048383146312,0.22767037617934,-3.59007333527359));
#26289=CARTESIAN_POINT('Ctrl Pts',(95.3095805711071,0.250150591116389,-3.59159687691451));
#26290=CARTESIAN_POINT('Ctrl Pts',(95.3111327728463,0.257188188268535,-3.59207676071437));
#26291=CARTESIAN_POINT('Ctrl Pts',(95.3139792477609,0.269553265249039,-3.59292528637033));
#26292=CARTESIAN_POINT('Ctrl Pts',(95.3152463260638,0.274886832075314,-3.59329305823462));
#26293=CARTESIAN_POINT('Ctrl Pts',(95.3179658266052,0.285988880647027,-3.59406237518671));
#26294=CARTESIAN_POINT('Ctrl Pts',(95.3194248049891,0.29175558046656,-3.59446411949715));
#26295=CARTESIAN_POINT('Ctrl Pts',(95.3233450973738,0.306771444794223,-3.59551594036567));
#26296=CARTESIAN_POINT('Ctrl Pts',(95.3258755418078,0.316001938273036,-3.59616820373848));
#26297=CARTESIAN_POINT('Ctrl Pts',(95.3370214427277,0.354798778111042,-3.59893449446566));
#26298=CARTESIAN_POINT('Ctrl Pts',(95.3466816220361,0.384049727401228,-3.60108156331856));
#26299=CARTESIAN_POINT('Ctrl Pts',(95.3866479761879,0.490817801548664,-3.60915376741557));
#26300=CARTESIAN_POINT('Ctrl Pts',(95.4239942613389,0.565430217690965,-3.61528688016901));
#26301=CARTESIAN_POINT('Ctrl Pts',(95.4970510205316,0.679428746232457,-3.62519851346871));
#26302=CARTESIAN_POINT('Ctrl Pts',(95.5281152794503,0.721468092900924,-3.62898630661707));
#26303=CARTESIAN_POINT('Ctrl Pts',(95.5663688436828,0.766620524406078,-3.63310231939359));
#26304=CARTESIAN_POINT('Ctrl Pts',(95.5709141479166,0.771890146059535,-3.63358343452079));
#26305=CARTESIAN_POINT('Ctrl Pts',(95.5779221076076,0.779870733286376,-3.63431280417285));
#26306=CARTESIAN_POINT('Ctrl Pts',(95.5803510473422,0.782610903504199,-3.63456337241033));
#26307=CARTESIAN_POINT('Ctrl Pts',(95.5848212635766,0.787606774359508,-3.63502038600803));
#26308=CARTESIAN_POINT('Ctrl Pts',(95.5868585072208,0.789865903405021,-3.63522710739106));
#26309=CARTESIAN_POINT('Ctrl Pts',(95.591477679009,0.794948435498007,-3.63569233929621));
#26310=CARTESIAN_POINT('Ctrl Pts',(95.5940646260103,0.797767168194389,-3.635950471679));
#26311=CARTESIAN_POINT('Ctrl Pts',(95.6007867201475,0.805020283055485,-3.63661515804458));
#26312=CARTESIAN_POINT('Ctrl Pts',(95.6049425181058,0.809435494859631,-3.63702022809975));
#26313=CARTESIAN_POINT('Ctrl Pts',(95.6330751039406,0.838865444032705,-3.63972494587747));
#26314=CARTESIAN_POINT('Ctrl Pts',(95.6581141449915,0.862846268399949,-3.64195202212529));
#26315=CARTESIAN_POINT('Ctrl Pts',(95.7053846884277,0.904278720673471,-3.64592386524868));
#26316=CARTESIAN_POINT('Ctrl Pts',(95.727254140592,0.922100285014337,-3.64767986637031));
#26317=CARTESIAN_POINT('Ctrl Pts',(95.7879764152464,0.968055663958696,-3.65240143967931));
#26318=CARTESIAN_POINT('Ctrl Pts',(95.8279404400586,0.994628839711344,-3.65535005607151));
#26319=CARTESIAN_POINT('Ctrl Pts',(95.8866360330971,1.02868537170764,-3.65959362283606));
#26320=CARTESIAN_POINT('Ctrl Pts',(95.9041048308538,1.03823730619562,-3.66084605093489));
#26321=CARTESIAN_POINT('Ctrl Pts',(95.9218017102038,1.04733936217842,-3.66210953954391));
#26322=CARTESIAN_POINT('Origin',(96.460480949577,-7.19464945638997E-16,
0.924367114736168));
#26323=CARTESIAN_POINT('',(95.9218016729659,1.04733934302581,-4.26051510683823));
#26324=CARTESIAN_POINT('',(95.9218017335164,1.04733937416884,-4.16230107423304));
#26325=CARTESIAN_POINT('',(95.9218016730721,1.04733934308042,0.924367114736168));
#26326=CARTESIAN_POINT('',(97.6382304695238,-0.00104852062301618,-3.92438110998958));
#26327=CARTESIAN_POINT('Ctrl Pts',(95.9218016729659,1.04733934302581,-4.26051510683823));
#26328=CARTESIAN_POINT('Ctrl Pts',(95.9188215355377,1.04580656543591,-4.26028177707212));
#26329=CARTESIAN_POINT('Ctrl Pts',(95.9158478598941,1.04426102683307,-4.26004910401954));
#26330=CARTESIAN_POINT('Ctrl Pts',(95.9080700984155,1.04017634993692,-4.25944101180714));
#26331=CARTESIAN_POINT('Ctrl Pts',(95.9032768919896,1.037616609602,-4.25906673765364));
#26332=CARTESIAN_POINT('Ctrl Pts',(95.8955739714834,1.03343420948893,-4.25846623425049));
#26333=CARTESIAN_POINT('Ctrl Pts',(95.8926531955007,1.03183225460391,-4.25823876447539));
#26334=CARTESIAN_POINT('Ctrl Pts',(95.8870124124072,1.02870725518024,-4.25779995986589));
#26335=CARTESIAN_POINT('Ctrl Pts',(95.8842916159851,1.02718578265178,-4.2575885377243));
#26336=CARTESIAN_POINT('Ctrl Pts',(95.8777283936761,1.02348133845189,-4.25707902852195));
#26337=CARTESIAN_POINT('Ctrl Pts',(95.8738921009329,1.02128747949717,-4.25678162146082));
#26338=CARTESIAN_POINT('Ctrl Pts',(95.8604422314703,1.01349512083887,-4.25574003595753));
#26339=CARTESIAN_POINT('Ctrl Pts',(95.8508953607436,1.00778184901058,-4.25500271280772));
#26340=CARTESIAN_POINT('Ctrl Pts',(95.8274118415054,0.993272424760727,-4.25319035488317));
#26341=CARTESIAN_POINT('Ctrl Pts',(95.8135758092324,0.984317225977614,-4.25212371861783));
#26342=CARTESIAN_POINT('Ctrl Pts',(95.7544233807811,0.944245299800212,-4.24754799908496));
#26343=CARTESIAN_POINT('Ctrl Pts',(95.7111257036779,0.910265957092341,-4.24415579942139));
#26344=CARTESIAN_POINT('Ctrl Pts',(95.6121084665285,0.820688116726456,-4.23589674640043));
#26345=CARTESIAN_POINT('Ctrl Pts',(95.5592843367647,0.762304109621516,-4.23103137637637));
#26346=CARTESIAN_POINT('Ctrl Pts',(95.503472015115,0.686635918194949,-4.22490415859336));
#26347=CARTESIAN_POINT('Ctrl Pts',(95.4945248122245,0.673990867318193,-4.22388625902733));
#26348=CARTESIAN_POINT('Ctrl Pts',(95.4818557318674,0.655315085264326,-4.2223894992221));
#26349=CARTESIAN_POINT('Ctrl Pts',(95.4779345315283,0.649421057891322,-4.22191806447771));
#26350=CARTESIAN_POINT('Ctrl Pts',(95.4710717917935,0.638901110122984,-4.22107808566589));
#26351=CARTESIAN_POINT('Ctrl Pts',(95.4681089404117,0.634289290242098,-4.22071034006781));
#26352=CARTESIAN_POINT('Ctrl Pts',(95.4619963827024,0.624627134709062,-4.2199408091851));
#26353=CARTESIAN_POINT('Ctrl Pts',(95.4588525578356,0.619573280829297,-4.21953882284913));
#26354=CARTESIAN_POINT('Ctrl Pts',(95.4507459676092,0.606318571260493,-4.21848576426071));
#26355=CARTESIAN_POINT('Ctrl Pts',(95.445844860502,0.598080714446914,-4.21783249599246));
#26356=CARTESIAN_POINT('Ctrl Pts',(95.4238603149811,0.56008064903702,-4.21482384246334));
#26357=CARTESIAN_POINT('Ctrl Pts',(95.4079837456875,0.529643177178622,-4.21242654021555));
#26358=CARTESIAN_POINT('Ctrl Pts',(95.3651696292797,0.438011884448065,-4.20524130982053));
#26359=CARTESIAN_POINT('Ctrl Pts',(95.3420871710673,0.375173065989842,-4.20034631197919));
#26360=CARTESIAN_POINT('Ctrl Pts',(95.3086347324428,0.252869407464614,-4.19104137635901));
#26361=CARTESIAN_POINT('Ctrl Pts',(95.2972514231438,0.193884379330255,-4.18664885652213));
#26362=CARTESIAN_POINT('Ctrl Pts',(95.2892665473949,0.124308871235898,-4.18173764880226));
#26363=CARTESIAN_POINT('Ctrl Pts',(95.2882493267785,0.114319335857526,-4.18103904539758));
#26364=CARTESIAN_POINT('Ctrl Pts',(95.2870107407519,0.100390610904378,-4.18007514959461));
#26365=CARTESIAN_POINT('Ctrl Pts',(95.2866812539225,0.0964618129432036,
-4.17980439568779));
#26366=CARTESIAN_POINT('Ctrl Pts',(95.2861469340296,0.0896819492625977,
-4.17933918684036));
#26367=CARTESIAN_POINT('Ctrl Pts',(95.2859327425362,0.0868316870583113,
-4.17914422981957));
#26368=CARTESIAN_POINT('Ctrl Pts',(95.2855027979959,0.0808174646131285,
-4.17873420021916));
#26369=CARTESIAN_POINT('Ctrl Pts',(95.2852894438399,0.0776533615249369,
-4.17851926750525));
#26370=CARTESIAN_POINT('Ctrl Pts',(95.2847917942317,0.0698006836629429,
-4.17798771022529));
#26371=CARTESIAN_POINT('Ctrl Pts',(95.2845227583069,0.0651111333339425,
-4.17767191548024));
#26372=CARTESIAN_POINT('Ctrl Pts',(95.2836141369934,0.0474229567656407,
-4.17648657481495));
#26373=CARTESIAN_POINT('Ctrl Pts',(95.2831619322355,0.0344150738771813,
-4.17562664249958));
#26374=CARTESIAN_POINT('Ctrl Pts',(95.2825544460545,0.000990245263173205,
-4.1734410560954));
#26375=CARTESIAN_POINT('Ctrl Pts',(95.2827142263405,-0.019428654245409,
-4.17212893859638));
#26376=CARTESIAN_POINT('Ctrl Pts',(95.2853629410118,-0.0976964847208325,
-4.16715319170785));
#26377=CARTESIAN_POINT('Ctrl Pts',(95.2915850881283,-0.15533901963567,-4.16359823879228));
#26378=CARTESIAN_POINT('Ctrl Pts',(95.3156314500694,-0.286557312319542,
-4.1553380793406));
#26379=CARTESIAN_POINT('Ctrl Pts',(95.3363480036909,-0.359330461262717,
-4.15062288797782));
#26380=CARTESIAN_POINT('Ctrl Pts',(95.367673455852,-0.439288951056962,-4.14498682695457));
#26381=CARTESIAN_POINT('Ctrl Pts',(95.3715909734151,-0.448911583144755,
-4.14430099649661));
#26382=CARTESIAN_POINT('Ctrl Pts',(95.3782533655663,-0.464675965387144,
-4.1431642558651));
#26383=CARTESIAN_POINT('Ctrl Pts',(95.3809245207711,-0.47084839415314,-4.14271580523754));
#26384=CARTESIAN_POINT('Ctrl Pts',(95.3858470347871,-0.481961080404928,
-4.14190215135114));
#26385=CARTESIAN_POINT('Ctrl Pts',(95.3880799799546,-0.486909326783869,
-4.14153757771319));
#26386=CARTESIAN_POINT('Ctrl Pts',(95.3929460450998,-0.497496756433642,
-4.14075254539853));
#26387=CARTESIAN_POINT('Ctrl Pts',(95.3955898041255,-0.503130838562036,
-4.14033173339041));
#26388=CARTESIAN_POINT('Ctrl Pts',(95.4029579410932,-0.518514729960688,
-4.13917414239387));
#26389=CARTESIAN_POINT('Ctrl Pts',(95.4077722944733,-0.528220515062181,
-4.13843430395658));
#26390=CARTESIAN_POINT('Ctrl Pts',(95.4370906488992,-0.585333399808519,
-4.13402279789795));
#26391=CARTESIAN_POINT('Ctrl Pts',(95.4646564533333,-0.631090322572359,
-4.13024508643766));
#26392=CARTESIAN_POINT('Ctrl Pts',(95.5226971689602,-0.714111703771539,
-4.12292352043515));
#26393=CARTESIAN_POINT('Ctrl Pts',(95.5525419545015,-0.751691620923437,
-4.11940223740577));
#26394=CARTESIAN_POINT('Ctrl Pts',(95.6034423108333,-0.808316094063832,
-4.11381600843628));
#26395=CARTESIAN_POINT('Ctrl Pts',(95.6230400956137,-0.82860306926117,-4.11175087348832));
#26396=CARTESIAN_POINT('Ctrl Pts',(95.6683026593464,-0.872209483707722,
-4.10719394997566));
#26397=CARTESIAN_POINT('Ctrl Pts',(95.6943092548852,-0.895140914568747,
-4.10471464788955));
#26398=CARTESIAN_POINT('Ctrl Pts',(95.7260124771976,-0.920699675540471,
-4.10188418026188));
#26399=CARTESIAN_POINT('Ctrl Pts',(95.7307624967136,-0.9244689355949,-4.10146492921322));
#26400=CARTESIAN_POINT('Ctrl Pts',(95.7385569562706,-0.930556526798279,
-4.10078508394169));
#26401=CARTESIAN_POINT('Ctrl Pts',(95.7415838861753,-0.932896947658568,
-4.10052303971565));
#26402=CARTESIAN_POINT('Ctrl Pts',(95.7470380538224,-0.937071796988144,
-4.10005446953611));
#26403=CARTESIAN_POINT('Ctrl Pts',(95.7494610351639,-0.938911604018742,
-4.09984757977509));
#26404=CARTESIAN_POINT('Ctrl Pts',(95.7548163014806,-0.942945320473388,
-4.09939310367173));
#26405=CARTESIAN_POINT('Ctrl Pts',(95.7577517033606,-0.945134953538001,
-4.09914580903525));
#26406=CARTESIAN_POINT('Ctrl Pts',(95.7662952303945,-0.951446102682716,
-4.09843115797298));
#26407=CARTESIAN_POINT('Ctrl Pts',(95.7719298517088,-0.955531731775664,
-4.09796616436047));
#26408=CARTESIAN_POINT('Ctrl Pts',(95.8201568581022,-0.989852699961186,
-4.0940366646929));
#26409=CARTESIAN_POINT('Ctrl Pts',(95.8646867980555,-1.0172777919514,-4.09073887976694));
#26410=CARTESIAN_POINT('Ctrl Pts',(95.9845471750855,-1.08051680214726,-4.08229739415115));
#26411=CARTESIAN_POINT('Ctrl Pts',(96.0621077855663,-1.11145307757198,-4.07722999925039));
#26412=CARTESIAN_POINT('Ctrl Pts',(96.1718551393677,-1.14224937672569,-4.06995889791469));
#26413=CARTESIAN_POINT('Ctrl Pts',(96.201739316398,-1.14938723252431,-4.06797165734062));
#26414=CARTESIAN_POINT('Ctrl Pts',(96.2412475420255,-1.15720491997214,-4.06531739560646));
#26415=CARTESIAN_POINT('Ctrl Pts',(96.2506506911962,-1.15894683553549,-4.064683725411));
#26416=CARTESIAN_POINT('Ctrl Pts',(96.2659340770745,-1.16158596063495,-4.0636501710267));
#26417=CARTESIAN_POINT('Ctrl Pts',(96.271801854891,-1.16255349407184,-4.0632524962546));
#26418=CARTESIAN_POINT('Ctrl Pts',(96.2830932902497,-1.16432759370111,-4.06248547878851));
#26419=CARTESIAN_POINT('Ctrl Pts',(96.2885157586713,-1.16514080630106,-4.06211635458374));
#26420=CARTESIAN_POINT('Ctrl Pts',(96.3010828405792,-1.16693586523239,-4.06125897403396));
#26421=CARTESIAN_POINT('Ctrl Pts',(96.308231125564,-1.16789000244121,-4.06076986800623));
#26422=CARTESIAN_POINT('Ctrl Pts',(96.3310620567884,-1.17072425788644,-4.05920294031248));
#26423=CARTESIAN_POINT('Ctrl Pts',(96.3467733872825,-1.17235450532021,-4.05811745166285));
#26424=CARTESIAN_POINT('Ctrl Pts',(96.3838021849195,-1.1754453857943,-4.05554104002007));
#26425=CARTESIAN_POINT('Ctrl Pts',(96.4051354426366,-1.17664279392305,-4.05404259029126));
#26426=CARTESIAN_POINT('Ctrl Pts',(96.4860425467768,-1.17897893349908,-4.04830591819803));
#26427=CARTESIAN_POINT('Ctrl Pts',(96.5456351264127,-1.17617687917045,-4.04396450259567));
#26428=CARTESIAN_POINT('Ctrl Pts',(96.6743251813363,-1.16029292362267,-4.03445186984287));
#26429=CARTESIAN_POINT('Ctrl Pts',(96.7429975345149,-1.14551088136044,-4.02928668292465));
#26430=CARTESIAN_POINT('Ctrl Pts',(96.8193217277633,-1.12179526804257,-4.02368470184939));
#26431=CARTESIAN_POINT('Ctrl Pts',(96.8286549516762,-1.11876684224169,-4.02300228900284));
#26432=CARTESIAN_POINT('Ctrl Pts',(96.8416479119142,-1.11437069799516,-4.02205699039771));
#26433=CARTESIAN_POINT('Ctrl Pts',(96.8453400355421,-1.11310097958984,-4.02178890610049));
#26434=CARTESIAN_POINT('Ctrl Pts',(96.8517149674126,-1.11087313422676,-4.02132703220032));
#26435=CARTESIAN_POINT('Ctrl Pts',(96.8544007110296,-1.10992360054031,-4.02113275675411));
#26436=CARTESIAN_POINT('Ctrl Pts',(96.8600796601408,-1.1078926217854,-4.02072266368408));
#26437=CARTESIAN_POINT('Ctrl Pts',(96.8630719802415,-1.10680877002707,-4.02050699389728));
#26438=CARTESIAN_POINT('Ctrl Pts',(96.8702961370049,-1.10415892641754,-4.01998723567396));
#26439=CARTESIAN_POINT('Ctrl Pts',(96.8745234882347,-1.10258070020744,-4.01968385423754));
#26440=CARTESIAN_POINT('Ctrl Pts',(96.8902420487293,-1.09660923066956,-4.01855827583403));
#26441=CARTESIAN_POINT('Ctrl Pts',(96.9016737482242,-1.0920601407146,-4.01774463809231));
#26442=CARTESIAN_POINT('Ctrl Pts',(96.9306303894835,-1.08000828382375,-4.01569128438336));
#26443=CARTESIAN_POINT('Ctrl Pts',(96.9480487847208,-1.07225746806751,-4.01446331133274));
#26444=CARTESIAN_POINT('Ctrl Pts',(97.0191164037625,-1.03854375300482,-4.00945272827282));
#26445=CARTESIAN_POINT('Ctrl Pts',(97.0709476135287,-1.00894900412825,-4.00579388535072));
#26446=CARTESIAN_POINT('Ctrl Pts',(97.1832585635141,-0.932985160593492,
-3.99739924829797));
#26447=CARTESIAN_POINT('Ctrl Pts',(97.2419224049484,-0.884429652000915,
-3.99265566083505));
#26448=CARTESIAN_POINT('Ctrl Pts',(97.3028258754823,-0.82319989374108,-3.98698773984564));
#26449=CARTESIAN_POINT('Ctrl Pts',(97.3100558781428,-0.815736151464084,
-3.98630178955589));
#26450=CARTESIAN_POINT('Ctrl Pts',(97.321801527665,-0.803285233095336,-3.9851648912569));
#26451=CARTESIAN_POINT('Ctrl Pts',(97.3263749828294,-0.798353195004882,
-3.98471640399275));
#26452=CARTESIAN_POINT('Ctrl Pts',(97.3345629269142,-0.789370148393381,
-3.98390271096816));
#26453=CARTESIAN_POINT('Ctrl Pts',(97.3381921531583,-0.785332780229276,
-3.98353813510746));
#26454=CARTESIAN_POINT('Ctrl Pts',(97.3459214540308,-0.776613741159297,
-3.98275312846434));
#26455=CARTESIAN_POINT('Ctrl Pts',(97.3500125786478,-0.771924392801422,
-3.98233234456633));
#26456=CARTESIAN_POINT('Ctrl Pts',(97.3605333015955,-0.759670576410502,
-3.98123629301274));
#26457=CARTESIAN_POINT('Ctrl Pts',(97.3669046470154,-0.752056973437907,
-3.98055870029925));
#26458=CARTESIAN_POINT('Ctrl Pts',(97.4010022670002,-0.710248358526442,
-3.97685525506667));
#26459=CARTESIAN_POINT('Ctrl Pts',(97.4268876166717,-0.674603870452686,
-3.97375827903032));
#26460=CARTESIAN_POINT('Ctrl Pts',(97.4820555408387,-0.588924269737015,
-3.96644873121523));
#26461=CARTESIAN_POINT('Ctrl Pts',(97.5097624452733,-0.538009126532806,
-3.96219973802592));
#26462=CARTESIAN_POINT('Ctrl Pts',(97.5452613737911,-0.459506128264437,
-3.9558783586982));
#26463=CARTESIAN_POINT('Ctrl Pts',(97.5559797741646,-0.433332285159325,
-3.95380738604897));
#26464=CARTESIAN_POINT('Ctrl Pts',(97.5777892088457,-0.374076231851213,
-3.94922854590822));
#26465=CARTESIAN_POINT('Ctrl Pts',(97.5883746661407,-0.340832863835478,
-3.94673338499372));
#26466=CARTESIAN_POINT('Ctrl Pts',(97.5990537983305,-0.301303505351245,
-3.94388728888438));
#26467=CARTESIAN_POINT('Ctrl Pts',(97.6005921574859,-0.295429131504577,
-3.94346743145868));
#26468=CARTESIAN_POINT('Ctrl Pts',(97.6030263232253,-0.285831752565939,
-3.94278680345621));
#26469=CARTESIAN_POINT('Ctrl Pts',(97.6039495065895,-0.282115901335005,
-3.94252457748723));
#26470=CARTESIAN_POINT('Ctrl Pts',(97.6055737362804,-0.275439337649384,
-3.9420558172051));
#26471=CARTESIAN_POINT('Ctrl Pts',(97.6062814441235,-0.272480359337039,
-3.94184891771273));
#26472=CARTESIAN_POINT('Ctrl Pts',(97.6078152215821,-0.265955870366845,
-3.94139458012618));
#26473=CARTESIAN_POINT('Ctrl Pts',(97.6086361425133,-0.262389234808589,
-3.94114743254129));
#26474=CARTESIAN_POINT('Ctrl Pts',(97.610305694187,-0.254977688742141,-3.94063626921036));
#26475=CARTESIAN_POINT('Ctrl Pts',(97.6111516979197,-0.251132226233793,
-3.9403723982116));
#26476=CARTESIAN_POINT('Ctrl Pts',(97.6133021511285,-0.241118411474756,
-3.93968858455184));
#26477=CARTESIAN_POINT('Ctrl Pts',(97.6145764032244,-0.234943608189631,
-3.93927019642514));
#26478=CARTESIAN_POINT('Ctrl Pts',(97.6306488144902,-0.153771707192968,
-3.93380950112707));
#26479=CARTESIAN_POINT('Ctrl Pts',(97.6381624101106,-0.0775084268869562,
-3.92911084375618));
#26480=CARTESIAN_POINT('Ctrl Pts',(97.6382304828084,-0.00104855774486002,
-3.92438113289323));
#26481=CARTESIAN_POINT('Ctrl Pts',(97.6382304828425,-0.00104851936493903,
-3.92438113051909));
#26482=CARTESIAN_POINT('Ctrl Pts',(97.6383002269576,0.0772915683713354,
-3.91953511170716));
#26483=CARTESIAN_POINT('Ctrl Pts',(97.6305539237946,0.155436028635755,-3.91467389969789));
#26484=CARTESIAN_POINT('Ctrl Pts',(97.6131372675276,0.242029690541228,-3.90890634965245));
#26485=CARTESIAN_POINT('Ctrl Pts',(97.6110418725032,0.251802524473686,-3.90825012618013));
#26486=CARTESIAN_POINT('Ctrl Pts',(97.6073712668865,0.267918573086483,-3.90715853485289));
#26487=CARTESIAN_POINT('Ctrl Pts',(97.6058671594109,0.274277576975191,-3.90672537462082));
#26488=CARTESIAN_POINT('Ctrl Pts',(97.6028218544812,0.28669031982019,-3.90587487533533));
#26489=CARTESIAN_POINT('Ctrl Pts',(97.6012852545469,0.292744970449118,-3.9054576932432));
#26490=CARTESIAN_POINT('Ctrl Pts',(97.5983238954102,0.304036085270877,-3.90467521197181));
#26491=CARTESIAN_POINT('Ctrl Pts',(97.5969109617455,0.30927550223791,-3.90431029913378));
#26492=CARTESIAN_POINT('Ctrl Pts',(97.5936742447718,0.320956122002058,-3.9034926128811));
#26493=CARTESIAN_POINT('Ctrl Pts',(97.5918316618733,0.3273918739262,-3.90303924704889));
#26494=CARTESIAN_POINT('Ctrl Pts',(97.5870188501328,0.343676056174618,-3.90188472558683));
#26495=CARTESIAN_POINT('Ctrl Pts',(97.5839743269869,0.353501757079863,-3.90118120533519));
#26496=CARTESIAN_POINT('Ctrl Pts',(97.5625332826516,0.41962277621498,-3.89639898927226));
#26497=CARTESIAN_POINT('Ctrl Pts',(97.5400445944713,0.474492345754514,-3.89218781070295));
#26498=CARTESIAN_POINT('Ctrl Pts',(97.4910687355275,0.572275608944413,-3.88424865580919));
#26499=CARTESIAN_POINT('Ctrl Pts',(97.4657669042832,0.615638191140721,-3.88055469308813));
#26500=CARTESIAN_POINT('Ctrl Pts',(97.4173021027298,0.687702537750321,-3.87419503402469));
#26501=CARTESIAN_POINT('Ctrl Pts',(97.3954115579605,0.717179626529923,-3.87152354180378));
#26502=CARTESIAN_POINT('Ctrl Pts',(97.3611212399367,0.759109498322487,-3.86766335613339));
#26503=CARTESIAN_POINT('Ctrl Pts',(97.3497633240153,0.772384035688475,-3.86643181847522));
#26504=CARTESIAN_POINT('Ctrl Pts',(97.3338899948569,0.790121393060307,-3.86477858823891));
#26505=CARTESIAN_POINT('Ctrl Pts',(97.3296282548875,0.794806984281414,-3.86434111211018));
#26506=CARTESIAN_POINT('Ctrl Pts',(97.3228819984587,0.802105034608602,-3.86365884752554));
#26507=CARTESIAN_POINT('Ctrl Pts',(97.3204230099361,0.804740771527269,-3.86341226192987));
#26508=CARTESIAN_POINT('Ctrl Pts',(97.3158635732534,0.809583170584965,-3.86295896534749));
#26509=CARTESIAN_POINT('Ctrl Pts',(97.3137666658123,0.811792972271169,-3.86275200975359));
#26510=CARTESIAN_POINT('Ctrl Pts',(97.3089673909662,0.816811491014688,-3.86228176094614));
#26511=CARTESIAN_POINT('Ctrl Pts',(97.3062596375748,0.819614949285999,-3.8620188827926));
#26512=CARTESIAN_POINT('Ctrl Pts',(97.299137653688,0.826915778886499,-3.86133363092183));
#26513=CARTESIAN_POINT('Ctrl Pts',(97.2947010883006,0.831391326112192,-3.86091289739467));
#26514=CARTESIAN_POINT('Ctrl Pts',(97.2609660255036,0.864880855351779,-3.85775756661836));
#26515=CARTESIAN_POINT('Ctrl Pts',(97.2301944185184,0.892377287020628,-3.85512602537788));
#26516=CARTESIAN_POINT('Ctrl Pts',(97.1313703769921,0.971758858477707,-3.84716879529666));
#26517=CARTESIAN_POINT('Ctrl Pts',(97.0590670773619,1.01789150203666,-3.84199035874457));
#26518=CARTESIAN_POINT('Ctrl Pts',(96.9486723009609,1.07246453983375,-3.83419594380122));
#26519=CARTESIAN_POINT('Ctrl Pts',(96.9141634461721,1.08751217833587,-3.83177690051543));
#26520=CARTESIAN_POINT('Ctrl Pts',(96.8694406830457,1.10451414676563,-3.82863012445964));
#26521=CARTESIAN_POINT('Ctrl Pts',(96.8598386509001,1.10802210250701,-3.8279539085823));
#26522=CARTESIAN_POINT('Ctrl Pts',(96.8443193132146,1.11346392284733,-3.82685941839377));
#26523=CARTESIAN_POINT('Ctrl Pts',(96.8384300791682,1.11547669174042,-3.82644372964281));
#26524=CARTESIAN_POINT('Ctrl Pts',(96.8273745084115,1.11915756270456,-3.82566258312755));
#26525=CARTESIAN_POINT('Ctrl Pts',(96.8222120338198,1.12083681001103,-3.82529749956686));
#26526=CARTESIAN_POINT('Ctrl Pts',(96.8106284182255,1.12451635991016,-3.82447751094567));
#26527=CARTESIAN_POINT('Ctrl Pts',(96.8042014244256,1.12649745913283,-3.82402199805452));
#26528=CARTESIAN_POINT('Ctrl Pts',(96.7878043896812,1.13139840544524,-3.82285828461382));
#26529=CARTESIAN_POINT('Ctrl Pts',(96.7778122096802,1.13424152880405,-3.82214765371291));
#26530=CARTESIAN_POINT('Ctrl Pts',(96.6949406321733,1.15664061680823,-3.81624030382034));
#26531=CARTESIAN_POINT('Ctrl Pts',(96.6203874049229,1.16927965196357,-3.81082198307269));
#26532=CARTESIAN_POINT('Ctrl Pts',(96.4875002722337,1.17885787862336,-3.80107581833461));
#26533=CARTESIAN_POINT('Ctrl Pts',(96.4296211536499,1.17876370206417,-3.79680681915103));
#26534=CARTESIAN_POINT('Ctrl Pts',(96.3515331266551,1.17287934927007,-3.79115184810892));
#26535=CARTESIAN_POINT('Ctrl Pts',(96.3311266675664,1.17080449503297,-3.78968436821272));
#26536=CARTESIAN_POINT('Ctrl Pts',(96.2978331152282,1.16653813278344,-3.78731711268388));
#26537=CARTESIAN_POINT('Ctrl Pts',(96.2849103727789,1.16466327375454,-3.78640498723211));
#26538=CARTESIAN_POINT('Ctrl Pts',(96.2673784809264,1.16182124995771,-3.78517901688589));
#26539=CARTESIAN_POINT('Ctrl Pts',(96.2627405802144,1.16104088147806,-3.78485579640214));
#26540=CARTESIAN_POINT('Ctrl Pts',(96.2549821511836,1.15968761766732,-3.78431708253762));
#26541=CARTESIAN_POINT('Ctrl Pts',(96.2518590779142,1.1591298642319,-3.78410076761551));
#26542=CARTESIAN_POINT('Ctrl Pts',(96.2459276071361,1.1580458061945,-3.78369100558806));
#26543=CARTESIAN_POINT('Ctrl Pts',(96.243118819702,1.15752189220615,-3.78349742270611));
#26544=CARTESIAN_POINT('Ctrl Pts',(96.2364430581388,1.15625152795087,-3.78303835076119));
#26545=CARTESIAN_POINT('Ctrl Pts',(96.2325778359534,1.15549588687873,-3.78277337005794));
#26546=CARTESIAN_POINT('Ctrl Pts',(96.2188972106962,1.15275004244836,-3.78183816293063));
#26547=CARTESIAN_POINT('Ctrl Pts',(96.2091031503131,1.15065397996251,-3.7811735180152));
#26548=CARTESIAN_POINT('Ctrl Pts',(96.1380417633,1.1344952006867,-3.77637880967278));
#26549=CARTESIAN_POINT('Ctrl Pts',(96.0779526476298,1.11567045718616,-3.77247141370119));
#26550=CARTESIAN_POINT('Ctrl Pts',(95.9863515882459,1.0786962632783,-3.76635554633995));
#26551=CARTESIAN_POINT('Ctrl Pts',(95.9537030471759,1.06374721732549,-3.76414223687867));
#26552=CARTESIAN_POINT('Ctrl Pts',(95.921801595944,1.04733930341107,-3.76190742309816));
#26553=CARTESIAN_POINT('Ctrl Pts',(95.9218017102038,1.04733936217842,-3.66210953954391));
#26554=CARTESIAN_POINT('Ctrl Pts',(95.9515268869871,1.06262794599194,-3.66423180197923));
#26555=CARTESIAN_POINT('Ctrl Pts',(95.9818955288735,1.07664727186504,-3.66638568234305));
#26556=CARTESIAN_POINT('Ctrl Pts',(96.0228467717177,1.09347553603074,-3.66929554572374));
#26557=CARTESIAN_POINT('Ctrl Pts',(96.0329230079188,1.09745460738624,-3.67001189273349));
#26558=CARTESIAN_POINT('Ctrl Pts',(96.048871483371,1.1034996311513,-3.6711469749985));
#26559=CARTESIAN_POINT('Ctrl Pts',(96.0547078278261,1.10565906127483,-3.67156261982445));
#26560=CARTESIAN_POINT('Ctrl Pts',(96.0656666565797,1.10961533993984,-3.67234369088225));
#26561=CARTESIAN_POINT('Ctrl Pts',(96.070785002189,1.11142322968553,-3.67270874303795));
#26562=CARTESIAN_POINT('Ctrl Pts',(96.0822719393112,1.11539151514891,-3.67352866999955));
#26563=CARTESIAN_POINT('Ctrl Pts',(96.0886468625273,1.11753286125163,-3.67398415260324));
#26564=CARTESIAN_POINT('Ctrl Pts',(96.1049151177559,1.12284278338375,-3.67514780463955));
#26565=CARTESIAN_POINT('Ctrl Pts',(96.1148325027915,1.12593521847783,-3.67585840429814));
#26566=CARTESIAN_POINT('Ctrl Pts',(96.197003849725,1.1503699241136,-3.68175763365032));
#26567=CARTESIAN_POINT('Ctrl Pts',(96.2710987987834,1.16486122859366,-3.68716712787284));
#26568=CARTESIAN_POINT('Ctrl Pts',(96.4040199070875,1.17783656282554,-3.69693638596119));
#26569=CARTESIAN_POINT('Ctrl Pts',(96.4623236931921,1.17918772060614,-3.70123818129027));
#26570=CARTESIAN_POINT('Ctrl Pts',(96.5407701351531,1.17518556088752,-3.7069088198823));
#26571=CARTESIAN_POINT('Ctrl Pts',(96.5610223131808,1.17362642584868,-3.70836162632931));
#26572=CARTESIAN_POINT('Ctrl Pts',(96.5941213928752,1.17021509719897,-3.71070792309368));
#26573=CARTESIAN_POINT('Ctrl Pts',(96.6069954733692,1.16867303846211,-3.71161351018801));
#26574=CARTESIAN_POINT('Ctrl Pts',(96.6244889818733,1.16628402372226,-3.71283217743795));
#26575=CARTESIAN_POINT('Ctrl Pts',(96.6291321218656,1.16562165500001,-3.71315449431352));
#26576=CARTESIAN_POINT('Ctrl Pts',(96.6369063434911,1.16446519441425,-3.71369211061008));
#26577=CARTESIAN_POINT('Ctrl Pts',(96.6400395725906,1.16398617273104,-3.71390822472739));
#26578=CARTESIAN_POINT('Ctrl Pts',(96.6459955072885,1.16305098191484,-3.7143179206363));
#26579=CARTESIAN_POINT('Ctrl Pts',(96.6488185360568,1.16259717512939,-3.71451163617588));
#26580=CARTESIAN_POINT('Ctrl Pts',(96.6555345358518,1.16149246204784,-3.71497141652787));
#26581=CARTESIAN_POINT('Ctrl Pts',(96.6594259737464,1.16083225290393,-3.71523696916608));
#26582=CARTESIAN_POINT('Ctrl Pts',(96.6732313306764,1.15841861855702,-3.71617624146788));
#26583=CARTESIAN_POINT('Ctrl Pts',(96.6831263395424,1.15655759362003,-3.71684431614451));
#26584=CARTESIAN_POINT('Ctrl Pts',(96.7513604548066,1.14281610849804,-3.72142318651043));
#26585=CARTESIAN_POINT('Ctrl Pts',(96.8087568803161,1.12665222691,-3.72513507346931));
#26586=CARTESIAN_POINT('Ctrl Pts',(96.9277443362566,1.08317431244778,-3.73298451711651));
#26587=CARTESIAN_POINT('Ctrl Pts',(96.9887091822793,1.05478718415412,-3.73710555889721));
#26588=CARTESIAN_POINT('Ctrl Pts',(97.0767544313278,1.00423373433936,-3.74355951432544));
#26589=CARTESIAN_POINT('Ctrl Pts',(97.105819040385,0.985807687838174,-3.74577974511669));
#26590=CARTESIAN_POINT('Ctrl Pts',(97.1419026430924,0.960651629002051,-3.74867849749104));
#26591=CARTESIAN_POINT('Ctrl Pts',(97.1497040161767,0.955069961950332,-3.74931408220337));
#26592=CARTESIAN_POINT('Ctrl Pts',(97.1622349803165,0.945870911919544,-3.75034996343363));
#26593=CARTESIAN_POINT('Ctrl Pts',(97.1670069518168,0.942311788970393,-3.75074803134951));
#26594=CARTESIAN_POINT('Ctrl Pts',(97.1761198859155,0.935406869561338,-3.75151526157703));
#26595=CARTESIAN_POINT('Ctrl Pts',(97.1804648885275,0.932066641790059,-3.75188420145349));
#26596=CARTESIAN_POINT('Ctrl Pts',(97.190365185883,0.924345237879084,-3.75273214712997));
#26597=CARTESIAN_POINT('Ctrl Pts',(97.1959045870653,0.919944121586319,-3.75321192730596));
#26598=CARTESIAN_POINT('Ctrl Pts',(97.2134273963945,0.90576264209704,-3.75474698366367));
#26599=CARTESIAN_POINT('Ctrl Pts',(97.225257510117,0.895796343278268,-3.75580960788472));
#26600=CARTESIAN_POINT('Ctrl Pts',(97.2966710054717,0.833188077926024,-3.76239118709433));
#26601=CARTESIAN_POINT('Ctrl Pts',(97.3509833129435,0.774866119990202,-3.76814816727417));
#26602=CARTESIAN_POINT('Ctrl Pts',(97.4270599432811,0.674520055100196,-3.77738369027458));
#26603=CARTESIAN_POINT('Ctrl Pts',(97.4529066846545,0.635880240891937,-3.78080193022208));
#26604=CARTESIAN_POINT('Ctrl Pts',(97.4870930839258,0.577588939991635,-3.78568600736881));
#26605=CARTESIAN_POINT('Ctrl Pts',(97.4972899128815,0.559078473068036,-3.78719921451562));
#26606=CARTESIAN_POINT('Ctrl Pts',(97.5131032635276,0.528449867987034,-3.78963151971322));
#26607=CARTESIAN_POINT('Ctrl Pts',(97.5190212880641,0.516493357386152,-3.79056377237304));
#26608=CARTESIAN_POINT('Ctrl Pts',(97.5267659304711,0.500153858393739,-3.79181211389401));
#26609=CARTESIAN_POINT('Ctrl Pts',(97.5287708202033,0.495857133452275,-3.79213801266752));
#26610=CARTESIAN_POINT('Ctrl Pts',(97.5320770302862,0.488658383488655,-3.79267993169569));
#26611=CARTESIAN_POINT('Ctrl Pts',(97.5333926242884,0.485763023458646,-3.79289679414801));
#26612=CARTESIAN_POINT('Ctrl Pts',(97.5358649758358,0.480262825189689,-3.79330663025232));
#26613=CARTESIAN_POINT('Ctrl Pts',(97.537024029107,0.47765906622593,-3.79349974579894));
#26614=CARTESIAN_POINT('Ctrl Pts',(97.5397510008933,0.471472705207028,-3.79395650784794));
#26615=CARTESIAN_POINT('Ctrl Pts',(97.5413105623929,0.467886422720148,-3.79421965789962));
#26616=CARTESIAN_POINT('Ctrl Pts',(97.5467354837077,0.455239695140926,-3.79514210961642));
#26617=CARTESIAN_POINT('Ctrl Pts',(97.5505051397222,0.44613828955518,-3.7957960258593));
#26618=CARTESIAN_POINT('Ctrl Pts',(97.5798555082221,0.372681527804028,-3.80100264574118));
#26619=CARTESIAN_POINT('Ctrl Pts',(97.5998322490202,0.306222441885801,-3.80528293609165));
#26620=CARTESIAN_POINT('Ctrl Pts',(97.6300381185647,0.160078133085932,-3.81451463964493));
#26621=CARTESIAN_POINT('Ctrl Pts',(97.6382047189824,0.0803358707141346,
-3.81945264061806));
#26622=CARTESIAN_POINT('Ctrl Pts',(97.6382363426027,-0.0162844948558244,
-3.82573338268351));
#26623=CARTESIAN_POINT('Ctrl Pts',(97.637887876712,-0.0329519786022189,
-3.82682672382451));
#26624=CARTESIAN_POINT('Ctrl Pts',(97.6368988735683,-0.0564122383090384,
-3.82838212366944));
#26625=CARTESIAN_POINT('Ctrl Pts',(97.6365528920283,-0.0632159430142647,
-3.82883515389796));
#26626=CARTESIAN_POINT('Ctrl Pts',(97.635846207896,-0.0750821372014775,
-3.82962885086424));
#26627=CARTESIAN_POINT('Ctrl Pts',(97.6355117687516,-0.0801460567420147,
-3.82996870034848));
#26628=CARTESIAN_POINT('Ctrl Pts',(97.6347412397145,-0.0907684961572817,
-3.83068405810339));
#26629=CARTESIAN_POINT('Ctrl Pts',(97.6342983863317,-0.0963263838305222,
-3.83105976722223));
#26630=CARTESIAN_POINT('Ctrl Pts',(97.6331438519652,-0.109622856386331,
-3.83196209773226));
#26631=CARTESIAN_POINT('Ctrl Pts',(97.6323950160105,-0.117357867915084,
-3.83248985639087));
#26632=CARTESIAN_POINT('Ctrl Pts',(97.6295399082135,-0.144088422782283,
-3.83432384392705));
#26633=CARTESIAN_POINT('Ctrl Pts',(97.6270479564917,-0.163038850508583,
-3.83564189020267));
#26634=CARTESIAN_POINT('Ctrl Pts',(97.6198477310537,-0.209093832604273,
-3.83889070061058));
#26635=CARTESIAN_POINT('Ctrl Pts',(97.6146489654909,-0.236109201794215,
-3.84083543160626));
#26636=CARTESIAN_POINT('Ctrl Pts',(97.5851904943787,-0.364740231850199,
-3.85027928674959));
#26637=CARTESIAN_POINT('Ctrl Pts',(97.5484325069005,-0.462995603980884,
-3.8581047594782));
#26638=CARTESIAN_POINT('Ctrl Pts',(97.4892455643655,-0.573746394863369,
-3.86708003621099));
#26639=CARTESIAN_POINT('Ctrl Pts',(97.4787856183896,-0.592112568877566,
-3.86857189979597));
#26640=CARTESIAN_POINT('Ctrl Pts',(97.4648236390865,-0.61516228612518,-3.87043967245905));
#26641=CARTESIAN_POINT('Ctrl Pts',(97.4617740552052,-0.6201136963075,-3.87084061983158));
#26642=CARTESIAN_POINT('Ctrl Pts',(97.456875314224,-0.627937096285412,-3.87147344293429));
#26643=CARTESIAN_POINT('Ctrl Pts',(97.4550501708214,-0.630823899116125,
-3.87170680191852));
#26644=CARTESIAN_POINT('Ctrl Pts',(97.451553757369,-0.636301230139754,-3.87214922306961));
#26645=CARTESIAN_POINT('Ctrl Pts',(97.4498848868775,-0.63889311695495,-3.87235842122598));
#26646=CARTESIAN_POINT('Ctrl Pts',(97.4459108392278,-0.645012208429669,
-3.87285199448922));
#26647=CARTESIAN_POINT('Ctrl Pts',(97.4435968817139,-0.648533639668521,
-3.87313579247093));
#26648=CARTESIAN_POINT('Ctrl Pts',(97.4357999837315,-0.660261500875621,
-3.87408041025011));
#26649=CARTESIAN_POINT('Ctrl Pts',(97.4302326213255,-0.66841168361064,-3.8747359590946));
#26650=CARTESIAN_POINT('Ctrl Pts',(97.4164945853823,-0.687990055566336,
-3.87631103018823));
#26651=CARTESIAN_POINT('Ctrl Pts',(97.4082204708455,-0.699344139352951,
-3.87722472673215));
#26652=CARTESIAN_POINT('Ctrl Pts',(97.3746373162585,-0.743737261580293,
-3.88081002187701));
#26653=CARTESIAN_POINT('Ctrl Pts',(97.3477863046998,-0.775575087314057,
-3.88341080970137));
#26654=CARTESIAN_POINT('Ctrl Pts',(97.2521186001174,-0.877521896547881,
-3.89208627008442));
#26655=CARTESIAN_POINT('Ctrl Pts',(97.1762527327695,-0.940427330348799,
-3.89807945080254));
#26656=CARTESIAN_POINT('Ctrl Pts',(97.081528532809,-1.00079733566589,-3.90541590736069));
#26657=CARTESIAN_POINT('Ctrl Pts',(97.069456530984,-1.00818853447668,-3.90634758187269));
#26658=CARTESIAN_POINT('Ctrl Pts',(97.0513018631366,-1.01885886540171,-3.9077453944503));
#26659=CARTESIAN_POINT('Ctrl Pts',(97.0453185162524,-1.02230511918389,-3.90820555403357));
#26660=CARTESIAN_POINT('Ctrl Pts',(97.0345639164,-1.02837417792903,-3.90903189827456));
#26661=CARTESIAN_POINT('Ctrl Pts',(97.0298040893007,-1.0310169074773,-3.90939736398695));
#26662=CARTESIAN_POINT('Ctrl Pts',(97.0196686280309,-1.03655268493383,-3.9101751149256));
#26663=CARTESIAN_POINT('Ctrl Pts',(97.0142884976244,-1.03943711963902,-3.91058768937873));
#26664=CARTESIAN_POINT('Ctrl Pts',(96.9997823754827,-1.0470696540993,-3.91169949766233));
#26665=CARTESIAN_POINT('Ctrl Pts',(96.9906163697165,-1.05174013577109,-3.91240139870975));
#26666=CARTESIAN_POINT('Ctrl Pts',(96.9423934816961,-1.07552126805308,-3.91609191939869));
#26667=CARTESIAN_POINT('Ctrl Pts',(96.9023660789787,-1.09257603743239,-3.91914953686418));
#26668=CARTESIAN_POINT('Ctrl Pts',(96.8088226234813,-1.12645059794053,-3.92628206706657));
#26669=CARTESIAN_POINT('Ctrl Pts',(96.7548636229608,-1.14174025254999,-3.9303889318132));
#26670=CARTESIAN_POINT('Ctrl Pts',(96.6409953673109,-1.16539462608383,-3.93892369958369));
#26671=CARTESIAN_POINT('Ctrl Pts',(96.5811038662848,-1.17310769041009,-3.94333982433224));
#26672=CARTESIAN_POINT('Ctrl Pts',(96.510870684196,-1.17671423361306,-3.94827141649339));
#26673=CARTESIAN_POINT('Ctrl Pts',(96.5008548027134,-1.17710045515829,-3.94896875577648));
#26674=CARTESIAN_POINT('Ctrl Pts',(96.4868967771687,-1.17746031140682,-3.94993118794331));
#26675=CARTESIAN_POINT('Ctrl Pts',(96.4829581918344,-1.17754208229713,-3.95020172170389));
#26676=CARTESIAN_POINT('Ctrl Pts',(96.4761622693112,-1.17764906605842,-3.95066664405474));
#26677=CARTESIAN_POINT('Ctrl Pts',(96.4733051452017,-1.17768364471443,-3.95086153344227));
#26678=CARTESIAN_POINT('Ctrl Pts',(96.4672762475857,-1.17773466724409,-3.95127152854621));
#26679=CARTESIAN_POINT('Ctrl Pts',(96.4641044818367,-1.17774869685962,-3.95148649384838));
#26680=CARTESIAN_POINT('Ctrl Pts',(96.4562321255529,-1.17775171621336,-3.95201831150723));
#26681=CARTESIAN_POINT('Ctrl Pts',(96.451531520822,-1.17772537849062,-3.95233433207218));
#26682=CARTESIAN_POINT('Ctrl Pts',(96.4337912423027,-1.17751975897642,-3.95352166041228));
#26683=CARTESIAN_POINT('Ctrl Pts',(96.4207541241647,-1.1771520451121,-3.95438331243923));
#26684=CARTESIAN_POINT('Ctrl Pts',(96.3872725585644,-1.17565077445741,-3.95657432247968));
#26685=CARTESIAN_POINT('Ctrl Pts',(96.3668461195623,-1.17420050673262,-3.95789005850836));
#26686=CARTESIAN_POINT('Ctrl Pts',(96.2889044961393,-1.16661962028242,-3.96286507304348));
#26687=CARTESIAN_POINT('Ctrl Pts',(96.2318294492956,-1.15678827488558,-3.96641624874181));
#26688=CARTESIAN_POINT('Ctrl Pts',(96.1024735014979,-1.12455395035829,-3.97467078426801));
#26689=CARTESIAN_POINT('Ctrl Pts',(96.0311759619673,-1.09931157537654,-3.97938421108425));
#26690=CARTESIAN_POINT('Ctrl Pts',(95.9533724197388,-1.0630352425865,-3.98501826155924));
#26691=CARTESIAN_POINT('Ctrl Pts',(95.9440156051416,-1.05852091373772,-3.98570405191449));
#26692=CARTESIAN_POINT('Ctrl Pts',(95.9287021473321,-1.0508813421123,-3.98684071923677));
#26693=CARTESIAN_POINT('Ctrl Pts',(95.9227102560455,-1.0478277376299,-3.98728913689945));
#26694=CARTESIAN_POINT('Ctrl Pts',(95.9119297936061,-1.0422169438252,-3.98810272596984));
#26695=CARTESIAN_POINT('Ctrl Pts',(95.9071320928837,-1.03967762783687,-3.98846726782112));
#26696=CARTESIAN_POINT('Ctrl Pts',(95.8968724016518,-1.03415627051593,-3.98925222574626));
#26697=CARTESIAN_POINT('Ctrl Pts',(95.8914161692256,-1.03116393475531,-3.98967299504892));
#26698=CARTESIAN_POINT('Ctrl Pts',(95.8765274877327,-1.02284444768929,-3.99083045167009));
#26699=CARTESIAN_POINT('Ctrl Pts',(95.8671446173764,-1.01743028904605,-3.99157019762072));
#26700=CARTESIAN_POINT('Ctrl Pts',(95.8120016807602,-0.984589191429312,
-3.99598053235804));
#26701=CARTESIAN_POINT('Ctrl Pts',(95.7680798404003,-0.954211962455254,
-3.99975710092738));
#26702=CARTESIAN_POINT('Ctrl Pts',(95.688870807386,-0.89107398379887,-4.00707829284397));
#26703=CARTESIAN_POINT('Ctrl Pts',(95.6532313882539,-0.858919535469922,
-4.01060041738607));
#26704=CARTESIAN_POINT('Ctrl Pts',(95.5999011707109,-0.804545348895044,
-4.01618833019146));
#26705=CARTESIAN_POINT('Ctrl Pts',(95.5808784047342,-0.783702897460052,
-4.01825429723871));
#26706=CARTESIAN_POINT('Ctrl Pts',(95.540198999677,-0.73578303617225,-4.02281172736505));
#26707=CARTESIAN_POINT('Ctrl Pts',(95.5189501991657,-0.708389642230496,
-4.02529072609573));
#26708=CARTESIAN_POINT('Ctrl Pts',(95.4954373241675,-0.675146372559369,
-4.02812086975255));
#26709=CARTESIAN_POINT('Ctrl Pts',(95.4919743636547,-0.670169247442457,
-4.02854008529184));
#26710=CARTESIAN_POINT('Ctrl Pts',(95.4863891867297,-0.662008260324498,
-4.0292198728282));
#26711=CARTESIAN_POINT('Ctrl Pts',(95.4842438275171,-0.658840482770103,
-4.02948189459992));
#26712=CARTESIAN_POINT('Ctrl Pts',(95.4804203726468,-0.653135194363557,
-4.02995042402147));
#26713=CARTESIAN_POINT('Ctrl Pts',(95.4787366424171,-0.65060159281068,-4.03015729542395));
#26714=CARTESIAN_POINT('Ctrl Pts',(95.475047837898,-0.645003916828311,-4.03061172876866));
#26715=CARTESIAN_POINT('Ctrl Pts',(95.4730472263281,-0.641937001129624,
-4.03085899907545));
#26716=CARTESIAN_POINT('Ctrl Pts',(95.4672861632851,-0.63301469504223,-4.03157357152226));
#26717=CARTESIAN_POINT('Ctrl Pts',(95.4635631838213,-0.627135122405331,
-4.03203851142165));
#26718=CARTESIAN_POINT('Ctrl Pts',(95.4323527311959,-0.576865195737454,
-4.0359665542258));
#26719=CARTESIAN_POINT('Ctrl Pts',(95.4077892952618,-0.530719166968396,
-4.03926307066568));
#26720=CARTESIAN_POINT('Ctrl Pts',(95.3522331404061,-0.407194169962118,
-4.04769989110471));
#26721=CARTESIAN_POINT('Ctrl Pts',(95.3262401268905,-0.327898860002954,
-4.05276392249761));
#26722=CARTESIAN_POINT('Ctrl Pts',(95.3023784675555,-0.216428134594552,
-4.06003510820345));
#26723=CARTESIAN_POINT('Ctrl Pts',(95.2971183977458,-0.186090875366485,
-4.06202644634381));
#26724=CARTESIAN_POINT('Ctrl Pts',(95.2917886172872,-0.146098828993867,
-4.06468537289301));
#26725=CARTESIAN_POINT('Ctrl Pts',(95.290640159318,-0.136598506399567,-4.06531945702201));
#26726=CARTESIAN_POINT('Ctrl Pts',(95.2889657955983,-0.121172133677074,
-4.06635349674472));
#26727=CARTESIAN_POINT('Ctrl Pts',(95.2883687839174,-0.115254114454532,
-4.06675123865691));
#26728=CARTESIAN_POINT('Ctrl Pts',(95.2873077223108,-0.103873457179195,
-4.06751825497637));
#26729=CARTESIAN_POINT('Ctrl Pts',(95.2868369348506,-0.0984115909536513,
-4.0678873099811));
#26730=CARTESIAN_POINT('Ctrl Pts',(95.2858354959576,-0.0857616977923087,
-4.06874433526918));
#26731=CARTESIAN_POINT('Ctrl Pts',(95.2853326669055,-0.0785717522666438,
-4.06923315330876));
#26732=CARTESIAN_POINT('Ctrl Pts',(95.2839399005712,-0.0556330266776116,
-4.07079834455299));
#26733=CARTESIAN_POINT('Ctrl Pts',(95.2833003742687,-0.0398713554988464,
-4.07188236138014));
#26734=CARTESIAN_POINT('Ctrl Pts',(95.2825411383615,-0.00277924115063064,
-4.07445468362038));
#26735=CARTESIAN_POINT('Ctrl Pts',(95.2826839780099,0.0185504439796918,
-4.07595048387227));
#26736=CARTESIAN_POINT('Ctrl Pts',(95.2854163022941,0.0992297589523076,
-4.08167153140116));
#26737=CARTESIAN_POINT('Ctrl Pts',(95.2919149668333,0.158352731941786,-4.08599935465944));
#26738=CARTESIAN_POINT('Ctrl Pts',(95.3157921576293,0.285891698711965,-4.09551816113143));
#26739=CARTESIAN_POINT('Ctrl Pts',(95.3349144130465,0.353762984175862,-4.10070379119663));
#26740=CARTESIAN_POINT('Ctrl Pts',(95.3634864226039,0.428712890323207,-4.10632574896784));
#26741=CARTESIAN_POINT('Ctrl Pts',(95.3671037967118,0.437856314178465,-4.10700956872219));
#26742=CARTESIAN_POINT('Ctrl Pts',(95.3723113352837,0.450551971229827,-4.10795518502667));
#26743=CARTESIAN_POINT('Ctrl Pts',(95.3738051131456,0.454142946483366,-4.10822221711789));
#26744=CARTESIAN_POINT('Ctrl Pts',(95.3764222522237,0.460347581128313,-4.10868276865391));
#26745=CARTESIAN_POINT('Ctrl Pts',(95.3775373338572,0.462964664276499,-4.10887676762747));
#26746=CARTESIAN_POINT('Ctrl Pts',(95.3799216710069,0.468504923724802,-4.10928686590806));
#26747=CARTESIAN_POINT('Ctrl Pts',(95.3811933314758,0.471427042060231,-4.1095028142886));
#26748=CARTESIAN_POINT('Ctrl Pts',(95.3843991402755,0.478712630193634,-4.11004043745148));
#26749=CARTESIAN_POINT('Ctrl Pts',(95.3863480067776,0.483069628273673,-4.11036124024081));
#26750=CARTESIAN_POINT('Ctrl Pts',(95.3939410585981,0.49977192997102,-4.11158872913198));
#26751=CARTESIAN_POINT('Ctrl Pts',(95.3997722821058,0.512031720372891,-4.11248489789159));
#26752=CARTESIAN_POINT('Ctrl Pts',(95.4154502778989,0.543575819331392,-4.11478509982836));
#26753=CARTESIAN_POINT('Ctrl Pts',(95.4256194330087,0.562694883782038,-4.11617374178505));
#26754=CARTESIAN_POINT('Ctrl Pts',(95.4868495938651,0.670532461383294,-4.12403552393305));
#26755=CARTESIAN_POINT('Ctrl Pts',(95.5487760141044,0.752574273259843,-4.13017236595481));
#26756=CARTESIAN_POINT('Ctrl Pts',(95.6432647185861,0.848707438179883,-4.13875420775945));
#26757=CARTESIAN_POINT('Ctrl Pts',(95.6669403009432,0.870884394127228,-4.1408491807657));
#26758=CARTESIAN_POINT('Ctrl Pts',(95.698882231083,0.898419429826612,-4.14362734368396));
#26759=CARTESIAN_POINT('Ctrl Pts',(95.7063438938649,0.904691865624664,-4.14427304451585));
#26760=CARTESIAN_POINT('Ctrl Pts',(95.7185126598875,0.914666039006842,-4.14532134415218));
#26761=CARTESIAN_POINT('Ctrl Pts',(95.7231717429527,0.918425847527388,-4.14572161274511));
#26762=CARTESIAN_POINT('Ctrl Pts',(95.732142513252,0.925552867965071,-4.14649033778117));
#26763=CARTESIAN_POINT('Ctrl Pts',(95.7364494030045,0.928925888896804,-4.1468585515916));
#26764=CARTESIAN_POINT('Ctrl Pts',(95.7464184930705,0.936621918562234,-4.14770899166935));
#26765=CARTESIAN_POINT('Ctrl Pts',(95.7520966820182,0.940923767230999,-4.148192023732));
#26766=CARTESIAN_POINT('Ctrl Pts',(95.7701038910706,0.954310809135408,-4.14971984176694));
#26767=CARTESIAN_POINT('Ctrl Pts',(95.7825708610125,0.963206871293486,-4.15077176554917));
#26768=CARTESIAN_POINT('Ctrl Pts',(95.8121427510015,0.983449974141895,-4.1532546369016));
#26769=CARTESIAN_POINT('Ctrl Pts',(95.8293774407727,0.994597679933277,-4.15469239065058));
#26770=CARTESIAN_POINT('Ctrl Pts',(95.8713523060206,1.02021742212127,-4.15817255954176));
#26771=CARTESIAN_POINT('Ctrl Pts',(95.8963386428299,1.03424291463737,-4.16022718895624));
#26772=CARTESIAN_POINT('Ctrl Pts',(95.9218017335164,1.04733937416884,-4.16230107423304));
#26773=CARTESIAN_POINT('Origin',(96.460480949577,-7.19464945638997E-16,
0.924367114736168));
#26774=CARTESIAN_POINT('',(95.9218016616991,1.04733933723095,-4.76237177033706));
#26775=CARTESIAN_POINT('',(95.9218016730721,1.04733934308042,-4.66392061240651));
#26776=CARTESIAN_POINT('',(95.9218016730721,1.04733934308042,0.924367114736168));
#26777=CARTESIAN_POINT('Ctrl Pts',(95.9218016616992,1.04733933723097,-4.76237177033706));
#26778=CARTESIAN_POINT('Ctrl Pts',(95.8347012246739,1.00254086578743,-4.75539525775616));
#26779=CARTESIAN_POINT('Ctrl Pts',(95.7535208930734,0.947046519428651,-4.74809443105733));
#26780=CARTESIAN_POINT('Ctrl Pts',(95.6639682705235,0.867830384068402,-4.73944764246191));
#26781=CARTESIAN_POINT('Ctrl Pts',(95.6481787712183,0.853069345358054,-4.73789897688971));
#26782=CARTESIAN_POINT('Ctrl Pts',(95.623159246682,0.828354513726947,-4.73541640195253));
#26783=CARTESIAN_POINT('Ctrl Pts',(95.6136796585851,0.818661375359814,-4.73446869999629));
#26784=CARTESIAN_POINT('Ctrl Pts',(95.6010928263053,0.805338361061766,-4.73320319573871));
#26785=CARTESIAN_POINT('Ctrl Pts',(95.5978376230209,0.801850556732903,-4.73287524435591));
#26786=CARTESIAN_POINT('Ctrl Pts',(95.5924436469209,0.796000287382914,-4.73233084194692));
#26787=CARTESIAN_POINT('Ctrl Pts',(95.5902931386447,0.79364878299064,-4.73211353296923));
#26788=CARTESIAN_POINT('Ctrl Pts',(95.5862404547181,0.789181041216751,-4.73170355806071));
#26789=CARTESIAN_POINT('Ctrl Pts',(95.5843363648138,0.787066595463981,-4.731510745704));
#26790=CARTESIAN_POINT('Ctrl Pts',(95.5798464708034,0.782044192749404,-4.73105557329713));
#26791=CARTESIAN_POINT('Ctrl Pts',(95.5772673586259,0.779130257687243,-4.73079370130664));
#26792=CARTESIAN_POINT('Ctrl Pts',(95.5682150608007,0.768800069573509,-4.72987289190035));
#26793=CARTESIAN_POINT('Ctrl Pts',(95.5618202438687,0.761315253233388,-4.729219344919));
#26794=CARTESIAN_POINT('Ctrl Pts',(95.5106391866561,0.699866738242112,-4.72395504992573));
#26795=CARTESIAN_POINT('Ctrl Pts',(95.4706544204621,0.642073980367331,-4.71962399360956));
#26796=CARTESIAN_POINT('Ctrl Pts',(95.4066641675925,0.52925621426904,-4.7116008978476));
#26797=CARTESIAN_POINT('Ctrl Pts',(95.3812550137345,0.475302714960825,-4.70792249209459));
#26798=CARTESIAN_POINT('Ctrl Pts',(95.3524247886639,0.39970344956206,-4.70276663622895));
#26799=CARTESIAN_POINT('Ctrl Pts',(95.3453584807824,0.379543279563745,-4.70139218763886));
#26800=CARTESIAN_POINT('Ctrl Pts',(95.3340279881147,0.344163024903087,-4.69897246612008));
#26801=CARTESIAN_POINT('Ctrl Pts',(95.329514641391,0.329028317124056,-4.69793502616144));
#26802=CARTESIAN_POINT('Ctrl Pts',(95.3233857146382,0.306857444477711,-4.69640968434447));
#26803=CARTESIAN_POINT('Ctrl Pts',(95.321528213299,0.299889521674802,-4.69592950486378));
#26804=CARTESIAN_POINT('Ctrl Pts',(95.3183712201385,0.287594319115543,-4.69508061451651));
#26805=CARTESIAN_POINT('Ctrl Pts',(95.3170447123704,0.282274150739022,-4.69471277575428));
#26806=CARTESIAN_POINT('Ctrl Pts',(95.3143569496039,0.271164541353731,-4.69394347500008));
#26807=CARTESIAN_POINT('Ctrl Pts',(95.3130023044034,0.265373676984706,-4.69354181479479));
#26808=CARTESIAN_POINT('Ctrl Pts',(95.3095837409847,0.250244172384122,-4.69249056270591));
#26809=CARTESIAN_POINT('Ctrl Pts',(95.3075896492725,0.240890371092452,-4.69183878871913));
#26810=CARTESIAN_POINT('Ctrl Pts',(95.299670255675,0.201389065660143,-4.689077943422));
#26811=CARTESIAN_POINT('Ctrl Pts',(95.2948123800131,0.171042420152743,-4.68693599530511));
#26812=CARTESIAN_POINT('Ctrl Pts',(95.2812094443827,0.0578642779716065,
-4.67886519686011));
#26813=CARTESIAN_POINT('Ctrl Pts',(95.2800702457139,-0.0256267804325326,
-4.67272768336147));
#26814=CARTESIAN_POINT('Ctrl Pts',(95.2925546425887,-0.160534256850619,
-4.6628097713229));
#26815=CARTESIAN_POINT('Ctrl Pts',(95.3008225244471,-0.212171503525447,
-4.65902020042589));
#26816=CARTESIAN_POINT('Ctrl Pts',(95.3140476679167,-0.269878174347515,
-4.65490248137147));
#26817=CARTESIAN_POINT('Ctrl Pts',(95.3156624972256,-0.276648179640297,
-4.6544213060363));
#26818=CARTESIAN_POINT('Ctrl Pts',(95.3182184900759,-0.286958091906697,
-4.65369185114534));
#26819=CARTESIAN_POINT('Ctrl Pts',(95.3191162755502,-0.290508441696048,
-4.65344125728871));
#26820=CARTESIAN_POINT('Ctrl Pts',(95.3207902178706,-0.29700059664494,-4.65298419978233));
#26821=CARTESIAN_POINT('Ctrl Pts',(95.3215612159557,-0.299943593296958,
-4.65277746003812));
#26822=CARTESIAN_POINT('Ctrl Pts',(95.323327609944,-0.306581121299168,-4.65231218853159));
#26823=CARTESIAN_POINT('Ctrl Pts',(95.3243296107321,-0.310273811414395,
-4.65205403496205));
#26824=CARTESIAN_POINT('Ctrl Pts',(95.3269660312562,-0.319805815961665,
-4.6513892961044));
#26825=CARTESIAN_POINT('Ctrl Pts',(95.3286276065488,-0.325637595607847,
-4.65098419495902));
#26826=CARTESIAN_POINT('Ctrl Pts',(95.3400866508788,-0.364708799308417,
-4.6482792332123));
#26827=CARTESIAN_POINT('Ctrl Pts',(95.3513030034805,-0.397518153382198,
-4.64605195702448));
#26828=CARTESIAN_POINT('Ctrl Pts',(95.3742389034827,-0.456035101690588,
-4.6420805647027));
#26829=CARTESIAN_POINT('Ctrl Pts',(95.3854659330351,-0.48190521010964,-4.64032519009879));
#26830=CARTESIAN_POINT('Ctrl Pts',(95.4182613070449,-0.550609915934103,
-4.63560491775258));
#26831=CARTESIAN_POINT('Ctrl Pts',(95.441533316629,-0.592569567299774,-4.63265697659181));
#26832=CARTESIAN_POINT('Ctrl Pts',(95.4959840975354,-0.678004239902656,
-4.62632165899971));
#26833=CARTESIAN_POINT('Ctrl Pts',(95.527693938371,-0.721007095967666,-4.62292878703207));
#26834=CARTESIAN_POINT('Ctrl Pts',(95.569214637721,-0.769971954652902,-4.6187093853385));
#26835=CARTESIAN_POINT('Ctrl Pts',(95.5763353552728,-0.77813816568108,-4.61799295403379));
#26836=CARTESIAN_POINT('Ctrl Pts',(95.5877221186251,-0.790838680966592,
-4.61685774570912));
#26837=CARTESIAN_POINT('Ctrl Pts',(95.5919133010307,-0.795439522345213,
-4.61644205991704));
#26838=CARTESIAN_POINT('Ctrl Pts',(95.5998282497927,-0.80399096019547,-4.61566091602712));
#26839=CARTESIAN_POINT('Ctrl Pts',(95.6035432632299,-0.80794946237382,-4.6152958321088));
#26840=CARTESIAN_POINT('Ctrl Pts',(95.6119216571035,-0.81675419895231,-4.614475838832));
#26841=CARTESIAN_POINT('Ctrl Pts',(95.6165994181131,-0.821586423913875,
-4.61402032161194));
#26842=CARTESIAN_POINT('Ctrl Pts',(95.6286076465615,-0.833780425713611,
-4.61285658961946));
#26843=CARTESIAN_POINT('Ctrl Pts',(95.6359944784468,-0.841085630309066,
-4.61214594436212));
#26844=CARTESIAN_POINT('Ctrl Pts',(95.6977145935018,-0.900529304723208,
-4.60624922040344));
#26845=CARTESIAN_POINT('Ctrl Pts',(95.7568270082685,-0.947434860721522,
-4.6008425117736));
#26846=CARTESIAN_POINT('Ctrl Pts',(95.8688255642208,-1.02001177470005,-4.59108030257034));
#26847=CARTESIAN_POINT('Ctrl Pts',(95.9199293773333,-1.04799063362938,-4.58678278428259));
#26848=CARTESIAN_POINT('Ctrl Pts',(95.9914305047523,-1.08050982922471,-4.58111165693349));
#26849=CARTESIAN_POINT('Ctrl Pts',(96.0101853335513,-1.08845935483474,-4.57965459046969));
#26850=CARTESIAN_POINT('Ctrl Pts',(96.0412267064569,-1.10067693675347,-4.57730219417807));
#26851=CARTESIAN_POINT('Ctrl Pts',(96.0533940070274,-1.10523485992692,-4.57639469465947));
#26852=CARTESIAN_POINT('Ctrl Pts',(96.0700571698512,-1.11116441993027,-4.57517387845173));
#26853=CARTESIAN_POINT('Ctrl Pts',(96.0744889555346,-1.11271167797678,-4.57485128466334));
#26854=CARTESIAN_POINT('Ctrl Pts',(96.0819295432561,-1.11525958762172,-4.57431332295994));
#26855=CARTESIAN_POINT('Ctrl Pts',(96.0849333124509,-1.11627464722792,-4.57409713830684));
#26856=CARTESIAN_POINT('Ctrl Pts',(96.0906532448045,-1.11818187437826,-4.5736873975995));
#26857=CARTESIAN_POINT('Ctrl Pts',(96.0933686059131,-1.11907629899786,-4.57349370720699));
#26858=CARTESIAN_POINT('Ctrl Pts',(96.0998384417324,-1.12118134359577,-4.57303409712102));
#26859=CARTESIAN_POINT('Ctrl Pts',(96.103595824904,-1.12238301510144,-4.57276868859318));
#26860=CARTESIAN_POINT('Ctrl Pts',(96.1169505731618,-1.12658023389055,-4.57183047573469));
#26861=CARTESIAN_POINT('Ctrl Pts',(96.1265805030767,-1.12947184614344,-4.57116329968445));
#26862=CARTESIAN_POINT('Ctrl Pts',(96.1936821126324,-1.14868742231013,-4.56657146246185));
#26863=CARTESIAN_POINT('Ctrl Pts',(96.2522935904987,-1.16074298340619,-4.56284722074856));
#26864=CARTESIAN_POINT('Ctrl Pts',(96.3757629681837,-1.1764799858717,-4.55513535410812));
#26865=CARTESIAN_POINT('Ctrl Pts',(96.4405141830677,-1.1793570731058,-4.5511616457911));
#26866=CARTESIAN_POINT('Ctrl Pts',(96.5414528611269,-1.17552404531606,-4.54475317905771));
#26867=CARTESIAN_POINT('Ctrl Pts',(96.5776469915129,-1.17246959302739,-4.54241357809435));
#26868=CARTESIAN_POINT('Ctrl Pts',(96.6233142054462,-1.16648000324601,-4.53937944958983));
#26869=CARTESIAN_POINT('Ctrl Pts',(96.6329722487484,-1.16509098764696,-4.53873312316518));
#26870=CARTESIAN_POINT('Ctrl Pts',(96.6485289970504,-1.16265595374776,-4.5376840328032));
#26871=CARTESIAN_POINT('Ctrl Pts',(96.6544390626157,-1.16168463151129,-4.53728360526223));
#26872=CARTESIAN_POINT('Ctrl Pts',(96.6657325195258,-1.15973996300852,-4.53651472578175));
#26873=CARTESIAN_POINT('Ctrl Pts',(96.6711170547628,-1.15877410146491,-4.53614651764069));
#26874=CARTESIAN_POINT('Ctrl Pts',(96.6833776198437,-1.15648655946073,-4.53530432027431));
#26875=CARTESIAN_POINT('Ctrl Pts',(96.690248930002,-1.15514101275008,-4.5348295926145));
#26876=CARTESIAN_POINT('Ctrl Pts',(96.7118647970285,-1.1507076761245,-4.5333273536103));
#26877=CARTESIAN_POINT('Ctrl Pts',(96.7265618346173,-1.14739832701777,-4.53229293134626));
#26878=CARTESIAN_POINT('Ctrl Pts',(96.8273990957307,-1.12265115980613,-4.52510234999425));
#26879=CARTESIAN_POINT('Ctrl Pts',(96.9109237320985,-1.09181964092174,-4.51864161842532));
#26880=CARTESIAN_POINT('Ctrl Pts',(97.0073579413313,-1.04325962846799,-4.51071740751488));
#26881=CARTESIAN_POINT('Ctrl Pts',(97.0243245022384,-1.03418835750193,-4.50930576916079));
#26882=CARTESIAN_POINT('Ctrl Pts',(97.0702300348611,-1.00817907524102,-4.50544814754966));
#26883=CARTESIAN_POINT('Ctrl Pts',(97.0986817754473,-0.990413552212167,
-4.5030140277712));
#26884=CARTESIAN_POINT('Ctrl Pts',(97.1414414291249,-0.961105172002238,
-4.49932555233204));
#26885=CARTESIAN_POINT('Ctrl Pts',(97.1563020462211,-0.950401714632761,
-4.49803776434283));
#26886=CARTESIAN_POINT('Ctrl Pts',(97.1751522891448,-0.936145425003434,
-4.49640249695755));
#26887=CARTESIAN_POINT('Ctrl Pts',(97.1793748957116,-0.932906681969083,
-4.49603606978881));
#26888=CARTESIAN_POINT('Ctrl Pts',(97.1861853252887,-0.927609375516879,
-4.49544508483991));
#26889=CARTESIAN_POINT('Ctrl Pts',(97.1887866272117,-0.925568384876944,
-4.49521935478727));
#26890=CARTESIAN_POINT('Ctrl Pts',(97.1938059771246,-0.92159592197977,-4.49478385592261));
#26891=CARTESIAN_POINT('Ctrl Pts',(97.1962250459675,-0.919665843841556,
-4.49457400008569));
#26892=CARTESIAN_POINT('Ctrl Pts',(97.201568836087,-0.915367668419748,-4.49411042843509));
#26893=CARTESIAN_POINT('Ctrl Pts',(97.2044898992085,-0.912995020664015,
-4.49385703007945));
#26894=CARTESIAN_POINT('Ctrl Pts',(97.2145693318613,-0.904727453223364,
-4.49298246162963));
#26895=CARTESIAN_POINT('Ctrl Pts',(97.221669642541,-0.898761837050916,-4.49236604818108));
#26896=CARTESIAN_POINT('Ctrl Pts',(97.2902489084566,-0.839746402344359,
-4.48640059101291));
#26897=CARTESIAN_POINT('Ctrl Pts',(97.3461654807295,-0.780548362330831,
-4.48143326757323));
#26898=CARTESIAN_POINT('Ctrl Pts',(97.4273599773606,-0.67452006980631,-4.47316752189625));
#26899=CARTESIAN_POINT('Ctrl Pts',(97.4563644964034,-0.630910246115097,
-4.46991576860415));
#26900=CARTESIAN_POINT('Ctrl Pts',(97.4922181820308,-0.568335790685192,
-4.46530751887286));
#26901=CARTESIAN_POINT('Ctrl Pts',(97.5016286453381,-0.550907157973189,
-4.46403017302286));
#26902=CARTESIAN_POINT('Ctrl Pts',(97.5173409640515,-0.519965355814765,
-4.46176651236397));
#26903=CARTESIAN_POINT('Ctrl Pts',(97.5238341073371,-0.506554134239694,
-4.46078668075241));
#26904=CARTESIAN_POINT('Ctrl Pts',(97.5330208361816,-0.486623996754391,
-4.45933065680798));
#26905=CARTESIAN_POINT('Ctrl Pts',(97.535913258294,-0.480197947027818,-4.4588612098649));
#26906=CARTESIAN_POINT('Ctrl Pts',(97.5409444617384,-0.468746716288336,
-4.45802449417507));
#26907=CARTESIAN_POINT('Ctrl Pts',(97.5431063043181,-0.463731845684422,
-4.45765801507503));
#26908=CARTESIAN_POINT('Ctrl Pts',(97.5475802070877,-0.453151831021365,
-4.45688463958896));
#26909=CARTESIAN_POINT('Ctrl Pts',(97.5498845804596,-0.447583628309523,
-4.45647749841987));
#26910=CARTESIAN_POINT('Ctrl Pts',(97.5558712789293,-0.432797432693821,
-4.45539590302844));
#26911=CARTESIAN_POINT('Ctrl Pts',(97.5594799074409,-0.423550317600299,
-4.45471902859541));
#26912=CARTESIAN_POINT('Ctrl Pts',(97.5749835281572,-0.382289675627383,
-4.45169602282746));
#26913=CARTESIAN_POINT('Ctrl Pts',(97.5855985605515,-0.349816162994044,
-4.44930872869938));
#26914=CARTESIAN_POINT('Ctrl Pts',(97.6236688017928,-0.21356115932731,-4.43925350913957));
#26915=CARTESIAN_POINT('Ctrl Pts',(97.6382813346104,-0.106748830692155,
-4.43122188222926));
#26916=CARTESIAN_POINT('Ctrl Pts',(97.6382188276505,0.0260264136737434,
-4.42168050861395));
#26917=CARTESIAN_POINT('Ctrl Pts',(97.6373804869628,0.0514935380240259,
-4.41987383687667));
#26918=CARTESIAN_POINT('Ctrl Pts',(97.6353178817726,0.0830092683104523,
-4.41768227628789));
#26919=CARTESIAN_POINT('Ctrl Pts',(97.6348716614224,0.0891000326231811,
-4.41726079187598));
#26920=CARTESIAN_POINT('Ctrl Pts',(97.6340939644511,0.0986909873160142,
-4.41660062081228));
#26921=CARTESIAN_POINT('Ctrl Pts',(97.6337941655065,0.102193531104669,-4.41636027383454));
#26922=CARTESIAN_POINT('Ctrl Pts',(97.6332317415458,0.108435299120317,-4.4159333454051));
#26923=CARTESIAN_POINT('Ctrl Pts',(97.6329751998713,0.111174940632863,-4.41574643996885));
#26924=CARTESIAN_POINT('Ctrl Pts',(97.6323360421851,0.117752185414445,-4.41529885623522));
#26925=CARTESIAN_POINT('Ctrl Pts',(97.6319441761344,0.121588836339259,-4.41503869126701));
#26926=CARTESIAN_POINT('Ctrl Pts',(97.6306900550845,0.133298291849693,-4.41424729003307));
#26927=CARTESIAN_POINT('Ctrl Pts',(97.6297672085535,0.14116457830115,-4.41371925800698));
#26928=CARTESIAN_POINT('Ctrl Pts',(97.6274311148989,0.159478890337525,-4.41249709186862));
#26929=CARTESIAN_POINT('Ctrl Pts',(97.6259567737815,0.169918583420597,-4.41180589953393));
#26930=CARTESIAN_POINT('Ctrl Pts',(97.620284302685,0.206527562241394,-4.4093969341489));
#26931=CARTESIAN_POINT('Ctrl Pts',(97.6153430592409,0.23257503949253,-4.40770961720868));
#26932=CARTESIAN_POINT('Ctrl Pts',(97.5923711993018,0.334711730910872,-4.40112232704819));
#26933=CARTESIAN_POINT('Ctrl Pts',(97.5676631781332,0.409091364103382,-4.39637688490095));
#26934=CARTESIAN_POINT('Ctrl Pts',(97.5166152067053,0.523334619492289,-4.38851878235687));
#26935=CARTESIAN_POINT('Ctrl Pts',(97.4949212365808,0.565005487096903,-4.38552174812203));
#26936=CARTESIAN_POINT('Ctrl Pts',(97.4652765133273,0.614488798130523,-4.38173090018636));
#26937=CARTESIAN_POINT('Ctrl Pts',(97.4596264693501,0.623633566928062,-4.38102020894016));
#26938=CARTESIAN_POINT('Ctrl Pts',(97.4504852250847,0.637985798154637,-4.37988797536627));
#26939=CARTESIAN_POINT('Ctrl Pts',(97.4470761666952,0.643245069293355,-4.37946942968615));
#26940=CARTESIAN_POINT('Ctrl Pts',(97.4409370880032,0.65255241979169,-4.37872207873026));
#26941=CARTESIAN_POINT('Ctrl Pts',(97.4382235460922,0.656611234814684,-4.37839388868141));
#26942=CARTESIAN_POINT('Ctrl Pts',(97.4318792876369,0.665974208798717,-4.37763143923391));
#26943=CARTESIAN_POINT('Ctrl Pts',(97.4282302570304,0.671265709734011,-4.37719650234518));
#26944=CARTESIAN_POINT('Ctrl Pts',(97.4177651952761,0.686178519428217,-4.37595906563329));
#26945=CARTESIAN_POINT('Ctrl Pts',(97.4108479010198,0.695727480897372,-4.37515276539066));
#26946=CARTESIAN_POINT('Ctrl Pts',(97.3538195817302,0.772014331851954,-4.36859523000623));
#26947=CARTESIAN_POINT('Ctrl Pts',(97.2968970398898,0.833344500572717,-4.36257031313806));
#26948=CARTESIAN_POINT('Ctrl Pts',(97.1779761153996,0.93691644309143,-4.35100827918186));
#26949=CARTESIAN_POINT('Ctrl Pts',(97.1174728085043,0.980293475811746,-4.34552241967781));
#26950=CARTESIAN_POINT('Ctrl Pts',(97.044956389199,1.02253428325201,-4.33964257189854));
#26951=CARTESIAN_POINT('Ctrl Pts',(97.0365711342112,1.02728185711396,-4.33897262106573));
#26952=CARTESIAN_POINT('Ctrl Pts',(97.0247336215906,1.03379349722139,-4.3380416770788));
#26953=CARTESIAN_POINT('Ctrl Pts',(97.0213297585565,1.03564409296838,-4.33777568363323));
#26954=CARTESIAN_POINT('Ctrl Pts',(97.0151654093495,1.03895619153181,-4.3372971160242));
#26955=CARTESIAN_POINT('Ctrl Pts',(97.0124081295427,1.04042357078429,-4.33708418341315));
#26956=CARTESIAN_POINT('Ctrl Pts',(97.006761035785,1.04340009478161,-4.33665043217467));
#26957=CARTESIAN_POINT('Ctrl Pts',(97.0038707413471,1.04490823770965,-4.33642967537922));
#26958=CARTESIAN_POINT('Ctrl Pts',(96.9964330093848,1.04875000655281,-4.3358646867897));
#26959=CARTESIAN_POINT('Ctrl Pts',(96.9918765168696,1.05106609692002,-4.33552152082154));
#26960=CARTESIAN_POINT('Ctrl Pts',(96.9726963770908,1.06065885780377,-4.33408875104513));
#26961=CARTESIAN_POINT('Ctrl Pts',(96.9579364493386,1.06766097054071,-4.33301468913035));
#26962=CARTESIAN_POINT('Ctrl Pts',(96.9172806444448,1.08592181360353,-4.33012040167329));
#26963=CARTESIAN_POINT('Ctrl Pts',(96.891117083937,1.09656048035367,-4.32832732341106));
#26964=CARTESIAN_POINT('Ctrl Pts',(96.7843827455991,1.13555062878009,-4.32119342848089));
#26965=CARTESIAN_POINT('Ctrl Pts',(96.7012227226418,1.15604133647805,-4.31602210525761));
#26966=CARTESIAN_POINT('Ctrl Pts',(96.5786702770097,1.17242863806958,-4.30819773050146));
#26967=CARTESIAN_POINT('Ctrl Pts',(96.5405432495682,1.17564756446844,-4.30573910599759));
#26968=CARTESIAN_POINT('Ctrl Pts',(96.4920489606173,1.1773717997126,-4.30254619707199));
#26969=CARTESIAN_POINT('Ctrl Pts',(96.4817639383707,1.17760261441919,-4.30186535312159));
#26970=CARTESIAN_POINT('Ctrl Pts',(96.4653727626991,1.1777556637092,-4.30077385968397));
#26971=CARTESIAN_POINT('Ctrl Pts',(96.4592678009129,1.17776519694514,-4.30036590724007));
#26972=CARTESIAN_POINT('Ctrl Pts',(96.4482630094765,1.17769681863065,-4.29962785248133));
#26973=CARTESIAN_POINT('Ctrl Pts',(96.4433631846486,1.17763579070686,-4.29929827959192));
#26974=CARTESIAN_POINT('Ctrl Pts',(96.4318272110866,1.17742009810423,-4.29852001879087));
#26975=CARTESIAN_POINT('Ctrl Pts',(96.4251917640885,1.17723990520999,-4.29807055270068));
#26976=CARTESIAN_POINT('Ctrl Pts',(96.4057603250423,1.17654779417199,-4.29674882408161));
#26977=CARTESIAN_POINT('Ctrl Pts',(96.3929710837099,1.17588326559371,-4.29587189834016));
#26978=CARTESIAN_POINT('Ctrl Pts',(96.3099134757336,1.17020816215441,-4.29012921911651));
#26979=CARTESIAN_POINT('Ctrl Pts',(96.2402162297934,1.15911087088923,-4.28507542885213));
#26980=CARTESIAN_POINT('Ctrl Pts',(96.0989802678761,1.12342118331545,-4.27442998008216));
#26981=CARTESIAN_POINT('Ctrl Pts',(96.027954793011,1.09803455198337,-4.26884939094858));
#26982=CARTESIAN_POINT('Ctrl Pts',(95.9470466697245,1.06003769830293,-4.26249433370216));
#26983=CARTESIAN_POINT('Ctrl Pts',(95.9343667356133,1.05380194648143,-4.26149888802261));
#26984=CARTESIAN_POINT('Ctrl Pts',(95.9218016729659,1.04733934302581,-4.26051510683823));
#26985=CARTESIAN_POINT('',(97.6382304530324,-0.00105496753745055,-4.32555915085301));
#26986=CARTESIAN_POINT('Ctrl Pts',(95.9218017335164,1.04733937416884,-4.16230107423304));
#26987=CARTESIAN_POINT('Ctrl Pts',(95.9457162450475,1.0596393512744,-4.16424883281337));
#26988=CARTESIAN_POINT('Ctrl Pts',(95.9700512852212,1.07111986665047,-4.16621353099733));
#26989=CARTESIAN_POINT('Ctrl Pts',(96.0647000849988,1.11186780571143,-4.17376600339058));
#26990=CARTESIAN_POINT('Ctrl Pts',(96.1373956001256,1.13512566236667,-4.17939543747484));
#26991=CARTESIAN_POINT('Ctrl Pts',(96.221115133895,1.15320824440095,-4.18539442314298));
#26992=CARTESIAN_POINT('Ctrl Pts',(96.2304219996601,1.15510092306814,-4.18605457887953));
#26993=CARTESIAN_POINT('Ctrl Pts',(96.2435331394711,1.15760249426119,-4.18697420245168));
#26994=CARTESIAN_POINT('Ctrl Pts',(96.2473187610821,1.15830555962964,-4.1872385174085));
#26995=CARTESIAN_POINT('Ctrl Pts',(96.2541749520513,1.15954413979634,-4.18771495064252));
#26996=CARTESIAN_POINT('Ctrl Pts',(96.257244323834,1.16008605349809,-4.18792741769356));
#26997=CARTESIAN_POINT('Ctrl Pts',(96.263537265392,1.16117136278808,-4.18836129499613));
#26998=CARTESIAN_POINT('Ctrl Pts',(96.266761001518,1.16171353219465,-4.1885826366211));
#26999=CARTESIAN_POINT('Ctrl Pts',(96.2750717470111,1.16307568080579,-4.18915097039064));
#27000=CARTESIAN_POINT('Ctrl Pts',(96.2801620219128,1.16387572293439,-4.18949687208251));
#27001=CARTESIAN_POINT('Ctrl Pts',(96.3017797399913,1.16712816446043,-4.19095718053255));
#27002=CARTESIAN_POINT('Ctrl Pts',(96.3183540485649,1.16926226311029,-4.1920552904058));
#27003=CARTESIAN_POINT('Ctrl Pts',(96.3639988661453,1.17415445074933,-4.1950343413314));
#27004=CARTESIAN_POINT('Ctrl Pts',(96.3931363272957,1.17618553286863,-4.19688615796863));
#27005=CARTESIAN_POINT('Ctrl Pts',(96.5141901216589,1.1801098179909,-4.20448096090975));
#27006=CARTESIAN_POINT('Ctrl Pts',(96.6060894507238,1.17232351091294,-4.21003735479366));
#27007=CARTESIAN_POINT('Ctrl Pts',(96.727039674914,1.14762166589799,-4.21790456378743));
#27008=CARTESIAN_POINT('Ctrl Pts',(96.757661313432,1.14007569949948,-4.21994287512952));
#27009=CARTESIAN_POINT('Ctrl Pts',(96.7972182407172,1.12862585831167,-4.22265629272679));
#27010=CARTESIAN_POINT('Ctrl Pts',(96.8064614033248,1.12582673968716,-4.22329612357076));
#27011=CARTESIAN_POINT('Ctrl Pts',(96.8213583232834,1.12111470960772,-4.22433721650482));
#27012=CARTESIAN_POINT('Ctrl Pts',(96.8270339204875,1.11927190094823,-4.22473620755997));
#27013=CARTESIAN_POINT('Ctrl Pts',(96.8378906958944,1.11565538340907,-4.22550405427505));
#27014=CARTESIAN_POINT('Ctrl Pts',(96.8430739996599,1.11388850763256,-4.22587267897033));
#27015=CARTESIAN_POINT('Ctrl Pts',(96.8546135731407,1.10986487077006,-4.22669799026334));
#27016=CARTESIAN_POINT('Ctrl Pts',(96.8609631159107,1.10758953927005,-4.2271552746661));
#27017=CARTESIAN_POINT('Ctrl Pts',(96.8807835456759,1.10029425672701,-4.2285928523958));
#27018=CARTESIAN_POINT('Ctrl Pts',(96.8941818494641,1.09508228980156,-4.22957940891503));
#27019=CARTESIAN_POINT('Ctrl Pts',(96.9251704421334,1.08236977009613,-4.23189682790372));
#27020=CARTESIAN_POINT('Ctrl Pts',(96.9426797211388,1.07468363575531,-4.23323351717457));
#27021=CARTESIAN_POINT('Ctrl Pts',(97.0047071395935,1.04563414446829,-4.23806834117014));
#27022=CARTESIAN_POINT('Ctrl Pts',(97.0480552104024,1.02190433296309,-4.24163728652058));
#27023=CARTESIAN_POINT('Ctrl Pts',(97.1499071456353,0.957520783112995,-4.25044523361146));
#27024=CARTESIAN_POINT('Ctrl Pts',(97.2064664820061,0.914144840576898,-4.2557144806438));
#27025=CARTESIAN_POINT('Ctrl Pts',(97.2736535014771,0.852206183019933,-4.26223793033431));
#27026=CARTESIAN_POINT('Ctrl Pts',(97.2881842193577,0.838100467955295,-4.26366596117625));
#27027=CARTESIAN_POINT('Ctrl Pts',(97.3063518759381,0.819530516450613,-4.26546601863086));
#27028=CARTESIAN_POINT('Ctrl Pts',(97.3103289107347,0.815405627716726,-4.26586099621162));
#27029=CARTESIAN_POINT('Ctrl Pts',(97.3166153271874,0.808789543714443,-4.26648658819141));
#27030=CARTESIAN_POINT('Ctrl Pts',(97.3189442459837,0.806317163410141,-4.26671863009636));
#27031=CARTESIAN_POINT('Ctrl Pts',(97.3233708420217,0.801576969850555,-4.26716015123629));
#27032=CARTESIAN_POINT('Ctrl Pts',(97.325470316733,0.799310953258028,-4.26736975891984));
#27033=CARTESIAN_POINT('Ctrl Pts',(97.3304402501196,0.793904264175833,-4.26786648562027));
#27034=CARTESIAN_POINT('Ctrl Pts',(97.3333026826138,0.790756213391443,-4.26815301015439));
#27035=CARTESIAN_POINT('Ctrl Pts',(97.3426426176655,0.780371817689689,-4.26908963197026));
#27036=CARTESIAN_POINT('Ctrl Pts',(97.3490478823332,0.773070632916621,-4.26973469230489));
#27037=CARTESIAN_POINT('Ctrl Pts',(97.3815700112641,0.735061230626066,-4.27302930677366));
#27038=CARTESIAN_POINT('Ctrl Pts',(97.4061907091836,0.703102986382873,-4.27558964153519));
#27039=CARTESIAN_POINT('Ctrl Pts',(97.4620625049863,0.622319933320045,-4.28173855853479));
#27040=CARTESIAN_POINT('Ctrl Pts',(97.4914428460861,0.572333441733387,-4.28528276355393));
#27041=CARTESIAN_POINT('Ctrl Pts',(97.5435694844135,0.466500380239278,-4.29262798170492));
#27042=CARTESIAN_POINT('Ctrl Pts',(97.5659462505032,0.410668279389681,-4.29642401419777));
#27043=CARTESIAN_POINT('Ctrl Pts',(97.5870592784507,0.343544176072423,-4.30104299682733));
#27044=CARTESIAN_POINT('Ctrl Pts',(97.5900230283504,0.333670516136409,-4.30172359705247));
#27045=CARTESIAN_POINT('Ctrl Pts',(97.5946987397951,0.317316825295883,-4.30285343429817));
#27046=CARTESIAN_POINT('Ctrl Pts',(97.5964857184333,0.310858690217144,-4.3033002637008));
#27047=CARTESIAN_POINT('Ctrl Pts',(97.5996199451794,0.299143542621406,-4.30411216041211));
#27048=CARTESIAN_POINT('Ctrl Pts',(97.6009861623459,0.293891762997231,-4.30447661026915));
#27049=CARTESIAN_POINT('Ctrl Pts',(97.6038454386111,0.282580351082738,-4.30526270218992));
#27050=CARTESIAN_POINT('Ctrl Pts',(97.6053267188345,0.276517940878452,-4.30568470691842));
#27051=CARTESIAN_POINT('Ctrl Pts',(97.6082583603111,0.264092164704042,-4.30655119583667));
#27052=CARTESIAN_POINT('Ctrl Pts',(97.6097041462393,0.257727952168722,-4.30699580908717));
#27053=CARTESIAN_POINT('Ctrl Pts',(97.6132259145132,0.241606336744269,-4.30812427783247));
#27054=CARTESIAN_POINT('Ctrl Pts',(97.6152309243582,0.231834124568334,-4.30881032795707));
#27055=CARTESIAN_POINT('Ctrl Pts',(97.6312287180095,0.148499076971638,-4.3146790396435));
#27056=CARTESIAN_POINT('Ctrl Pts',(97.6382975384426,0.0737968844927355,
-4.32007700864419));
#27057=CARTESIAN_POINT('Ctrl Pts',(97.6382304769022,-0.0010551707271996,
-4.32555912700301));
#27058=CARTESIAN_POINT('Ctrl Pts',(97.6382304770817,-0.00105497038035304,
-4.32555911232973));
#27059=CARTESIAN_POINT('Ctrl Pts',(97.6381590127215,-0.0808364676042963,
-4.33140225987333));
#27060=CARTESIAN_POINT('Ctrl Pts',(97.6299811960951,-0.160412517676923,
-4.33731172291847));
#27061=CARTESIAN_POINT('Ctrl Pts',(97.6125249667081,-0.244806794199073,
-4.34334031373377));
#27062=CARTESIAN_POINT('Ctrl Pts',(97.6111816025224,-0.251045405210151,
-4.34378442241072));
#27063=CARTESIAN_POINT('Ctrl Pts',(97.608920682197,-0.261145536909812,-4.3445005960345));
#27064=CARTESIAN_POINT('Ctrl Pts',(97.6080342186751,-0.265013785676053,
-4.34477420834012));
#27065=CARTESIAN_POINT('Ctrl Pts',(97.6062877123972,-0.272461884815933,
-4.34529963603447));
#27066=CARTESIAN_POINT('Ctrl Pts',(97.6054304039228,-0.276042323432719,
-4.34555159410763));
#27067=CARTESIAN_POINT('Ctrl Pts',(97.6038342640051,-0.282573017039366,
-4.34600994908937));
#27068=CARTESIAN_POINT('Ctrl Pts',(97.6031007912454,-0.285524446360398,
-4.34621663282572));
#27069=CARTESIAN_POINT('Ctrl Pts',(97.6014243762727,-0.292160268300362,
-4.34668030507632));
#27070=CARTESIAN_POINT('Ctrl Pts',(97.6004750161854,-0.295842955648073,
-4.34693692730569));
#27071=CARTESIAN_POINT('Ctrl Pts',(97.5979850549535,-0.305311848728775,
-4.34759509535677));
#27072=CARTESIAN_POINT('Ctrl Pts',(97.5964181144976,-0.311091105237087,
-4.34799520533479));
#27073=CARTESIAN_POINT('Ctrl Pts',(97.5859054453073,-0.348725579592806,
-4.35059179372531));
#27074=CARTESIAN_POINT('Ctrl Pts',(97.5756638780198,-0.380206929209565,
-4.35272214029631));
#27075=CARTESIAN_POINT('Ctrl Pts',(97.5607027344933,-0.420359675527784,
-4.35543449619461));
#27076=CARTESIAN_POINT('Ctrl Pts',(97.5571830232217,-0.429458730726963,
-4.35604880694301));
#27077=CARTESIAN_POINT('Ctrl Pts',(97.5455701993813,-0.458405696016684,
-4.35800505541286));
#27078=CARTESIAN_POINT('Ctrl Pts',(97.5370480587913,-0.47807715370527,-4.35933744420477));
#27079=CARTESIAN_POINT('Ctrl Pts',(97.5055014729214,-0.545767623324874,
-4.36396592454119));
#27080=CARTESIAN_POINT('Ctrl Pts',(97.4797630093447,-0.592447534941329,
-4.36723890911897));
#27081=CARTESIAN_POINT('Ctrl Pts',(97.4253685574996,-0.676995818616726,
-4.3735535583009));
#27082=CARTESIAN_POINT('Ctrl Pts',(97.3974127317104,-0.715184915811135,
-4.37657393646717));
#27083=CARTESIAN_POINT('Ctrl Pts',(97.3607674773099,-0.759395871460964,
-4.38035025250674));
#27084=CARTESIAN_POINT('Ctrl Pts',(97.3541949200233,-0.767120101510726,
-4.38102102844242));
#27085=CARTESIAN_POINT('Ctrl Pts',(97.3440903625904,-0.778689094559577,
-4.3820430787077));
#27086=CARTESIAN_POINT('Ctrl Pts',(97.340631091064,-0.782596976557167,-4.38239139078954));
#27087=CARTESIAN_POINT('Ctrl Pts',(97.3335546868617,-0.790484809686945,
-4.38310080296619));
#27088=CARTESIAN_POINT('Ctrl Pts',(97.3299360422196,-0.794463230943686,
-4.38346196065832));
#27089=CARTESIAN_POINT('Ctrl Pts',(97.3220812392535,-0.802981041625491,
-4.3842425466257));
#27090=CARTESIAN_POINT('Ctrl Pts',(97.3178361946371,-0.807511977372892,
-4.38466234280406));
#27091=CARTESIAN_POINT('Ctrl Pts',(97.3063214176267,-0.819609089013073,
-4.38579569184843));
#27092=CARTESIAN_POINT('Ctrl Pts',(97.2989862145478,-0.827111881455714,
-4.38651202721525));
#27093=CARTESIAN_POINT('Ctrl Pts',(97.2611887074042,-0.864753379323755,
-4.39017597154798));
#27094=CARTESIAN_POINT('Ctrl Pts',(97.2292015092608,-0.893308030011768,
-4.39319019462524));
#27095=CARTESIAN_POINT('Ctrl Pts',(97.1242259797899,-0.977198211523787,
-4.40282393658955));
#27096=CARTESIAN_POINT('Ctrl Pts',(97.0463098422742,-1.02580495150212,-4.40964147106556));
#27097=CARTESIAN_POINT('Ctrl Pts',(96.9447059589486,-1.07380440723321,-4.41776000124902));
#27098=CARTESIAN_POINT('Ctrl Pts',(96.9256199042467,-1.08220867744155,-4.4192526955667));
#27099=CARTESIAN_POINT('Ctrl Pts',(96.8941626346657,-1.09507432368605,-4.42165032767276));
#27100=CARTESIAN_POINT('Ctrl Pts',(96.8819226021935,-1.09984296505078,-4.42256816157993));
#27101=CARTESIAN_POINT('Ctrl Pts',(96.8651414385208,-1.10605949478209,-4.42380372714481));
#27102=CARTESIAN_POINT('Ctrl Pts',(96.8606680616567,-1.107685873607,-4.42413091014296));
#27103=CARTESIAN_POINT('Ctrl Pts',(96.853185939306,-1.11035489436167,-4.42467437438377));
#27104=CARTESIAN_POINT('Ctrl Pts',(96.8501826467349,-1.11141251943367,-4.42489150772265));
#27105=CARTESIAN_POINT('Ctrl Pts',(96.8444859836768,-1.1133926984969,-4.42530140673185));
#27106=CARTESIAN_POINT('Ctrl Pts',(96.8417935030906,-1.11431768551511,-4.42549431716674));
#27107=CARTESIAN_POINT('Ctrl Pts',(96.8354065372272,-1.11648603256416,-4.42595003672646));
#27108=CARTESIAN_POINT('Ctrl Pts',(96.8317091522699,-1.11772084161616,-4.42621235482406));
#27109=CARTESIAN_POINT('Ctrl Pts',(96.8186909794605,-1.12199677375328,-4.42713093051323));
#27110=CARTESIAN_POINT('Ctrl Pts',(96.8093381059047,-1.12493994757703,-4.42778185371708));
#27111=CARTESIAN_POINT('Ctrl Pts',(96.7325203172675,-1.14806282773389,-4.43306286875708));
#27112=CARTESIAN_POINT('Ctrl Pts',(96.6633971727737,-1.16227425203348,-4.43741078147543));
#27113=CARTESIAN_POINT('Ctrl Pts',(96.5344288176955,-1.17692415923969,-4.44543969979147));
#27114=CARTESIAN_POINT('Ctrl Pts',(96.4750292299028,-1.1791549739972,-4.44910666175506));
#27115=CARTESIAN_POINT('Ctrl Pts',(96.3944125090177,-1.17608866889308,-4.45424789918991));
#27116=CARTESIAN_POINT('Ctrl Pts',(96.3731350917396,-1.1747000534647,-4.45561985497873));
#27117=CARTESIAN_POINT('Ctrl Pts',(96.3362056892201,-1.17128109253765,-4.4580355687082));
#27118=CARTESIAN_POINT('Ctrl Pts',(96.3205348099975,-1.16951219654817,-4.45907152978353));
#27119=CARTESIAN_POINT('Ctrl Pts',(96.2977611770346,-1.16647729297186,-4.46059507133588));
#27120=CARTESIAN_POINT('Ctrl Pts',(96.2906266291146,-1.16545978281375,-4.46107495512229));
#27121=CARTESIAN_POINT('Ctrl Pts',(96.2780822236582,-1.16355310143397,-4.4619234807627));
#27122=CARTESIAN_POINT('Ctrl Pts',(96.2726683455444,-1.1626915064229,-4.46229125262517));
#27123=CARTESIAN_POINT('Ctrl Pts',(96.2613929450991,-1.16081626993552,-4.46306056958167));
#27124=CARTESIAN_POINT('Ctrl Pts',(96.2555327056261,-1.15979595668282,-4.46346231389843));
#27125=CARTESIAN_POINT('Ctrl Pts',(96.2402641362235,-1.15701824567792,-4.46451413480269));
#27126=CARTESIAN_POINT('Ctrl Pts',(96.2308692153122,-1.15519050715775,-4.46516639820493));
#27127=CARTESIAN_POINT('Ctrl Pts',(96.1913428258655,-1.14699961076327,-4.46793268923841));
#27128=CARTESIAN_POINT('Ctrl Pts',(96.1614471385815,-1.13957093472753,-4.47007975837751));
#27129=CARTESIAN_POINT('Ctrl Pts',(96.0519711435078,-1.1077631095234,-4.47815196254911));
#27130=CARTESIAN_POINT('Ctrl Pts',(95.9747568183585,-1.0761449966183,-4.48428507505218));
#27131=CARTESIAN_POINT('Ctrl Pts',(95.8555775850517,-1.0118856500779,-4.49419670799488));
#27132=CARTESIAN_POINT('Ctrl Pts',(95.8113170751539,-0.984077342442661,
-4.49798450104213));
#27133=CARTESIAN_POINT('Ctrl Pts',(95.7634106201733,-0.94933473665084,-4.50210051372358));
#27134=CARTESIAN_POINT('Ctrl Pts',(95.7578134929777,-0.945199416861917,
-4.50258162884902));
#27135=CARTESIAN_POINT('Ctrl Pts',(95.7493275472846,-0.938812712197127,
-4.50331099849869));
#27136=CARTESIAN_POINT('Ctrl Pts',(95.7464121476213,-0.936597147745537,
-4.50356156673596));
#27137=CARTESIAN_POINT('Ctrl Pts',(95.741093650821,-0.932516075513854,-4.5040185803336));
#27138=CARTESIAN_POINT('Ctrl Pts',(95.7386874388978,-0.93065484745509,-4.50422530171658));
#27139=CARTESIAN_POINT('Ctrl Pts',(95.7332713034991,-0.926431772992456,
-4.50469053362215));
#27140=CARTESIAN_POINT('Ctrl Pts',(95.7302656589297,-0.924064570090515,
-4.50494866600544));
#27141=CARTESIAN_POINT('Ctrl Pts',(95.7225266572997,-0.917908103654629,
-4.50561335237244));
#27142=CARTESIAN_POINT('Ctrl Pts',(95.7178108600713,-0.914096803526146,
-4.50601842242882));
#27143=CARTESIAN_POINT('Ctrl Pts',(95.6863447999047,-0.888261722910321,
-4.50872314023797));
#27144=CARTESIAN_POINT('Ctrl Pts',(95.6605454706052,-0.865100804245516,
-4.51095021651394));
#27145=CARTESIAN_POINT('Ctrl Pts',(95.6156696949907,-0.821087240804572,
-4.51492199762463));
#27146=CARTESIAN_POINT('Ctrl Pts',(95.5962515941291,-0.800623541267971,
-4.51667793852155));
#27147=CARTESIAN_POINT('Ctrl Pts',(95.545853186944,-0.74353883393383,-4.52139933902527));
#27148=CARTESIAN_POINT('Ctrl Pts',(95.5163452324756,-0.705692282249907,
-4.52434784306921));
#27149=CARTESIAN_POINT('Ctrl Pts',(95.4590437540472,-0.622146425964342,
-4.53068303098925));
#27150=CARTESIAN_POINT('Ctrl Pts',(95.4318903058464,-0.576144802910152,
-4.5340751677861));
#27151=CARTESIAN_POINT('Ctrl Pts',(95.4030896757561,-0.518783305602544,
-4.53829370492658));
#27152=CARTESIAN_POINT('Ctrl Pts',(95.3983626212747,-0.509035429050284,
-4.53901005972738));
#27153=CARTESIAN_POINT('Ctrl Pts',(95.3911330082118,-0.493587651021954,
-4.5401451515588));
#27154=CARTESIAN_POINT('Ctrl Pts',(95.3885399397014,-0.487930587054474,
-4.54056079807132));
#27155=CARTESIAN_POINT('Ctrl Pts',(95.383769154985,-0.477300995120827,-4.54134187062565));
#27156=CARTESIAN_POINT('Ctrl Pts',(95.381580740406,-0.472333426212919,-4.54170692257745));
#27157=CARTESIAN_POINT('Ctrl Pts',(95.3767582149237,-0.461178188369389,
-4.54252684688482));
#27158=CARTESIAN_POINT('Ctrl Pts',(95.3741426218582,-0.454982770572812,
-4.54298232702065));
#27159=CARTESIAN_POINT('Ctrl Pts',(95.3676220450393,-0.439161006106172,
-4.54414596848129));
#27160=CARTESIAN_POINT('Ctrl Pts',(95.3637911710571,-0.429504938528318,
-4.54485655995583));
#27161=CARTESIAN_POINT('Ctrl Pts',(95.333194912088,-0.349305056106681,-4.55076339538371));
#27162=CARTESIAN_POINT('Ctrl Pts',(95.3131424443414,-0.27640243780273,-4.55618119939496));
#27163=CARTESIAN_POINT('Ctrl Pts',(95.2902843587849,-0.145169035259185,
-4.56592568141551));
#27164=CARTESIAN_POINT('Ctrl Pts',(95.284571674238,-0.0875884456413804,
-4.57019350228826));
#27165=CARTESIAN_POINT('Ctrl Pts',(95.282588917164,-0.0093047954862436,
-4.57584854251918));
#27166=CARTESIAN_POINT('Ctrl Pts',(95.2826055807556,0.0112220653214549,
-4.57731713905188));
#27167=CARTESIAN_POINT('Ctrl Pts',(95.2835107354156,0.0447975927934336,
-4.57968597059511));
#27168=CARTESIAN_POINT('Ctrl Pts',(95.28408002885,0.0578499656139854,-4.58059857526384));
#27169=CARTESIAN_POINT('Ctrl Pts',(95.2851495262588,0.0755859247006364,
-4.58182506206358));
#27170=CARTESIAN_POINT('Ctrl Pts',(95.2854607761377,0.0802793905693871,
-4.5821483302139));
#27171=CARTESIAN_POINT('Ctrl Pts',(95.2860290187556,0.0881350586497589,
-4.58268708816283));
#27172=CARTESIAN_POINT('Ctrl Pts',(95.2862706821197,0.0912982746195974,
-4.58290339994693));
#27173=CARTESIAN_POINT('Ctrl Pts',(95.2867542498045,0.0973080551311807,
-4.58331312787679));
#27174=CARTESIAN_POINT('Ctrl Pts',(95.2869937335371,0.100154768164082,-4.583506679955));
#27175=CARTESIAN_POINT('Ctrl Pts',(95.2875878982213,0.106922651816111,-4.58396564238258));
#27176=CARTESIAN_POINT('Ctrl Pts',(95.2879518909175,0.110843001998878,-4.58423054482192));
#27177=CARTESIAN_POINT('Ctrl Pts',(95.2893108424806,0.124722992397453,-4.58516528074529));
#27178=CARTESIAN_POINT('Ctrl Pts',(95.2904131288713,0.13467203057951,-4.58582953972797));
#27179=CARTESIAN_POINT('Ctrl Pts',(95.2993739978702,0.207101918053159,-4.59063133904514));
#27180=CARTESIAN_POINT('Ctrl Pts',(95.3121067829252,0.268885518810642,-4.59454535885249));
#27181=CARTESIAN_POINT('Ctrl Pts',(95.3471684112106,0.38925873646743,-4.60230755711784));
#27182=CARTESIAN_POINT('Ctrl Pts',(95.3693456094675,0.447672079174441,-4.60614556528667));
#27183=CARTESIAN_POINT('Ctrl Pts',(95.4112738234477,0.536214320762865,-4.61236555844668));
#27184=CARTESIAN_POINT('Ctrl Pts',(95.4279521566382,0.56766654011599,-4.61466006267309));
#27185=CARTESIAN_POINT('Ctrl Pts',(95.4509530069537,0.606664986294496,-4.61764306619461));
#27186=CARTESIAN_POINT('Ctrl Pts',(95.4559814662184,0.614955161970502,-4.61828539210684));
#27187=CARTESIAN_POINT('Ctrl Pts',(95.4642734694365,0.628252677811625,-4.61932954803901));
#27188=CARTESIAN_POINT('Ctrl Pts',(95.4674738454123,0.633299028515112,-4.61972908194516));
#27189=CARTESIAN_POINT('Ctrl Pts',(95.473679108493,0.642920796603565,-4.62049729839353));
#27190=CARTESIAN_POINT('Ctrl Pts',(95.4766777700103,0.647500059005047,-4.62086574499462));
#27191=CARTESIAN_POINT('Ctrl Pts',(95.4835991262727,0.657910598658043,-4.62170996432585));
#27192=CARTESIAN_POINT('Ctrl Pts',(95.4875422818925,0.663727954623449,-4.62218648836277));
#27193=CARTESIAN_POINT('Ctrl Pts',(95.5001825439267,0.682021499083477,-4.62370042877183));
#27194=CARTESIAN_POINT('Ctrl Pts',(95.5090690636578,0.694364269649437,-4.62474491069148));
#27195=CARTESIAN_POINT('Ctrl Pts',(95.5699501598089,0.775560421020918,-4.63177485300641));
#27196=CARTESIAN_POINT('Ctrl Pts',(95.629127894075,0.83868102583114,-4.63804598630359));
#27197=CARTESIAN_POINT('Ctrl Pts',(95.7321239454832,0.926835401469966,-4.64799537611612));
#27198=CARTESIAN_POINT('Ctrl Pts',(95.7715752031079,0.956523488697504,-4.65161801347587));
#27199=CARTESIAN_POINT('Ctrl Pts',(95.8257328350741,0.99218478542195,-4.65626278907697));
#27200=CARTESIAN_POINT('Ctrl Pts',(95.8388600005971,1.00046152448989,-4.65736474698867));
#27201=CARTESIAN_POINT('Ctrl Pts',(95.8612552849237,1.01397080836982,-4.65920035201054));
#27202=CARTESIAN_POINT('Ctrl Pts',(95.8704374474205,1.01934139656302,-4.65994073574979));
#27203=CARTESIAN_POINT('Ctrl Pts',(95.8834681120871,1.02672785761334,-4.66097304730748));
#27204=CARTESIAN_POINT('Ctrl Pts',(95.8872566056097,1.02884778330312,-4.66127101985226));
#27205=CARTESIAN_POINT('Ctrl Pts',(95.8937732886332,1.03244715118033,-4.66177976852051));
#27206=CARTESIAN_POINT('Ctrl Pts',(95.8964957396692,1.03393683408772,-4.66199117583912));
#27207=CARTESIAN_POINT('Ctrl Pts',(95.9021782187256,1.03701707508994,-4.66243004923524));
#27208=CARTESIAN_POINT('Ctrl Pts',(95.9051391973361,1.0386057443689,-4.66265739947779));
#27209=CARTESIAN_POINT('Ctrl Pts',(95.9126560784275,1.04259747894743,-4.66323129406324));
#27210=CARTESIAN_POINT('Ctrl Pts',(95.9172210732586,1.04498339778935,-4.66357679554692));
#27211=CARTESIAN_POINT('Ctrl Pts',(95.921801673072,1.04733934308038,-4.66392061240651));
#27212=CARTESIAN_POINT('Origin',(96.460480949577,-7.19464945638997E-16,
0.924367114736168));
#27213=CARTESIAN_POINT('',(95.921801349668,1.04733917674356,-5.26198394263683));
#27214=CARTESIAN_POINT('',(95.9218017437159,1.04733937941474,-5.16217169173788));
#27215=CARTESIAN_POINT('',(95.9218016730721,1.04733934308042,0.924367114736168));
#27216=CARTESIAN_POINT('',(97.6382308254874,0.000540641388559765,-4.92534013812095));
#27217=CARTESIAN_POINT('Ctrl Pts',(95.921801349668,1.04733917674357,-5.26198394263684));
#27218=CARTESIAN_POINT('Ctrl Pts',(95.8863949474338,1.02912854640219,-5.25949681132839));
#27219=CARTESIAN_POINT('Ctrl Pts',(95.8519052197883,1.00911906816238,-5.25697856025019));
#27220=CARTESIAN_POINT('Ctrl Pts',(95.8012871418023,0.976206235024907,-5.25307639562409));
#27221=CARTESIAN_POINT('Ctrl Pts',(95.7844007619948,0.964588299927166,-5.25173772463044));
#27222=CARTESIAN_POINT('Ctrl Pts',(95.7611771527045,0.947700829467667,-5.24983910458976));
#27223=CARTESIAN_POINT('Ctrl Pts',(95.7545784186168,0.942795987258968,-5.24929290723313));
#27224=CARTESIAN_POINT('Ctrl Pts',(95.7439732518351,0.934739406751148,-5.24840381804272));
#27225=CARTESIAN_POINT('Ctrl Pts',(95.7399348994296,0.931629984322131,-5.24806256718612));
#27226=CARTESIAN_POINT('Ctrl Pts',(95.7315359121621,0.925075713708643,-5.24734709620885));
#27227=CARTESIAN_POINT('Ctrl Pts',(95.7271792314717,0.921626026146741,-5.246972692029));
#27228=CARTESIAN_POINT('Ctrl Pts',(95.7168700304592,0.913343664411881,-5.24607879522826));
#27229=CARTESIAN_POINT('Ctrl Pts',(95.7109400305796,0.908483491477129,-5.2455582200061));
#27230=CARTESIAN_POINT('Ctrl Pts',(95.6908969574289,0.891726553748058,-5.2437764394318));
#27231=CARTESIAN_POINT('Ctrl Pts',(95.6770169091999,0.879556591911642,-5.2425043028009));
#27232=CARTESIAN_POINT('Ctrl Pts',(95.6120262097248,0.81981379811033,-5.23635773731462));
#27233=CARTESIAN_POINT('Ctrl Pts',(95.5649349053213,0.768091508187358,-5.23131133852742));
#27234=CARTESIAN_POINT('Ctrl Pts',(95.4755240763808,0.650413370964499,-5.22048397740461));
#27235=CARTESIAN_POINT('Ctrl Pts',(95.4346229773269,0.583776441392637,-5.21471180321565));
#27236=CARTESIAN_POINT('Ctrl Pts',(95.3965003090428,0.505102965199593,-5.20858970277224));
#27237=CARTESIAN_POINT('Ctrl Pts',(95.3924940058633,0.496575986991457,-5.20793492514289));
#27238=CARTESIAN_POINT('Ctrl Pts',(95.3870003333577,0.484509188270785,-5.20702150567266));
#27239=CARTESIAN_POINT('Ctrl Pts',(95.3854274190753,0.481009037863543,-5.20675810003064));
#27240=CARTESIAN_POINT('Ctrl Pts',(95.3826092790025,0.474655051933135,-5.20628280122511));
#27241=CARTESIAN_POINT('Ctrl Pts',(95.3813582115873,0.471803850906519,-5.20607056465033));
#27242=CARTESIAN_POINT('Ctrl Pts',(95.3788145854194,0.465943840074813,-5.20563654197352));
#27243=CARTESIAN_POINT('Ctrl Pts',(95.37752324603,0.462934550930948,-5.2054148284205));
#27244=CARTESIAN_POINT('Ctrl Pts',(95.3742226322402,0.4551535304282,-5.20484446706169));
#27245=CARTESIAN_POINT('Ctrl Pts',(95.3722322147991,0.450373802485238,-5.20449692444453));
#27246=CARTESIAN_POINT('Ctrl Pts',(95.3638671871024,0.429907002987363,-5.203020109879));
#27247=CARTESIAN_POINT('Ctrl Pts',(95.3577993939736,0.414095682871752,-5.20190759531882));
#27248=CARTESIAN_POINT('Ctrl Pts',(95.342006432324,0.370130669177825,-5.19887730198996));
#27249=CARTESIAN_POINT('Ctrl Pts',(95.3330044858246,0.34172947262847,-5.19698987751931));
#27250=CARTESIAN_POINT('Ctrl Pts',(95.2983321117703,0.215963392391423,-5.18881499321327));
#27251=CARTESIAN_POINT('Ctrl Pts',(95.2841303589861,0.115885999306558,-5.18274298776355));
#27252=CARTESIAN_POINT('Ctrl Pts',(95.282520897245,-0.0086415898098256,
-5.17473148115871));
#27253=CARTESIAN_POINT('Ctrl Pts',(95.2829378364975,-0.0325062091223059,
-5.17317787910972));
#27254=CARTESIAN_POINT('Ctrl Pts',(95.2844965378622,-0.0650522509333797,
-5.17102619768557));
#27255=CARTESIAN_POINT('Ctrl Pts',(95.2850105145556,-0.0737589423348358,
-5.17044737673944));
#27256=CARTESIAN_POINT('Ctrl Pts',(95.2859844824655,-0.0876358593066876,
-5.16951937834214));
#27257=CARTESIAN_POINT('Ctrl Pts',(95.2863820398042,-0.0928102564561942,
-5.16917213567926));
#27258=CARTESIAN_POINT('Ctrl Pts',(95.2872710256096,-0.103458903315663,
-5.16845494886006));
#27259=CARTESIAN_POINT('Ctrl Pts',(95.2877666015458,-0.108932669734362,
-5.16808488471937));
#27260=CARTESIAN_POINT('Ctrl Pts',(95.2890095689832,-0.121668228612362,
-5.16722050295995));
#27261=CARTESIAN_POINT('Ctrl Pts',(95.2897861941,-0.128926873651446,-5.16672529112122));
#27262=CARTESIAN_POINT('Ctrl Pts',(95.2925136765484,-0.152357637371185,
-5.16511822866275));
#27263=CARTESIAN_POINT('Ctrl Pts',(95.2947325017154,-0.168496026239607,
-5.16399814703587));
#27264=CARTESIAN_POINT('Ctrl Pts',(95.3007711502575,-0.206550169858913,
-5.16132441417298));
#27265=CARTESIAN_POINT('Ctrl Pts',(95.3048784954533,-0.228413329369444,
-5.15976244206133));
#27266=CARTESIAN_POINT('Ctrl Pts',(95.3331721169167,-0.358587464523163,
-5.15030672285739));
#27267=CARTESIAN_POINT('Ctrl Pts',(95.3719441862428,-0.463132723739411,
-5.14198966251668));
#27268=CARTESIAN_POINT('Ctrl Pts',(95.4359701446762,-0.581400727260943,
-5.13234744333606));
#27269=CARTESIAN_POINT('Ctrl Pts',(95.447796071451,-0.60176300393703,-5.13068112479173));
#27270=CARTESIAN_POINT('Ctrl Pts',(95.4634080093114,-0.626878743439909,
-5.12863006279034));
#27271=CARTESIAN_POINT('Ctrl Pts',(95.466630013006,-0.631974466992667,-5.12821415461369));
#27272=CARTESIAN_POINT('Ctrl Pts',(95.47176393676,-0.639957592135436,-5.12756321656541));
#27273=CARTESIAN_POINT('Ctrl Pts',(95.4736496493511,-0.642861600067037,
-5.12732656013158));
#27274=CARTESIAN_POINT('Ctrl Pts',(95.4772312874345,-0.648324446193072,
-5.12688169258991));
#27275=CARTESIAN_POINT('Ctrl Pts',(95.4789243972829,-0.650884951832206,
-5.12667331763676));
#27276=CARTESIAN_POINT('Ctrl Pts',(95.4829137392218,-0.656867102985931,
-5.12618676808588));
#27277=CARTESIAN_POINT('Ctrl Pts',(95.4852179413447,-0.660283354173536,
-5.12590912282841));
#27278=CARTESIAN_POINT('Ctrl Pts',(95.492800225436,-0.671398697006397,-5.1250061996922));
#27279=CARTESIAN_POINT('Ctrl Pts',(95.4981520732879,-0.679047377938776,
-5.12438557778369));
#27280=CARTESIAN_POINT('Ctrl Pts',(95.5281763068772,-0.720888984611513,
-5.12098951830207));
#27281=CARTESIAN_POINT('Ctrl Pts',(95.5545828511405,-0.753805209553397,
-5.11831370604711));
#27282=CARTESIAN_POINT('Ctrl Pts',(95.591666117294,-0.795258862296566,-5.11483471483392));
#27283=CARTESIAN_POINT('Ctrl Pts',(95.6008023625744,-0.805126455067585,
-5.11399781957354));
#27284=CARTESIAN_POINT('Ctrl Pts',(95.6787449622545,-0.886468580596394,
-5.10700472735521));
#27285=CARTESIAN_POINT('Ctrl Pts',(95.7561514345742,-0.949134142475318,
-5.1009533562629));
#27286=CARTESIAN_POINT('Ctrl Pts',(95.8524205550059,-1.00873901196754,-5.09355640369785));
#27287=CARTESIAN_POINT('Ctrl Pts',(95.8644777883831,-1.01590946563433,-5.09263292055487));
#27288=CARTESIAN_POINT('Ctrl Pts',(95.8826356128607,-1.02627343980089,-5.09124500376506));
#27289=CARTESIAN_POINT('Ctrl Pts',(95.8886410817923,-1.02963176361733,-5.09078642239786));
#27290=CARTESIAN_POINT('Ctrl Pts',(95.8994485838952,-1.03555172003439,-5.08996178690195));
#27291=CARTESIAN_POINT('Ctrl Pts',(95.9042396348135,-1.03813307348434,-5.08959643952062));
#27292=CARTESIAN_POINT('Ctrl Pts',(95.9144561967008,-1.04354659109289,-5.08881773826864));
#27293=CARTESIAN_POINT('Ctrl Pts',(95.9198862203446,-1.04636984609748,-5.08840408683912));
#27294=CARTESIAN_POINT('Ctrl Pts',(95.9345641053784,-1.05385663388473,-5.08728640219269));
#27295=CARTESIAN_POINT('Ctrl Pts',(95.9438517065304,-1.05844061956436,-5.08657965300326));
#27296=CARTESIAN_POINT('Ctrl Pts',(95.9934162055791,-1.0820958808033,-5.08280949181167));
#27297=CARTESIAN_POINT('Ctrl Pts',(96.0346860376224,-1.09898989154639,-5.07967342924336));
#27298=CARTESIAN_POINT('Ctrl Pts',(96.128083675089,-1.13117121123118,-5.07258429166374));
#27299=CARTESIAN_POINT('Ctrl Pts',(96.1805136844178,-1.14527454181078,-5.06860869686611));
#27300=CARTESIAN_POINT('Ctrl Pts',(96.2934723911407,-1.16743755504154,-5.06016077701003));
#27301=CARTESIAN_POINT('Ctrl Pts',(96.3540455617583,-1.17451065872026,-5.05569937904056));
#27302=CARTESIAN_POINT('Ctrl Pts',(96.4248959008259,-1.17725479458165,-5.05072747573586));
#27303=CARTESIAN_POINT('Ctrl Pts',(96.4348975786546,-1.17751460912993,-5.05003142879462));
#27304=CARTESIAN_POINT('Ctrl Pts',(96.4488379187933,-1.17769902709576,-5.04907046552561));
#27305=CARTESIAN_POINT('Ctrl Pts',(96.4527743887818,-1.1777313652192,-5.04880012961801));
#27306=CARTESIAN_POINT('Ctrl Pts',(96.4595677311515,-1.17775311055907,-5.04833544370388));
#27307=CARTESIAN_POINT('Ctrl Pts',(96.4624245081339,-1.17775186114214,-5.04814059416617));
#27308=CARTESIAN_POINT('Ctrl Pts',(96.468454219585,-1.17772728469232,-5.04773055888914));
#27309=CARTESIAN_POINT('Ctrl Pts',(96.4716271163979,-1.17770152990905,-5.04751551425137));
#27310=CARTESIAN_POINT('Ctrl Pts',(96.479505009166,-1.17760574426296,-5.0469832895037));
#27311=CARTESIAN_POINT('Ctrl Pts',(96.484209826273,-1.17752033784881,-5.04666694381643));
#27312=CARTESIAN_POINT('Ctrl Pts',(96.501984895155,-1.17709108832297,-5.04547704469838));
#27313=CARTESIAN_POINT('Ctrl Pts',(96.5150501959939,-1.17655779289567,-5.04461320046953));
#27314=CARTESIAN_POINT('Ctrl Pts',(96.5486171539396,-1.17462727285692,-5.04241534191477));
#27315=CARTESIAN_POINT('Ctrl Pts',(96.569096604823,-1.17291089193164,-5.0410950563964));
#27316=CARTESIAN_POINT('Ctrl Pts',(96.6469300457998,-1.16433137283572,-5.03612100145978));
#27317=CARTESIAN_POINT('Ctrl Pts',(96.7037983899,-1.15378864259685,-5.03257461021558));
#27318=CARTESIAN_POINT('Ctrl Pts',(96.8326194826648,-1.11995413798603,-5.02432752590203));
#27319=CARTESIAN_POINT('Ctrl Pts',(96.9035529262069,-1.09383242625444,-5.01961666833807));
#27320=CARTESIAN_POINT('Ctrl Pts',(96.9808586597993,-1.05660307731737,-5.01398537807644));
#27321=CARTESIAN_POINT('Ctrl Pts',(96.9901597823292,-1.05197117224223,-5.01329947448174));
#27322=CARTESIAN_POINT('Ctrl Pts',(97.0053786698346,-1.04413925099332,-5.01216263762108));
#27323=CARTESIAN_POINT('Ctrl Pts',(97.0113325915872,-1.04101045448719,-5.01171416463297));
#27324=CARTESIAN_POINT('Ctrl Pts',(97.0218142541754,-1.03538722363846,-5.01091787315539));
#27325=CARTESIAN_POINT('Ctrl Pts',(97.026353022843,-1.03291363480598,-5.01057079150637));
#27326=CARTESIAN_POINT('Ctrl Pts',(97.0361164876793,-1.0275089670874,-5.00981917504025));
#27327=CARTESIAN_POINT('Ctrl Pts',(97.0413353773573,-1.02456775354864,-5.00941428929032));
#27328=CARTESIAN_POINT('Ctrl Pts',(97.0520142635072,-1.01844163024283,-5.00857926842199));
#27329=CARTESIAN_POINT('Ctrl Pts',(97.0574715036771,-1.01525232888928,-5.00814898620579));
#27330=CARTESIAN_POINT('Ctrl Pts',(97.0710447434838,-1.00717262621326,-5.00706973108455));
#27331=CARTESIAN_POINT('Ctrl Pts',(97.0791277719823,-1.00222799076971,-5.00641883479909));
#27332=CARTESIAN_POINT('Ctrl Pts',(97.1018766351386,-0.987931758311911,
-5.00456324447949));
#27333=CARTESIAN_POINT('Ctrl Pts',(97.1163956911033,-0.978352381338273,
-5.00335052409774));
#27334=CARTESIAN_POINT('Ctrl Pts',(97.1656109530749,-0.944293155305185,
-4.99913971703986));
#27335=CARTESIAN_POINT('Ctrl Pts',(97.1991896560734,-0.918262865612945,
-4.99608937971528));
#27336=CARTESIAN_POINT('Ctrl Pts',(97.2780930069972,-0.849963469299813,
-4.9884963204906));
#27337=CARTESIAN_POINT('Ctrl Pts',(97.3216303845538,-0.805821814943679,
-4.98391829555737));
#27338=CARTESIAN_POINT('Ctrl Pts',(97.3706501988728,-0.747588828411519,
-4.97838655316168));
#27339=CARTESIAN_POINT('Ctrl Pts',(97.3796070088654,-0.736549001064288,
-4.9773584794489));
#27340=CARTESIAN_POINT('Ctrl Pts',(97.4036155383651,-0.705836822745895,
-4.97455942836815));
#27341=CARTESIAN_POINT('Ctrl Pts',(97.4182510799551,-0.685846234172395,
-4.9728040077675));
#27342=CARTESIAN_POINT('Ctrl Pts',(97.4356676152608,-0.660411006653339,
-4.97066528858081));
#27343=CARTESIAN_POINT('Ctrl Pts',(97.4390503265042,-0.655388212501684,
-4.97024740590606));
#27344=CARTESIAN_POINT('Ctrl Pts',(97.4443288332128,-0.647418472827872,
-4.96959162340487));
#27345=CARTESIAN_POINT('Ctrl Pts',(97.4462504189586,-0.644488860366185,
-4.96935209833419));
#27346=CARTESIAN_POINT('Ctrl Pts',(97.4496588929402,-0.639241457663262,
-4.96892586616344));
#27347=CARTESIAN_POINT('Ctrl Pts',(97.4511507225163,-0.636927033532626,
-4.96873884162254));
#27348=CARTESIAN_POINT('Ctrl Pts',(97.4547217537303,-0.631344035892799,
-4.96828999097046));
#27349=CARTESIAN_POINT('Ctrl Pts',(97.4567929624061,-0.628070412027001,
-4.96802868666455));
#27350=CARTESIAN_POINT('Ctrl Pts',(97.4630960970019,-0.61799842535261,-4.96723029048899));
#27351=CARTESIAN_POINT('Ctrl Pts',(97.4672749771739,-0.611166902101886,
-4.96669648583553));
#27352=CARTESIAN_POINT('Ctrl Pts',(97.4768708747801,-0.595114223770564,
-4.96545877901235));
#27353=CARTESIAN_POINT('Ctrl Pts',(97.4822327025247,-0.585860727820751,
-4.96475792286878));
#27354=CARTESIAN_POINT('Ctrl Pts',(97.5007237189864,-0.552922520800517,
-4.96230274421573));
#27355=CARTESIAN_POINT('Ctrl Pts',(97.5131621147691,-0.528858107079123,
-4.96058015464498));
#27356=CARTESIAN_POINT('Ctrl Pts',(97.5670866081688,-0.415074449010268,
-4.95266338362854));
#27357=CARTESIAN_POINT('Ctrl Pts',(97.5980022321457,-0.320794307986144,
-4.9467107817822));
#27358=CARTESIAN_POINT('Ctrl Pts',(97.6221910474631,-0.195795567192737,
-4.93856790084562));
#27359=CARTESIAN_POINT('Ctrl Pts',(97.6265856949111,-0.167647763682192,
-4.93672154156754));
#27360=CARTESIAN_POINT('Ctrl Pts',(97.6310567883002,-0.130130150370132,
-4.93422998123106));
#27361=CARTESIAN_POINT('Ctrl Pts',(97.6320483631002,-0.12087777970812,-4.9336131097182));
#27362=CARTESIAN_POINT('Ctrl Pts',(97.6334884652477,-0.105750341674214,
-4.93260015605715));
#27363=CARTESIAN_POINT('Ctrl Pts',(97.6340027370177,-0.0998818244306157,
-4.93220611905824));
#27364=CARTESIAN_POINT('Ctrl Pts',(97.6348892665153,-0.0888108647380515,
-4.93146063662626));
#27365=CARTESIAN_POINT('Ctrl Pts',(97.6352710356966,-0.0836093095477796,
-4.9311094952366));
#27366=CARTESIAN_POINT('Ctrl Pts',(97.6359741471251,-0.0730711092015981,
-4.93039622912685));
#27367=CARTESIAN_POINT('Ctrl Pts',(97.6362937254813,-0.0677344732917057,
-4.93003405828905));
#27368=CARTESIAN_POINT('Ctrl Pts',(97.6370681607453,-0.0531372016219196,
-4.92904068274541));
#27369=CARTESIAN_POINT('Ctrl Pts',(97.6374500051863,-0.0438732412298451,
-4.92840724397924));
#27370=CARTESIAN_POINT('Ctrl Pts',(97.6380667310664,-0.0228931782140255,
-4.9269655944772));
#27371=CARTESIAN_POINT('Ctrl Pts',(97.638236204125,-0.011176348649317,-4.92615545629199));
#27372=CARTESIAN_POINT('Ctrl Pts',(97.6382308254874,0.000540641388559765,
-4.92534013812095));
#27373=CARTESIAN_POINT('Ctrl Pts',(97.6382308259868,0.000539552390703118,
-4.92534021389806));
#27374=CARTESIAN_POINT('Ctrl Pts',(97.6381825996176,0.105809404331348,-4.91801509121512));
#27375=CARTESIAN_POINT('Ctrl Pts',(97.6240200727271,0.210588653155426,-4.91024330285112));
#27376=CARTESIAN_POINT('Ctrl Pts',(97.5846280733161,0.353940616701876,-4.89938094608901));
#27377=CARTESIAN_POINT('Ctrl Pts',(97.5708137622644,0.395148756127041,-4.89623916600129));
#27378=CARTESIAN_POINT('Ctrl Pts',(97.551252259339,0.444300184375672,-4.89253604397674));
#27379=CARTESIAN_POINT('Ctrl Pts',(97.5476451622415,0.453054845377181,-4.89187827616222));
#27380=CARTESIAN_POINT('Ctrl Pts',(97.542307919798,0.465577751964426,-4.89094096264452));
#27381=CARTESIAN_POINT('Ctrl Pts',(97.540662957022,0.469381581150236,-4.89065673304485));
#27382=CARTESIAN_POINT('Ctrl Pts',(97.5377633647082,0.475990654213664,-4.89016382484868));
#27383=CARTESIAN_POINT('Ctrl Pts',(97.5365177854713,0.478799784392014,-4.88995461710823));
#27384=CARTESIAN_POINT('Ctrl Pts',(97.5338503969027,0.484752508857821,-4.88951195641959));
#27385=CARTESIAN_POINT('Ctrl Pts',(97.5324257593637,0.487894753852724,-4.88927867547932));
#27386=CARTESIAN_POINT('Ctrl Pts',(97.5284974460808,0.496458951539987,-4.88864379918167));
#27387=CARTESIAN_POINT('Ctrl Pts',(97.5259662644863,0.501868284315993,-4.88824382162014));
#27388=CARTESIAN_POINT('Ctrl Pts',(97.5135433144474,0.527899433068322,-4.88632287042263));
#27389=CARTESIAN_POINT('Ctrl Pts',(97.503092687984,0.548250931473133,-4.88483274675239));
#27390=CARTESIAN_POINT('Ctrl Pts',(97.4425272916067,0.658191394000198,-4.87677759668569));
#27391=CARTESIAN_POINT('Ctrl Pts',(97.3814564194461,0.741241479014468,-4.87063628108073));
#27392=CARTESIAN_POINT('Ctrl Pts',(97.2914426349604,0.835072740120318,-4.86242727616788));
#27393=CARTESIAN_POINT('Ctrl Pts',(97.2718185350027,0.854151608082793,-4.86068095991212));
#27394=CARTESIAN_POINT('Ctrl Pts',(97.2419392730528,0.881241284186539,-4.85806730035447));
#27395=CARTESIAN_POINT('Ctrl Pts',(97.2321867356845,0.88979406127399,-4.85722093424411));
#27396=CARTESIAN_POINT('Ctrl Pts',(97.2163846722061,0.903196928110292,-4.85585868697372));
#27397=CARTESIAN_POINT('Ctrl Pts',(97.2104249034407,0.908151523832824,-4.85534692716612));
#27398=CARTESIAN_POINT('Ctrl Pts',(97.1991921130397,0.917303820166746,-4.85438580159248));
#27399=CARTESIAN_POINT('Ctrl Pts',(97.1939310938734,0.921515797038926,-4.8539370202997));
#27400=CARTESIAN_POINT('Ctrl Pts',(97.1844741014515,0.928954786245003,-4.85313257649093));
#27401=CARTESIAN_POINT('Ctrl Pts',(97.1802919430436,0.932199126246907,-4.85277760619345));
#27402=CARTESIAN_POINT('Ctrl Pts',(97.1714469397591,0.938965691794266,-4.85202841062739));
#27403=CARTESIAN_POINT('Ctrl Pts',(97.1667794777384,0.942481616032628,-4.85163395400226));
#27404=CARTESIAN_POINT('Ctrl Pts',(97.1547887149101,0.951374970894183,-4.85062273168189));
#27405=CARTESIAN_POINT('Ctrl Pts',(97.1474291130166,0.956702577070535,-4.8500040838758));
#27406=CARTESIAN_POINT('Ctrl Pts',(97.1182931628985,0.977284525055812,-4.8475622054245));
#27407=CARTESIAN_POINT('Ctrl Pts',(97.0960659652995,0.991883784928601,-4.84571487321962));
#27408=CARTESIAN_POINT('Ctrl Pts',(96.9903440454676,1.05631073253277,-4.83699276730838));
#27409=CARTESIAN_POINT('Ctrl Pts',(96.9013855576243,1.09642365897743,-4.82979275792665));
#27410=CARTESIAN_POINT('Ctrl Pts',(96.7801085359821,1.13393938001223,-4.82053466748179));
#27411=CARTESIAN_POINT('Ctrl Pts',(96.7513593237808,1.14165245180465,-4.81838219493692));
#27412=CARTESIAN_POINT('Ctrl Pts',(96.7058486639721,1.15203129344284,-4.81506803314242));
#27413=CARTESIAN_POINT('Ctrl Pts',(96.6892700015894,1.15543803788808,-4.81387986422216));
#27414=CARTESIAN_POINT('Ctrl Pts',(96.6675310453554,1.15941886915581,-4.81235152599497));
#27415=CARTESIAN_POINT('Ctrl Pts',(96.6624332246221,1.16031768813986,-4.81199524599042));
#27416=CARTESIAN_POINT('Ctrl Pts',(96.6541012470027,1.16173015981304,-4.81141656756626));
#27417=CARTESIAN_POINT('Ctrl Pts',(96.6508706489711,1.16226397467406,-4.81119308306013));
#27418=CARTESIAN_POINT('Ctrl Pts',(96.6445636517208,1.16327912239248,-4.81075856970003));
#27419=CARTESIAN_POINT('Ctrl Pts',(96.6414875142851,1.16376173750699,-4.81054747530442));
#27420=CARTESIAN_POINT('Ctrl Pts',(96.6346156506074,1.16481195805586,-4.81007769327211));
#27421=CARTESIAN_POINT('Ctrl Pts',(96.6308189547716,1.16537322637189,-4.80981935410606));
#27422=CARTESIAN_POINT('Ctrl Pts',(96.6176900749443,1.16724854583192,-4.80893000661741));
#27423=CARTESIAN_POINT('Ctrl Pts',(96.6083446125399,1.16846918133681,-4.80830389146124));
#27424=CARTESIAN_POINT('Ctrl Pts',(96.5216064622259,1.17874092259645,-4.80254857468887));
#27425=CARTESIAN_POINT('Ctrl Pts',(96.4434976580434,1.18020405445402,-4.79776875738766));
#27426=CARTESIAN_POINT('Ctrl Pts',(96.3116099222756,1.16956786298637,-4.78958234826573));
#27427=CARTESIAN_POINT('Ctrl Pts',(96.2577827761113,1.16144926411757,-4.78620904856263));
#27428=CARTESIAN_POINT('Ctrl Pts',(96.1849318684126,1.1452416328441,-4.7814441130559));
#27429=CARTESIAN_POINT('Ctrl Pts',(96.1652692377537,1.14033138513873,-4.78013804928604));
#27430=CARTESIAN_POINT('Ctrl Pts',(96.1311297363394,1.13086375793522,-4.77782810874798));
#27431=CARTESIAN_POINT('Ctrl Pts',(96.1165958225777,1.12652920334162,-4.77683109983049));
#27432=CARTESIAN_POINT('Ctrl Pts',(96.0953900374026,1.11975624565842,-4.7753543743319));
#27433=CARTESIAN_POINT('Ctrl Pts',(96.0886496781884,1.11753609595964,-4.77488168766651));
#27434=CARTESIAN_POINT('Ctrl Pts',(96.0767526897184,1.11349790160669,-4.77404131980248));
#27435=CARTESIAN_POINT('Ctrl Pts',(96.0715878386512,1.11170459244003,-4.77367445306594));
#27436=CARTESIAN_POINT('Ctrl Pts',(96.0607805295306,1.10786761362216,-4.77290242003057));
#27437=CARTESIAN_POINT('Ctrl Pts',(96.0551408451198,1.10581665411519,-4.77249702352789));
#27438=CARTESIAN_POINT('Ctrl Pts',(96.0403229510976,1.10029931026965,-4.77142508551925));
#27439=CARTESIAN_POINT('Ctrl Pts',(96.031172117544,1.09676124681055,-4.77075620061471));
#27440=CARTESIAN_POINT('Ctrl Pts',(95.991448503128,1.08082926811975,-4.76782157783471));
#27441=CARTESIAN_POINT('Ctrl Pts',(95.9613625562976,1.0672693211444,-4.76551759496211));
#27442=CARTESIAN_POINT('Ctrl Pts',(95.9285169888683,1.05077287490871,-4.76290853512532));
#27443=CARTESIAN_POINT('Ctrl Pts',(95.9251549404675,1.04906403309099,-4.76264035901828));
#27444=CARTESIAN_POINT('Ctrl Pts',(95.9218016616992,1.04733933723097,-4.76237177033706));
#27445=CARTESIAN_POINT('Ctrl Pts',(95.921801673072,1.04733934308038,-4.66392061240651));
#27446=CARTESIAN_POINT('Ctrl Pts',(95.9221705646186,1.04752907550354,-4.66394830116743));
#27447=CARTESIAN_POINT('Ctrl Pts',(95.9225395573735,1.04771861352914,-4.66397597900242));
#27448=CARTESIAN_POINT('Ctrl Pts',(95.9395117997437,1.05642530124754,-4.66524820462356));
#27449=CARTESIAN_POINT('Ctrl Pts',(95.9563161643211,1.06454743235825,-4.66647055066501));
#27450=CARTESIAN_POINT('Ctrl Pts',(96.0707824950419,1.1165540077375,-4.67459565258095));
#27451=CARTESIAN_POINT('Ctrl Pts',(96.1738488912569,1.14734691528063,-4.68098157065748));
#27452=CARTESIAN_POINT('Ctrl Pts',(96.3210300509534,1.17021395041679,-4.69038080141231));
#27453=CARTESIAN_POINT('Ctrl Pts',(96.3627019195113,1.17443003821052,-4.69306605453373));
#27454=CARTESIAN_POINT('Ctrl Pts',(96.4146735100156,1.17690285932458,-4.69649042384808));
#27455=CARTESIAN_POINT('Ctrl Pts',(96.4248459551064,1.17725477205649,-4.69716416865052));
#27456=CARTESIAN_POINT('Ctrl Pts',(96.4411008831706,1.17760623834006,-4.69824691702232));
#27457=CARTESIAN_POINT('Ctrl Pts',(96.4471811664844,1.17769060154973,-4.69865329929652));
#27458=CARTESIAN_POINT('Ctrl Pts',(96.4587102597247,1.17776127236764,-4.69942658239779));
#27459=CARTESIAN_POINT('Ctrl Pts',(96.4641588700541,1.17775685997684,-4.69979318661607));
#27460=CARTESIAN_POINT('Ctrl Pts',(96.4765522646717,1.17766082234335,-4.70062977949987));
#27461=CARTESIAN_POINT('Ctrl Pts',(96.4834966093245,1.17754557257178,-4.7011004851427));
#27462=CARTESIAN_POINT('Ctrl Pts',(96.5047994475771,1.1770035164188,-4.70255061925052));
#27463=CARTESIAN_POINT('Ctrl Pts',(96.5191510279033,1.17637544909335,-4.70353619086242));
#27464=CARTESIAN_POINT('Ctrl Pts',(96.6297028295073,1.16950938978424,-4.71119795696563));
#27465=CARTESIAN_POINT('Ctrl Pts',(96.7248036524084,1.15174412415181,-4.71824198481139));
#27466=CARTESIAN_POINT('Ctrl Pts',(96.8730652775247,1.10470433450429,-4.72965288664079));
#27467=CARTESIAN_POINT('Ctrl Pts',(96.9280526792058,1.08257827227701,-4.7339766794005));
#27468=CARTESIAN_POINT('Ctrl Pts',(96.9887551864931,1.05266011230374,-4.73870277340241));
#27469=CARTESIAN_POINT('Ctrl Pts',(96.9963215241315,1.04882880892294,-4.73929090046884));
#27470=CARTESIAN_POINT('Ctrl Pts',(97.0073631309057,1.0430870801246,-4.74014703946401));
#27471=CARTESIAN_POINT('Ctrl Pts',(97.0108709870057,1.04124040683633,-4.74041871259547));
#27472=CARTESIAN_POINT('Ctrl Pts',(97.0170383142447,1.03795380798756,-4.74089570559588));
#27473=CARTESIAN_POINT('Ctrl Pts',(97.0197016405743,1.03652131053901,-4.74110147352221));
#27474=CARTESIAN_POINT('Ctrl Pts',(97.0254751909377,1.0333872157502,-4.74154704493221));
#27475=CARTESIAN_POINT('Ctrl Pts',(97.028583266506,1.03168182535968,-4.74178660832252));
#27476=CARTESIAN_POINT('Ctrl Pts',(97.0371394048963,1.02693671105166,-4.74244539644105));
#27477=CARTESIAN_POINT('Ctrl Pts',(97.0425711850867,1.02386764014367,-4.7428628347188));
#27478=CARTESIAN_POINT('Ctrl Pts',(97.0717558146544,1.00707037778058,-4.74510286148963));
#27479=CARTESIAN_POINT('Ctrl Pts',(97.0950499210339,0.992557402848831,-4.7468805895713));
#27480=CARTESIAN_POINT('Ctrl Pts',(97.1741465874145,0.939353474041304,-4.75295762864868));
#27481=CARTESIAN_POINT('Ctrl Pts',(97.2270977096641,0.896662486993835,-4.7571051882413));
#27482=CARTESIAN_POINT('Ctrl Pts',(97.3180208416616,0.80938282512673,-4.76492450685179));
#27483=CARTESIAN_POINT('Ctrl Pts',(97.3569200318188,0.766075133480703,-4.7685677265626));
#27484=CARTESIAN_POINT('Ctrl Pts',(97.4035480472587,0.705725424600364,-4.77351674610085));
#27485=CARTESIAN_POINT('Ctrl Pts',(97.4143020868223,0.691121629339043,-4.77470492971462));
#27486=CARTESIAN_POINT('Ctrl Pts',(97.4290863302964,0.670042277254638,-4.77641020172323));
#27487=CARTESIAN_POINT('Ctrl Pts',(97.4333977763163,0.663766435260243,-4.77691670134802));
#27488=CARTESIAN_POINT('Ctrl Pts',(97.4407446465999,0.652846781226984,-4.77779616247406));
#27489=CARTESIAN_POINT('Ctrl Pts',(97.4438087061145,0.648222459415354,-4.77816804538233));
#27490=CARTESIAN_POINT('Ctrl Pts',(97.4496310545137,0.639299008009149,-4.77888468482447));
#27491=CARTESIAN_POINT('Ctrl Pts',(97.4523942746596,0.635003232941863,-4.77922924875282));
#27492=CARTESIAN_POINT('Ctrl Pts',(97.4588489425677,0.624823701167232,-4.7800448168545));
#27493=CARTESIAN_POINT('Ctrl Pts',(97.462516422323,0.618925047761424,-4.78051668118401));
#27494=CARTESIAN_POINT('Ctrl Pts',(97.4733264490928,0.601190613889158,-4.78193339084917));
#27495=CARTESIAN_POINT('Ctrl Pts',(97.4803127978783,0.589261515108182,-4.78288377427852));
#27496=CARTESIAN_POINT('Ctrl Pts',(97.5278598815303,0.504696251920259,-4.78960562340895));
#27497=CARTESIAN_POINT('Ctrl Pts',(97.5608270618603,0.428076795848594,-4.79564211032697));
#27498=CARTESIAN_POINT('Ctrl Pts',(97.5927919549359,0.324935000251129,-4.80356519361236));
#27499=CARTESIAN_POINT('Ctrl Pts',(97.5993874225799,0.301003379707759,-4.80538805973982));
#27500=CARTESIAN_POINT('Ctrl Pts',(97.6156597218724,0.233726962044449,-4.8104478104215));
#27501=CARTESIAN_POINT('Ctrl Pts',(97.6236500608284,0.190012429149564,-4.81366274102418));
#27502=CARTESIAN_POINT('Ctrl Pts',(97.6303388625139,0.136451792809364,-4.81744204259469));
#27503=CARTESIAN_POINT('Ctrl Pts',(97.6314089380747,0.126942067867184,-4.81810694778348));
#27504=CARTESIAN_POINT('Ctrl Pts',(97.6327779409745,0.113279061882614,-4.8190525075962));
#27505=CARTESIAN_POINT('Ctrl Pts',(97.6331709090606,0.109135888470177,-4.81933795751664));
#27506=CARTESIAN_POINT('Ctrl Pts',(97.633816041812,0.101927816928756,-4.81983224042097));
#27507=CARTESIAN_POINT('Ctrl Pts',(97.634078176545,0.0988638876425055,-4.8200416116822));
#27508=CARTESIAN_POINT('Ctrl Pts',(97.6346081749494,0.0923696851907753,
-4.8204838051852));
#27509=CARTESIAN_POINT('Ctrl Pts',(97.6348730104365,0.0889392391256996,
-4.82071646097562));
#27510=CARTESIAN_POINT('Ctrl Pts',(97.6355533306411,0.0795934927289862,
-4.82134789939502));
#27511=CARTESIAN_POINT('Ctrl Pts',(97.635939187809,0.0736760384583882,-4.82174509330303));
#27512=CARTESIAN_POINT('Ctrl Pts',(97.637568465268,0.0454023806028048,-4.82363148964865));
#27513=CARTESIAN_POINT('Ctrl Pts',(97.6382189761102,0.0230150375271749,
-4.82509116130169));
#27514=CARTESIAN_POINT('Ctrl Pts',(97.6382560001883,-0.0471910872588473,
-4.82960001635612));
#27515=CARTESIAN_POINT('Ctrl Pts',(97.6353696927734,-0.0949642835910884,
-4.832569571209));
#27516=CARTESIAN_POINT('Ctrl Pts',(97.6188906997424,-0.230225778237202,
-4.84100497441288));
#27517=CARTESIAN_POINT('Ctrl Pts',(97.5983419198175,-0.316523842856713,
-4.84644244000345));
#27518=CARTESIAN_POINT('Ctrl Pts',(97.5632110705512,-0.413894778747374,
-4.85319261988044));
#27519=CARTESIAN_POINT('Ctrl Pts',(97.5578197198743,-0.427983874916434,
-4.85418439438245));
#27520=CARTESIAN_POINT('Ctrl Pts',(97.5495306791967,-0.448458271723652,
-4.85564975043778));
#27521=CARTESIAN_POINT('Ctrl Pts',(97.5468440687512,-0.45492780175818,-4.85611634835398));
#27522=CARTESIAN_POINT('Ctrl Pts',(97.5419569091997,-0.466406194533013,
-4.85695077095576));
#27523=CARTESIAN_POINT('Ctrl Pts',(97.5397788548255,-0.471424457941079,
-4.85731783337144));
#27524=CARTESIAN_POINT('Ctrl Pts',(97.5351441387186,-0.481902411786874,
-4.85808908413645));
#27525=CARTESIAN_POINT('Ctrl Pts',(97.5326806556856,-0.48735889498491,-4.85849349462092));
#27526=CARTESIAN_POINT('Ctrl Pts',(97.526097268077,-0.501649212625475,-4.85956007762258));
#27527=CARTESIAN_POINT('Ctrl Pts',(97.5219091843042,-0.510450941229398,
-4.86022455170116));
#27528=CARTESIAN_POINT('Ctrl Pts',(97.5016571727848,-0.551685652117717,
-4.86337403754441));
#27529=CARTESIAN_POINT('Ctrl Pts',(97.4842145716792,-0.583415781406397,
-4.86590595561628));
#27530=CARTESIAN_POINT('Ctrl Pts',(97.4317828707908,-0.669183913258349,
-4.87306172654879));
#27531=CARTESIAN_POINT('Ctrl Pts',(97.3937865131363,-0.721230667587447,
-4.8777748154155));
#27532=CARTESIAN_POINT('Ctrl Pts',(97.3123170935076,-0.815540476956679,
-4.88692064865298));
#27533=CARTESIAN_POINT('Ctrl Pts',(97.2694483699655,-0.858081727212322,
-4.89133740014115));
#27534=CARTESIAN_POINT('Ctrl Pts',(97.2158714965398,-0.903648508265781,
-4.89626953920377));
#27535=CARTESIAN_POINT('Ctrl Pts',(97.2081542385449,-0.9100440508581,-4.89696685021218));
#27536=CARTESIAN_POINT('Ctrl Pts',(97.1972910434755,-0.91881525123025,-4.89792924994538));
#27537=CARTESIAN_POINT('Ctrl Pts',(97.1942136672407,-0.9212745956056,-4.89819977908327));
#27538=CARTESIAN_POINT('Ctrl Pts',(97.1888829769944,-0.925491065832029,
-4.89866469565099));
#27539=CARTESIAN_POINT('Ctrl Pts',(97.1866355257515,-0.92725549792166,-4.89885958384979));
#27540=CARTESIAN_POINT('Ctrl Pts',(97.1818797462606,-0.930961276728047,
-4.89926957901612));
#27541=CARTESIAN_POINT('Ctrl Pts',(97.1793699562479,-0.932900701655032,
-4.89948454555573));
#27542=CARTESIAN_POINT('Ctrl Pts',(97.1731212455115,-0.937689163329424,
-4.90001637059439));
#27543=CARTESIAN_POINT('Ctrl Pts',(97.1693729946145,-0.940526038323484,
-4.90033239725096));
#27544=CARTESIAN_POINT('Ctrl Pts',(97.1551620300666,-0.951148430627917,
-4.90151977598607));
#27545=CARTESIAN_POINT('Ctrl Pts',(97.1445867757886,-0.958782766813826,
-4.90238147125986));
#27546=CARTESIAN_POINT('Ctrl Pts',(97.1170887560734,-0.977947064022778,
-4.90457261695953));
#27547=CARTESIAN_POINT('Ctrl Pts',(97.0999877150538,-0.98921457122118,-4.90588844327649));
#27548=CARTESIAN_POINT('Ctrl Pts',(97.0334950154001,-1.03057970089655,-4.91086343910632));
#27549=CARTESIAN_POINT('Ctrl Pts',(96.9822031333988,-1.05747170458792,-4.9144145201672));
#27550=CARTESIAN_POINT('Ctrl Pts',(96.8599028743865,-1.11051921516038,-4.92266891278167));
#27551=CARTESIAN_POINT('Ctrl Pts',(96.7879490157584,-1.13382241066399,-4.9273822933451));
#27552=CARTESIAN_POINT('Ctrl Pts',(96.7041214963406,-1.15232038598896,-4.93301629207463));
#27553=CARTESIAN_POINT('Ctrl Pts',(96.6939479312492,-1.15442459488227,-4.93370208235926));
#27554=CARTESIAN_POINT('Ctrl Pts',(96.6771449474128,-1.15766877894936,-4.93483874958851));
#27555=CARTESIAN_POINT('Ctrl Pts',(96.6705310950574,-1.15888706220545,-4.93528716722955));
#27556=CARTESIAN_POINT('Ctrl Pts',(96.6585605921416,-1.16098621176764,-4.93610075627695));
#27557=CARTESIAN_POINT('Ctrl Pts',(96.653207559021,-1.16188681937624,-4.93646529812694));
#27558=CARTESIAN_POINT('Ctrl Pts',(96.6417049079532,-1.16374037656825,-4.93725025606719));
#27559=CARTESIAN_POINT('Ctrl Pts',(96.6355536032837,-1.16468165199916,-4.93767102538642));
#27560=CARTESIAN_POINT('Ctrl Pts',(96.6186745240865,-1.16712775769264,-4.93882848210026));
#27561=CARTESIAN_POINT('Ctrl Pts',(96.6079332177222,-1.1685333648726,-4.93956822812783));
#27562=CARTESIAN_POINT('Ctrl Pts',(96.5441853166413,-1.17598249113657,-4.94397856460056));
#27563=CARTESIAN_POINT('Ctrl Pts',(96.4908445990453,-1.178566000117,-4.94775513492852));
#27564=CARTESIAN_POINT('Ctrl Pts',(96.3895698413714,-1.17659112237072,-4.95507632748259));
#27565=CARTESIAN_POINT('Ctrl Pts',(96.3417247429082,-1.17272826537954,-4.95859845079308));
#27566=CARTESIAN_POINT('Ctrl Pts',(96.266325107793,-1.16197860683751,-4.96418636160127));
#27567=CARTESIAN_POINT('Ctrl Pts',(96.2385503432698,-1.15699510534415,-4.96625232789598));
#27568=CARTESIAN_POINT('Ctrl Pts',(96.1771190299253,-1.14367896115836,-4.97080975736508));
#27569=CARTESIAN_POINT('Ctrl Pts',(96.1435941925275,-1.13484748863921,-4.97328875617494));
#27570=CARTESIAN_POINT('Ctrl Pts',(96.1047153041129,-1.12274780286211,-4.97611889990995));
#27571=CARTESIAN_POINT('Ctrl Pts',(96.0989399558145,-1.12090139487028,-4.97653811545212));
#27572=CARTESIAN_POINT('Ctrl Pts',(96.0895439912383,-1.11781728029376,-4.97721790299206));
#27573=CARTESIAN_POINT('Ctrl Pts',(96.0859147786827,-1.11660641402698,-4.97747992476473));
#27574=CARTESIAN_POINT('Ctrl Pts',(96.0794105199354,-1.11440102486579,-4.97794845418759));
#27575=CARTESIAN_POINT('Ctrl Pts',(96.0765333766969,-1.11341303139861,-4.97815532558996));
#27576=CARTESIAN_POINT('Ctrl Pts',(96.0702014500086,-1.11121122318567,-4.97860975893374));
#27577=CARTESIAN_POINT('Ctrl Pts',(96.0667484824984,-1.10999243943222,-4.97885702923968));
#27578=CARTESIAN_POINT('Ctrl Pts',(96.0567500249524,-1.10641078635289,-4.97957160168267));
#27579=CARTESIAN_POINT('Ctrl Pts',(96.0502195851766,-1.10400593581433,-4.98003654157876));
#27580=CARTESIAN_POINT('Ctrl Pts',(95.9948776583237,-1.08306724738804,-4.9839645841931));
#27581=CARTESIAN_POINT('Ctrl Pts',(95.9473204222118,-1.0613617790898,-4.98726110046474));
#27582=CARTESIAN_POINT('Ctrl Pts',(95.8281131971778,-0.997061343697797,
-4.99569792028873));
#27583=CARTESIAN_POINT('Ctrl Pts',(95.7592678105945,-0.9499052788285,-5.00076195123938));
#27584=CARTESIAN_POINT('Ctrl Pts',(95.6725536163826,-0.875906966767105,
-5.00803313694736));
#27585=CARTESIAN_POINT('Ctrl Pts',(95.6499337088355,-0.855017784576169,
-5.0100244756171));
#27586=CARTESIAN_POINT('Ctrl Pts',(95.6213888251713,-0.826505318896142,
-5.01268340277329));
#27587=CARTESIAN_POINT('Ctrl Pts',(95.6147012565486,-0.819660501294488,
-5.0133174869601));
#27588=CARTESIAN_POINT('Ctrl Pts',(95.6039933897057,-0.808430270196311,
-5.01435152675391));
#27589=CARTESIAN_POINT('Ctrl Pts',(95.5999215175054,-0.804094461901574,
-5.01474926867878));
#27590=CARTESIAN_POINT('Ctrl Pts',(95.5921601906039,-0.795703572831049,
-5.01551628500619));
#27591=CARTESIAN_POINT('Ctrl Pts',(95.5884658556924,-0.791653200949639,
-5.01588534000642));
#27592=CARTESIAN_POINT('Ctrl Pts',(95.5799802362742,-0.782218322710378,
-5.01674236526036));
#27593=CARTESIAN_POINT('Ctrl Pts',(95.5752098756405,-0.776815378429923,
-5.01723118327001));
#27594=CARTESIAN_POINT('Ctrl Pts',(95.5601584581916,-0.759449330161668,
-5.01879637431942));
#27595=CARTESIAN_POINT('Ctrl Pts',(95.550068384301,-0.747323753659946,-5.01988039097897));
#27596=CARTESIAN_POINT('Ctrl Pts',(95.5269154244496,-0.718335112006344,
-5.02245271275015));
#27597=CARTESIAN_POINT('Ctrl Pts',(95.5140614568668,-0.70131303199242,-5.02394851269682));
#27598=CARTESIAN_POINT('Ctrl Pts',(95.467181882569,-0.635594549512398,-5.02966955841261));
#27599=CARTESIAN_POINT('Ctrl Pts',(95.4363978618898,-0.584701522818449,
-5.03399738009116));
#27600=CARTESIAN_POINT('Ctrl Pts',(95.3778184412167,-0.468922585421363,
-5.04351618725935));
#27601=CARTESIAN_POINT('Ctrl Pts',(95.3517386823039,-0.403409055696163,
-5.04870181968));
#27602=CARTESIAN_POINT('Ctrl Pts',(95.328858353833,-0.326530297693514,-5.05432377948637));
#27603=CARTESIAN_POINT('Ctrl Pts',(95.3261717160383,-0.317071463481642,
-5.05500759914016));
#27604=CARTESIAN_POINT('Ctrl Pts',(95.3225880496707,-0.303825503523244,
-5.05595321532764));
#27605=CARTESIAN_POINT('Ctrl Pts',(95.3215909393134,-0.300066215765981,
-5.05622024740033));
#27606=CARTESIAN_POINT('Ctrl Pts',(95.3198967759879,-0.293548799547081,
-5.05668079891315));
#27607=CARTESIAN_POINT('Ctrl Pts',(95.3191910677639,-0.290792986276538,
-5.05687479788204));
#27608=CARTESIAN_POINT('Ctrl Pts',(95.3177159722246,-0.284944599169217,
-5.05728489616348));
#27609=CARTESIAN_POINT('Ctrl Pts',(95.3169491375731,-0.281851403239069,
-5.05750084454948));
#27610=CARTESIAN_POINT('Ctrl Pts',(95.3150651976784,-0.274117854075262,
-5.05803846774445));
#27611=CARTESIAN_POINT('Ctrl Pts',(95.3139637127855,-0.269473691315058,
-5.05835927056009));
#27612=CARTESIAN_POINT('Ctrl Pts',(95.309838244532,-0.251596276689614,-5.05958675967539));
#27613=CARTESIAN_POINT('Ctrl Pts',(95.3070147527344,-0.23831721032918,-5.06048292862793));
#27614=CARTESIAN_POINT('Ctrl Pts',(95.3002854599901,-0.203740526996326,
-5.0627831311805));
#27615=CARTESIAN_POINT('Ctrl Pts',(95.2967360834668,-0.182378117106677,
-5.06417177354963));
#27616=CARTESIAN_POINT('Ctrl Pts',(95.2797914601859,-0.0595327570435999,
-5.07203356250995));
#27617=CARTESIAN_POINT('Ctrl Pts',(95.279082211168,0.0432546870418731,-5.07817041039214));
#27618=CARTESIAN_POINT('Ctrl Pts',(95.2956597998526,0.177026458367084,-5.08675225369376));
#27619=CARTESIAN_POINT('Ctrl Pts',(95.3009751395235,0.209027891472727,-5.08884722088288));
#27620=CARTESIAN_POINT('Ctrl Pts',(95.309596302135,0.250309024981939,-5.09162537709721));
#27621=CARTESIAN_POINT('Ctrl Pts',(95.3117073495849,0.259825491994906,-5.09227107727238));
#27622=CARTESIAN_POINT('Ctrl Pts',(95.3153052491891,0.275142728474053,-5.0933193761027));
#27623=CARTESIAN_POINT('Ctrl Pts',(95.3167186704959,0.280960410919459,-5.09371964455285));
#27624=CARTESIAN_POINT('Ctrl Pts',(95.3195083690748,0.29207286723613,-5.09448836948864));
#27625=CARTESIAN_POINT('Ctrl Pts',(95.3208773057176,0.29736933669096,-5.09485658334345));
#27626=CARTESIAN_POINT('Ctrl Pts',(95.3241137182056,0.309540507290239,-5.09570702377823));
#27627=CARTESIAN_POINT('Ctrl Pts',(95.3260067529637,0.316408128132529,-5.09619005615569));
#27628=CARTESIAN_POINT('Ctrl Pts',(95.3321653903272,0.337984619261349,-5.09771787620785));
#27629=CARTESIAN_POINT('Ctrl Pts',(95.3366555047764,0.35262719047301,-5.0987698017193));
#27630=CARTESIAN_POINT('Ctrl Pts',(95.3478280874545,0.386678007584853,-5.10125267787087));
#27631=CARTESIAN_POINT('Ctrl Pts',(95.3547347764921,0.406006879533665,-5.1026904347257));
#27632=CARTESIAN_POINT('Ctrl Pts',(95.3822010244374,0.47696448555228,-5.10807517442894));
#27633=CARTESIAN_POINT('Ctrl Pts',(95.4058995232217,0.52729451275876,-5.1121118988069));
#27634=CARTESIAN_POINT('Ctrl Pts',(95.4702810301025,0.642181114430442,-5.12176407325156));
#27635=CARTESIAN_POINT('Ctrl Pts',(95.5138597117022,0.704842250797179,-5.12739348410932));
#27636=CARTESIAN_POINT('Ctrl Pts',(95.5693374635881,0.770096446118507,-5.13339244988422));
#27637=CARTESIAN_POINT('Ctrl Pts',(95.5755762408864,0.777257305993525,-5.13405260663785));
#27638=CARTESIAN_POINT('Ctrl Pts',(95.5844653436938,0.787214421423958,-5.13497223138542));
#27639=CARTESIAN_POINT('Ctrl Pts',(95.5870436070076,0.79007410835775,-5.13523654651609));
#27640=CARTESIAN_POINT('Ctrl Pts',(95.5917342609425,0.795225733827696,-5.13571297996965));
#27641=CARTESIAN_POINT('Ctrl Pts',(95.593841810491,0.797522024882389,-5.13592544706737));
#27642=CARTESIAN_POINT('Ctrl Pts',(95.5981784369695,0.802209527021386,-5.13635932435101));
#27643=CARTESIAN_POINT('Ctrl Pts',(95.6004083914253,0.804599865689834,-5.13658066591109));
#27644=CARTESIAN_POINT('Ctrl Pts',(95.6061787964826,0.810733891514326,-5.13714899931682));
#27645=CARTESIAN_POINT('Ctrl Pts',(95.6097339605441,0.814463734438341,-5.1374949007123));
#27646=CARTESIAN_POINT('Ctrl Pts',(95.6249205423656,0.830188551318374,-5.13895520616683));
#27647=CARTESIAN_POINT('Ctrl Pts',(95.6367826798277,0.841959295319741,-5.14005331342416));
#27648=CARTESIAN_POINT('Ctrl Pts',(95.6700492244388,0.873593239648491,-5.14303235507286));
#27649=CARTESIAN_POINT('Ctrl Pts',(95.69194876966,0.892919922577796,-5.14488416526939));
#27650=CARTESIAN_POINT('Ctrl Pts',(95.7786842299896,0.963907493491577,-5.15191236718003));
#27651=CARTESIAN_POINT('Ctrl Pts',(95.8481569370433,1.00946156563831,-5.15693593302965));
#27652=CARTESIAN_POINT('Ctrl Pts',(95.9218017437159,1.04733937941473,-5.16217169173788));
#27653=CARTESIAN_POINT('Origin',(96.460480949577,-7.19464945638997E-16,
0.924367114736168));
#27654=CARTESIAN_POINT('',(95.921801673071,1.04733934307987,-5.76048914482438));
#27655=CARTESIAN_POINT('',(95.9218018640415,1.0473394413019,-5.66223110129989));
#27656=CARTESIAN_POINT('',(95.9218016730721,1.04733934308042,0.924367114736168));
#27657=CARTESIAN_POINT('Ctrl Pts',(95.921801673071,1.04733934307989,-5.76048914482438));
#27658=CARTESIAN_POINT('Ctrl Pts',(95.9182792703783,1.04552766155889,-5.76021575466029));
#27659=CARTESIAN_POINT('Ctrl Pts',(95.9147659592519,1.04369818558514,-5.75994336455603));
#27660=CARTESIAN_POINT('Ctrl Pts',(95.9083340398797,1.04030755404686,-5.75944532432093));
#27661=CARTESIAN_POINT('Ctrl Pts',(95.9054126772423,1.03875176564439,-5.7592193566938));
#27662=CARTESIAN_POINT('Ctrl Pts',(95.8997741700574,1.03571836688476,-5.75878374118157));
#27663=CARTESIAN_POINT('Ctrl Pts',(95.8970562448979,1.03424234612522,-5.75857400405198));
#27664=CARTESIAN_POINT('Ctrl Pts',(95.8910507559638,1.03095025235945,-5.75811104399781));
#27665=CARTESIAN_POINT('Ctrl Pts',(95.8877659703997,1.02912910843476,-5.75785813547155));
#27666=CARTESIAN_POINT('Ctrl Pts',(95.8761075000208,1.02259233701673,-5.75696141955584));
#27667=CARTESIAN_POINT('Ctrl Pts',(95.8677826103802,1.01778981600199,-5.75632279569602));
#27668=CARTESIAN_POINT('Ctrl Pts',(95.7920261476623,0.972842106316879,-5.75051808766608));
#27669=CARTESIAN_POINT('Ctrl Pts',(95.7286961979165,0.926147007071749,-5.74570644331157));
#27670=CARTESIAN_POINT('Ctrl Pts',(95.630418325696,0.837262388101087,-5.73750754102063));
#27671=CARTESIAN_POINT('Ctrl Pts',(95.5929021564932,0.798322417069381,-5.73415567233252));
#27672=CARTESIAN_POINT('Ctrl Pts',(95.5452201168959,0.741485039964303,-5.72941832147816));
#27673=CARTESIAN_POINT('Ctrl Pts',(95.5326479713191,0.725691635990643,-5.72811725936082));
#27674=CARTESIAN_POINT('Ctrl Pts',(95.5113789973254,0.69751641219175,-5.7258153715045));
#27675=CARTESIAN_POINT('Ctrl Pts',(95.5025032228997,0.685275347883298,-5.72482134574947));
#27676=CARTESIAN_POINT('Ctrl Pts',(95.489816379428,0.667049919035916,-5.72334821345533));
#27677=CARTESIAN_POINT('Ctrl Pts',(95.4858195670488,0.661196255253561,-5.72287608700587));
#27678=CARTESIAN_POINT('Ctrl Pts',(95.4788344687226,0.650765033421525,-5.72203635217434));
#27679=CARTESIAN_POINT('Ctrl Pts',(95.4758247319586,0.646202037667464,-5.72166955395892));
#27680=CARTESIAN_POINT('Ctrl Pts',(95.4695753175003,0.636582402064186,-5.72089729611531));
#27681=CARTESIAN_POINT('Ctrl Pts',(95.4663423419096,0.631521617002292,-5.72049160379644));
#27682=CARTESIAN_POINT('Ctrl Pts',(95.4579195315733,0.618111885446169,-5.7194180284362));
#27683=CARTESIAN_POINT('Ctrl Pts',(95.4527953726369,0.609722451338708,-5.71874778904177));
#27684=CARTESIAN_POINT('Ctrl Pts',(95.430850584584,0.57276139946719,-5.71580033007014));
#27685=CARTESIAN_POINT('Ctrl Pts',(95.415137157913,0.543553394594989,-5.71348445856564));
#27686=CARTESIAN_POINT('Ctrl Pts',(95.3563772424238,0.422332742654527,-5.70392025898488));
#27687=CARTESIAN_POINT('Ctrl Pts',(95.3240872874809,0.325598630340479,-5.69634748999376));
#27688=CARTESIAN_POINT('Ctrl Pts',(95.300464323838,0.204750875911249,-5.68744238117124));
#27689=CARTESIAN_POINT('Ctrl Pts',(95.2969045661051,0.18344374177579,-5.68589462020311));
#27690=CARTESIAN_POINT('Ctrl Pts',(95.2920681372671,0.148627673997437,-5.68341332514271));
#27691=CARTESIAN_POINT('Ctrl Pts',(95.2904353332735,0.135173890054132,-5.68246601490637));
#27692=CARTESIAN_POINT('Ctrl Pts',(95.2885421434898,0.116949775552905,-5.68120094494768));
#27693=CARTESIAN_POINT('Ctrl Pts',(95.288078089193,0.112202273345499,-5.68087304481481));
#27694=CARTESIAN_POINT('Ctrl Pts',(95.2873521747314,0.10427891907399,-5.68032870412396));
#27695=CARTESIAN_POINT('Ctrl Pts',(95.287074341012,0.101104634078135,-5.68011140601076));
#27696=CARTESIAN_POINT('Ctrl Pts',(95.2865727868972,0.0950935589645371,
-5.67970143388091));
#27697=CARTESIAN_POINT('Ctrl Pts',(95.286346459544,0.0922570274612839,-5.67950861355182));
#27698=CARTESIAN_POINT('Ctrl Pts',(95.2858349315525,0.0855391184827548,
-5.67905340038521));
#27699=CARTESIAN_POINT('Ctrl Pts',(95.2855586825128,0.0816570626192244,
-5.67879149581972));
#27700=CARTESIAN_POINT('Ctrl Pts',(95.2846586381988,0.0680571666291416,
-5.67787776797413));
#27701=CARTESIAN_POINT('Ctrl Pts',(95.2841361036617,0.0583327044476577,
-5.67723119768886));
#27702=CARTESIAN_POINT('Ctrl Pts',(95.2807707702813,-0.0231475728569918,
-5.67186202260817));
#27703=CARTESIAN_POINT('Ctrl Pts',(95.2843753718439,-0.095028845834061,
-5.66743346157478));
#27704=CARTESIAN_POINT('Ctrl Pts',(95.3027482586768,-0.223968492128474,
-5.65937737689349));
#27705=CARTESIAN_POINT('Ctrl Pts',(95.3152778584639,-0.281098013369817,
-5.65576623500236));
#27706=CARTESIAN_POINT('Ctrl Pts',(95.3380386338425,-0.357301815401976,
-5.6506962472904));
#27707=CARTESIAN_POINT('Ctrl Pts',(95.3446276939245,-0.377376167546177,
-5.64933642128387));
#27708=CARTESIAN_POINT('Ctrl Pts',(95.3570346614309,-0.412003109071487,
-5.64694012448366));
#27709=CARTESIAN_POINT('Ctrl Pts',(95.3626098538399,-0.426637190606166,
-5.64591127443769));
#27710=CARTESIAN_POINT('Ctrl Pts',(95.3711670526367,-0.44781910534316,-5.64439624875106));
#27711=CARTESIAN_POINT('Ctrl Pts',(95.3739200557026,-0.454458069850465,
-5.64391764568959));
#27712=CARTESIAN_POINT('Ctrl Pts',(95.3788787941259,-0.466113576535248,
-5.64307055663204));
#27713=CARTESIAN_POINT('Ctrl Pts',(95.3810591206591,-0.471140745884402,
-5.64270293058108));
#27714=CARTESIAN_POINT('Ctrl Pts',(95.3856832030918,-0.481601874131068,
-5.64193309564437));
#27715=CARTESIAN_POINT('Ctrl Pts',(95.3881332660104,-0.487032857533316,
-5.64153068200183));
#27716=CARTESIAN_POINT('Ctrl Pts',(95.3946441178202,-0.501177946739725,
-5.64047525685493));
#27717=CARTESIAN_POINT('Ctrl Pts',(95.3987705132837,-0.509861183256431,
-5.63982003105973));
#27718=CARTESIAN_POINT('Ctrl Pts',(95.4167347212565,-0.546499615684872,
-5.63702336286759));
#27719=CARTESIAN_POINT('Ctrl Pts',(95.4315727757329,-0.573947450620124,
-5.63484796475069));
#27720=CARTESIAN_POINT('Ctrl Pts',(95.5003974252902,-0.689997021034247,
-5.62529010168684));
#27721=CARTESIAN_POINT('Ctrl Pts',(95.5648682690301,-0.771834586700886,
-5.6175542614041));
#27722=CARTESIAN_POINT('Ctrl Pts',(95.6547827204412,-0.859312490623622,
-5.60848026762067));
#27723=CARTESIAN_POINT('Ctrl Pts',(95.6707809644618,-0.874037551648785,
-5.60692212977617));
#27724=CARTESIAN_POINT('Ctrl Pts',(95.6974466788012,-0.89725085600912,-5.60442615975323));
#27725=CARTESIAN_POINT('Ctrl Pts',(95.7078695679955,-0.906011338315213,
-5.60347436226587));
#27726=CARTESIAN_POINT('Ctrl Pts',(95.7221532384821,-0.917600177844721,
-5.60220431860783));
#27727=CARTESIAN_POINT('Ctrl Pts',(95.7258822842986,-0.92058823493353,-5.60187583249435));
#27728=CARTESIAN_POINT('Ctrl Pts',(95.7321295098562,-0.925531958840676,
-5.60133078601179));
#27729=CARTESIAN_POINT('Ctrl Pts',(95.7346375935797,-0.927500215551443,
-5.60111336355869));
#27730=CARTESIAN_POINT('Ctrl Pts',(95.7393981997716,-0.931205036166788,
-5.60070335906815));
#27731=CARTESIAN_POINT('Ctrl Pts',(95.741649066718,-0.932943661788935,-5.60051062942343));
#27732=CARTESIAN_POINT('Ctrl Pts',(95.7469903425233,-0.937038589629881,
-5.60005588041998));
#27733=CARTESIAN_POINT('Ctrl Pts',(95.7500861831338,-0.939387801540041,
-5.59979434691962));
#27734=CARTESIAN_POINT('Ctrl Pts',(95.7610379419842,-0.947613204065069,
-5.59887609961655));
#27735=CARTESIAN_POINT('Ctrl Pts',(95.7689558551335,-0.953406715171152,
-5.59822473640774));
#27736=CARTESIAN_POINT('Ctrl Pts',(95.8346585394253,-1.00023193802587,-5.59291328236898));
#27737=CARTESIAN_POINT('Ctrl Pts',(95.8959747132288,-1.03607583160094,-5.58853916238241));
#27738=CARTESIAN_POINT('Ctrl Pts',(95.9893717519733,-1.07990423901555,-5.58215750248245));
#27739=CARTESIAN_POINT('Ctrl Pts',(96.0191448159215,-1.0924099011946,-5.58016236542273));
#27740=CARTESIAN_POINT('Ctrl Pts',(96.0841198429742,-1.1166112185005,-5.575833384827));
#27741=CARTESIAN_POINT('Ctrl Pts',(96.1194350390286,-1.12789878028869,-5.57349535293581));
#27742=CARTESIAN_POINT('Ctrl Pts',(96.1705962544478,-1.14162836724377,-5.57008488847906));
#27743=CARTESIAN_POINT('Ctrl Pts',(96.186052376743,-1.14544200520022,-5.56905172734688));
#27744=CARTESIAN_POINT('Ctrl Pts',(96.2138386284544,-1.15170331222544,-5.56718606237049));
#27745=CARTESIAN_POINT('Ctrl Pts',(96.2261397704475,-1.1542690960081,-5.5663572519445));
#27746=CARTESIAN_POINT('Ctrl Pts',(96.2449498724244,-1.15787945351502,-5.56508444074358));
#27747=CARTESIAN_POINT('Ctrl Pts',(96.2514307037255,-1.15906706701358,-5.56464492929147));
#27748=CARTESIAN_POINT('Ctrl Pts',(96.2627433148094,-1.16104214108223,-5.56387589064436));
#27749=CARTESIAN_POINT('Ctrl Pts',(96.2675707187557,-1.16185397842449,-5.56354713586417));
#27750=CARTESIAN_POINT('Ctrl Pts',(96.2784635032953,-1.16361608911865,-5.56280393188108));
#27751=CARTESIAN_POINT('Ctrl Pts',(96.2845314965744,-1.16454907201559,-5.56238895219395));
#27752=CARTESIAN_POINT('Ctrl Pts',(96.3009424486907,-1.16694114365526,-5.56126388603723));
#27753=CARTESIAN_POINT('Ctrl Pts',(96.3112977735901,-1.16831011886119,-5.56055102137778));
#27754=CARTESIAN_POINT('Ctrl Pts',(96.3616154086442,-1.17428225257527,-5.55707191237516));
#27755=CARTESIAN_POINT('Ctrl Pts',(96.4017732889135,-1.17697321977398,-5.55424747332402));
#27756=CARTESIAN_POINT('Ctrl Pts',(96.5255688587743,-1.17891746530055,-5.54539287080836));
#27757=CARTESIAN_POINT('Ctrl Pts',(96.6090494376241,-1.17132736313746,-5.53919640709423));
#27758=CARTESIAN_POINT('Ctrl Pts',(96.7183874491382,-1.14950364492487,-5.53107756824948));
#27759=CARTESIAN_POINT('Ctrl Pts',(96.7455628764944,-1.14306731825633,-5.52906182501057));
#27760=CARTESIAN_POINT('Ctrl Pts',(96.7830066083711,-1.1327803450723,-5.52630803074809));
#27761=CARTESIAN_POINT('Ctrl Pts',(96.7934874546576,-1.12974368657491,-5.52553986236412));
#27762=CARTESIAN_POINT('Ctrl Pts',(96.8117049614386,-1.1241898902565,-5.52421099644646));
#27763=CARTESIAN_POINT('Ctrl Pts',(96.8194604244305,-1.12173747448683,-5.52364730690342));
#27764=CARTESIAN_POINT('Ctrl Pts',(96.830894466228,-1.11799109320917,-5.52281987989255));
#27765=CARTESIAN_POINT('Ctrl Pts',(96.8345928285508,-1.11675895381272,-5.52255281307399));
#27766=CARTESIAN_POINT('Ctrl Pts',(96.8411704705455,-1.11453121609244,-5.52207892117662));
#27767=CARTESIAN_POINT('Ctrl Pts',(96.8440520716712,-1.11354278679734,-5.5218716945255));
#27768=CARTESIAN_POINT('Ctrl Pts',(96.8503345082934,-1.11136054235327,-5.52142074201043));
#27769=CARTESIAN_POINT('Ctrl Pts',(96.8537337158952,-1.11016229218871,-5.52117727638184));
#27770=CARTESIAN_POINT('Ctrl Pts',(96.8632466959516,-1.10675970835665,-5.52049725960169));
#27771=CARTESIAN_POINT('Ctrl Pts',(96.8693479162596,-1.10452030619149,-5.52006268610357));
#27772=CARTESIAN_POINT('Ctrl Pts',(96.9053012610343,-1.09098518504615,-5.51750931701474));
#27773=CARTESIAN_POINT('Ctrl Pts',(96.9347056582239,-1.07852914466909,-5.51545158913015));
#27774=CARTESIAN_POINT('Ctrl Pts',(97.0484599631954,-1.02478796095945,-5.50747684340306));
#27775=CARTESIAN_POINT('Ctrl Pts',(97.1282516015357,-0.974676283019627,
-5.50182500432036));
#27776=CARTESIAN_POINT('Ctrl Pts',(97.2324486018821,-0.890377193533662,
-5.49335376062515));
#27777=CARTESIAN_POINT('Ctrl Pts',(97.2623345652234,-0.863559988907316,
-5.49077574323717));
#27778=CARTESIAN_POINT('Ctrl Pts',(97.2979235537985,-0.828182392055194,
-5.48747220191942));
#27779=CARTESIAN_POINT('Ctrl Pts',(97.3049642361021,-0.821001923493989,
-5.48680640957296));
#27780=CARTESIAN_POINT('Ctrl Pts',(97.3160951657908,-0.809355319620759,
-5.48573340927773));
#27781=CARTESIAN_POINT('Ctrl Pts',(97.3202445181321,-0.804946162335179,
-5.48532873850814));
#27782=CARTESIAN_POINT('Ctrl Pts',(97.3280670439595,-0.796504352581008,
-5.48455674466188));
#27783=CARTESIAN_POINT('Ctrl Pts',(97.3317465694028,-0.792477780660205,
-5.48418970310066));
#27784=CARTESIAN_POINT('Ctrl Pts',(97.3400798211692,-0.78323036248578,-5.48334934717114));
#27785=CARTESIAN_POINT('Ctrl Pts',(97.3447152422995,-0.777993372432849,
-5.48287529192542));
#27786=CARTESIAN_POINT('Ctrl Pts',(97.3588940316143,-0.761684097040048,
-5.48140442817136));
#27787=CARTESIAN_POINT('Ctrl Pts',(97.3682778079847,-0.750475556050734,
-5.48040121905146));
#27788=CARTESIAN_POINT('Ctrl Pts',(97.436473413914,-0.665867739332167,-5.47288111427207));
#27789=CARTESIAN_POINT('Ctrl Pts',(97.4865016509802,-0.585846323151347,
-5.46601669660043));
#27790=CARTESIAN_POINT('Ctrl Pts',(97.5339384633548,-0.484862985224618,
-5.45783004902265));
#27791=CARTESIAN_POINT('Ctrl Pts',(97.5410453059725,-0.468811087128935,
-5.45654325510106));
#27792=CARTESIAN_POINT('Ctrl Pts',(97.5598981192014,-0.423520388132378,
-5.45296097173667));
#27793=CARTESIAN_POINT('Ctrl Pts',(97.5708343322387,-0.393958456902307,
-5.45067781824604));
#27794=CARTESIAN_POINT('Ctrl Pts',(97.5860054142911,-0.347273325861935,
-5.44718901233288));
#27795=CARTESIAN_POINT('Ctrl Pts',(97.5910637033339,-0.330434262781404,
-5.44595372779672));
#27796=CARTESIAN_POINT('Ctrl Pts',(97.5971398660988,-0.308430048561292,
-5.4443746873436));
#27797=CARTESIAN_POINT('Ctrl Pts',(97.5985025546664,-0.303363505224976,
-5.44401350535972));
#27798=CARTESIAN_POINT('Ctrl Pts',(97.6006645749986,-0.295105380370486,
-5.44342888241791));
#27799=CARTESIAN_POINT('Ctrl Pts',(97.6014844520393,-0.291919326607394,
-5.44320431402822));
#27800=CARTESIAN_POINT('Ctrl Pts',(97.6030519666137,-0.28572043865021,-5.4427693524694));
#27801=CARTESIAN_POINT('Ctrl Pts',(97.6038010562302,-0.282708033228517,
-5.44255888327028));
#27802=CARTESIAN_POINT('Ctrl Pts',(97.605610563367,-0.275306409867426,-5.44204389264466));
#27803=CARTESIAN_POINT('Ctrl Pts',(97.6066576801282,-0.270913926734831,
-5.44174011582839));
#27804=CARTESIAN_POINT('Ctrl Pts',(97.6096044133528,-0.258229903016054,
-5.44086793137785));
#27805=CARTESIAN_POINT('Ctrl Pts',(97.6114395452146,-0.249923466283105,
-5.4403029308484));
#27806=CARTESIAN_POINT('Ctrl Pts',(97.6297635801912,-0.162496345475907,
-5.43441381042546));
#27807=CARTESIAN_POINT('Ctrl Pts',(97.6381589362903,-0.0818864593552734,
-5.42946830519488));
#27808=CARTESIAN_POINT('Ctrl Pts',(97.6382994290975,0.0768514002990383,
-5.41964384216038));
#27809=CARTESIAN_POINT('Ctrl Pts',(97.6306411435783,0.154548747557045,-5.41478873483599));
#27810=CARTESIAN_POINT('Ctrl Pts',(97.6133286927285,0.241134252189176,-5.40899400712145));
#27811=CARTESIAN_POINT('Ctrl Pts',(97.6111501544426,0.251324523573465,-5.40830616440694));
#27812=CARTESIAN_POINT('Ctrl Pts',(97.6073414308672,0.26805122568323,-5.40716677634204));
#27813=CARTESIAN_POINT('Ctrl Pts',(97.60578984222,0.274605099016429,-5.40671771070679));
#27814=CARTESIAN_POINT('Ctrl Pts',(97.6028860716366,0.286417664239892,-5.40590339921509));
#27815=CARTESIAN_POINT('Ctrl Pts',(97.601553565,0.291681034595023,-5.4055387876645));
#27816=CARTESIAN_POINT('Ctrl Pts',(97.598617359946,0.302950857302568,-5.40475418342152));
#27817=CARTESIAN_POINT('Ctrl Pts',(97.5970024068985,0.308954179512459,-5.40433384099797));
#27818=CARTESIAN_POINT('Ctrl Pts',(97.5924512798941,0.325353546610647,-5.40317887652352));
#27819=CARTESIAN_POINT('Ctrl Pts',(97.5894195419895,0.335722206733086,-5.40244121817134));
#27820=CARTESIAN_POINT('Ctrl Pts',(97.5707633930291,0.396414569854131,-5.39807833650425));
#27821=CARTESIAN_POINT('Ctrl Pts',(97.5519207142527,0.44567862147027,-5.39434985427729));
#27822=CARTESIAN_POINT('Ctrl Pts',(97.4960200978936,0.566807208304178,-5.38471244433334));
#27823=CARTESIAN_POINT('Ctrl Pts',(97.4547501518101,0.636427082316978,-5.37871355981902));
#27824=CARTESIAN_POINT('Ctrl Pts',(97.3881225908172,0.726325048281785,-5.37062514353316));
#27825=CARTESIAN_POINT('Ctrl Pts',(97.3685692265334,0.750628503650095,-5.36840156045603));
#27826=CARTESIAN_POINT('Ctrl Pts',(97.3438262925529,0.778997946605039,-5.36578658686824));
#27827=CARTESIAN_POINT('Ctrl Pts',(97.3395399745868,0.783831634365499,-5.36534033699336));
#27828=CARTESIAN_POINT('Ctrl Pts',(97.3328064593485,0.791300318824106,-5.3646500522102));
#27829=CARTESIAN_POINT('Ctrl Pts',(97.3303866815795,0.7939597016652,-5.36440410748264));
#27830=CARTESIAN_POINT('Ctrl Pts',(97.325893600454,0.798852484575092,-5.36395139596623));
#27831=CARTESIAN_POINT('Ctrl Pts',(97.3238238103004,0.801088917421071,-5.363744389655));
#27832=CARTESIAN_POINT('Ctrl Pts',(97.3190785226344,0.806176504433217,-5.36327327255492));
#27833=CARTESIAN_POINT('Ctrl Pts',(97.3163974895489,0.809022389345375,-5.36300958313007));
#27834=CARTESIAN_POINT('Ctrl Pts',(97.308054015397,0.817790988240682,-5.36219642777955));
#27835=CARTESIAN_POINT('Ctrl Pts',(97.3023437559443,0.823668153348542,-5.36165042765428));
#27836=CARTESIAN_POINT('Ctrl Pts',(97.288814036332,0.837305623865464,-5.36037975620669));
#27837=CARTESIAN_POINT('Ctrl Pts',(97.2809460012071,0.845016880650662,-5.35965835878946));
#27838=CARTESIAN_POINT('Ctrl Pts',(97.2524648315658,0.872157623555244,-5.35710365577217));
#27839=CARTESIAN_POINT('Ctrl Pts',(97.2312592988316,0.890953617489837,-5.35530492022628));
#27840=CARTESIAN_POINT('Ctrl Pts',(97.1430395633735,0.963639379116592,-5.34812958377198));
#27841=CARTESIAN_POINT('Ctrl Pts',(97.0708978518712,1.01088024767369,-5.34292399197283));
#27842=CARTESIAN_POINT('Ctrl Pts',(96.9607245276159,1.0668956568461,-5.33509787021397));
#27843=CARTESIAN_POINT('Ctrl Pts',(96.9263997047152,1.08232585333287,-5.33267840654164));
#27844=CARTESIAN_POINT('Ctrl Pts',(96.8818677017838,1.09983322899141,-5.32952959915147));
#27845=CARTESIAN_POINT('Ctrl Pts',(96.8722892319809,1.10345541561006,-5.32885182274335));
#27846=CARTESIAN_POINT('Ctrl Pts',(96.8569366488752,1.10903340188167,-5.32776409832691));
#27847=CARTESIAN_POINT('Ctrl Pts',(96.8511923325133,1.11107012419607,-5.32735681445409));
#27848=CARTESIAN_POINT('Ctrl Pts',(96.840799922149,1.114664330606,-5.32661931059646));
#27849=CARTESIAN_POINT('Ctrl Pts',(96.8361573912865,1.11623756464453,-5.326289614486));
#27850=CARTESIAN_POINT('Ctrl Pts',(96.8251908348327,1.11987768379753,-5.32551018268503));
#27851=CARTESIAN_POINT('Ctrl Pts',(96.8188589037513,1.12192003542727,-5.32505966150492));
#27852=CARTESIAN_POINT('Ctrl Pts',(96.8002177201358,1.12775880240779,-5.32373171085577));
#27853=CARTESIAN_POINT('Ctrl Pts',(96.7878634256494,1.1314069476608,-5.32284955112851));
#27854=CARTESIAN_POINT('Ctrl Pts',(96.7596209580207,1.13924547484234,-5.32082746164635));
#27855=CARTESIAN_POINT('Ctrl Pts',(96.7437002266553,1.14330739159579,-5.31968369510516));
#27856=CARTESIAN_POINT('Ctrl Pts',(96.6898312963472,1.15585698978664,-5.31579983411951));
#27857=CARTESIAN_POINT('Ctrl Pts',(96.6515520616501,1.16279760964249,-5.3130160256141));
#27858=CARTESIAN_POINT('Ctrl Pts',(96.5416988677981,1.17714472093669,-5.30498036705704));
#27859=CARTESIAN_POINT('Ctrl Pts',(96.4696951751851,1.17990704433475,-5.29964893226738));
#27860=CARTESIAN_POINT('Ctrl Pts',(96.3644121172927,1.17430398017979,-5.29201178424458));
#27861=CARTESIAN_POINT('Ctrl Pts',(96.331021232215,1.17109337628063,-5.28961545520223));
#27862=CARTESIAN_POINT('Ctrl Pts',(96.2918498230298,1.16563065230088,-5.28686688124989));
#27863=CARTESIAN_POINT('Ctrl Pts',(96.2858961654597,1.16475380719038,-5.28645085604166));
#27864=CARTESIAN_POINT('Ctrl Pts',(96.2761821506405,1.16324698511417,-5.28577517633201));
#27865=CARTESIAN_POINT('Ctrl Pts',(96.2724177571025,1.16264432752759,-5.28551410035349));
#27866=CARTESIAN_POINT('Ctrl Pts',(96.2656551243243,1.16152796469055,-5.28504653959556));
#27867=CARTESIAN_POINT('Ctrl Pts',(96.2626559005756,1.16102091521025,-5.28483969832842));
#27868=CARTESIAN_POINT('Ctrl Pts',(96.2560383190335,1.15987575711783,-5.2843844692746));
#27869=CARTESIAN_POINT('Ctrl Pts',(96.2524209652957,1.15923233434639,-5.2841363796478));
#27870=CARTESIAN_POINT('Ctrl Pts',(96.2419036282824,1.15731078757132,-5.2834170984713));
#27871=CARTESIAN_POINT('Ctrl Pts',(96.235011838196,1.15598788494674,-5.2829483169619));
#27872=CARTESIAN_POINT('Ctrl Pts',(96.1734638051566,1.14360214650284,-5.27878128716008));
#27873=CARTESIAN_POINT('Ctrl Pts',(96.1196379030029,1.12873046166619,-5.27527322457391));
#27874=CARTESIAN_POINT('Ctrl Pts',(96.0172455471707,1.09244260747017,-5.26851957117317));
#27875=CARTESIAN_POINT('Ctrl Pts',(95.9687186069067,1.07147020317641,-5.26527965674562));
#27876=CARTESIAN_POINT('Ctrl Pts',(95.921801349668,1.04733917674357,-5.26198394263684));
#27877=CARTESIAN_POINT('',(97.6382308590426,0.000461794101737356,-5.32468518566653));
#27878=CARTESIAN_POINT('Ctrl Pts',(95.9218017437159,1.04733937941473,-5.16217169173788));
#27879=CARTESIAN_POINT('Ctrl Pts',(95.9325114231549,1.05284770052691,-5.16293309366042));
#27880=CARTESIAN_POINT('Ctrl Pts',(95.9433093591508,1.05819369090224,-5.16369858274992));
#27881=CARTESIAN_POINT('Ctrl Pts',(95.980440187364,1.07587223909229,-5.16632690890821));
#27882=CARTESIAN_POINT('Ctrl Pts',(96.0071401828503,1.08739235765067,-5.16821049507675));
#27883=CARTESIAN_POINT('Ctrl Pts',(96.0429821275043,1.10130731070932,-5.17074547651919));
#27884=CARTESIAN_POINT('Ctrl Pts',(96.0517669104993,1.10459761222691,-5.17136726210828));
#27885=CARTESIAN_POINT('Ctrl Pts',(96.0661459615139,1.10978821073429,-5.17238621639936));
#27886=CARTESIAN_POINT('Ctrl Pts',(96.0717169906452,1.11175201262678,-5.17278129224412));
#27887=CARTESIAN_POINT('Ctrl Pts',(96.08249975661,1.11546200730409,-5.17354663900523));
#27888=CARTESIAN_POINT('Ctrl Pts',(96.0877094180057,1.11721379129877,-5.17391671576547));
#27889=CARTESIAN_POINT('Ctrl Pts',(96.0998698778694,1.12120830338109,-5.17478135081686));
#27890=CARTESIAN_POINT('Ctrl Pts',(96.1068295928854,1.12342294722857,-5.17527680526923));
#27891=CARTESIAN_POINT('Ctrl Pts',(96.129397858974,1.13037387781512,-5.17688562150878));
#27892=CARTESIAN_POINT('Ctrl Pts',(96.1450837378275,1.13485050521425,-5.17800724002358));
#27893=CARTESIAN_POINT('Ctrl Pts',(96.1824060124109,1.14466846368908,-5.18068535063957));
#27894=CARTESIAN_POINT('Ctrl Pts',(96.2041104000099,1.14972413773879,-5.18225020093183));
#27895=CARTESIAN_POINT('Ctrl Pts',(96.288938193836,1.16696199047061,-5.1883948937014));
#27896=CARTESIAN_POINT('Ctrl Pts',(96.3528683155052,1.17458292080017,-5.19309491776227));
#27897=CARTESIAN_POINT('Ctrl Pts',(96.4804886117314,1.17928757440343,-5.20246763211301));
#27898=CARTESIAN_POINT('Ctrl Pts',(96.5439754131948,1.17649892969447,-5.20712347759578));
#27899=CARTESIAN_POINT('Ctrl Pts',(96.6168562138963,1.16736534236046,-5.21227396370946));
#27900=CARTESIAN_POINT('Ctrl Pts',(96.6267629389786,1.1659954469632,-5.2129697231798));
#27901=CARTESIAN_POINT('Ctrl Pts',(96.6405427691712,1.16391077529573,-5.21393034287619));
#27902=CARTESIAN_POINT('Ctrl Pts',(96.6444312206168,1.16330256194206,-5.21420061809634));
#27903=CARTESIAN_POINT('Ctrl Pts',(96.6511364027448,1.16221930778189,-5.21466521704936));
#27904=CARTESIAN_POINT('Ctrl Pts',(96.6539545580521,1.16175349557094,-5.2148600400038));
#27905=CARTESIAN_POINT('Ctrl Pts',(96.6598994657244,1.16074863112626,-5.21527003888125));
#27906=CARTESIAN_POINT('Ctrl Pts',(96.6630257858721,1.16020718795231,-5.21548507362493));
#27907=CARTESIAN_POINT('Ctrl Pts',(96.6707833108322,1.15883136088811,-5.21601730513316));
#27908=CARTESIAN_POINT('Ctrl Pts',(96.6754118376694,1.15798183118038,-5.21633366725215));
#27909=CARTESIAN_POINT('Ctrl Pts',(96.6928842217307,1.15466654135741,-5.2175238241673));
#27910=CARTESIAN_POINT('Ctrl Pts',(96.7056923580069,1.1520145410591,-5.21838790381682));
#27911=CARTESIAN_POINT('Ctrl Pts',(96.7385100491239,1.14464727587447,-5.22058653337873));
#27912=CARTESIAN_POINT('Ctrl Pts',(96.7584457068214,1.13962040619926,-5.22190734172225));
#27913=CARTESIAN_POINT('Ctrl Pts',(96.8630663760272,1.11030641302517,-5.22880885995858));
#27914=CARTESIAN_POINT('Ctrl Pts',(96.9449609144002,1.07709625997903,-5.23412641153768));
#27915=CARTESIAN_POINT('Ctrl Pts',(97.0630166444056,1.01300679332722,-5.24256641136791));
#27916=CARTESIAN_POINT('Ctrl Pts',(97.1023053083475,0.98858118792749,-5.24551906601836));
#27917=CARTESIAN_POINT('Ctrl Pts',(97.1488517974383,0.955696953102273,-5.24926420194541));
#27918=CARTESIAN_POINT('Ctrl Pts',(97.1575634536765,0.949361396033293,-5.24997635012737));
#27919=CARTESIAN_POINT('Ctrl Pts',(97.1712083271043,0.939149082161794,-5.25111036606283));
#27920=CARTESIAN_POINT('Ctrl Pts',(97.1761997120439,0.935350765317167,-5.25152922066824));
#27921=CARTESIAN_POINT('Ctrl Pts',(97.1852673607145,0.928335436848108,-5.2522976687945));
#27922=CARTESIAN_POINT('Ctrl Pts',(97.1893531671586,0.925130971288498,-5.25264676651902));
#27923=CARTESIAN_POINT('Ctrl Pts',(97.1935394262451,0.921802775277868,-5.25300742559174));
#27924=CARTESIAN_POINT('Ctrl Pts',(97.1936612390565,0.921705891184178,-5.25301792275109));
#27925=CARTESIAN_POINT('Ctrl Pts',(97.1938925314831,0.92152185736795,-5.25303785922484));
#27926=CARTESIAN_POINT('Ctrl Pts',(97.194002014803,0.92143471225615,-5.25304729835756));
#27927=CARTESIAN_POINT('Ctrl Pts',(97.1942103985456,0.921268784993963,-5.25306526823877));
#27928=CARTESIAN_POINT('Ctrl Pts',(97.1943093017797,0.921190006454349,-5.25307379884187));
#27929=CARTESIAN_POINT('Ctrl Pts',(97.1944979534539,0.921039691702677,-5.25309007372226));
#27930=CARTESIAN_POINT('Ctrl Pts',(97.1945877042653,0.920968158186419,-5.25309781790002));
#27931=CARTESIAN_POINT('Ctrl Pts',(97.194759229824,0.920831407260833,-5.25311262075844));
#27932=CARTESIAN_POINT('Ctrl Pts',(97.1948410062387,0.920766192157478,-5.25311967934184));
#27933=CARTESIAN_POINT('Ctrl Pts',(97.1949975640776,0.920641306196632,-5.25313319499576));
#27934=CARTESIAN_POINT('Ctrl Pts',(97.1950723470267,0.920581637034882,-5.25313965200468));
#27935=CARTESIAN_POINT('Ctrl Pts',(97.1952157427541,0.920467193279049,-5.25315203516747));
#27936=CARTESIAN_POINT('Ctrl Pts',(97.1952843565894,0.920412420195925,-5.25315796125634));
#27937=CARTESIAN_POINT('Ctrl Pts',(97.1954161121977,0.920307218147145,-5.25316934242036));
#27938=CARTESIAN_POINT('Ctrl Pts',(97.1954792549115,0.920256790350043,-5.25317479744935));
#27939=CARTESIAN_POINT('Ctrl Pts',(97.1956006635515,0.920159809048524,-5.25318528755037));
#27940=CARTESIAN_POINT('Ctrl Pts',(97.195658930367,0.920113256411223,-5.25319032259453));
#27941=CARTESIAN_POINT('Ctrl Pts',(97.1957710986809,0.920023621377334,-5.25320001661933));
#27942=CARTESIAN_POINT('Ctrl Pts',(97.1958250007531,0.91998053982756,-5.25320467556288));
#27943=CARTESIAN_POINT('Ctrl Pts',(97.1959288813152,0.919897497711922,-5.2532136553148));
#27944=CARTESIAN_POINT('Ctrl Pts',(97.1959788602175,0.919857537903602,-5.25321797608661));
#27945=CARTESIAN_POINT('Ctrl Pts',(97.2013289860205,0.915579218119432,-5.25368055218572));
#27946=CARTESIAN_POINT('Ctrl Pts',(97.2065923057161,0.911295209390987,-5.25414061265473));
#27947=CARTESIAN_POINT('Ctrl Pts',(97.2176641728282,0.902123194033613,-5.25511917498667));
#27948=CARTESIAN_POINT('Ctrl Pts',(97.2234630506065,0.897224052072272,-5.25563811122635));
#27949=CARTESIAN_POINT('Ctrl Pts',(97.2387430188533,0.884059621304366,-5.25702287318334));
#27950=CARTESIAN_POINT('Ctrl Pts',(97.2481395368949,0.875698116540824,-5.25789255003654));
#27951=CARTESIAN_POINT('Ctrl Pts',(97.2766665918279,0.84948263079792,-5.26058997347246));
#27952=CARTESIAN_POINT('Ctrl Pts',(97.2953364183069,0.831141332368948,-5.26243701815565));
#27953=CARTESIAN_POINT('Ctrl Pts',(97.3454627794579,0.778502882479704,-5.26762876682549));
#27954=CARTESIAN_POINT('Ctrl Pts',(97.3755196509311,0.742942201573209,-5.27101751918493));
#27955=CARTESIAN_POINT('Ctrl Pts',(97.4482753649633,0.645730634051767,-5.27991884891027));
#27956=CARTESIAN_POINT('Ctrl Pts',(97.4873382723476,0.581611364097249,-5.28545317347696));
#27957=CARTESIAN_POINT('Ctrl Pts',(97.5242300271725,0.505593435052069,-5.29137252419021));
#27958=CARTESIAN_POINT('Ctrl Pts',(97.528307182252,0.49692451444722,-5.29203850791343));
#27959=CARTESIAN_POINT('Ctrl Pts',(97.5338801976453,0.484689644019447,-5.29296486162387));
#27960=CARTESIAN_POINT('Ctrl Pts',(97.5354648330367,0.481164886634185,-5.29323016966514));
#27961=CARTESIAN_POINT('Ctrl Pts',(97.5382976439475,0.474779921264936,-5.29370785763682));
#27962=CARTESIAN_POINT('Ctrl Pts',(97.5395518532134,0.471922436451773,-5.29392059211006));
#27963=CARTESIAN_POINT('Ctrl Pts',(97.5420944159229,0.466066541990372,-5.29435436675902));
#27964=CARTESIAN_POINT('Ctrl Pts',(97.5433816878933,0.463067709687528,-5.29457534241328));
#27965=CARTESIAN_POINT('Ctrl Pts',(97.546659349676,0.45534364417822,-5.29514162070483));
#27966=CARTESIAN_POINT('Ctrl Pts',(97.5486314038657,0.450610632768498,-5.29548584793617));
#27967=CARTESIAN_POINT('Ctrl Pts',(97.5568112728848,0.430611730348203,-5.29692933806477));
#27968=CARTESIAN_POINT('Ctrl Pts',(97.5627295750134,0.415228461125412,-5.29801276699189));
#27969=CARTESIAN_POINT('Ctrl Pts',(97.5780322361848,0.372816971000223,-5.30093996531587));
#27970=CARTESIAN_POINT('Ctrl Pts',(97.5867581948483,0.345562102544989,-5.30275582802512));
#27971=CARTESIAN_POINT('Ctrl Pts',(97.6234718630875,0.214645550701067,-5.31128789975765));
#27972=CARTESIAN_POINT('Ctrl Pts',(97.6381887681913,0.107809410902377,-5.31774410507905));
#27973=CARTESIAN_POINT('Ctrl Pts',(97.6382308590426,0.000461794101737356,
-5.32468518566653));
#27974=CARTESIAN_POINT('Ctrl Pts',(97.638230859503,0.000460618401015764,
-5.32468526168717));
#27975=CARTESIAN_POINT('Ctrl Pts',(97.6382378236093,-0.0173458250786842,
-5.32583662409341));
#27976=CARTESIAN_POINT('Ctrl Pts',(97.6378409637853,-0.0351495341057705,
-5.3269987006894));
#27977=CARTESIAN_POINT('Ctrl Pts',(97.6367313540619,-0.0598113954557334,
-5.32862679494736));
#27978=CARTESIAN_POINT('Ctrl Pts',(97.6363618105115,-0.0666829413758868,
-5.32908240637083));
#27979=CARTESIAN_POINT('Ctrl Pts',(97.6356001256255,-0.0788558086913148,
-5.32989321504635));
#27980=CARTESIAN_POINT('Ctrl Pts',(97.6352322688323,-0.0841584982872386,
-5.33024766120918));
#27981=CARTESIAN_POINT('Ctrl Pts',(97.6344302213695,-0.0946872137314863,
-5.33095399399462));
#27982=CARTESIAN_POINT('Ctrl Pts',(97.6339969971204,-0.099913191460944,
-5.33130584291699));
#27983=CARTESIAN_POINT('Ctrl Pts',(97.6329978402688,-0.111061214489211,
-5.33205917212182));
#27984=CARTESIAN_POINT('Ctrl Pts',(97.6324219107043,-0.116982194009348,
-5.33246095289328));
#27985=CARTESIAN_POINT('Ctrl Pts',(97.630802174728,-0.132419567441288,-5.33351297572821));
#27986=CARTESIAN_POINT('Ctrl Pts',(97.6296871666797,-0.14192788445596,-5.33416540616123));
#27987=CARTESIAN_POINT('Ctrl Pts',(97.6244929331619,-0.18199316363182,-5.33693407147658));
#27988=CARTESIAN_POINT('Ctrl Pts',(97.6193310265985,-0.212394929965198,
-5.33908342214081));
#27989=CARTESIAN_POINT('Ctrl Pts',(97.5929021273988,-0.33797105029485,-5.34817017477487));
#27990=CARTESIAN_POINT('Ctrl Pts',(97.5610507856395,-0.430515144994756,
-5.35541367492539));
#27991=CARTESIAN_POINT('Ctrl Pts',(97.5067139889575,-0.541451832904505,
-5.36439309909972));
#27992=CARTESIAN_POINT('Ctrl Pts',(97.4944816094563,-0.564461223123242,
-5.36627019358033));
#27993=CARTESIAN_POINT('Ctrl Pts',(97.4763004907727,-0.596082497040434,
-5.3688537006441));
#27994=CARTESIAN_POINT('Ctrl Pts',(97.4709856868373,-0.60504865614563,-5.36958667748986));
#27995=CARTESIAN_POINT('Ctrl Pts',(97.4614605742922,-0.620641979600681,
-5.37086067588182));
#27996=CARTESIAN_POINT('Ctrl Pts',(97.4573017846765,-0.627299694666744,
-5.37140437779457));
#27997=CARTESIAN_POINT('Ctrl Pts',(97.4510084106993,-0.637153965702715,
-5.37220819786072));
#27998=CARTESIAN_POINT('Ctrl Pts',(97.4489243435179,-0.640382296191599,
-5.37247138468805));
#27999=CARTESIAN_POINT('Ctrl Pts',(97.4453217458339,-0.645903421974288,
-5.3729211532705));
#28000=CARTESIAN_POINT('Ctrl Pts',(97.443810948052,-0.648201156388453,-5.37310822989889));
#28001=CARTESIAN_POINT('Ctrl Pts',(97.4403453926368,-0.653431831299147,
-5.3735338521341));
#28002=CARTESIAN_POINT('Ctrl Pts',(97.4383855073629,-0.656361304166322,
-5.37377205496725));
#28003=CARTESIAN_POINT('Ctrl Pts',(97.4329708054791,-0.664376657797896,
-5.37442346710587));
#28004=CARTESIAN_POINT('Ctrl Pts',(97.429489209423,-0.669444441046857,-5.37483495441179));
#28005=CARTESIAN_POINT('Ctrl Pts',(97.4110385993011,-0.695855448986054,
-5.37697879156716));
#28006=CARTESIAN_POINT('Ctrl Pts',(97.3954024539975,-0.716726354976169,
-5.37867072954338));
#28007=CARTESIAN_POINT('Ctrl Pts',(97.3359828655634,-0.790781217796423,
-5.3847350472745));
#28008=CARTESIAN_POINT('Ctrl Pts',(97.2882486473289,-0.840619167683486,
-5.38894242112025));
#28009=CARTESIAN_POINT('Ctrl Pts',(97.2015819794642,-0.916520606239502,
-5.3960885207993));
#28010=CARTESIAN_POINT('Ctrl Pts',(97.1649674287411,-0.944954525189039,
-5.39898351779418));
#28011=CARTESIAN_POINT('Ctrl Pts',(97.1116203950136,-0.981555032600435,
-5.40312843161472));
#28012=CARTESIAN_POINT('Ctrl Pts',(97.0962244432419,-0.991596195692752,
-5.40431647152264));
#28013=CARTESIAN_POINT('Ctrl Pts',(97.0722309882125,-1.00645609388381,-5.40616008147104));
#28014=CARTESIAN_POINT('Ctrl Pts',(97.0637970750983,-1.01153429109864,-5.40680666712876));
#28015=CARTESIAN_POINT('Ctrl Pts',(97.0497143895474,-1.01977493011572,-5.40788452336012));
#28016=CARTESIAN_POINT('Ctrl Pts',(97.04410133097,-1.02299765519692,-5.40831366865909));
#28017=CARTESIAN_POINT('Ctrl Pts',(97.0344968791195,-1.02840725681958,-5.40904734033586));
#28018=CARTESIAN_POINT('Ctrl Pts',(97.0305188094087,-1.0306175869972,-5.40935103628488));
#28019=CARTESIAN_POINT('Ctrl Pts',(97.0218411399399,-1.0353735389047,-5.41001317456163));
#28020=CARTESIAN_POINT('Ctrl Pts',(97.0171368399942,-1.03791032678431,-5.41037191703864));
#28021=CARTESIAN_POINT('Ctrl Pts',(97.0070639276849,-1.04325395264039,-5.41113969520755));
#28022=CARTESIAN_POINT('Ctrl Pts',(97.0016906173684,-1.04605155455228,-5.41154904044489));
#28023=CARTESIAN_POINT('Ctrl Pts',(96.9873255178304,-1.05339040079975,-5.41264294414645));
#28024=CARTESIAN_POINT('Ctrl Pts',(96.9782968104723,-1.05785786326406,-5.41333002248117));
#28025=CARTESIAN_POINT('Ctrl Pts',(96.9374302897532,-1.07743035514373,-5.41643869698796));
#28026=CARTESIAN_POINT('Ctrl Pts',(96.9049844806845,-1.09121629757378,-5.41890424100877));
#28027=CARTESIAN_POINT('Ctrl Pts',(96.7789755310914,-1.13820349061619,-5.42847459571587));
#28028=CARTESIAN_POINT('Ctrl Pts',(96.6819712358574,-1.16098395846934,-5.4358738488012));
#28029=CARTESIAN_POINT('Ctrl Pts',(96.5619597130911,-1.17356582914659,-5.44459881579802));
#28030=CARTESIAN_POINT('Ctrl Pts',(96.5405791338558,-1.1752187400789,-5.44613493297173));
#28031=CARTESIAN_POINT('Ctrl Pts',(96.50570128527,-1.17695874316459,-5.44859972673861));
#28032=CARTESIAN_POINT('Ctrl Pts',(96.4922271668712,-1.17739924338115,-5.44954196900938));
#28033=CARTESIAN_POINT('Ctrl Pts',(96.4739881237726,-1.17768216354567,-5.45080140057567));
#28034=CARTESIAN_POINT('Ctrl Pts',(96.4692279804066,-1.17772713881187,-5.45112861861907));
#28035=CARTESIAN_POINT('Ctrl Pts',(96.4612835012376,-1.17775403075986,-5.45167212504533));
#28036=CARTESIAN_POINT('Ctrl Pts',(96.4580993213388,-1.17775189646947,-5.4518892657946));
#28037=CARTESIAN_POINT('Ctrl Pts',(96.4520683585878,-1.17772339499165,-5.45229916661042));
#28038=CARTESIAN_POINT('Ctrl Pts',(96.4492216051707,-1.17769961976727,-5.4524920715195));
#28039=CARTESIAN_POINT('Ctrl Pts',(96.4424775110639,-1.17761883932614,-5.45294776291437));
#28040=CARTESIAN_POINT('Ctrl Pts',(96.4385802816529,-1.17755280830645,-5.4532100585192));
#28041=CARTESIAN_POINT('Ctrl Pts',(96.4249119360751,-1.17725334350479,-5.45412657123468));
#28042=CARTESIAN_POINT('Ctrl Pts',(96.415143142031,-1.17691762155923,-5.45477549306419));
#28043=CARTESIAN_POINT('Ctrl Pts',(96.3344933813667,-1.17314024223382,-5.46009074903455));
#28044=CARTESIAN_POINT('Ctrl Pts',(96.2640422679642,-1.16341976501805,-5.46447028486917));
#28045=CARTESIAN_POINT('Ctrl Pts',(96.1374195657284,-1.13411017828015,-5.47250973570675));
#28046=CARTESIAN_POINT('Ctrl Pts',(96.0810362311465,-1.11651045763795,-5.47615475961267));
#28047=CARTESIAN_POINT('Ctrl Pts',(96.0064639804205,-1.08692913343066,-5.48126800021397));
#28048=CARTESIAN_POINT('Ctrl Pts',(95.9869338523051,-1.07856358893874,-5.48263520065668));
#28049=CARTESIAN_POINT('Ctrl Pts',(95.9533583934763,-1.06309411042212,-5.48504329802931));
#28050=CARTESIAN_POINT('Ctrl Pts',(95.939209151816,-1.05622821845859,-5.48607646728509));
#28051=CARTESIAN_POINT('Ctrl Pts',(95.9187897278934,-1.0458094983757,-5.48759665637089));
#28052=CARTESIAN_POINT('Ctrl Pts',(95.9124075671126,-1.042478992656,-5.48807602827467));
#28053=CARTESIAN_POINT('Ctrl Pts',(95.9012208319326,-1.03651011748646,-5.48892396877215));
#28054=CARTESIAN_POINT('Ctrl Pts',(95.896403348143,-1.03389630073277,-5.48929167132338));
#28055=CARTESIAN_POINT('Ctrl Pts',(95.8863927958785,-1.02837409517696,-5.49006116053804));
#28056=CARTESIAN_POINT('Ctrl Pts',(95.8812031911007,-1.02545978182514,-5.49046314854303));
#28057=CARTESIAN_POINT('Ctrl Pts',(95.8677126132603,-1.01774882656706,-5.49151631923112));
#28058=CARTESIAN_POINT('Ctrl Pts',(95.859447867508,-1.01289002332626,-5.49216969912916));
#28059=CARTESIAN_POINT('Ctrl Pts',(95.8247574794527,-0.991921642050991,
-5.49494767095819));
#28060=CARTESIAN_POINT('Ctrl Pts',(95.7989150422382,-0.974875950549584,
-5.49710565566995));
#28061=CARTESIAN_POINT('Ctrl Pts',(95.706279430953,-0.908392762490096,-5.50518071900474));
#28062=CARTESIAN_POINT('Ctrl Pts',(95.6441051078397,-0.852950450643157,
-5.51130429991718));
#28063=CARTESIAN_POINT('Ctrl Pts',(95.5532410473624,-0.752815428918454,
-5.5212023291402));
#28064=CARTESIAN_POINT('Ctrl Pts',(95.5207925828441,-0.711900543259572,
-5.52498626150539));
#28065=CARTESIAN_POINT('Ctrl Pts',(95.487208750986,-0.663238042333523,-5.52909863909753));
#28066=CARTESIAN_POINT('Ctrl Pts',(95.483307413545,-0.657476508841074,-5.52957968866295));
#28067=CARTESIAN_POINT('Ctrl Pts',(95.4774312689445,-0.648630707070114,
-5.53030897987359));
#28068=CARTESIAN_POINT('Ctrl Pts',(95.4754194871042,-0.645571363067762,
-5.53055953449048));
#28069=CARTESIAN_POINT('Ctrl Pts',(95.4717624122841,-0.639953100449615,
-5.53101653503211));
#28070=CARTESIAN_POINT('Ctrl Pts',(95.4701127593949,-0.637397180009341,
-5.53122325687331));
#28071=CARTESIAN_POINT('Ctrl Pts',(95.4664106398737,-0.63161215985099,-5.53168850446219));
#28072=CARTESIAN_POINT('Ctrl Pts',(95.4643639926712,-0.628379431795095,
-5.53194665195216));
#28073=CARTESIAN_POINT('Ctrl Pts',(95.4591144466176,-0.619997548518764,
-5.53261140361551));
#28074=CARTESIAN_POINT('Ctrl Pts',(95.4559354483774,-0.614833451641219,
-5.53301652337617));
#28075=CARTESIAN_POINT('Ctrl Pts',(95.4348507485854,-0.579982464840983,
-5.53572253217352));
#28076=CARTESIAN_POINT('Ctrl Pts',(95.4182216341332,-0.549538892354571,
-5.5379507701974));
#28077=CARTESIAN_POINT('Ctrl Pts',(95.3905176189747,-0.493023743390293,
-5.54192771611037));
#28078=CARTESIAN_POINT('Ctrl Pts',(95.3789937844784,-0.467203995578871,
-5.54368757396448));
#28079=CARTESIAN_POINT('Ctrl Pts',(95.3503928273341,-0.396376954943047,
-5.54842340347874));
#28080=CARTESIAN_POINT('Ctrl Pts',(95.3351274094051,-0.350698793242993,
-5.55138237740456));
#28081=CARTESIAN_POINT('Ctrl Pts',(95.3089759934743,-0.252891090980864,
-5.55771452055728));
#28082=CARTESIAN_POINT('Ctrl Pts',(95.2987431469547,-0.200703192690539,
-5.56109232144069));
#28083=CARTESIAN_POINT('Ctrl Pts',(95.2907078964055,-0.137270506138952,
-5.56529477092193));
#28084=CARTESIAN_POINT('Ctrl Pts',(95.2894959390874,-0.126515928830653,
-5.56601041612388));
#28085=CARTESIAN_POINT('Ctrl Pts',(95.287821037343,-0.109555875515638,-5.56714463664446));
#28086=CARTESIAN_POINT('Ctrl Pts',(95.2872587480136,-0.103360644712729,
-5.5675601295288));
#28087=CARTESIAN_POINT('Ctrl Pts',(95.2862977354553,-0.0917513530614053,
-5.56834106588334));
#28088=CARTESIAN_POINT('Ctrl Pts',(95.2858873137597,-0.086338404674241,
-5.56870613651701));
#28089=CARTESIAN_POINT('Ctrl Pts',(95.2850520423498,-0.0742106119814917,
-5.56952630307908));
#28090=CARTESIAN_POINT('Ctrl Pts',(95.284647286223,-0.067494620169433,-5.5699820084033));
#28091=CARTESIAN_POINT('Ctrl Pts',(95.2837634917776,-0.0503906954931974,
-5.57114661504496));
#28092=CARTESIAN_POINT('Ctrl Pts',(95.2833644581691,-0.039999391485766,
-5.57185795346008));
#28093=CARTESIAN_POINT('Ctrl Pts',(95.2812174229251,0.0453888502322086,
-5.57773583824771));
#28094=CARTESIAN_POINT('Ctrl Pts',(95.2865012949004,0.120376768314819,-5.58312120834398));
#28095=CARTESIAN_POINT('Ctrl Pts',(95.3082424323486,0.250327253599703,-5.59275807377661));
#28096=CARTESIAN_POINT('Ctrl Pts',(95.3216446802525,0.305564218632168,-5.59695003686976));
#28097=CARTESIAN_POINT('Ctrl Pts',(95.3455190167178,0.380018182784622,-5.602603277735));
#28098=CARTESIAN_POINT('Ctrl Pts',(95.3526155817885,0.400235391954122,-5.60413808164149));
#28099=CARTESIAN_POINT('Ctrl Pts',(95.36506707584,0.432833675955351,-5.60660101504056));
#28100=CARTESIAN_POINT('Ctrl Pts',(95.370089882657,0.445335722447427,-5.60754268650243));
#28101=CARTESIAN_POINT('Ctrl Pts',(95.3771760676975,0.462134444453824,-5.60880148476715));
#28102=CARTESIAN_POINT('Ctrl Pts',(95.3790523752516,0.466508255489532,-5.60912862775357));
#28103=CARTESIAN_POINT('Ctrl Pts',(95.3822281183213,0.473789015824457,-5.60967204383177));
#28104=CARTESIAN_POINT('Ctrl Pts',(95.3835129041438,0.476702244041119,-5.60988916871125));
#28105=CARTESIAN_POINT('Ctrl Pts',(95.385968878002,0.482210509913384,-5.61029906566339));
#28106=CARTESIAN_POINT('Ctrl Pts',(95.387137684739,0.484806563587004,-5.61049198241161));
#28107=CARTESIAN_POINT('Ctrl Pts',(95.3899292279519,0.490947320534827,-5.61094773414656));
#28108=CARTESIAN_POINT('Ctrl Pts',(95.3915601857716,0.494488282968222,-5.61121007793835));
#28109=CARTESIAN_POINT('Ctrl Pts',(95.3973540539785,0.506904692767635,-5.6121286021303));
#28110=CARTESIAN_POINT('Ctrl Pts',(95.4016103026919,0.515736494935508,-5.61277944987483));
#28111=CARTESIAN_POINT('Ctrl Pts',(95.4373376312303,0.587564116471556,-5.61806046933466));
#28112=CARTESIAN_POINT('Ctrl Pts',(95.4742948396696,0.647683220535143,-5.62240845072104));
#28113=CARTESIAN_POINT('Ctrl Pts',(95.5518977328858,0.75172814692553,-5.63043739231747));
#28114=CARTESIAN_POINT('Ctrl Pts',(95.5909315187167,0.796556210939607,-5.63410430716551));
#28115=CARTESIAN_POINT('Ctrl Pts',(95.6483503045073,0.853225295165076,-5.63924548449146));
#28116=CARTESIAN_POINT('Ctrl Pts',(95.6639273942333,0.867785653831878,-5.64061743009629));
#28117=CARTESIAN_POINT('Ctrl Pts',(95.6916986814796,0.892366269762142,-5.6430331275175));
#28118=CARTESIAN_POINT('Ctrl Pts',(95.7037152219328,0.902579265438339,-5.6440690826172));
#28119=CARTESIAN_POINT('Ctrl Pts',(95.7215166634698,0.917103474539165,-5.64559261699479));
#28120=CARTESIAN_POINT('Ctrl Pts',(95.7271421785552,0.921607965574694,-5.64607249968651));
#28121=CARTESIAN_POINT('Ctrl Pts',(95.7371190688649,0.929447526533811,-5.64692102407508));
#28122=CARTESIAN_POINT('Ctrl Pts',(95.7414530936686,0.932804403796896,-5.64728879578888));
#28123=CARTESIAN_POINT('Ctrl Pts',(95.7505384148764,0.939740412872528,-5.64805811311137));
#28124=CARTESIAN_POINT('Ctrl Pts',(95.7552936968788,0.943314042383193,-5.6484598579474));
#28125=CARTESIAN_POINT('Ctrl Pts',(95.7677703649107,0.95254328629406,-5.64951168172808));
#28126=CARTESIAN_POINT('Ctrl Pts',(95.7755338502618,0.95814097508483,-5.6501639475096));
#28127=CARTESIAN_POINT('Ctrl Pts',(95.8085620128926,0.98134864181115,-5.65293026343886));
#28128=CARTESIAN_POINT('Ctrl Pts',(95.8344420576964,0.998057343695313,-5.65507735584128));
#28129=CARTESIAN_POINT('Ctrl Pts',(95.8809073276512,1.02553759155734,-5.65889973545223));
#28130=CARTESIAN_POINT('Ctrl Pts',(95.901202188743,1.03674439082019,-5.66055885234695));
#28131=CARTESIAN_POINT('Ctrl Pts',(95.9218018640414,1.04733944130189,-5.66223110129989));
#28132=CARTESIAN_POINT('Origin',(96.460480949577,-7.19464945638997E-16,
0.924367114736168));
#28133=CARTESIAN_POINT('',(95.9218016184021,1.04733931496196,-6.2623154905088));
#28134=CARTESIAN_POINT('',(95.9218016730721,1.04733934308043,-6.16392795844921));
#28135=CARTESIAN_POINT('',(95.9218016730721,1.04733934308042,0.924367114736168));
#28136=CARTESIAN_POINT('',(97.6382308542487,0.000473862668674378,-5.92345611052503));
#28137=CARTESIAN_POINT('Ctrl Pts',(95.9218016184021,1.04733931496196,-6.26231549050881));
#28138=CARTESIAN_POINT('Ctrl Pts',(95.9027034372951,1.03751652374386,-6.26077924530074));
#28139=CARTESIAN_POINT('Ctrl Pts',(95.8838728183822,1.02717078126495,-6.25922892834475));
#28140=CARTESIAN_POINT('Ctrl Pts',(95.8384588123809,1.00057647339736,-6.25540622018832));
#28141=CARTESIAN_POINT('Ctrl Pts',(95.812221971306,0.983780972517538,-6.25312452485025));
#28142=CARTESIAN_POINT('Ctrl Pts',(95.7321245931071,0.927909962335828,-6.24595783254306));
#28143=CARTESIAN_POINT('Ctrl Pts',(95.6808838306992,0.885296495316674,-6.24106678465804));
#28144=CARTESIAN_POINT('Ctrl Pts',(95.626445505066,0.83161194890941,-6.23570647197124));
#28145=CARTESIAN_POINT('Ctrl Pts',(95.6194672107343,0.824554099799341,-6.23501607191353));
#28146=CARTESIAN_POINT('Ctrl Pts',(95.6098558098326,0.814584142833932,-6.23406159144968));
#28147=CARTESIAN_POINT('Ctrl Pts',(95.607147012134,0.811746047992397,-6.23379218353898));
#28148=CARTESIAN_POINT('Ctrl Pts',(95.6024926690338,0.806820497166007,-6.23332865759519));
#28149=CARTESIAN_POINT('Ctrl Pts',(95.6005404558491,0.804739431049845,-6.2331340456809));
#28150=CARTESIAN_POINT('Ctrl Pts',(95.5964307527875,0.800326440989442,-6.23272399221954));
#28151=CARTESIAN_POINT('Ctrl Pts',(95.594275098128,0.797992843385805,-6.2325086945338));
#28152=CARTESIAN_POINT('Ctrl Pts',(95.5889373682523,0.792167385344054,-6.23197496648532));
#28153=CARTESIAN_POINT('Ctrl Pts',(95.5857667682458,0.788665000759619,-6.23165738092683));
#28154=CARTESIAN_POINT('Ctrl Pts',(95.5738098886506,0.775296094781045,-6.23045716577272));
#28155=CARTESIAN_POINT('Ctrl Pts',(95.565168378576,0.765300621383421,-6.22958446358446));
#28156=CARTESIAN_POINT('Ctrl Pts',(95.5433302029879,0.739164478987613,-6.22735872991474));
#28157=CARTESIAN_POINT('Ctrl Pts',(95.5303902007487,0.722814583418428,-6.22601986943513));
#28158=CARTESIAN_POINT('Ctrl Pts',(95.4907716172202,0.66992890209069,-6.22182465452319));
#28159=CARTESIAN_POINT('Ctrl Pts',(95.4657592764875,0.632194723616556,-6.21902745778775));
#28160=CARTESIAN_POINT('Ctrl Pts',(95.4020667482809,0.522928430592512,-6.21120409595732));
#28161=CARTESIAN_POINT('Ctrl Pts',(95.3685312980728,0.448707803518177,-6.20618228758337));
#28162=CARTESIAN_POINT('Ctrl Pts',(95.3380358388676,0.357001057416308,-6.19988363956184));
#28163=CARTESIAN_POINT('Ctrl Pts',(95.3334587000167,0.342277073073985,-6.19887033907451));
#28164=CARTESIAN_POINT('Ctrl Pts',(95.3272073191105,0.320680329876448,-6.19737909877741));
#28165=CARTESIAN_POINT('Ctrl Pts',(95.32530372324,0.313875224646292,-6.19690850567546));
#28166=CARTESIAN_POINT('Ctrl Pts',(95.3220328984528,0.301763357924753,-6.19606949219819));
#28167=CARTESIAN_POINT('Ctrl Pts',(95.3206412410178,0.296463364273207,-6.19570186395337));
#28168=CARTESIAN_POINT('Ctrl Pts',(95.3178137632152,0.285380904872879,-6.19493203468788));
#28169=CARTESIAN_POINT('Ctrl Pts',(95.3163847382833,0.279596882509461,-6.19452962897953));
#28170=CARTESIAN_POINT('Ctrl Pts',(95.312764813897,0.264452544022053,-6.19347424777148));
#28171=CARTESIAN_POINT('Ctrl Pts',(95.3106445624014,0.255075967834139,-6.19281905832067));
#28172=CARTESIAN_POINT('Ctrl Pts',(95.3014159894006,0.211807967644579,-6.18978691945086));
#28173=CARTESIAN_POINT('Ctrl Pts',(95.295690441113,0.177642458967405,-6.18736724273637));
#28174=CARTESIAN_POINT('Ctrl Pts',(95.2832098098899,0.0758126820904066,
-6.1800764368519));
#28175=CARTESIAN_POINT('Ctrl Pts',(95.2807976416746,0.00776555586291238,
-6.1750941075766));
#28176=CARTESIAN_POINT('Ctrl Pts',(95.2855481287778,-0.0852039474893144,
-6.16826343550903));
#28177=CARTESIAN_POINT('Ctrl Pts',(95.2876341029811,-0.110259595075508,
-6.16642150066938));
#28178=CARTESIAN_POINT('Ctrl Pts',(95.2924675193683,-0.152076612366585,
-6.16336067574171));
#28179=CARTESIAN_POINT('Ctrl Pts',(95.2947784826401,-0.168880049028224,
-6.16213441156213));
#28180=CARTESIAN_POINT('Ctrl Pts',(95.3010894354126,-0.208420479074215,
-6.15926525802658));
#28181=CARTESIAN_POINT('Ctrl Pts',(95.3053967531312,-0.231102681213478,
-6.15763225098994));
#28182=CARTESIAN_POINT('Ctrl Pts',(95.3116583222109,-0.259494726059863,
-6.15561599368471));
#28183=CARTESIAN_POINT('Ctrl Pts',(95.3129929837369,-0.265334343893482,
-6.15520279585967));
#28184=CARTESIAN_POINT('Ctrl Pts',(95.3151674153232,-0.27452486360076,-6.15455513495145));
#28185=CARTESIAN_POINT('Ctrl Pts',(95.3159774505275,-0.277882590168632,
-6.15431907167494));
#28186=CARTESIAN_POINT('Ctrl Pts',(95.3175357960826,-0.284219765338305,
-6.15387465644792));
#28187=CARTESIAN_POINT('Ctrl Pts',(95.3182809854777,-0.287199827906534,
-6.15366614563864));
#28188=CARTESIAN_POINT('Ctrl Pts',(95.3200570385646,-0.294186126814854,
-6.15317839164159));
#28189=CARTESIAN_POINT('Ctrl Pts',(95.321097360191,-0.298189891762895,-6.15289968599989));
#28190=CARTESIAN_POINT('Ctrl Pts',(95.3245770466254,-0.311297632741616,
-6.15198968594972));
#28191=CARTESIAN_POINT('Ctrl Pts',(95.3271046737384,-0.320378095447187,
-6.15136314904091));
#28192=CARTESIAN_POINT('Ctrl Pts',(95.3417730365526,-0.370726343863668,
-6.14790576293948));
#28193=CARTESIAN_POINT('Ctrl Pts',(95.3560598869303,-0.411339709255548,
-6.14517852513907));
#28194=CARTESIAN_POINT('Ctrl Pts',(95.3840109161201,-0.47875307494232,-6.14061700839035));
#28195=CARTESIAN_POINT('Ctrl Pts',(95.3965346349489,-0.505974857824101,
-6.13876500369727));
#28196=CARTESIAN_POINT('Ctrl Pts',(95.4460162743963,-0.603546460294404,
-6.1319980489023));
#28197=CARTESIAN_POINT('Ctrl Pts',(95.4890221970525,-0.670576476632717,
-6.12708033453048));
#28198=CARTESIAN_POINT('Ctrl Pts',(95.5480689366773,-0.744874945999224,
-6.12089562403105));
#28199=CARTESIAN_POINT('Ctrl Pts',(95.5579308989155,-0.756794381829892,
-6.11987901299108));
#28200=CARTESIAN_POINT('Ctrl Pts',(95.572641433413,-0.773877328917242,-6.11838379939193));
#28201=CARTESIAN_POINT('Ctrl Pts',(95.5773066049556,-0.779197150933951,
-6.11791260021202));
#28202=CARTESIAN_POINT('Ctrl Pts',(95.5856701436583,-0.788562716622741,
-6.1170728917149));
#28203=CARTESIAN_POINT('Ctrl Pts',(95.5893493835353,-0.792625319501041,
-6.11670517909261));
#28204=CARTESIAN_POINT('Ctrl Pts',(95.5970839648839,-0.801046911589094,
-6.11593556534024));
#28205=CARTESIAN_POINT('Ctrl Pts',(95.6011442607899,-0.80540111795582,-6.11553346214387));
#28206=CARTESIAN_POINT('Ctrl Pts',(95.6118328261157,-0.81669054999094,-6.11447975630646));
#28207=CARTESIAN_POINT('Ctrl Pts',(95.618513013011,-0.823575786587198,-6.11382595265674));
#28208=CARTESIAN_POINT('Ctrl Pts',(95.6495323993175,-0.854775454429458,
-6.11081077782381));
#28209=CARTESIAN_POINT('Ctrl Pts',(95.6748433441457,-0.878095532601403,
-6.1084072655057));
#28210=CARTESIAN_POINT('Ctrl Pts',(95.7524612090611,-0.943563147588889,
-6.10119289820404));
#28211=CARTESIAN_POINT('Ctrl Pts',(95.8073889823616,-0.982380988018991,
-6.09627384408467));
#28212=CARTESIAN_POINT('Ctrl Pts',(95.9167433583124,-1.04642063506708,-6.08697431757348));
#28213=CARTESIAN_POINT('Ctrl Pts',(95.970386765049,-1.07259303998043,-6.08261109668552));
#28214=CARTESIAN_POINT('Ctrl Pts',(96.0350967775283,-1.09829128012328,-6.07772861390346));
#28215=CARTESIAN_POINT('Ctrl Pts',(96.0444549616281,-1.10187014832249,-6.07703156783505));
#28216=CARTESIAN_POINT('Ctrl Pts',(96.0575546989859,-1.10668921274995,-6.07606945828578));
#28217=CARTESIAN_POINT('Ctrl Pts',(96.0612582109591,-1.10803058762701,-6.07579895885625));
#28218=CARTESIAN_POINT('Ctrl Pts',(96.0676598361303,-1.11031292869552,-6.07533406840223));
#28219=CARTESIAN_POINT('Ctrl Pts',(96.0703547433169,-1.11126269191018,-6.0751391768499));
#28220=CARTESIAN_POINT('Ctrl Pts',(96.0760488470797,-1.11324619220005,-6.07472914397748));
#28221=CARTESIAN_POINT('Ctrl Pts',(96.0790488125957,-1.11427763649572,-6.07451414327494));
#28222=CARTESIAN_POINT('Ctrl Pts',(96.086505781488,-1.11680783784859,-6.0739821803486));
#28223=CARTESIAN_POINT('Ctrl Pts',(96.0909677225731,-1.11829206827427,-6.07366605074161));
#28224=CARTESIAN_POINT('Ctrl Pts',(96.1078466892266,-1.12379467265748,-6.07247794131675));
#28225=CARTESIAN_POINT('Ctrl Pts',(96.1203218682422,-1.12763346085623,-6.07161563310831));
#28226=CARTESIAN_POINT('Ctrl Pts',(96.15254473122,-1.13696542723526,-6.06942259602257));
#28227=CARTESIAN_POINT('Ctrl Pts',(96.1723772073523,-1.14215210488523,-6.06810552025532));
#28228=CARTESIAN_POINT('Ctrl Pts',(96.248628526104,-1.15998090245398,-6.06313080173876));
#28229=CARTESIAN_POINT('Ctrl Pts',(96.3058169985225,-1.16898118351778,-6.05958104630404));
#28230=CARTESIAN_POINT('Ctrl Pts',(96.4386392566096,-1.17996266025842,-6.05132873566836));
#28231=CARTESIAN_POINT('Ctrl Pts',(96.5142532006359,-1.17893819890441,-6.04661608460665));
#28232=CARTESIAN_POINT('Ctrl Pts',(96.5995711055442,-1.16955415778022,-6.0409828660632));
#28233=CARTESIAN_POINT('Ctrl Pts',(96.6098823391683,-1.16828173531115,-6.04029703995749));
#28234=CARTESIAN_POINT('Ctrl Pts',(96.6268386108504,-1.16596115915744,-6.03916030505212));
#28235=CARTESIAN_POINT('Ctrl Pts',(96.6334940401457,-1.16499217313702,-6.03871185575503));
#28236=CARTESIAN_POINT('Ctrl Pts',(96.6455059058222,-1.16313812567222,-6.03789820329052));
#28237=CARTESIAN_POINT('Ctrl Pts',(96.6508652524335,-1.16227292378605,-6.03753362973343));
#28238=CARTESIAN_POINT('Ctrl Pts',(96.6623553514322,-1.16033638269191,-6.03674859648554));
#28239=CARTESIAN_POINT('Ctrl Pts',(96.6684839537484,-1.15925344201018,-6.03632778345609));
#28240=CARTESIAN_POINT('Ctrl Pts',(96.6852571237432,-1.15615228740285,-6.03517018674572));
#28241=CARTESIAN_POINT('Ctrl Pts',(96.6958826554317,-1.15403572883338,-6.03443034356532));
#28242=CARTESIAN_POINT('Ctrl Pts',(96.7586666758923,-1.14062628720696,-6.03001873047136));
#28243=CARTESIAN_POINT('Ctrl Pts',(96.8100305438424,-1.12594700656359,-6.02624091054148));
#28244=CARTESIAN_POINT('Ctrl Pts',(96.9340457390375,-1.08119928844566,-6.01671173642312));
#28245=CARTESIAN_POINT('Ctrl Pts',(97.0050223430032,-1.04724839893012,-6.01088343267503));
#28246=CARTESIAN_POINT('Ctrl Pts',(97.0998905060409,-0.98960019688799,-6.00284912981804));
#28247=CARTESIAN_POINT('Ctrl Pts',(97.1269797058838,-0.971562123928781,
-6.00052625031948));
#28248=CARTESIAN_POINT('Ctrl Pts',(97.1585839164231,-0.948572701511742,
-5.99781069598665));
#28249=CARTESIAN_POINT('Ctrl Pts',(97.1638460934559,-0.944677406127372,
-5.99735837111901));
#28250=CARTESIAN_POINT('Ctrl Pts',(97.1719630714385,-0.938563434212828,
-5.9966607171686));
#28251=CARTESIAN_POINT('Ctrl Pts',(97.1748405000553,-0.936375225694146,
-5.99641341485543));
#28252=CARTESIAN_POINT('Ctrl Pts',(97.1800490161815,-0.932376303820347,
-5.99596585712887));
#28253=CARTESIAN_POINT('Ctrl Pts',(97.182383376658,-0.930570072886297,-5.99576531052032));
#28254=CARTESIAN_POINT('Ctrl Pts',(97.1847269553212,-0.928742583320426,
-5.99556400351155));
#28255=CARTESIAN_POINT('Ctrl Pts',(97.1847429039152,-0.928730146171248,
-5.9955626335721));
#28256=CARTESIAN_POINT('Ctrl Pts',(97.184774498043,-0.928705506898879,-5.99555991972768));
#28257=CARTESIAN_POINT('Ctrl Pts',(97.184790144265,-0.928693304263706,-5.99555857576354));
#28258=CARTESIAN_POINT('Ctrl Pts',(97.1848211446973,-0.928669125475988,
-5.99555591292053));
#28259=CARTESIAN_POINT('Ctrl Pts',(97.1848364985207,-0.928657149648654,
-5.99555459407484));
#28260=CARTESIAN_POINT('Ctrl Pts',(97.1848669215787,-0.928633418757059,
-5.995551980831));
#28261=CARTESIAN_POINT('Ctrl Pts',(97.1848819913527,-0.928621663294376,
-5.99555068638648));
#28262=CARTESIAN_POINT('Ctrl Pts',(97.1849118558488,-0.928598365759052,
-5.99554812112562));
#28263=CARTESIAN_POINT('Ctrl Pts',(97.1849266503091,-0.928586823911997,
-5.99554685033174));
#28264=CARTESIAN_POINT('Ctrl Pts',(97.1849559732172,-0.928563946619245,
-5.99554433159558));
#28265=CARTESIAN_POINT('Ctrl Pts',(97.1849705011142,-0.928552611623555,
-5.99554308370057));
#28266=CARTESIAN_POINT('Ctrl Pts',(97.1849992968908,-0.928530143416615,
-5.99554061024712));
#28267=CARTESIAN_POINT('Ctrl Pts',(97.1850135655155,-0.928519009643252,
-5.99553938462462));
#28268=CARTESIAN_POINT('Ctrl Pts',(97.1850418509155,-0.928496937565013,
-5.99553695501443));
#28269=CARTESIAN_POINT('Ctrl Pts',(97.1850558679194,-0.928485999100242,
-5.99553575100707));
#28270=CARTESIAN_POINT('Ctrl Pts',(97.1850836575746,-0.928464311843944,
-5.99553336398313));
#28271=CARTESIAN_POINT('Ctrl Pts',(97.1850974301347,-0.928453563141104,
-5.99553218097434));
#28272=CARTESIAN_POINT('Ctrl Pts',(97.1851247389717,-0.928432249163397,
-5.99552983525428));
#28273=CARTESIAN_POINT('Ctrl Pts',(97.185138274497,-0.928421684491844,-5.99552867260754));
#28274=CARTESIAN_POINT('Ctrl Pts',(97.1851651158827,-0.928400733460897,
-5.995526367043));
#28275=CARTESIAN_POINT('Ctrl Pts',(97.1851784215235,-0.928390347288889,
-5.99552522414402));
#28276=CARTESIAN_POINT('Ctrl Pts',(97.1852048066402,-0.9283697505729,-5.9955229577743));
#28277=CARTESIAN_POINT('Ctrl Pts',(97.1852178876494,-0.928359538847369,
-5.99552183417181));
#28278=CARTESIAN_POINT('Ctrl Pts',(97.1852438322286,-0.928339284258116,
-5.99551960564546));
#28279=CARTESIAN_POINT('Ctrl Pts',(97.1852566953784,-0.928329241737194,
-5.99551850075766));
#28280=CARTESIAN_POINT('Ctrl Pts',(97.1852822112146,-0.92830932015475,-5.99551630906141));
#28281=CARTESIAN_POINT('Ctrl Pts',(97.1852948631045,-0.928299441729095,
-5.99551522232134));
#28282=CARTESIAN_POINT('Ctrl Pts',(97.1853199600008,-0.928279845583848,
-5.99551306661298));
#28283=CARTESIAN_POINT('Ctrl Pts',(97.1853324055851,-0.928270127426433,
-5.99551199759503));
#28284=CARTESIAN_POINT('Ctrl Pts',(97.1853570971651,-0.928250846161321,
-5.9955098767042));
#28285=CARTESIAN_POINT('Ctrl Pts',(97.1853693425941,-0.928241283509049,
-5.99550882488));
#28286=CARTESIAN_POINT('Ctrl Pts',(97.188438685684,-0.925844286384764,-5.99524518304663));
#28287=CARTESIAN_POINT('Ctrl Pts',(97.191484024883,-0.923441721579667,-5.99498364406355));
#28288=CARTESIAN_POINT('Ctrl Pts',(97.1979193183567,-0.918312930149093,
-5.99443092295136));
#28289=CARTESIAN_POINT('Ctrl Pts',(97.2013061610469,-0.915582870579692,
-5.99414000233541));
#28290=CARTESIAN_POINT('Ctrl Pts',(97.2103567834104,-0.908204261977934,
-5.99336226312612));
#28291=CARTESIAN_POINT('Ctrl Pts',(97.2159925400035,-0.903521438907313,
-5.99287763580293));
#28292=CARTESIAN_POINT('Ctrl Pts',(97.2334556755209,-0.888733436358291,
-5.99137357042186));
#28293=CARTESIAN_POINT('Ctrl Pts',(97.2451272339687,-0.878445960104843,
-5.9903648493703));
#28294=CARTESIAN_POINT('Ctrl Pts',(97.2931014510356,-0.834441466236788,
-5.98618700847161));
#28295=CARTESIAN_POINT('Ctrl Pts',(97.3274643086825,-0.798680206876593,
-5.98311499050986));
#28296=CARTESIAN_POINT('Ctrl Pts',(97.4150047339152,-0.695246641984305,
-5.97472955877326));
#28297=CARTESIAN_POINT('Ctrl Pts',(97.4631787887382,-0.623761559067209,
-5.96943500998131));
#28298=CARTESIAN_POINT('Ctrl Pts',(97.5102240747314,-0.534196802675814,
-5.96283935810681));
#28299=CARTESIAN_POINT('Ctrl Pts',(97.5170415245034,-0.520582913475649,
-5.96183854300716));
#28300=CARTESIAN_POINT('Ctrl Pts',(97.5266187673362,-0.500494408964516,
-5.96036229672799));
#28301=CARTESIAN_POINT('Ctrl Pts',(97.529587658197,-0.494120776590511,-5.95989400045444));
#28302=CARTESIAN_POINT('Ctrl Pts',(97.5347663521593,-0.482737928510596,
-5.95905761462385));
#28303=CARTESIAN_POINT('Ctrl Pts',(97.5369986498103,-0.477739126703279,
-5.95869029992104));
#28304=CARTESIAN_POINT('Ctrl Pts',(97.5415941555605,-0.46725260495907,-5.95791962323901));
#28305=CARTESIAN_POINT('Ctrl Pts',(97.5439506114233,-0.461762114712368,
-5.95751604649715));
#28306=CARTESIAN_POINT('Ctrl Pts',(97.550019245722,-0.447320099982346,-5.95645418144808));
#28307=CARTESIAN_POINT('Ctrl Pts',(97.5536628327313,-0.438340428464417,
-5.95579362883106));
#28308=CARTESIAN_POINT('Ctrl Pts',(97.5701423286806,-0.396242643946171,
-5.95269466548414));
#28309=CARTESIAN_POINT('Ctrl Pts',(97.5815854644715,-0.362602837894717,
-5.95021117507097));
#28310=CARTESIAN_POINT('Ctrl Pts',(97.6225446599052,-0.22158247036711,-5.93976532406914));
#28311=CARTESIAN_POINT('Ctrl Pts',(97.6382756354914,-0.110826536906557,
-5.93141223446537));
#28312=CARTESIAN_POINT('Ctrl Pts',(97.6382308542487,0.000473862668674378,
-5.92345611052503));
#28313=CARTESIAN_POINT('Ctrl Pts',(97.6382308536216,0.00047541875814493,
-5.9234559992906));
#28314=CARTESIAN_POINT('Ctrl Pts',(97.6382224132776,0.0213845943457944,
-5.92196134253803));
#28315=CARTESIAN_POINT('Ctrl Pts',(97.6376571556521,0.0422916652363726,
-5.92048465166223));
#28316=CARTESIAN_POINT('Ctrl Pts',(97.6363006548358,0.0675443221931847,
-5.91873085816825));
#28317=CARTESIAN_POINT('Ctrl Pts',(97.636041549317,0.0719130901754064,-5.91842853155492));
#28318=CARTESIAN_POINT('Ctrl Pts',(97.6355535230143,0.0794322719830097,
-5.91791017054684));
#28319=CARTESIAN_POINT('Ctrl Pts',(97.6353362717538,0.0825833591550827,
-5.91769353855461));
#28320=CARTESIAN_POINT('Ctrl Pts',(97.6348986671935,0.0885789262473102,
-5.9172825417018));
#28321=CARTESIAN_POINT('Ctrl Pts',(97.6346806497204,0.0914235546101246,
-5.91708805167027));
#28322=CARTESIAN_POINT('Ctrl Pts',(97.6342245265763,0.0971039430504702,
-5.91670073301855));
#28323=CARTESIAN_POINT('Ctrl Pts',(97.6339864761895,0.0999396805640717,
-5.91650790191768));
#28324=CARTESIAN_POINT('Ctrl Pts',(97.6333984785972,0.106652162415221,-5.91605263369416));
#28325=CARTESIAN_POINT('Ctrl Pts',(97.6330395832733,0.110528119691324,-5.91579068513029));
#28326=CARTESIAN_POINT('Ctrl Pts',(97.6317054486579,0.124197833378635,-5.9148699201821));
#28327=CARTESIAN_POINT('Ctrl Pts',(97.6306266369606,0.133981397560573,-5.91421649116507));
#28328=CARTESIAN_POINT('Ctrl Pts',(97.6264401654554,0.168024730127037,-5.91195863660057));
#28329=CARTESIAN_POINT('Ctrl Pts',(97.6226994607609,0.192201748569384,-5.91038321946628));
#28330=CARTESIAN_POINT('Ctrl Pts',(97.5993060263675,0.317444132439284,-5.90228802715373));
#28331=CARTESIAN_POINT('Ctrl Pts',(97.567217343523,0.415728716761013,-5.89612095009754));
#28332=CARTESIAN_POINT('Ctrl Pts',(97.5080065308723,0.539399432810971,-5.88740242428797));
#28333=CARTESIAN_POINT('Ctrl Pts',(97.4919256242229,0.569546427275296,-5.88519756575344));
#28334=CARTESIAN_POINT('Ctrl Pts',(97.4696913734066,0.607191062969501,-5.88231623434587));
#28335=CARTESIAN_POINT('Ctrl Pts',(97.4647238466902,0.615372132313187,-5.88168204408834));
#28336=CARTESIAN_POINT('Ctrl Pts',(97.4565080558396,0.628538347127185,-5.88064785152489));
#28337=CARTESIAN_POINT('Ctrl Pts',(97.453320688939,0.633561125674799,-5.88025006379852));
#28338=CARTESIAN_POINT('Ctrl Pts',(97.4471228870298,0.643166236888714,-5.87948297266832));
#28339=CARTESIAN_POINT('Ctrl Pts',(97.4441182303692,0.647752127828456,-5.8791138888068));
#28340=CARTESIAN_POINT('Ctrl Pts',(97.4371570112647,0.658216639324499,-5.87826504099892));
#28341=CARTESIAN_POINT('Ctrl Pts',(97.4331792266071,0.664080817237229,-5.8777844974268));
#28342=CARTESIAN_POINT('Ctrl Pts',(97.4203169927848,0.682679223464562,-5.876244600224));
#28343=CARTESIAN_POINT('Ctrl Pts',(97.4112338498441,0.695273352541443,-5.87517783354379));
#28344=CARTESIAN_POINT('Ctrl Pts',(97.3562931934426,0.768360296896599,-5.86884081723093));
#28345=CARTESIAN_POINT('Ctrl Pts',(97.3049303409396,0.824474760709458,-5.86335568679117));
#28346=CARTESIAN_POINT('Ctrl Pts',(97.2061723055963,0.913394336994797,-5.85361578766679));
#28347=CARTESIAN_POINT('Ctrl Pts',(97.1610925994946,0.948413749704477,-5.84941185117743));
#28348=CARTESIAN_POINT('Ctrl Pts',(97.0996696954013,0.989350885420907,-5.84411220737891));
#28349=CARTESIAN_POINT('Ctrl Pts',(97.0854883460824,0.998370292918983,-5.84291629732138));
#28350=CARTESIAN_POINT('Ctrl Pts',(97.0645078536697,1.01109164855347,-5.84119191042594));
#28351=CARTESIAN_POINT('Ctrl Pts',(97.0578580918265,1.01503466930285,-5.84065179139598));
#28352=CARTESIAN_POINT('Ctrl Pts',(97.0472675919713,1.02117424736929,-5.83980226745843));
#28353=CARTESIAN_POINT('Ctrl Pts',(97.0433523559463,1.02341405717112,-5.83949048643955));
#28354=CARTESIAN_POINT('Ctrl Pts',(97.035943283143,1.02759629397588,-5.83890490824164));
#28355=CARTESIAN_POINT('Ctrl Pts',(97.0324522481458,1.02954352775238,-5.83863083032843));
#28356=CARTESIAN_POINT('Ctrl Pts',(97.0263133842871,1.03292680793241,-5.83815217512753));
#28357=CARTESIAN_POINT('Ctrl Pts',(97.0236698644401,1.03437052438671,-5.83794712518217));
#28358=CARTESIAN_POINT('Ctrl Pts',(97.0179843479686,1.03744732062911,-5.83750843196941));
#28359=CARTESIAN_POINT('Ctrl Pts',(97.0149406881814,1.03907717775735,-5.83727498836125));
#28360=CARTESIAN_POINT('Ctrl Pts',(97.0066029016581,1.04349493291057,-5.83663920173035));
#28361=CARTESIAN_POINT('Ctrl Pts',(97.0012945390218,1.04625595662263,-5.83623848429078));
#28362=CARTESIAN_POINT('Ctrl Pts',(96.9754782513966,1.05943472319369,-5.83430815259919));
#28363=CARTESIAN_POINT('Ctrl Pts',(96.9546876389131,1.06929138666187,-5.83280975205383));
#28364=CARTESIAN_POINT('Ctrl Pts',(96.8397446977243,1.119715414067,-5.82475639510858));
#28365=CARTESIAN_POINT('Ctrl Pts',(96.7408890138456,1.14846797841612,-5.81862247803248));
#28366=CARTESIAN_POINT('Ctrl Pts',(96.6125171454055,1.16821582236168,-5.81042245254633));
#28367=CARTESIAN_POINT('Ctrl Pts',(96.5853477319366,1.1714313221552,-5.80867680181951));
#28368=CARTESIAN_POINT('Ctrl Pts',(96.5391241512246,1.17527553822152,-5.8056709347373));
#28369=CARTESIAN_POINT('Ctrl Pts',(96.5201214162402,1.17639291599921,-5.80442503424251));
#28370=CARTESIAN_POINT('Ctrl Pts',(96.4933461522842,1.17731692707259,-5.80265134578002));
#28371=CARTESIAN_POINT('Ctrl Pts',(96.4855892312208,1.17750789284731,-5.80213536380762));
#28372=CARTESIAN_POINT('Ctrl Pts',(96.4722580457959,1.17770430441587,-5.8012446647939));
#28373=CARTESIAN_POINT('Ctrl Pts',(96.466684520839,1.17774684993088,-5.80087110235214));
#28374=CARTESIAN_POINT('Ctrl Pts',(96.4560331009796,1.17775254788481,-5.80015485636917));
#28375=CARTESIAN_POINT('Ctrl Pts',(96.4509553228979,1.17772242419563,-5.79981238888875));
#28376=CARTESIAN_POINT('Ctrl Pts',(96.4390552107819,1.17757486274269,-5.79900733783508));
#28377=CARTESIAN_POINT('Ctrl Pts',(96.4322334470866,1.17743097243756,-5.79854394809531));
#28378=CARTESIAN_POINT('Ctrl Pts',(96.4086894839268,1.1767296399401,-5.79693789664575));
#28379=CARTESIAN_POINT('Ctrl Pts',(96.3919788294519,1.17587516820561,-5.79578617651147));
#28380=CARTESIAN_POINT('Ctrl Pts',(96.2788656927806,1.1676720613959,-5.78790629559718));
#28381=CARTESIAN_POINT('Ctrl Pts',(96.1836823324974,1.1488332110388,-5.78081633474949));
#28382=CARTESIAN_POINT('Ctrl Pts',(96.0845430228272,1.11616558790066,-5.77316459701475));
#28383=CARTESIAN_POINT('Ctrl Pts',(96.0772174083829,1.11367140749982,-5.77259783640592));
#28384=CARTESIAN_POINT('Ctrl Pts',(96.0378803339102,1.09984405021605,-5.76954849044065));
#28385=CARTESIAN_POINT('Ctrl Pts',(96.0063435715721,1.08720180671491,-5.76708197271567));
#28386=CARTESIAN_POINT('Ctrl Pts',(95.9585707903413,1.06560881758346,-5.76335092717144));
#28387=CARTESIAN_POINT('Ctrl Pts',(95.9419261490843,1.05760908299373,-5.76205213037112));
#28388=CARTESIAN_POINT('Ctrl Pts',(95.9242497424212,1.04859575044457,-5.76067918647434));
#28389=CARTESIAN_POINT('Ctrl Pts',(95.9230251593067,1.04796862019487,-5.76058410531922));
#28390=CARTESIAN_POINT('Ctrl Pts',(95.921801673071,1.04733934307989,-5.76048914482438));
#28391=CARTESIAN_POINT('Ctrl Pts',(95.9218018640414,1.04733944130189,-5.66223110129989));
#28392=CARTESIAN_POINT('Ctrl Pts',(95.9751129005066,1.07475895711457,-5.66655880664564));
#28393=CARTESIAN_POINT('Ctrl Pts',(96.0304650866842,1.09808108406502,-5.67097997349678));
#28394=CARTESIAN_POINT('Ctrl Pts',(96.1368980474905,1.13362901486336,-5.67919426223618));
#28395=CARTESIAN_POINT('Ctrl Pts',(96.1874673220581,1.14685897108738,-5.68298204705487));
#28396=CARTESIAN_POINT('Ctrl Pts',(96.2455873631558,1.15800010053294,-5.68709805198905));
#28397=CARTESIAN_POINT('Ctrl Pts',(96.2524333381618,1.15924962089989,-5.68757916697497));
#28398=CARTESIAN_POINT('Ctrl Pts',(96.262898016566,1.16106393224263,-5.68830853645777));
#28399=CARTESIAN_POINT('Ctrl Pts',(96.2665088027049,1.16167262054602,-5.68855910466603));
#28400=CARTESIAN_POINT('Ctrl Pts',(96.2731245040068,1.16275615629704,-5.68901611823567));
#28401=CARTESIAN_POINT('Ctrl Pts',(96.2761284314487,1.16323620396293,-5.68922283961971));
#28402=CARTESIAN_POINT('Ctrl Pts',(96.2829144878416,1.16429371338558,-5.68968807155876));
#28403=CARTESIAN_POINT('Ctrl Pts',(96.2866975926095,1.16486438920441,-5.68994620397421));
#28404=CARTESIAN_POINT('Ctrl Pts',(96.2964831325831,1.16629179037074,-5.69061089048023));
#28405=CARTESIAN_POINT('Ctrl Pts',(96.3024896121094,1.16712063016978,-5.69101596064249));
#28406=CARTESIAN_POINT('Ctrl Pts',(96.3428624545419,1.172374325467,-5.69372068120018));
#28407=CARTESIAN_POINT('Ctrl Pts',(96.3774068425609,1.17532755755173,-5.6959477599496));
#28408=CARTESIAN_POINT('Ctrl Pts',(96.4402153744239,1.17791335521369,-5.69991982688038));
#28409=CARTESIAN_POINT('Ctrl Pts',(96.4684298611127,1.17806090739991,-5.70167604289869));
#28410=CARTESIAN_POINT('Ctrl Pts',(96.5653392229808,1.1750855806629,-5.70768745599493));
#28411=CARTESIAN_POINT('Ctrl Pts',(96.6337346523555,1.1669635713583,-5.71190245428575));
#28412=CARTESIAN_POINT('Ctrl Pts',(96.7236338575945,1.14820677606705,-5.71773762997425));
#28413=CARTESIAN_POINT('Ctrl Pts',(96.7460932749141,1.14282708771586,-5.71921978550804));
#28414=CARTESIAN_POINT('Ctrl Pts',(96.7845562063631,1.1324094615372,-5.72181122197745));
#28415=CARTESIAN_POINT('Ctrl Pts',(96.8006372842522,1.12768328134515,-5.72291100719064));
#28416=CARTESIAN_POINT('Ctrl Pts',(96.8236480241402,1.12038352149864,-5.7245109946853));
#28417=CARTESIAN_POINT('Ctrl Pts',(96.8306633537164,1.11808521268099,-5.7250023436126));
#28418=CARTESIAN_POINT('Ctrl Pts',(96.842874904989,1.11395703211738,-5.72586408182899));
#28419=CARTESIAN_POINT('Ctrl Pts',(96.8480808097367,1.11215635285133,-5.7262335121111));
#28420=CARTESIAN_POINT('Ctrl Pts',(96.858143522423,1.10859651023689,-5.72695169341057));
#28421=CARTESIAN_POINT('Ctrl Pts',(96.8630017741062,1.10684178124442,-5.72730029190871));
#28422=CARTESIAN_POINT('Ctrl Pts',(96.8759131412568,1.10208213753629,-5.72823179229434));
#28423=CARTESIAN_POINT('Ctrl Pts',(96.8839450435126,1.0990209725564,-5.72881653361714));
#28424=CARTESIAN_POINT('Ctrl Pts',(96.9133216651725,1.08745494921108,-5.73097511408993));
#28425=CARTESIAN_POINT('Ctrl Pts',(96.9344485038801,1.07841439637011,-5.73256650408518));
#28426=CARTESIAN_POINT('Ctrl Pts',(97.0473751696591,1.02613164001487,-5.74129221035787));
#28427=CARTESIAN_POINT('Ctrl Pts',(97.1335479907659,0.971784402148248,-5.74880368552043));
#28428=CARTESIAN_POINT('Ctrl Pts',(97.2348101072412,0.887925644902729,-5.75839429059497));
#28429=CARTESIAN_POINT('Ctrl Pts',(97.2572081820215,0.867884528658782,-5.76056830569385));
#28430=CARTESIAN_POINT('Ctrl Pts',(97.2870494042917,0.839053453328704,-5.76351482141321));
#28431=CARTESIAN_POINT('Ctrl Pts',(97.2951660967796,0.830979442941155,-5.76432167805576));
#28432=CARTESIAN_POINT('Ctrl Pts',(97.3090608174001,0.816748746452408,-5.76571049998446));
#28433=CARTESIAN_POINT('Ctrl Pts',(97.314892653803,0.810646012011345,-5.76629581896176));
#28434=CARTESIAN_POINT('Ctrl Pts',(97.3233612145196,0.801591146244275,-5.76714866373568));
#28435=CARTESIAN_POINT('Ctrl Pts',(97.3260493192466,0.798687746204728,-5.76741981189418));
#28436=CARTESIAN_POINT('Ctrl Pts',(97.3307841738626,0.793521687238794,-5.76789810551688));
#28437=CARTESIAN_POINT('Ctrl Pts',(97.3328368210176,0.791264560465882,-5.76810568314704));
#28438=CARTESIAN_POINT('Ctrl Pts',(97.3372666061745,0.786355300402215,-5.76855413657115));
#28439=CARTESIAN_POINT('Ctrl Pts',(97.3396404981839,0.783700347722821,-5.7687947757105));
#28440=CARTESIAN_POINT('Ctrl Pts',(97.3461870699038,0.776311503625451,-5.76945941157289));
#28441=CARTESIAN_POINT('Ctrl Pts',(97.3503338776922,0.771554698594552,-5.76988156999867));
#28442=CARTESIAN_POINT('Ctrl Pts',(97.3730498177602,0.74507046570746,-5.77220208953741));
#28443=CARTESIAN_POINT('Ctrl Pts',(97.3908631711767,0.722704062826822,-5.77405167845208));
#28444=CARTESIAN_POINT('Ctrl Pts',(97.4564965076343,0.633840395969172,-5.78108366123805));
#28445=CARTESIAN_POINT('Ctrl Pts',(97.4981468236522,0.563073650517971,-5.78604378228458));
#28446=CARTESIAN_POINT('Ctrl Pts',(97.5546267303585,0.439185480955545,-5.79455302259547));
#28447=CARTESIAN_POINT('Ctrl Pts',(97.5736925800913,0.388326682819808,-5.79799958116884));
#28448=CARTESIAN_POINT('Ctrl Pts',(97.5922895461358,0.325918098068583,-5.80227919122276));
#28449=CARTESIAN_POINT('Ctrl Pts',(97.5952503505255,0.315454750547279,-5.80299818705806));
#28450=CARTESIAN_POINT('Ctrl Pts',(97.599679363699,0.298932887760326,-5.80413652162038));
#28451=CARTESIAN_POINT('Ctrl Pts',(97.6012451288838,0.292900977833946,-5.80455273966153));
#28452=CARTESIAN_POINT('Ctrl Pts',(97.6040848457101,0.281593054039978,-5.80533432073931));
#28453=CARTESIAN_POINT('Ctrl Pts',(97.6053703444761,0.276320088110755,-5.80569930503148));
#28454=CARTESIAN_POINT('Ctrl Pts',(97.6081641885741,0.26450578143945,-5.80651833698623));
#28455=CARTESIAN_POINT('Ctrl Pts',(97.6096531351444,0.257960094166874,-5.80697298646781));
#28456=CARTESIAN_POINT('Ctrl Pts',(97.6132950031252,0.241292170957103,-5.80813306947874));
#28457=CARTESIAN_POINT('Ctrl Pts',(97.6153705807465,0.231153805496216,-5.80884090761837));
#28458=CARTESIAN_POINT('Ctrl Pts',(97.6312955305549,0.14779027378089,-5.81468069717354));
#28459=CARTESIAN_POINT('Ctrl Pts',(97.6382972287035,0.0734425629974218,
-5.82002849412964));
#28460=CARTESIAN_POINT('Ctrl Pts',(97.6381596114607,-0.08014390216321,-5.83125971083814));
#28461=CARTESIAN_POINT('Ctrl Pts',(97.6301226225534,-0.159027589705757,
-5.83712704988531));
#28462=CARTESIAN_POINT('Ctrl Pts',(97.6116248238539,-0.249263388658251,
-5.8436258323391));
#28463=CARTESIAN_POINT('Ctrl Pts',(97.6087998454002,-0.261969854422392,
-5.84453549485481));
#28464=CARTESIAN_POINT('Ctrl Pts',(97.6046353006604,-0.279337325100714,
-5.84576900199256));
#28465=CARTESIAN_POINT('Ctrl Pts',(97.6034768683157,-0.284040229718555,
-5.84610202357358));
#28466=CARTESIAN_POINT('Ctrl Pts',(97.6015824904897,-0.291531560896638,
-5.84663076159496));
#28467=CARTESIAN_POINT('Ctrl Pts',(97.6008652746701,-0.294324598377501,
-5.84682750753017));
#28468=CARTESIAN_POINT('Ctrl Pts',(97.5993443178567,-0.30015859794374,-5.8472376144273));
#28469=CARTESIAN_POINT('Ctrl Pts',(97.5985386431533,-0.303199013760541,
-5.84745085529625));
#28470=CARTESIAN_POINT('Ctrl Pts',(97.5965327927153,-0.310647947196378,
-5.84797216986756));
#28471=CARTESIAN_POINT('Ctrl Pts',(97.5953191086098,-0.315052839883116,
-5.84827948364811));
#28472=CARTESIAN_POINT('Ctrl Pts',(97.5907938302741,-0.331111189825382,
-5.84939667298815));
#28473=CARTESIAN_POINT('Ctrl Pts',(97.5873279853533,-0.342720898745185,
-5.85019830380809));
#28474=CARTESIAN_POINT('Ctrl Pts',(97.5781189845763,-0.371917299589439,
-5.85220373708087));
#28475=CARTESIAN_POINT('Ctrl Pts',(97.5721393386185,-0.389426447013213,
-5.85339665234328));
#28476=CARTESIAN_POINT('Ctrl Pts',(97.5430920787854,-0.468349590123832,
-5.85875973596306));
#28477=CARTESIAN_POINT('Ctrl Pts',(97.5153296619533,-0.527914381370928,
-5.86277357260598));
#28478=CARTESIAN_POINT('Ctrl Pts',(97.4475888539103,-0.646317465626108,
-5.8712297563051));
#28479=CARTESIAN_POINT('Ctrl Pts',(97.4069629838279,-0.70447006052,-5.87566738503542));
#28480=CARTESIAN_POINT('Ctrl Pts',(97.3546402894488,-0.766604944021316,
-5.88099798617316));
#28481=CARTESIAN_POINT('Ctrl Pts',(97.3478096233866,-0.774501051359329,
-5.88168713099483));
#28482=CARTESIAN_POINT('Ctrl Pts',(97.3363975636134,-0.787344007577879,
-5.88282821142463));
#28483=CARTESIAN_POINT('Ctrl Pts',(97.3318769712508,-0.792344288333332,
-5.8832776540684));
#28484=CARTESIAN_POINT('Ctrl Pts',(97.323638199661,-0.801301505600868,-5.88409233983769));
#28485=CARTESIAN_POINT('Ctrl Pts',(97.3199350820164,-0.805272086811368,
-5.88445694559869));
#28486=CARTESIAN_POINT('Ctrl Pts',(97.311936751896,-0.813730092694751,-5.88524119357729));
#28487=CARTESIAN_POINT('Ctrl Pts',(97.3076332428558,-0.818209408709606,
-5.88566118304231));
#28488=CARTESIAN_POINT('Ctrl Pts',(97.2957644002983,-0.830369098362103,
-5.88681427867046));
#28489=CARTESIAN_POINT('Ctrl Pts',(97.288128884719,-0.837979811584242,-5.88755040507936));
#28490=CARTESIAN_POINT('Ctrl Pts',(97.2428859115296,-0.881854223154703,
-5.8918806536321));
#28491=CARTESIAN_POINT('Ctrl Pts',(97.2030087229751,-0.915683085681758,
-5.89557619288589));
#28492=CARTESIAN_POINT('Ctrl Pts',(97.0995241842134,-0.992255868331486,
-5.90487297801863));
#28493=CARTESIAN_POINT('Ctrl Pts',(97.0337423295437,-1.0316580336404,-5.91054821157257));
#28494=CARTESIAN_POINT('Ctrl Pts',(96.9325306807919,-1.07959428336482,-5.91867330416047));
#28495=CARTESIAN_POINT('Ctrl Pts',(96.8997803342307,-1.09333039034675,-5.92121461183439));
#28496=CARTESIAN_POINT('Ctrl Pts',(96.8607333041868,-1.10766885168813,-5.92410611400547));
#28497=CARTESIAN_POINT('Ctrl Pts',(96.8549938688502,-1.10972599898721,-5.92452769180868));
#28498=CARTESIAN_POINT('Ctrl Pts',(96.845617633187,-1.11300472228518,-5.92521052811567));
#28499=CARTESIAN_POINT('Ctrl Pts',(96.8419904693556,-1.11425323165662,-5.92547325743078));
#28500=CARTESIAN_POINT('Ctrl Pts',(96.8354755622793,-1.116460191735,-5.92594252804679));
#28501=CARTESIAN_POINT('Ctrl Pts',(96.832590153211,-1.11742519235339,-5.92614943843938));
#28502=CARTESIAN_POINT('Ctrl Pts',(96.8262320099972,-1.11952426022755,-5.92660333746621));
#28503=CARTESIAN_POINT('Ctrl Pts',(96.8227577226697,-1.12065335765313,-5.92685003909689));
#28504=CARTESIAN_POINT('Ctrl Pts',(96.8126892865827,-1.12387374946385,-5.92756130759393));
#28505=CARTESIAN_POINT('Ctrl Pts',(96.8060817582553,-1.12592317860074,-5.92802354564298));
#28506=CARTESIAN_POINT('Ctrl Pts',(96.7514813399379,-1.14233240293969,-5.93180883078943));
#28507=CARTESIAN_POINT('Ctrl Pts',(96.702628665276,-1.15367688326447,-5.93497861184306));
#28508=CARTESIAN_POINT('Ctrl Pts',(96.5763889960245,-1.17461568911899,-5.94296005245186));
#28509=CARTESIAN_POINT('Ctrl Pts',(96.498510344349,-1.1797077471644,-5.94769956346187));
#28510=CARTESIAN_POINT('Ctrl Pts',(96.3836244399372,-1.1758249117246,-5.95498205271896));
#28511=CARTESIAN_POINT('Ctrl Pts',(96.3466332245655,-1.1728211359748,-5.95736908685501));
#28512=CARTESIAN_POINT('Ctrl Pts',(96.2997322596512,-1.16677287862026,-5.96048128352236));
#28513=CARTESIAN_POINT('Ctrl Pts',(96.2896342031307,-1.16533706287848,-5.96115640114669));
#28514=CARTESIAN_POINT('Ctrl Pts',(96.2735430830912,-1.16283546968183,-5.96224083626712));
#28515=CARTESIAN_POINT('Ctrl Pts',(96.2675372773464,-1.16185404955828,-5.96264751785578));
#28516=CARTESIAN_POINT('Ctrl Pts',(96.2561699742928,-1.15990592974048,-5.96342103750785));
#28517=CARTESIAN_POINT('Ctrl Pts',(96.250807035844,-1.15894848404034,-5.96378757638779));
#28518=CARTESIAN_POINT('Ctrl Pts',(96.2386302914167,-1.15668728463125,-5.96462355704434));
#28519=CARTESIAN_POINT('Ctrl Pts',(96.2318210271839,-1.15536047417377,-5.96509371184269));
#28520=CARTESIAN_POINT('Ctrl Pts',(96.2109900773673,-1.15111012413355,-5.96654043305423));
#28521=CARTESIAN_POINT('Ctrl Pts',(96.1970101161149,-1.14799098506005,-5.9675231006559));
#28522=CARTESIAN_POINT('Ctrl Pts',(96.1293686296342,-1.13159855558318,-5.97233705223512));
#28523=CARTESIAN_POINT('Ctrl Pts',(96.0766371957147,-1.11481526090167,-5.97627734729979));
#28524=CARTESIAN_POINT('Ctrl Pts',(96.0087311372148,-1.08781181259783,-5.98158497952861));
#28525=CARTESIAN_POINT('Ctrl Pts',(95.9923289587445,-1.08085434687124,-5.98288536168809));
#28526=CARTESIAN_POINT('Ctrl Pts',(95.9021463523877,-1.04016277809069,-5.99012804347023));
#28527=CARTESIAN_POINT('Ctrl Pts',(95.8318417451423,-0.999245121751286,
-5.99614220333807));
#28528=CARTESIAN_POINT('Ctrl Pts',(95.7594468072158,-0.946423857211277,
-6.00241446591645));
#28529=CARTESIAN_POINT('Ctrl Pts',(95.7526497150005,-0.94135112457957,-6.00300402275569));
#28530=CARTESIAN_POINT('Ctrl Pts',(95.7423238777272,-0.933469769071108,
-6.00389994466016));
#28531=CARTESIAN_POINT('Ctrl Pts',(95.7387556410253,-0.930713688673121,
-6.00420959730892));
#28532=CARTESIAN_POINT('Ctrl Pts',(95.7327587544793,-0.926026508948025,
-6.00472997848996));
#28533=CARTESIAN_POINT('Ctrl Pts',(95.7303217721668,-0.924106197905514,
-6.00494143900239));
#28534=CARTESIAN_POINT('Ctrl Pts',(95.7253150869039,-0.92012882305955,-6.00537581188725));
#28535=CARTESIAN_POINT('Ctrl Pts',(95.7227463794406,-0.918070586264534,
-6.00559863937361));
#28536=CARTESIAN_POINT('Ctrl Pts',(95.7160990673194,-0.912698357915788,
-6.00617529583538));
#28537=CARTESIAN_POINT('Ctrl Pts',(95.7120338989592,-0.90936774418891,-6.00652797270699));
#28538=CARTESIAN_POINT('Ctrl Pts',(95.6944015633905,-0.894723143351059,
-6.00805846434382));
#28539=CARTESIAN_POINT('Ctrl Pts',(95.6810668262231,-0.883131267123109,
-6.00921797313003));
#28540=CARTESIAN_POINT('Ctrl Pts',(95.6445169961382,-0.849885491410347,
-6.01241860812787));
#28541=CARTESIAN_POINT('Ctrl Pts',(95.6219081173027,-0.827585897682627,
-6.01442508734404));
#28542=CARTESIAN_POINT('Ctrl Pts',(95.5831667469715,-0.786154395061466,
-6.01797186058589));
#28543=CARTESIAN_POINT('Ctrl Pts',(95.566691478387,-0.767371732940789,-6.01951938595918));
#28544=CARTESIAN_POINT('Ctrl Pts',(95.4966602615577,-0.682214597378204,
-6.02634163973363));
#28545=CARTESIAN_POINT('Ctrl Pts',(95.4498147219456,-0.610670738457653,
-6.03159699690171));
#28546=CARTESIAN_POINT('Ctrl Pts',(95.4041781380538,-0.521106713352949,
-6.03815005201377));
#28547=CARTESIAN_POINT('Ctrl Pts',(95.397516541759,-0.50738000485435,-6.03915294986812));
#28548=CARTESIAN_POINT('Ctrl Pts',(95.3881750283886,-0.487139188377189,
-6.04063167420698));
#28549=CARTESIAN_POINT('Ctrl Pts',(95.3852837248031,-0.48072393503152,-6.04110033046827));
#28550=CARTESIAN_POINT('Ctrl Pts',(95.3802453364569,-0.469271838329592,
-6.04193710082632));
#28551=CARTESIAN_POINT('Ctrl Pts',(95.3780755433262,-0.464245164644548,
-6.04230443719358));
#28552=CARTESIAN_POINT('Ctrl Pts',(95.3736127033821,-0.453704897874547,
-6.04307489387727));
#28553=CARTESIAN_POINT('Ctrl Pts',(95.3713263884722,-0.448188641871719,
-6.04347822714097));
#28554=CARTESIAN_POINT('Ctrl Pts',(95.3654454394189,-0.433688735638682,
-6.04453884700305));
#28555=CARTESIAN_POINT('Ctrl Pts',(95.3619194579964,-0.424677910251511,
-6.04519838854339));
#28556=CARTESIAN_POINT('Ctrl Pts',(95.3460284655378,-0.382544986985547,
-6.04828502867238));
#28557=CARTESIAN_POINT('Ctrl Pts',(95.3350490270743,-0.348923404741576,
-6.05075676979272));
#28558=CARTESIAN_POINT('Ctrl Pts',(95.3091133940262,-0.255441513658896,
-6.05765645693756));
#28559=CARTESIAN_POINT('Ctrl Pts',(95.2973215400775,-0.19482389157392,-6.06216530922561));
#28560=CARTESIAN_POINT('Ctrl Pts',(95.2830716488148,-0.0699851970086391,
-6.07138696368523));
#28561=CARTESIAN_POINT('Ctrl Pts',(95.2810076555278,-0.00590972651939632,
-6.07608536700387));
#28562=CARTESIAN_POINT('Ctrl Pts',(95.2846532215387,0.0680002942624265,
-6.0812742434572));
#28563=CARTESIAN_POINT('Ctrl Pts',(95.2852724147278,0.0779730858810877,
-6.08196936667564));
#28564=CARTESIAN_POINT('Ctrl Pts',(95.2863122156596,0.0918603519664206,
-6.08292925626069));
#28565=CARTESIAN_POINT('Ctrl Pts',(95.2866256207638,0.0957820865274885,
-6.08319942721361));
#28566=CARTESIAN_POINT('Ctrl Pts',(95.2872004482296,0.102547960475035,-6.08366389577261));
#28567=CARTESIAN_POINT('Ctrl Pts',(95.2874525730672,0.10539282416953,-6.08385869196536));
#28568=CARTESIAN_POINT('Ctrl Pts',(95.2880066725187,0.111396596054765,-6.08426869253285));
#28569=CARTESIAN_POINT('Ctrl Pts',(95.28831107007,0.11455525302986,-6.08448375541922));
#28570=CARTESIAN_POINT('Ctrl Pts',(95.2890987636025,0.122396896150111,-6.08501615447631));
#28571=CARTESIAN_POINT('Ctrl Pts',(95.2895973855799,0.127078350799416,-6.08533265484531));
#28572=CARTESIAN_POINT('Ctrl Pts',(95.2915888597733,0.144768031462634,-6.08652395838492));
#28573=CARTESIAN_POINT('Ctrl Pts',(95.2932705925018,0.157754613208788,-6.08738902227571));
#28574=CARTESIAN_POINT('Ctrl Pts',(95.2981528161411,0.191081768161256,-6.08959074361957));
#28575=CARTESIAN_POINT('Ctrl Pts',(95.3016708081423,0.211371920667645,-6.09091361081455));
#28576=CARTESIAN_POINT('Ctrl Pts',(95.3170661007777,0.288146203006812,-6.09588715099225));
#28577=CARTESIAN_POINT('Ctrl Pts',(95.3325575505042,0.343824592369923,-6.0994308518145));
#28578=CARTESIAN_POINT('Ctrl Pts',(95.3775621783982,0.469114566228311,-6.10767410206813));
#28579=CARTESIAN_POINT('Ctrl Pts',(95.409807556875,0.537461401389556,-6.11238387805394));
#28580=CARTESIAN_POINT('Ctrl Pts',(95.4536733280804,0.611180333613756,-6.11801384643724));
#28581=CARTESIAN_POINT('Ctrl Pts',(95.4591034105055,0.620037095624473,-6.1186996333092));
#28582=CARTESIAN_POINT('Ctrl Pts',(95.4682404535251,0.634506964100623,-6.11983629604845));
#28583=CARTESIAN_POINT('Ctrl Pts',(95.4718796737029,0.640162326046138,-6.12028471264617));
#28584=CARTESIAN_POINT('Ctrl Pts',(95.4785435096522,0.65032560519661,-6.12109830057862));
#28585=CARTESIAN_POINT('Ctrl Pts',(95.4815512582076,0.654844398594778,-6.12146284236517));
#28586=CARTESIAN_POINT('Ctrl Pts',(95.4880738875715,0.664498527500613,-6.12224780103712));
#28587=CARTESIAN_POINT('Ctrl Pts',(95.4915984334809,0.669627101248582,-6.12266857115714));
#28588=CARTESIAN_POINT('Ctrl Pts',(95.5013694303232,0.683606249670348,-6.12382603235099));
#28589=CARTESIAN_POINT('Ctrl Pts',(95.5076974777963,0.692398767520332,-6.12456578209746));
#28590=CARTESIAN_POINT('Ctrl Pts',(95.5459048791662,0.74397041321109,-6.12897620245101));
#28591=CARTESIAN_POINT('Ctrl Pts',(95.5805353828447,0.784624554238826,-6.13275285778048));
#28592=CARTESIAN_POINT('Ctrl Pts',(95.6513005757577,0.857100985021329,-6.14007408115646));
#28593=CARTESIAN_POINT('Ctrl Pts',(95.6868671642407,0.889334725291908,-6.14359614494818));
#28594=CARTESIAN_POINT('Ctrl Pts',(95.7463154850342,0.936940998695649,-6.14918395913571));
#28595=CARTESIAN_POINT('Ctrl Pts',(95.7689605264007,0.953776883903202,-6.15124988896251));
#28596=CARTESIAN_POINT('Ctrl Pts',(95.8207187335665,0.989444214867675,-6.15580728664749));
#28597=CARTESIAN_POINT('Ctrl Pts',(95.8501054047277,1.00783815029033,-6.15828628935765));
#28598=CARTESIAN_POINT('Ctrl Pts',(95.885539553619,1.02789795921767,-6.16111643693731));
#28599=CARTESIAN_POINT('Ctrl Pts',(95.890838935762,1.03084421874284,-6.16153565262914));
#28600=CARTESIAN_POINT('Ctrl Pts',(95.8995189946897,1.03558263038677,-6.1622154403622));
#28601=CARTESIAN_POINT('Ctrl Pts',(95.9028859895067,1.03739942198447,-6.1624774621797));
#28602=CARTESIAN_POINT('Ctrl Pts',(95.9089460211027,1.04063131763476,-6.16294599164961));
#28603=CARTESIAN_POINT('Ctrl Pts',(95.9116357334695,1.0420524199697,-6.16315286305428));
#28604=CARTESIAN_POINT('Ctrl Pts',(95.9168165849491,1.04476408419073,-6.16354925492291));
#28605=CARTESIAN_POINT('Ctrl Pts',(95.9193068175126,1.04605616108533,-6.16373887357585));
#28606=CARTESIAN_POINT('Ctrl Pts',(95.9218016730721,1.04733934308042,-6.16392795844921));
#28607=CARTESIAN_POINT('Origin',(96.460480949577,-7.19464945638997E-16,
0.924367114736168));
#28608=CARTESIAN_POINT('',(95.9218016727113,1.04733934289485,-6.7620578065779));
#28609=CARTESIAN_POINT('',(95.9218016806086,1.04733934695669,-6.66223764680097));
#28610=CARTESIAN_POINT('',(95.9218016730721,1.04733934308042,0.924367114736168));
#28611=CARTESIAN_POINT('Ctrl Pts',(95.9218016727113,1.04733934289486,-6.7620578065779));
#28612=CARTESIAN_POINT('Ctrl Pts',(95.8770371194504,1.02431553753191,-6.75890350241157));
#28613=CARTESIAN_POINT('Ctrl Pts',(95.8337985320487,0.998447554458193,-6.75569629601541));
#28614=CARTESIAN_POINT('Ctrl Pts',(95.7834943659939,0.963794505789377,-6.75168090394736));
#28615=CARTESIAN_POINT('Ctrl Pts',(95.7747235353619,0.957573725666344,-6.75096979162344));
#28616=CARTESIAN_POINT('Ctrl Pts',(95.7610269580201,0.947574635754814,-6.74984111488974));
#28617=CARTESIAN_POINT('Ctrl Pts',(95.7560436588742,0.943875880405588,-6.74942658133005));
#28618=CARTESIAN_POINT('Ctrl Pts',(95.7467549464507,0.936866984251905,-6.74864645378421));
#28619=CARTESIAN_POINT('Ctrl Pts',(95.7424427278433,0.933566100582952,-6.74828122455537));
#28620=CARTESIAN_POINT('Ctrl Pts',(95.7328219697637,0.926095587260169,-6.74745938926478));
#28621=CARTESIAN_POINT('Ctrl Pts',(95.7275261751977,0.921909932195247,-6.74700216308137));
#28622=CARTESIAN_POINT('Ctrl Pts',(95.7141084267697,0.91111621041443,-6.74583110095309));
#28623=CARTESIAN_POINT('Ctrl Pts',(95.7060382225205,0.904445051402049,-6.74511478153101));
#28624=CARTESIAN_POINT('Ctrl Pts',(95.64241746702,0.85040954813092,-6.73936978293451));
#28625=CARTESIAN_POINT('Ctrl Pts',(95.5913011040246,0.798089670711083,-6.73413479314144));
#28626=CARTESIAN_POINT('Ctrl Pts',(95.5122470941611,0.700510562234574,-6.72495563380379));
#28627=CARTESIAN_POINT('Ctrl Pts',(95.4819076367488,0.657462410372481,-6.72107325774696));
#28628=CARTESIAN_POINT('Ctrl Pts',(95.4350517157121,0.580512826719415,-6.71452929555936));
#28629=CARTESIAN_POINT('Ctrl Pts',(95.4170933497884,0.547579384063923,-6.71184211918865));
#28630=CARTESIAN_POINT('Ctrl Pts',(95.3978770438336,0.507947746161185,-6.70878235784957));
#28631=CARTESIAN_POINT('Ctrl Pts',(95.3950682017809,0.502029536064706,-6.70832987232336));
#28632=CARTESIAN_POINT('Ctrl Pts',(95.3908027257513,0.492845152670233,-6.70763482944402));
#28633=CARTESIAN_POINT('Ctrl Pts',(95.3893113955276,0.489595378216683,-6.70739027261354));
#28634=CARTESIAN_POINT('Ctrl Pts',(95.3865756224066,0.483561485219329,-6.70693881126955));
#28635=CARTESIAN_POINT('Ctrl Pts',(95.3853271949711,0.480779331932569,-6.70673167829666));
#28636=CARTESIAN_POINT('Ctrl Pts',(95.3824916276898,0.474393914186683,-6.70625860540465));
#28637=CARTESIAN_POINT('Ctrl Pts',(95.3809117382395,0.470787513613135,-6.70599310093264));
#28638=CARTESIAN_POINT('Ctrl Pts',(95.3767973173392,0.461265931236913,-6.70529636298389));
#28639=CARTESIAN_POINT('Ctrl Pts',(95.3742930880558,0.455337685803935,-6.70486686023385));
#28640=CARTESIAN_POINT('Ctrl Pts',(95.350748802712,0.398301734954217,-6.70077285439712));
#28641=CARTESIAN_POINT('Ctrl Pts',(95.3332793260234,0.345785903789721,-6.69729505969813));
#28642=CARTESIAN_POINT('Ctrl Pts',(95.3174223898593,0.283877687875081,-6.69332141647806));
#28643=CARTESIAN_POINT('Ctrl Pts',(95.3153746662151,0.275501387219925,-6.69278642430557));
#28644=CARTESIAN_POINT('Ctrl Pts',(95.2981235502004,0.201417327575342,-6.68807267907344));
#28645=CARTESIAN_POINT('Ctrl Pts',(95.2884991461971,0.134542665200355,-6.68393349144852));
#28646=CARTESIAN_POINT('Ctrl Pts',(95.2826823498589,0.0327840150691671,
-6.67745481190683));
#28647=CARTESIAN_POINT('Ctrl Pts',(95.28222756025,-0.00171249894724128,
-6.67522918194241));
#28648=CARTESIAN_POINT('Ctrl Pts',(95.2835816054693,-0.0457730014912438,
-6.67232426632857));
#28649=CARTESIAN_POINT('Ctrl Pts',(95.2839938235383,-0.0553648545971774,
-6.67168814806046));
#28650=CARTESIAN_POINT('Ctrl Pts',(95.2848516661288,-0.0708965079276218,
-6.67065158941566));
#28651=CARTESIAN_POINT('Ctrl Pts',(95.2852251720243,-0.0768399769841434,
-6.67025338279986));
#28652=CARTESIAN_POINT('Ctrl Pts',(95.2860289396269,-0.0882472378186994,
-6.6694860163606));
#28653=CARTESIAN_POINT('Ctrl Pts',(95.2864522976471,-0.0937113726519938,
-6.66911707997508));
#28654=CARTESIAN_POINT('Ctrl Pts',(95.2875092817689,-0.106219322765645,
-6.66826932806204));
#28655=CARTESIAN_POINT('Ctrl Pts',(95.2881682430029,-0.113260726815666,
-6.66778973968609));
#28656=CARTESIAN_POINT('Ctrl Pts',(95.2904686796155,-0.135665274855846,
-6.66625606955345));
#28657=CARTESIAN_POINT('Ctrl Pts',(95.2923490111909,-0.15100170166125,-6.66519465902959));
#28658=CARTESIAN_POINT('Ctrl Pts',(95.3058518756613,-0.245674233697498,
-6.6585676260039));
#28659=CARTESIAN_POINT('Ctrl Pts',(95.3252477515618,-0.323674828359904,
-6.6527594652683));
#28660=CARTESIAN_POINT('Ctrl Pts',(95.367985807511,-0.442337745785066,-6.64350834176286));
#28661=CARTESIAN_POINT('Ctrl Pts',(95.3860823872989,-0.484640395431857,
-6.64012579657745));
#28662=CARTESIAN_POINT('Ctrl Pts',(95.4159892121333,-0.544585949723476,
-6.6352847014064));
#28663=CARTESIAN_POINT('Ctrl Pts',(95.4258748662814,-0.563140483989728,
-6.63377955208505));
#28664=CARTESIAN_POINT('Ctrl Pts',(95.4428132697675,-0.592979070246764,
-6.63135867429022));
#28665=CARTESIAN_POINT('Ctrl Pts',(95.4495696285024,-0.604425365480685,
-6.63042993498791));
#28666=CARTESIAN_POINT('Ctrl Pts',(95.4589941440449,-0.619791626180912,
-6.62918547982462));
#28667=CARTESIAN_POINT('Ctrl Pts',(95.4614940188893,-0.623812949350992,
-6.62886003069042));
#28668=CARTESIAN_POINT('Ctrl Pts',(95.4657127585979,-0.630508853916345,
-6.62831863929037));
#28669=CARTESIAN_POINT('Ctrl Pts',(95.4674183007945,-0.633191712671926,
-6.62810185836539));
#28670=CARTESIAN_POINT('Ctrl Pts',(95.470674236865,-0.638267863012345,-6.62769200723682));
#28671=CARTESIAN_POINT('Ctrl Pts',(95.4722224888696,-0.640662476476597,
-6.62749879619482));
#28672=CARTESIAN_POINT('Ctrl Pts',(95.4759174468369,-0.646332039068705,
-6.62704159637374));
#28673=CARTESIAN_POINT('Ctrl Pts',(95.4780718354806,-0.649601977583934,
-6.62677810620311));
#28674=CARTESIAN_POINT('Ctrl Pts',(95.4857192190023,-0.661084141783455,
-6.62585336052541));
#28675=CARTESIAN_POINT('Ctrl Pts',(95.4912993819246,-0.66923820760908,-6.62519752516876));
#28676=CARTESIAN_POINT('Ctrl Pts',(95.5363320299228,-0.733297782744541,
-6.62004388162376));
#28677=CARTESIAN_POINT('Ctrl Pts',(95.5804912541242,-0.78574650224787,-6.6158117083185));
#28678=CARTESIAN_POINT('Ctrl Pts',(95.6902664365645,-0.89518621107208,-6.60622216171109));
#28679=CARTESIAN_POINT('Ctrl Pts',(95.7581141935825,-0.949350995624699,
-6.60087817898132));
#28680=CARTESIAN_POINT('Ctrl Pts',(95.8424503091521,-1.00265039292678,-6.59435115039625));
#28681=CARTESIAN_POINT('Ctrl Pts',(95.853738516747,-1.00952131245255,-6.59348029524783));
#28682=CARTESIAN_POINT('Ctrl Pts',(95.8709380874977,-1.01959768482887,-6.59215626220949));
#28683=CARTESIAN_POINT('Ctrl Pts',(95.8767654580151,-1.02294498723317,-6.59170815778875));
#28684=CARTESIAN_POINT('Ctrl Pts',(95.8873511140098,-1.02890559397645,-6.59089487352994));
#28685=CARTESIAN_POINT('Ctrl Pts',(95.8920994600095,-1.03153623802809,-6.59053032067421));
#28686=CARTESIAN_POINT('Ctrl Pts',(95.9023337699283,-1.03711405772246,-6.58974504468454));
#28687=CARTESIAN_POINT('Ctrl Pts',(95.9078252422478,-1.04005072446527,-6.58932396618008));
#28688=CARTESIAN_POINT('Ctrl Pts',(95.9227020458748,-1.04785528182953,-6.58818384102774));
#28689=CARTESIAN_POINT('Ctrl Pts',(95.9321298731212,-1.05264047437733,-6.58746195533605));
#28690=CARTESIAN_POINT('Ctrl Pts',(95.9810959588417,-1.07667018221481,-6.58371488916381));
#28691=CARTESIAN_POINT('Ctrl Pts',(96.0216203840396,-1.09381406515535,-6.5806193826683));
#28692=CARTESIAN_POINT('Ctrl Pts',(96.1386261593378,-1.13576332831866,-6.57169916182054));
#28693=CARTESIAN_POINT('Ctrl Pts',(96.2168211188963,-1.15506573166786,-6.56574380785287));
#28694=CARTESIAN_POINT('Ctrl Pts',(96.3233663105552,-1.17005912738607,-6.55791348947447));
#28695=CARTESIAN_POINT('Ctrl Pts',(96.350497227059,-1.17292052713774,-6.55594570669523));
#28696=CARTESIAN_POINT('Ctrl Pts',(96.3884220147451,-1.17559261825991,-6.55325065614377));
#28697=CARTESIAN_POINT('Ctrl Pts',(96.3991496217172,-1.17620108002537,-6.55249451763901));
#28698=CARTESIAN_POINT('Ctrl Pts',(96.4179139396726,-1.17700794553109,-6.55118437050939));
#28699=CARTESIAN_POINT('Ctrl Pts',(96.4259470167422,-1.17727102679033,-6.55062747829001));
#28700=CARTESIAN_POINT('Ctrl Pts',(96.4378608406751,-1.17753914706734,-6.54980806483703));
#28701=CARTESIAN_POINT('Ctrl Pts',(96.4417397309224,-1.17760726900286,-6.54954230400516));
#28702=CARTESIAN_POINT('Ctrl Pts',(96.4483729542905,-1.17769098012333,-6.54908965952942));
#28703=CARTESIAN_POINT('Ctrl Pts',(96.4511270821563,-1.17771607527399,-6.5489022626791));
#28704=CARTESIAN_POINT('Ctrl Pts',(96.4573810237441,-1.17775112013457,-6.54847797465331));
#28705=CARTESIAN_POINT('Ctrl Pts',(96.460880812931,-1.17775513220227,-6.54824141232947));
#28706=CARTESIAN_POINT('Ctrl Pts',(96.4704194527739,-1.17772354841607,-6.54759892203324));
#28707=CARTESIAN_POINT('Ctrl Pts',(96.4764581961902,-1.17765710704174,-6.54719463930771));
#28708=CARTESIAN_POINT('Ctrl Pts',(96.5070392354961,-1.1770853638528,-6.54515857853924));
#28709=CARTESIAN_POINT('Ctrl Pts',(96.5315638859691,-1.17585927913545,-6.54356252610402));
#28710=CARTESIAN_POINT('Ctrl Pts',(96.6413452961866,-1.16692302732949,-6.53651201617018));
#28711=CARTESIAN_POINT('Ctrl Pts',(96.7256509405527,-1.15069914691953,-6.53133637836794));
#28712=CARTESIAN_POINT('Ctrl Pts',(96.8423662896013,-1.11471656023951,-6.52370707882488));
#28713=CARTESIAN_POINT('Ctrl Pts',(96.8767519601512,-1.10233731423134,-6.52140104235198));
#28714=CARTESIAN_POINT('Ctrl Pts',(96.9250767686707,-1.08235596042181,-6.51803320752284));
#28715=CARTESIAN_POINT('Ctrl Pts',(96.9395254836066,-1.07603903230836,-6.51700954238216));
#28716=CARTESIAN_POINT('Ctrl Pts',(96.9651675148167,-1.06420960559142,-6.51515952468187));
#28717=CARTESIAN_POINT('Ctrl Pts',(96.976408429865,-1.05880566184313,-6.51433677402654));
#28718=CARTESIAN_POINT('Ctrl Pts',(96.9934359994418,-1.05028431207131,-6.51307135825483));
#28719=CARTESIAN_POINT('Ctrl Pts',(96.9992861253679,-1.04729518329883,-6.51263310103723));
#28720=CARTESIAN_POINT('Ctrl Pts',(97.0094495739748,-1.04199446114889,-6.51186543272601));
#28721=CARTESIAN_POINT('Ctrl Pts',(97.0137741067745,-1.03970461603379,-6.51153678483164));
#28722=CARTESIAN_POINT('Ctrl Pts',(97.023504136168,-1.03447465738387,-6.5107927271788));
#28723=CARTESIAN_POINT('Ctrl Pts',(97.0289010784578,-1.03151901582678,-6.51037677949352));
#28724=CARTESIAN_POINT('Ctrl Pts',(97.0434524863879,-1.02340104621739,-6.50924632855243));
#28725=CARTESIAN_POINT('Ctrl Pts',(97.0525612338912,-1.01815835636783,-6.50852900134568));
#28726=CARTESIAN_POINT('Ctrl Pts',(97.0970351749597,-0.991762027325579,
-6.50497754541005));
#28727=CARTESIAN_POINT('Ctrl Pts',(97.1313396093513,-0.968886555653917,
-6.50208217499418));
#28728=CARTESIAN_POINT('Ctrl Pts',(97.2246286154107,-0.899345267029481,
-6.49375301315903));
#28729=CARTESIAN_POINT('Ctrl Pts',(97.2804437874361,-0.848765357205703,
-6.48820138308741));
#28730=CARTESIAN_POINT('Ctrl Pts',(97.3607237898152,-0.760656683276405,
-6.47948943620218));
#28731=CARTESIAN_POINT('Ctrl Pts',(97.3885467461173,-0.726450577163617,
-6.47630042458242));
#28732=CARTESIAN_POINT('Ctrl Pts',(97.419981390835,-0.683040888322591,-6.47254807776065));
#28733=CARTESIAN_POINT('Ctrl Pts',(97.4254792035999,-0.675251313284863,
-6.47188567271996));
#28734=CARTESIAN_POINT('Ctrl Pts',(97.4332369364403,-0.663971476982828,
-6.47094299065326));
#28735=CARTESIAN_POINT('Ctrl Pts',(97.4355737448172,-0.660534915212928,
-6.47065795757379));
#28736=CARTESIAN_POINT('Ctrl Pts',(97.4396076412911,-0.654534518784581,
-6.47016413491832));
#28737=CARTESIAN_POINT('Ctrl Pts',(97.4413129510756,-0.651976303583453,
-6.4699548102471));
#28738=CARTESIAN_POINT('Ctrl Pts',(97.4449073698435,-0.646538125384458,
-6.46951242701816));
#28739=CARTESIAN_POINT('Ctrl Pts',(97.4467938782767,-0.643656532585285,
-6.46927953689866));
#28740=CARTESIAN_POINT('Ctrl Pts',(97.4519022161957,-0.635778482086857,
-6.46864684674658));
#28741=CARTESIAN_POINT('Ctrl Pts',(97.4550989518948,-0.630765756304915,
-6.4682486458724));
#28742=CARTESIAN_POINT('Ctrl Pts',(97.4702440119052,-0.606615700005522,
-6.4663499910362));
#28743=CARTESIAN_POINT('Ctrl Pts',(97.4816796316555,-0.587160506480568,
-6.46487953164393));
#28744=CARTESIAN_POINT('Ctrl Pts',(97.5030883246456,-0.548218410019451,
-6.46202629314796));
#28745=CARTESIAN_POINT('Ctrl Pts',(97.5130909903189,-0.528758694738336,
-6.46064277683167));
#28746=CARTESIAN_POINT('Ctrl Pts',(97.5498478125473,-0.452067564998741,
-6.45531021791453));
#28747=CARTESIAN_POINT('Ctrl Pts',(97.5725228175004,-0.392999393906959,
-6.45145147319395));
#28748=CARTESIAN_POINT('Ctrl Pts',(97.6035632474028,-0.287487839187075,
-6.44459230214978));
#28749=CARTESIAN_POINT('Ctrl Pts',(97.6140845393863,-0.241835666300203,
-6.44163585950262));
#28750=CARTESIAN_POINT('Ctrl Pts',(97.6248372168816,-0.17801799557965,-6.43743474833347));
#28751=CARTESIAN_POINT('Ctrl Pts',(97.6274098763244,-0.160289577392258,
-6.43626082756384));
#28752=CARTESIAN_POINT('Ctrl Pts',(97.6304940943667,-0.134987882264762,
-6.43457247195045));
#28753=CARTESIAN_POINT('Ctrl Pts',(97.6313383982642,-0.127457121100252,
-6.4340683350963));
#28754=CARTESIAN_POINT('Ctrl Pts',(97.632674183451,-0.114406259897808,-6.43319162958434));
#28755=CARTESIAN_POINT('Ctrl Pts',(97.6331994912195,-0.108889807352842,
-6.43282012054389));
#28756=CARTESIAN_POINT('Ctrl Pts',(97.6341349203291,-0.0982730836760085,
-6.4321032435833));
#28757=CARTESIAN_POINT('Ctrl Pts',(97.6345507737163,-0.0931734332342861,
-6.43175806215189));
#28758=CARTESIAN_POINT('Ctrl Pts',(97.6355563586899,-0.0797637110079606,
-6.43084811551969));
#28759=CARTESIAN_POINT('Ctrl Pts',(97.6360911603116,-0.0714499330442044,
-6.43028166602089));
#28760=CARTESIAN_POINT('Ctrl Pts',(97.6376772222503,-0.0419036223203609,
-6.42826000418489));
#28761=CARTESIAN_POINT('Ctrl Pts',(97.6382417257713,-0.0206501988785537,
-6.42678999378801));
#28762=CARTESIAN_POINT('Ctrl Pts',(97.6382140000112,0.0332598275708147,
-6.42301894700937));
#28763=CARTESIAN_POINT('Ctrl Pts',(97.6368391832829,0.065896413955691,-6.42069626626272));
#28764=CARTESIAN_POINT('Ctrl Pts',(97.6298868297191,0.148791611277646,-6.41470261470262));
#28765=CARTESIAN_POINT('Ctrl Pts',(97.6224263379453,0.198825026263183,-6.41099429383886));
#28766=CARTESIAN_POINT('Ctrl Pts',(97.6110837334361,0.251434082744044,-6.4070450548286));
#28767=CARTESIAN_POINT('Ctrl Pts',(97.6103776089468,0.254643941617654,-6.4068039108287));
#28768=CARTESIAN_POINT('Ctrl Pts',(97.6049769058671,0.27871353615749,-6.40499438376585));
#28769=CARTESIAN_POINT('Ctrl Pts',(97.599728395594,0.299445359541044,-6.40342850915444));
#28770=CARTESIAN_POINT('Ctrl Pts',(97.5831333425461,0.358220641598347,-6.39898418391393));
#28771=CARTESIAN_POINT('Ctrl Pts',(97.57042310532,0.395852911075683,-6.39613195607784));
#28772=CARTESIAN_POINT('Ctrl Pts',(97.5535409305178,0.43858171554812,-6.39293680336859));
#28773=CARTESIAN_POINT('Ctrl Pts',(97.5512005187677,0.444370193353944,-6.39250491846749));
#28774=CARTESIAN_POINT('Ctrl Pts',(97.5473311181675,0.453725499701246,-6.39180878419786));
#28775=CARTESIAN_POINT('Ctrl Pts',(97.5458303760868,0.457303773767396,-6.3915429708514));
#28776=CARTESIAN_POINT('Ctrl Pts',(97.5431203141618,0.463676980146255,-6.39107041973514));
#28777=CARTESIAN_POINT('Ctrl Pts',(97.541917813519,0.466474699923981,-6.39086328978902));
#28778=CARTESIAN_POINT('Ctrl Pts',(97.5392628863272,0.472586166601736,-6.39041151453834));
#28779=CARTESIAN_POINT('Ctrl Pts',(97.5378060353482,0.475897901204183,-6.39016713702707));
#28780=CARTESIAN_POINT('Ctrl Pts',(97.5335875357173,0.485368806173461,-6.3894693658288));
#28781=CARTESIAN_POINT('Ctrl Pts',(97.5307881136972,0.491511142242594,-6.38901816654835));
#28782=CARTESIAN_POINT('Ctrl Pts',(97.5096267554015,0.536903968263261,-6.38569123003344));
#28783=CARTESIAN_POINT('Ctrl Pts',(97.4891616271496,0.575143260742656,-6.38292990678871));
#28784=CARTESIAN_POINT('Ctrl Pts',(97.4147699519221,0.697411795327552,-6.37395800888754));
#28785=CARTESIAN_POINT('Ctrl Pts',(97.3522885149229,0.775712726408799,-6.36794002487711));
#28786=CARTESIAN_POINT('Ctrl Pts',(97.2627906157386,0.862563547676247,-6.35992858924687));
#28787=CARTESIAN_POINT('Ctrl Pts',(97.2443526058202,0.879353034369116,-6.35830710163057));
#28788=CARTESIAN_POINT('Ctrl Pts',(97.218653605128,0.901303461059263,-6.35607605470773));
#28789=CARTESIAN_POINT('Ctrl Pts',(97.2118458023342,0.906986524420999,-6.35548769273213));
#28790=CARTESIAN_POINT('Ctrl Pts',(97.2009317177421,0.91589024760749,-6.35454825769523));
#28791=CARTESIAN_POINT('Ctrl Pts',(97.1968669970133,0.919161505610537,-6.35419920861212));
#28792=CARTESIAN_POINT('Ctrl Pts',(97.1884865346369,0.925814772599333,-6.35348115195328));
#28793=CARTESIAN_POINT('Ctrl Pts',(97.1841686497784,0.929193863450808,-6.35311204154711));
#28794=CARTESIAN_POINT('Ctrl Pts',(97.1741182418024,0.936946565517706,-6.35225476622127));
#28795=CARTESIAN_POINT('Ctrl Pts',(97.1683688851874,0.941297890205902,-6.35176575228866));
#28796=CARTESIAN_POINT('Ctrl Pts',(97.1499045966491,0.955007507601559,-6.35019942463083));
#28797=CARTESIAN_POINT('Ctrl Pts',(97.1370417562897,0.964162713264354,-6.34911445219719));
#28798=CARTESIAN_POINT('Ctrl Pts',(97.1063590465374,0.985084978912101,-6.34653948599908));
#28799=CARTESIAN_POINT('Ctrl Pts',(97.0883959686486,0.996631106529467,-6.34504197695392));
#28800=CARTESIAN_POINT('Ctrl Pts',(97.0192090762279,1.0384892691016,-6.33931090346108));
#28801=CARTESIAN_POINT('Ctrl Pts',(96.9660316459853,1.06538919758095,-6.33497436830918));
#28802=CARTESIAN_POINT('Ctrl Pts',(96.8462006986222,1.11500791331544,-6.32545956510982));
#28803=CARTESIAN_POINT('Ctrl Pts',(96.7790691923926,1.13601306406664,-6.3202870873618));
#28804=CARTESIAN_POINT('Ctrl Pts',(96.7008772836855,1.15299646752377,-6.31467876964369));
#28805=CARTESIAN_POINT('Ctrl Pts',(96.6912671254805,1.15495844436013,-6.31399663193341));
#28806=CARTESIAN_POINT('Ctrl Pts',(96.6777994931307,1.15753313023076,-6.31305168286904));
#28807=CARTESIAN_POINT('Ctrl Pts',(96.6739620997812,1.15824699289352,-6.31278367702705));
#28808=CARTESIAN_POINT('Ctrl Pts',(96.6673183216287,1.15944878152602,-6.31232190095664));
#28809=CARTESIAN_POINT('Ctrl Pts',(96.6645136143982,1.15994562268493,-6.31212764536109));
#28810=CARTESIAN_POINT('Ctrl Pts',(96.6585710386177,1.16097610212309,-6.31171754942728));
#28811=CARTESIAN_POINT('Ctrl Pts',(96.6554327538588,1.16150720513299,-6.31150185716318));
#28812=CARTESIAN_POINT('Ctrl Pts',(96.6476025712696,1.16279970509167,-6.31096580013974));
#28813=CARTESIAN_POINT('Ctrl Pts',(96.6429080831402,1.1635454431752,-6.31064629631608));
#28814=CARTESIAN_POINT('Ctrl Pts',(96.6249372747957,1.16628874031958,-6.30942996184777));
#28815=CARTESIAN_POINT('Ctrl Pts',(96.6116310703794,1.16808774814728,-6.30854340475372));
#28816=CARTESIAN_POINT('Ctrl Pts',(96.5771242340034,1.17215352552066,-6.30627382807899));
#28817=CARTESIAN_POINT('Ctrl Pts',(96.5558869972553,1.17407297024528,-6.30490569074452));
#28818=CARTESIAN_POINT('Ctrl Pts',(96.4372531592432,1.1815545770533,-6.29736534195314));
#28819=CARTESIAN_POINT('Ctrl Pts',(96.3395107043682,1.1755760214272,-6.29150426647801));
#28820=CARTESIAN_POINT('Ctrl Pts',(96.20736108397,1.1508198138611,-6.2829849723384));
#28821=CARTESIAN_POINT('Ctrl Pts',(96.171444548039,1.14232808364211,-6.28061083410622));
#28822=CARTESIAN_POINT('Ctrl Pts',(96.126190896751,1.12935782354046,-6.27751264577182));
#28823=CARTESIAN_POINT('Ctrl Pts',(96.1164307953046,1.12642283964321,-6.27683803425672));
#28824=CARTESIAN_POINT('Ctrl Pts',(96.1009071067815,1.12153409691083,-6.27575419847077));
#28825=CARTESIAN_POINT('Ctrl Pts',(96.0951182978829,1.1196616494983,-6.27534760455511));
#28826=CARTESIAN_POINT('Ctrl Pts',(96.0841733583678,1.11602748462523,-6.27457411431935));
#28827=CARTESIAN_POINT('Ctrl Pts',(96.0790144225876,1.11427466843559,-6.27420751617533));
#28828=CARTESIAN_POINT('Ctrl Pts',(96.0673113239119,1.11020758805205,-6.27337120888573));
#28829=CARTESIAN_POINT('Ctrl Pts',(96.0607751354811,1.10787115754674,-6.27290078496142));
#28830=CARTESIAN_POINT('Ctrl Pts',(96.0407986197154,1.10053054689853,-6.27145252376573));
#28831=CARTESIAN_POINT('Ctrl Pts',(96.0274291553537,1.09533869406666,-6.27046856689777));
#28832=CARTESIAN_POINT('Ctrl Pts',(95.9827623785651,1.07704736799627,-6.26713000623253));
#28833=CARTESIAN_POINT('Ctrl Pts',(95.9519486350283,1.06284486748073,-6.2647404968259));
#28834=CARTESIAN_POINT('Ctrl Pts',(95.9218016184021,1.04733931496196,-6.26231549050881));
#28835=CARTESIAN_POINT('',(97.6382310967021,0.000547024120039822,-6.32657975732822));
#28836=CARTESIAN_POINT('Ctrl Pts',(95.9218016730721,1.04733934308042,-6.16392795844921));
#28837=CARTESIAN_POINT('Ctrl Pts',(95.922563112493,1.04773097511363,-6.16398566787288));
#28838=CARTESIAN_POINT('Ctrl Pts',(95.9233249825432,1.04812177859259,-6.16404332757542));
#28839=CARTESIAN_POINT('Ctrl Pts',(95.9302824848695,1.05168107125754,-6.16456913886483));
#28840=CARTESIAN_POINT('Ctrl Pts',(95.936505840373,1.05479551493692,-6.16503407858795));
#28841=CARTESIAN_POINT('Ctrl Pts',(95.9896527061383,1.0808061053226,-6.16896211148023));
#28842=CARTESIAN_POINT('Ctrl Pts',(96.0380297290864,1.10061687438719,-6.17225861912953));
#28843=CARTESIAN_POINT('Ctrl Pts',(96.1665038556081,1.14350238451902,-6.18069540740678));
#28844=CARTESIAN_POINT('Ctrl Pts',(96.2480061203872,1.16141047430317,-6.18575941567));
#28845=CARTESIAN_POINT('Ctrl Pts',(96.3613081711256,1.17397073361564,-6.19303060148706));
#28846=CARTESIAN_POINT('Ctrl Pts',(96.3920204829251,1.17616131225994,-6.19502196731284));
#28847=CARTESIAN_POINT('Ctrl Pts',(96.4323459294853,1.17745278330718,-6.19768092560179));
#28848=CARTESIAN_POINT('Ctrl Pts',(96.4419135820801,1.17764250953152,-6.19831501275069));
#28849=CARTESIAN_POINT('Ctrl Pts',(96.4574301591676,1.1777610686296,-6.19934905617941));
#28850=CARTESIAN_POINT('Ctrl Pts',(96.4633782256095,1.17776145534552,-6.19974679874765));
#28851=CARTESIAN_POINT('Ctrl Pts',(96.4748079237645,1.1776756149533,-6.20051381549532));
#28852=CARTESIAN_POINT('Ctrl Pts',(96.4802894633657,1.17759616901684,-6.20088287026639));
#28853=CARTESIAN_POINT('Ctrl Pts',(96.4929759829276,1.17732369508064,-6.20173989376937));
#28854=CARTESIAN_POINT('Ctrl Pts',(96.5001800810567,1.17710279294289,-6.20222871024624));
#28855=CARTESIAN_POINT('Ctrl Pts',(96.5231426733327,1.17618764577807,-6.20379389131561));
#28856=CARTESIAN_POINT('Ctrl Pts',(96.5388888760486,1.17524296423839,-6.20487789939013));
#28857=CARTESIAN_POINT('Ctrl Pts',(96.5758697331021,1.17227784345375,-6.20745019712985));
#28858=CARTESIAN_POINT('Ctrl Pts',(96.5970772987344,1.16999626204206,-6.20894598144011));
#28859=CARTESIAN_POINT('Ctrl Pts',(96.6770743644979,1.15918533208471,-6.2146669342726));
#28860=CARTESIAN_POINT('Ctrl Pts',(96.7352462647189,1.14678940374526,-6.21899467502292));
#28861=CARTESIAN_POINT('Ctrl Pts',(96.8597490688461,1.11023957005936,-6.22851362957974));
#28862=CARTESIAN_POINT('Ctrl Pts',(96.9253628933871,1.08440467346871,-6.2336994955841));
#28863=CARTESIAN_POINT('Ctrl Pts',(96.9970705172817,1.04845760473146,-6.2393215817859));
#28864=CARTESIAN_POINT('Ctrl Pts',(97.0058040001702,1.04394180839303,-6.2400053243453));
#28865=CARTESIAN_POINT('Ctrl Pts',(97.0179121310306,1.0374876696322,-6.24095085073008));
#28866=CARTESIAN_POINT('Ctrl Pts',(97.0213349822347,1.03564131909707,-6.2412178688659));
#28867=CARTESIAN_POINT('Ctrl Pts',(97.0272455871402,1.03241512972441,-6.24167840302406));
#28868=CARTESIAN_POINT('Ctrl Pts',(97.0297375770687,1.03104318385395,-6.24187239849109));
#28869=CARTESIAN_POINT('Ctrl Pts',(97.0349546822618,1.02814626602596,-6.24227813774319));
#28870=CARTESIAN_POINT('Ctrl Pts',(97.0376787525753,1.02661945753236,-6.24248975956405));
#28871=CARTESIAN_POINT('Ctrl Pts',(97.0444083271762,1.0228123597931,-6.24301205897135));
#28872=CARTESIAN_POINT('Ctrl Pts',(97.048406628863,1.02051933007265,-6.2433219422143));
#28873=CARTESIAN_POINT('Ctrl Pts',(97.0570501933388,1.01549457826232,-6.24399113406132));
#28874=CARTESIAN_POINT('Ctrl Pts',(97.0616904004122,1.01275431369899,-6.24434992967829));
#28875=CARTESIAN_POINT('Ctrl Pts',(97.0748985415809,1.00483150247323,-6.24537041023857));
#28876=CARTESIAN_POINT('Ctrl Pts',(97.0834196253427,0.999571281453929,-6.24602777383116));
#28877=CARTESIAN_POINT('Ctrl Pts',(97.1125840214401,0.981049744280293,-6.24827797940317));
#28878=CARTESIAN_POINT('Ctrl Pts',(97.1328804702724,0.967251807148861,-6.24984455389308));
#28879=CARTESIAN_POINT('Ctrl Pts',(97.1957699914671,0.921561180436383,-6.25474975691232));
#28880=CARTESIAN_POINT('Ctrl Pts',(97.2366415940102,0.887412044365937,-6.25801736410874));
#28881=CARTESIAN_POINT('Ctrl Pts',(97.3283567274873,0.799581789929832,-6.26588334692849));
#28882=CARTESIAN_POINT('Ctrl Pts',(97.3767265850738,0.743660682474676,-6.27049781399808));
#28883=CARTESIAN_POINT('Ctrl Pts',(97.4255624071594,0.675144674849057,-6.2760201572786));
#28884=CARTESIAN_POINT('Ctrl Pts',(97.4314681037548,0.666623197197055,-6.27670458428418));
#28885=CARTESIAN_POINT('Ctrl Pts',(97.4410142309935,0.652452824303797,-6.27783945770471));
#28886=CARTESIAN_POINT('Ctrl Pts',(97.4447202628394,0.646848649218851,-6.27828745843873));
#28887=CARTESIAN_POINT('Ctrl Pts',(97.4513331977036,0.636660306721674,-6.2791006024171));
#28888=CARTESIAN_POINT('Ctrl Pts',(97.4542567652243,0.632087138235138,-6.27946511928141));
#28889=CARTESIAN_POINT('Ctrl Pts',(97.4604665555374,0.622223941011471,-6.28025037085191));
#28890=CARTESIAN_POINT('Ctrl Pts',(97.4637426277905,0.616927748892035,-6.28067146124422));
#28891=CARTESIAN_POINT('Ctrl Pts',(97.4726130712866,0.602330012569163,-6.28183071466693));
#28892=CARTESIAN_POINT('Ctrl Pts',(97.4781209830983,0.592976917207233,-6.28257195220699));
#28893=CARTESIAN_POINT('Ctrl Pts',(97.5101647293477,0.536801165153988,-6.28701620606528));
#28894=CARTESIAN_POINT('Ctrl Pts',(97.5335912196377,0.488287176819846,-6.29082716945488));
#28895=CARTESIAN_POINT('Ctrl Pts',(97.5851507511299,0.359709912925321,-6.30084307963857));
#28896=CARTESIAN_POINT('Ctrl Pts',(97.6081053575673,0.277904047255513,-6.30715021368868));
#28897=CARTESIAN_POINT('Ctrl Pts',(97.6260839112692,0.170446412269312,-6.31498837514428));
#28898=CARTESIAN_POINT('Ctrl Pts',(97.6293442998321,0.14642710755381,-6.31671076688734));
#28899=CARTESIAN_POINT('Ctrl Pts',(97.6326395923647,0.114870847708047,-6.31892135839255));
#28900=CARTESIAN_POINT('Ctrl Pts',(97.6333466432607,0.107411672180922,-6.319440080944));
#28901=CARTESIAN_POINT('Ctrl Pts',(97.6343067300385,0.0961389542123721,
-6.3202177571464));
#28902=CARTESIAN_POINT('Ctrl Pts',(97.6346124519052,0.0923302641037898,
-6.32047943412826));
#28903=CARTESIAN_POINT('Ctrl Pts',(97.6351141126204,0.0856746027480229,
-6.32093475840938));
#28904=CARTESIAN_POINT('Ctrl Pts',(97.6353182449771,0.082828347728783,-6.32112884702605));
#28905=CARTESIAN_POINT('Ctrl Pts',(97.6357079288444,0.0771033748498703,
-6.32151796995362));
#28906=CARTESIAN_POINT('Ctrl Pts',(97.6358932493507,0.074224720957689,-6.32171299255664));
#28907=CARTESIAN_POINT('Ctrl Pts',(97.6362833068183,0.0677975840028478,
-6.32214705208869));
#28908=CARTESIAN_POINT('Ctrl Pts',(97.6364825613619,0.0642487787548318,
-6.32238579392906));
#28909=CARTESIAN_POINT('Ctrl Pts',(97.6370764387331,0.0527410317584296,
-6.32315711372388));
#28910=CARTESIAN_POINT('Ctrl Pts',(97.6374063641442,0.0447787711189562,
-6.32368637478584));
#28911=CARTESIAN_POINT('Ctrl Pts',(97.6380333978018,0.0247283095537273,
-6.32500941512401));
#28912=CARTESIAN_POINT('Ctrl Pts',(97.6382252217385,0.0126375602041876,
-6.32579832911198));
#28913=CARTESIAN_POINT('Ctrl Pts',(97.6382308232104,0.000545579152858998,
-6.32658032579348));
#28914=CARTESIAN_POINT('Ctrl Pts',(97.638230822526,0.000547054579173728,
-6.32658023037662));
#28915=CARTESIAN_POINT('Ctrl Pts',(97.6382841975052,-0.114363554607446,
-6.33401158344397));
#28916=CARTESIAN_POINT('Ctrl Pts',(97.6215212050235,-0.228681168633696,
-6.3408298649339));
#28917=CARTESIAN_POINT('Ctrl Pts',(97.5782532072311,-0.37274396974925,-6.35038124470256));
#28918=CARTESIAN_POINT('Ctrl Pts',(97.5665233819034,-0.406229794622361,
-6.35266825828143));
#28919=CARTESIAN_POINT('Ctrl Pts',(97.5496903086269,-0.448120347660356,
-6.3556427710319));
#28920=CARTESIAN_POINT('Ctrl Pts',(97.5459683144041,-0.457062408679015,
-6.35628442907455));
#28921=CARTESIAN_POINT('Ctrl Pts',(97.5397732695014,-0.471443349841197,
-6.35732776507842));
#28922=CARTESIAN_POINT('Ctrl Pts',(97.5373683294266,-0.476911221145789,
-6.35772715364962));
#28923=CARTESIAN_POINT('Ctrl Pts',(97.532679841269,-0.48735466350336,-6.35849527059932));
#28924=CARTESIAN_POINT('Ctrl Pts',(97.5304029865321,-0.492333082868035,
-6.35886376436613));
#28925=CARTESIAN_POINT('Ctrl Pts',(97.525122173311,-0.503670111888112,-6.35970834484416));
#28926=CARTESIAN_POINT('Ctrl Pts',(97.522095828661,-0.510018001328114,-6.36018518509997));
#28927=CARTESIAN_POINT('Ctrl Pts',(97.5123344175467,-0.530029620593106,
-6.36170116777126));
#28928=CARTESIAN_POINT('Ctrl Pts',(97.5053912467714,-0.543589504999928,
-6.3627474028073));
#28929=CARTESIAN_POINT('Ctrl Pts',(97.4576207080709,-0.632585677250096,
-6.36974446189395));
#28930=CARTESIAN_POINT('Ctrl Pts',(97.4089266922658,-0.70348973500071,-6.37597722598481));
#28931=CARTESIAN_POINT('Ctrl Pts',(97.3205649228632,-0.806113269699055,
-6.3859155728305));
#28932=CARTESIAN_POINT('Ctrl Pts',(97.2857989419411,-0.841673204556276,
-6.38956512077702));
#28933=CARTESIAN_POINT('Ctrl Pts',(97.2373154659919,-0.885362029434795,
-6.39424050199586));
#28934=CARTESIAN_POINT('Ctrl Pts',(97.2255351438537,-0.895561230911203,
-6.39534708119846));
#28935=CARTESIAN_POINT('Ctrl Pts',(97.2079160242565,-0.910214078499494,
-6.39695551443686));
#28936=CARTESIAN_POINT('Ctrl Pts',(97.2022328558241,-0.914851340635053,
-6.39746741681967));
#28937=CARTESIAN_POINT('Ctrl Pts',(97.1931083269955,-0.922155700945378,
-6.39827788426448));
#28938=CARTESIAN_POINT('Ctrl Pts',(97.1896949613425,-0.924857252453686,
-6.39857856643817));
#28939=CARTESIAN_POINT('Ctrl Pts',(97.1832183978412,-0.929925063789778,
-6.39914425416295));
#28940=CARTESIAN_POINT('Ctrl Pts',(97.1801583700353,-0.932295261675217,
-6.39940951602619));
#28941=CARTESIAN_POINT('Ctrl Pts',(97.1770741684891,-0.934659949584272,
-6.3996748138989));
#28942=CARTESIAN_POINT('Ctrl Pts',(97.1770616775413,-0.93466952612027,-6.39967588831562));
#28943=CARTESIAN_POINT('Ctrl Pts',(97.1770365006298,-0.934688827905284,
-6.39967805385534));
#28944=CARTESIAN_POINT('Ctrl Pts',(97.1770238151556,-0.93469855276653,-6.39967914493518));
#28945=CARTESIAN_POINT('Ctrl Pts',(97.1769982440161,-0.934718155131924,
-6.3996813442431));
#28946=CARTESIAN_POINT('Ctrl Pts',(97.1769853579655,-0.934728032918421,
-6.39968245250321));
#28947=CARTESIAN_POINT('Ctrl Pts',(97.1769593795787,-0.934747945766344,
-6.39968468669242));
#28948=CARTESIAN_POINT('Ctrl Pts',(97.1769462879421,-0.934757980278049,
-6.39968581256022));
#28949=CARTESIAN_POINT('Ctrl Pts',(97.1769198932066,-0.93477821050335,-6.39968808240652));
#28950=CARTESIAN_POINT('Ctrl Pts',(97.1769065892131,-0.934788406888409,
-6.39968922646074));
#28951=CARTESIAN_POINT('Ctrl Pts',(97.1768797629196,-0.934808966062894,
-6.3996915332648));
#28952=CARTESIAN_POINT('Ctrl Pts',(97.1768662416346,-0.934819328059535,
-6.39969269592608));
#28953=CARTESIAN_POINT('Ctrl Pts',(97.1768389749724,-0.934840222846379,
-6.39969504043793));
#28954=CARTESIAN_POINT('Ctrl Pts',(97.1768252288227,-0.93485075621291,-6.39969622235359));
#28955=CARTESIAN_POINT('Ctrl Pts',(97.1767975058387,-0.934871998743925,
-6.39969860593701));
#28956=CARTESIAN_POINT('Ctrl Pts',(97.176783529133,-0.934882707793599,-6.39969980759232));
#28957=CARTESIAN_POINT('Ctrl Pts',(97.1767553380894,-0.934904306965047,
-6.39970223124818));
#28958=CARTESIAN_POINT('Ctrl Pts',(97.1767411235764,-0.934915197204015,
-6.39970345326234));
#28959=CARTESIAN_POINT('Ctrl Pts',(97.1767124495286,-0.934937164363926,
-6.39970591826676));
#28960=CARTESIAN_POINT('Ctrl Pts',(97.1766979903701,-0.934948240978808,
-6.39970716122316));
#28961=CARTESIAN_POINT('Ctrl Pts',(97.1766688198372,-0.934970586347813,
-6.39970966872592));
#28962=CARTESIAN_POINT('Ctrl Pts',(97.1766541082385,-0.934981855255116,
-6.39971093328997));
#28963=CARTESIAN_POINT('Ctrl Pts',(97.1766244253358,-0.935004590889115,
-6.39971348464696));
#28964=CARTESIAN_POINT('Ctrl Pts',(97.1766094537715,-0.935016057795706,
-6.39971477146062));
#28965=CARTESIAN_POINT('Ctrl Pts',(97.1765792424907,-0.935039195838656,
-6.39971736803779));
#28966=CARTESIAN_POINT('Ctrl Pts',(97.1765640031537,-0.935050866663774,
-6.39971867776693));
#28967=CARTESIAN_POINT('Ctrl Pts',(97.1765332480948,-0.935074418786677,
-6.39972132087734));
#28968=CARTESIAN_POINT('Ctrl Pts',(97.1765177322304,-0.935086300171969,
-6.39972265426901));
#28969=CARTESIAN_POINT('Ctrl Pts',(97.1764864154705,-0.935110279970557,
-6.3997253454419));
#28970=CARTESIAN_POINT('Ctrl Pts',(97.176470614582,-0.935122378355964,-6.3997267032206));
#28971=CARTESIAN_POINT('Ctrl Pts',(97.1764387189249,-0.935146798861671,
-6.39972944392213));
#28972=CARTESIAN_POINT('Ctrl Pts',(97.1764226237246,-0.935159121288783,
-6.39973082688002));
#28973=CARTESIAN_POINT('Ctrl Pts',(97.1763901295677,-0.935183997367168,
-6.39973361878238));
#28974=CARTESIAN_POINT('Ctrl Pts',(97.1763737309863,-0.935196550706058,
-6.39973502769248));
#28975=CARTESIAN_POINT('Ctrl Pts',(97.176340619982,-0.935221896252795,-6.39973787235927));
#28976=CARTESIAN_POINT('Ctrl Pts',(97.1763239078118,-0.935234688240603,
-6.399739308092));
#28977=CARTESIAN_POINT('Ctrl Pts',(97.1762901597669,-0.935260518554863,
-6.39974220724458));
#28978=CARTESIAN_POINT('Ctrl Pts',(97.1762731234986,-0.93527355715472,-6.39974367069588));
#28979=CARTESIAN_POINT('Ctrl Pts',(97.1762387164617,-0.935299888871347,
-6.39974662620581));
#28980=CARTESIAN_POINT('Ctrl Pts',(97.1762213456232,-0.935313182012339,
-6.39974811826794));
#28981=CARTESIAN_POINT('Ctrl Pts',(97.1761862580939,-0.935340031410167,
-6.39975113196709));
#28982=CARTESIAN_POINT('Ctrl Pts',(97.1761685412761,-0.935353587733377,
-6.39975265361238));
#28983=CARTESIAN_POINT('Ctrl Pts',(97.1761327497733,-0.935380972595524,
-6.39975572750177));
#28984=CARTESIAN_POINT('Ctrl Pts',(97.1761146753163,-0.935394800927575,
-6.39975727972353));
#28985=CARTESIAN_POINT('Ctrl Pts',(97.1760781562237,-0.935422739128583,
-6.39976041581479));
#28986=CARTESIAN_POINT('Ctrl Pts',(97.1760597115915,-0.935436848960471,
-6.39976199968107));
#28987=CARTESIAN_POINT('Ctrl Pts',(97.1760224395259,-0.935465359713352,
-6.3997652001364));
#28988=CARTESIAN_POINT('Ctrl Pts',(97.1760036117627,-0.935479760850346,
-6.39976681675068));
#28989=CARTESIAN_POINT('Ctrl Pts',(97.1759655597604,-0.935508864563288,
-6.39977008386683));
#28990=CARTESIAN_POINT('Ctrl Pts',(97.1759463355762,-0.935523567058997,
-6.39977173436072));
#28991=CARTESIAN_POINT('Ctrl Pts',(97.1759074762203,-0.935553284471883,
-6.39977507047207));
#28992=CARTESIAN_POINT('Ctrl Pts',(97.1758878414116,-0.935568299070985,
-6.39977675605493));
#28993=CARTESIAN_POINT('Ctrl Pts',(97.175848146239,-0.935598651707898,-6.39978016358431));
#28994=CARTESIAN_POINT('Ctrl Pts',(97.1758280856368,-0.935613989885082,
-6.39978188554764));
#28995=CARTESIAN_POINT('Ctrl Pts',(97.1757875228418,-0.935645001809037,
-6.39978536720339));
#28996=CARTESIAN_POINT('Ctrl Pts',(97.1757670213753,-0.935660674955053,
-6.39978712682958));
#28997=CARTESIAN_POINT('Ctrl Pts',(97.1757255610698,-0.935692368744376,
-6.39979068515381));
#28998=CARTESIAN_POINT('Ctrl Pts',(97.1757046015927,-0.935708389827328,
-6.39979248390251));
#28999=CARTESIAN_POINT('Ctrl Pts',(97.1756622083148,-0.935740792302029,
-6.3997961219141));
#29000=CARTESIAN_POINT('Ctrl Pts',(97.1756407741983,-0.935757173884042,
-6.39979796119972));
#29001=CARTESIAN_POINT('Ctrl Pts',(97.1755974129087,-0.935790311519394,
-6.39980168187941));
#29002=CARTESIAN_POINT('Ctrl Pts',(97.1755754862566,-0.935807067120386,
-6.39980356322415));
#29003=CARTESIAN_POINT('Ctrl Pts',(97.1755311209366,-0.935840967117804,
-6.3998073696348));
#29004=CARTESIAN_POINT('Ctrl Pts',(97.1755086823097,-0.935858111425278,
-6.39980929469228));
#29005=CARTESIAN_POINT('Ctrl Pts',(97.1754632737502,-0.935892803399708,
-6.3998131901684));
#29006=CARTESIAN_POINT('Ctrl Pts',(97.1754403030439,-0.935910351596695,
-6.39981516064821));
#29007=CARTESIAN_POINT('Ctrl Pts',(97.1753938086935,-0.935945867690039,
-6.39981914880877));
#29008=CARTESIAN_POINT('Ctrl Pts',(97.175370285554,-0.935963835136047,-6.3998211664407));
#29009=CARTESIAN_POINT('Ctrl Pts',(97.1753226644333,-0.936000206261072,
-6.39982525076739));
#29010=CARTESIAN_POINT('Ctrl Pts',(97.1752985659007,-0.936018610291878,
-6.39982731750352));
#29011=CARTESIAN_POINT('Ctrl Pts',(97.1752497704901,-0.936055872326055,
-6.39983150203635));
#29012=CARTESIAN_POINT('Ctrl Pts',(97.1752250737634,-0.93607473013996,-6.39983361981377));
#29013=CARTESIAN_POINT('Ctrl Pts',(97.1751750569551,-0.936112918612804,
-6.39983790855459));
#29014=CARTESIAN_POINT('Ctrl Pts',(97.1751497371715,-0.936132248965399,
-6.3998400794857));
#29015=CARTESIAN_POINT('Ctrl Pts',(97.1750984484514,-0.936171401971825,
-6.39984447672537));
#29016=CARTESIAN_POINT('Ctrl Pts',(97.1750724793537,-0.936191224664462,
-6.39984670304055));
#29017=CARTESIAN_POINT('Ctrl Pts',(97.1750198647355,-0.936231382911131,
-6.39985121336431));
#29018=CARTESIAN_POINT('Ctrl Pts',(97.1749932188897,-0.936251718623376,
-6.39985349739307));
#29019=CARTESIAN_POINT('Ctrl Pts',(97.1726272253054,-0.938057249818427,
-6.40005629199058));
#29020=CARTESIAN_POINT('Ctrl Pts',(97.1702812367697,-0.939833641971995,
-6.40025617973369));
#29021=CARTESIAN_POINT('Ctrl Pts',(97.1648112135038,-0.943943401375891,
-6.4007195121245));
#29022=CARTESIAN_POINT('Ctrl Pts',(97.1616822271723,-0.946270064555444,
-6.40098249706385));
#29023=CARTESIAN_POINT('Ctrl Pts',(97.1534614175341,-0.952319757004328,
-6.40166825470613));
#29024=CARTESIAN_POINT('Ctrl Pts',(97.1483510589329,-0.956017555007129,
-6.40208938309798));
#29025=CARTESIAN_POINT('Ctrl Pts',(97.1085855381425,-0.984307488837633,
-6.40532871813222));
#29026=CARTESIAN_POINT('Ctrl Pts',(97.0726478678027,-1.00705179393989,-6.40803731318252));
#29027=CARTESIAN_POINT('Ctrl Pts',(96.974726766229,-1.06184026835491,-6.41507365534411));
#29028=CARTESIAN_POINT('Ctrl Pts',(96.9109965698694,-1.09040800905937,-6.41932072037774));
#29029=CARTESIAN_POINT('Ctrl Pts',(96.7962659261205,-1.13005062010819,-6.42692029284604));
#29030=CARTESIAN_POINT('Ctrl Pts',(96.7463667607831,-1.1436932509894,-6.43020986564444));
#29031=CARTESIAN_POINT('Ctrl Pts',(96.6852005769809,-1.15616252520353,-6.43431330533018));
#29032=CARTESIAN_POINT('Ctrl Pts',(96.6746353788666,-1.1581660345286,-6.43502445352717));
#29033=CARTESIAN_POINT('Ctrl Pts',(96.6579321488437,-1.16109715261995,-6.43615315177178));
#29034=CARTESIAN_POINT('Ctrl Pts',(96.6518115094343,-1.16212141719024,-6.43656767040178));
#29035=CARTESIAN_POINT('Ctrl Pts',(96.6403206498091,-1.1639511288432,-6.43734774799026));
#29036=CARTESIAN_POINT('Ctrl Pts',(96.6349523784064,-1.16476790260801,-6.43771294208083));
#29037=CARTESIAN_POINT('Ctrl Pts',(96.6228995297434,-1.16651653138184,-6.43853466898798));
#29038=CARTESIAN_POINT('Ctrl Pts',(96.6162122498106,-1.16742810143477,-6.43899182158177));
#29039=CARTESIAN_POINT('Ctrl Pts',(96.5991338949827,-1.16960677140402,-6.44016263646328));
#29040=CARTESIAN_POINT('Ctrl Pts',(96.5887332699213,-1.1707928805093,-6.44087878075132));
#29041=CARTESIAN_POINT('Ctrl Pts',(96.5056709254437,-1.17914543877384,-6.44662444135765));
#29042=CARTESIAN_POINT('Ctrl Pts',(96.4325147777633,-1.17967811561584,-6.45186034899469));
#29043=CARTESIAN_POINT('Ctrl Pts',(96.3073637923528,-1.168939340988,-6.46104153441184));
#29044=CARTESIAN_POINT('Ctrl Pts',(96.255295850227,-1.16093203051648,-6.46492501050388));
#29045=CARTESIAN_POINT('Ctrl Pts',(96.1673718958634,-1.14130881234261,-6.47146845917004));
#29046=CARTESIAN_POINT('Ctrl Pts',(96.1312121400617,-1.13140681559021,-6.47415411926335));
#29047=CARTESIAN_POINT('Ctrl Pts',(96.0893553617421,-1.11776730841211,-6.47721236552547));
#29048=CARTESIAN_POINT('Ctrl Pts',(96.0831450520231,-1.11568614898265,-6.47766476742238));
#29049=CARTESIAN_POINT('Ctrl Pts',(96.0735720207166,-1.11238901676735,-6.47835969674646));
#29050=CARTESIAN_POINT('Ctrl Pts',(96.0701970517253,-1.11120939691399,-6.47860422285097));
#29051=CARTESIAN_POINT('Ctrl Pts',(96.0639536157802,-1.10899523609807,-6.47905563591088));
#29052=CARTESIAN_POINT('Ctrl Pts',(96.0610838014874,-1.10796492660114,-6.47926275121671));
#29053=CARTESIAN_POINT('Ctrl Pts',(96.0545176940618,-1.10557876132467,-6.47973579273178));
#29054=CARTESIAN_POINT('Ctrl Pts',(96.0508241706686,-1.10421550746967,-6.48000128349502));
#29055=CARTESIAN_POINT('Ctrl Pts',(96.0411117273122,-1.10057527154522,-6.4806980017482));
#29056=CARTESIAN_POINT('Ctrl Pts',(96.0351044146951,-1.09826739959844,-6.48112749848271));
#29057=CARTESIAN_POINT('Ctrl Pts',(95.9774134751159,-1.0755594834283,-6.48524106150865));
#29058=CARTESIAN_POINT('Ctrl Pts',(95.927208265915,-1.05157231623784,-6.48873639132756));
#29059=CARTESIAN_POINT('Ctrl Pts',(95.8338632344687,-0.998561590404792,
-6.49541014934479));
#29060=CARTESIAN_POINT('Ctrl Pts',(95.790582438158,-0.97005721240322,-6.49858717043135));
#29061=CARTESIAN_POINT('Ctrl Pts',(95.7196953881159,-0.916358448787677,
-6.5041389808654));
#29062=CARTESIAN_POINT('Ctrl Pts',(95.6911540623524,-0.892531158635892,
-6.50648334342522));
#29063=CARTESIAN_POINT('Ctrl Pts',(95.6520428067932,-0.856607943268382,
-6.5099022168641));
#29064=CARTESIAN_POINT('Ctrl Pts',(95.6405181628985,-0.845582870540394,
-6.51093722844887));
#29065=CARTESIAN_POINT('Ctrl Pts',(95.6203071008332,-0.825446127901601,
-6.51280592782262));
#29066=CARTESIAN_POINT('Ctrl Pts',(95.6115360733511,-0.816422674540213,
-6.51363590402667));
#29067=CARTESIAN_POINT('Ctrl Pts',(95.5983931846207,-0.802460717810089,
-6.51491011450978));
#29068=CARTESIAN_POINT('Ctrl Pts',(95.5939152535625,-0.797622974617202,
-6.515349843546));
#29069=CARTESIAN_POINT('Ctrl Pts',(95.5861832954868,-0.789127769847707,
-6.51611909496769));
#29070=CARTESIAN_POINT('Ctrl Pts',(95.5829109903501,-0.785487103980146,
-6.51644784319417));
#29071=CARTESIAN_POINT('Ctrl Pts',(95.5755882911183,-0.777237219476801,
-6.51719081003168));
#29072=CARTESIAN_POINT('Ctrl Pts',(95.5715510561389,-0.772616563651018,
-6.51760555752859));
#29073=CARTESIAN_POINT('Ctrl Pts',(95.5607483031821,-0.760055945659862,
-6.51872943611682));
#29074=CARTESIAN_POINT('Ctrl Pts',(95.554051997889,-0.752057457194885,-6.51944133570553));
#29075=CARTESIAN_POINT('Ctrl Pts',(95.5221794040186,-0.712942708511678,
-6.52290560649131));
#29076=CARTESIAN_POINT('Ctrl Pts',(95.4984968191547,-0.68064894314274,-6.52571556007509));
#29077=CARTESIAN_POINT('Ctrl Pts',(95.4304701434541,-0.577226604646416,
-6.53456693571664));
#29078=CARTESIAN_POINT('Ctrl Pts',(95.3920358304643,-0.502528974669699,
-6.54077664937646));
#29079=CARTESIAN_POINT('Ctrl Pts',(95.3517827984149,-0.398327278726985,
-6.54891112455067));
#29080=CARTESIAN_POINT('Ctrl Pts',(95.3426419881288,-0.371903851937086,
-6.55092928806967));
#29081=CARTESIAN_POINT('Ctrl Pts',(95.3312493144708,-0.334739007166689,
-6.55368602527304));
#29082=CARTESIAN_POINT('Ctrl Pts',(95.3281943239646,-0.324255000209573,
-6.55445478043008));
#29083=CARTESIAN_POINT('Ctrl Pts',(95.3231176488982,-0.305885619880339,
-6.55578454906964));
#29084=CARTESIAN_POINT('Ctrl Pts',(95.3210311172284,-0.298019091548349,
-6.55634856004119));
#29085=CARTESIAN_POINT('Ctrl Pts',(95.3180657794199,-0.286352653404706,
-6.55717635182223));
#29086=CARTESIAN_POINT('Ctrl Pts',(95.3171240869654,-0.282569193178977,
-6.55744346636159));
#29087=CARTESIAN_POINT('Ctrl Pts',(95.3155487410907,-0.276103056568104,
-6.55789761302853));
#29088=CARTESIAN_POINT('Ctrl Pts',(95.3149056974572,-0.273422753625324,
-6.55808516811796));
#29089=CARTESIAN_POINT('Ctrl Pts',(95.3134705907885,-0.267347067597208,
-6.55850872903258));
#29090=CARTESIAN_POINT('Ctrl Pts',(95.3126841898141,-0.263950405931354,
-6.55874441334441));
#29091=CARTESIAN_POINT('Ctrl Pts',(95.3105895415945,-0.254716693399316,
-6.5593822244395));
#29092=CARTESIAN_POINT('Ctrl Pts',(95.3093106396925,-0.248872990540468,
-6.55978274533025));
#29093=CARTESIAN_POINT('Ctrl Pts',(95.3031594006712,-0.219703675746438,
-6.56176757172747));
#29094=CARTESIAN_POINT('Ctrl Pts',(95.2989508532001,-0.196241923921446,
-6.5633182615217));
#29095=CARTESIAN_POINT('Ctrl Pts',(95.28055041391,-0.0720897623782146,-6.57136088446545));
#29096=CARTESIAN_POINT('Ctrl Pts',(95.2787294633223,0.0299997297889832,
-6.5774483670772));
#29097=CARTESIAN_POINT('Ctrl Pts',(95.2946345108674,0.172038832414202,-6.58647284917655));
#29098=CARTESIAN_POINT('Ctrl Pts',(95.3013713462114,0.212743129651664,-6.58911931492783));
#29099=CARTESIAN_POINT('Ctrl Pts',(95.3124049792911,0.26290557756243,-6.59249998636938));
#29100=CARTESIAN_POINT('Ctrl Pts',(95.3147097747432,0.272774963421777,-6.59317089344754));
#29101=CARTESIAN_POINT('Ctrl Pts',(95.3185984818661,0.288507112559284,-6.59425015523625));
#29102=CARTESIAN_POINT('Ctrl Pts',(95.320100900015,0.294389647052842,-6.59465591874002));
#29103=CARTESIAN_POINT('Ctrl Pts',(95.3230382809119,0.305530597296265,-6.59542871647041));
#29104=CARTESIAN_POINT('Ctrl Pts',(95.3244644001965,0.310791197117744,-6.59579545942917));
#29105=CARTESIAN_POINT('Ctrl Pts',(95.3277951677745,0.322748278822231,-6.59663333581609));
#29106=CARTESIAN_POINT('Ctrl Pts',(95.3297227672705,0.329438099385787,-6.59710519450473));
#29107=CARTESIAN_POINT('Ctrl Pts',(95.3358338968934,0.34996132691847,-6.59856248836821));
#29108=CARTESIAN_POINT('Ctrl Pts',(95.3402126930636,0.363734690005359,-6.59955415518562));
#29109=CARTESIAN_POINT('Ctrl Pts',(95.3754852987348,0.467998034780265,-6.60716887558589));
#29110=CARTESIAN_POINT('Ctrl Pts',(95.4170375677854,0.554487657150009,-6.61415289534093));
#29111=CARTESIAN_POINT('Ctrl Pts',(95.5010504861476,0.685724126710215,-6.62558519956806));
#29112=CARTESIAN_POINT('Ctrl Pts',(95.5373800074524,0.733900986044459,-6.62998846673897));
#29113=CARTESIAN_POINT('Ctrl Pts',(95.5826708531864,0.785246382824889,-6.6347665464085));
#29114=CARTESIAN_POINT('Ctrl Pts',(95.5881654461936,0.791345764529782,-6.6353355394489));
#29115=CARTESIAN_POINT('Ctrl Pts',(95.5963724363439,0.800266734892986,-6.63616919785251));
#29116=CARTESIAN_POINT('Ctrl Pts',(95.5990356998227,0.803132898344301,-6.63643726346569));
#29117=CARTESIAN_POINT('Ctrl Pts',(95.6037985737718,0.808207680542341,-6.63691221283939));
#29118=CARTESIAN_POINT('Ctrl Pts',(95.6058925230498,0.810421476686974,-6.6371195057559));
#29119=CARTESIAN_POINT('Ctrl Pts',(95.6104741235883,0.815227800589587,-6.63756977142483));
#29120=CARTESIAN_POINT('Ctrl Pts',(95.6129650577297,0.817817085301619,-6.63781249003034));
#29121=CARTESIAN_POINT('Ctrl Pts',(95.6199604459838,0.825022388779438,-6.63848847279569));
#29122=CARTESIAN_POINT('Ctrl Pts',(95.6244911085802,0.829612951522574,-6.63891979614913));
#29123=CARTESIAN_POINT('Ctrl Pts',(95.6510059526397,0.856040554960753,-6.64140838579666));
#29124=CARTESIAN_POINT('Ctrl Pts',(95.6738094448802,0.877042485824854,-6.64340815425057));
#29125=CARTESIAN_POINT('Ctrl Pts',(95.756649359032,0.947503505260597,-6.65030947190125));
#29126=CARTESIAN_POINT('Ctrl Pts',(95.8207282619404,0.991897012846869,-6.65502945493974));
#29127=CARTESIAN_POINT('Ctrl Pts',(95.8996533305313,1.03572384359127,-6.66066653919875));
#29128=CARTESIAN_POINT('Ctrl Pts',(95.9106824222252,1.04162036581191,-6.66145022930411));
#29129=CARTESIAN_POINT('Ctrl Pts',(95.9218016806086,1.0473393469567,-6.66223764680097));
#29130=CARTESIAN_POINT('Origin',(96.460480949577,-7.19464945638997E-16,
0.924367114736168));
#29131=CARTESIAN_POINT('',(95.9218016730718,1.04733934308027,-7.26047246820102));
#29132=CARTESIAN_POINT('',(95.921801726504,1.0473393705621,-7.16216478479583));
#29133=CARTESIAN_POINT('',(95.9218016730721,1.04733934308042,0.924367114736168));
#29134=CARTESIAN_POINT('',(97.6382304460792,-0.00103044978340366,-6.92454726424663));
#29135=CARTESIAN_POINT('Ctrl Pts',(95.9218016730718,1.04733934308028,-7.26047246820102));
#29136=CARTESIAN_POINT('Ctrl Pts',(95.9208597180712,1.04685486625662,-7.26040005122408));
#29137=CARTESIAN_POINT('Ctrl Pts',(95.9199184113506,1.04636911593881,-7.26032771122568));
#29138=CARTESIAN_POINT('Ctrl Pts',(95.9162760713822,1.04448330229007,-7.26004790400432));
#29139=CARTESIAN_POINT('Ctrl Pts',(95.9135798251374,1.04307405247191,-7.25984101423793));
#29140=CARTESIAN_POINT('Ctrl Pts',(95.9076501070122,1.03994544687482,-7.25938653821152));
#29141=CARTESIAN_POINT('Ctrl Pts',(95.9044191777612,1.03822145027119,-7.25913924365669));
#29142=CARTESIAN_POINT('Ctrl Pts',(95.8950714447966,1.03317742467046,-7.25842459306972));
#29143=CARTESIAN_POINT('Ctrl Pts',(95.8889758342753,1.02981814312404,-7.25795959984589));
#29144=CARTESIAN_POINT('Ctrl Pts',(95.8373899156303,1.00079010748118,-7.25403012205844));
#29145=CARTESIAN_POINT('Ctrl Pts',(95.7936176456544,0.972171835076872,-7.25073235653692));
#29146=CARTESIAN_POINT('Ctrl Pts',(95.6853708012808,0.890636646085197,-7.2422909419277));
#29147=CARTESIAN_POINT('Ctrl Pts',(95.6243603345841,0.833625394649087,-7.23722359809865));
#29148=CARTESIAN_POINT('Ctrl Pts',(95.549773628956,0.747429416561308,-7.22995249652568));
#29149=CARTESIAN_POINT('Ctrl Pts',(95.530592372067,0.723426247829695,-7.22796519482068));
#29150=CARTESIAN_POINT('Ctrl Pts',(95.5066989546608,0.691003923233239,-7.22531086301413));
#29151=CARTESIAN_POINT('Ctrl Pts',(95.5011197343357,0.683236829786034,-7.22467718615597));
#29152=CARTESIAN_POINT('Ctrl Pts',(95.4922254070386,0.670530859955909,-7.22364362359592));
#29153=CARTESIAN_POINT('Ctrl Pts',(95.4888519686875,0.665633195619573,-7.22324594737691));
#29154=CARTESIAN_POINT('Ctrl Pts',(95.4824398263498,0.656171234003264,-7.22247892896844));
#29155=CARTESIAN_POINT('Ctrl Pts',(95.4793956141347,0.651610842368795,-7.22210980528191));
#29156=CARTESIAN_POINT('Ctrl Pts',(95.4724214973662,0.641003579469308,-7.22125242868399));
#29157=CARTESIAN_POINT('Ctrl Pts',(95.468515102082,0.634941590538616,-7.22076332611468));
#29158=CARTESIAN_POINT('Ctrl Pts',(95.4562314263832,0.615489580921559,-7.21919642095604));
#29159=CARTESIAN_POINT('Ctrl Pts',(95.4480680248331,0.601967239079183,-7.21811095169418));
#29160=CARTESIAN_POINT('Ctrl Pts',(95.4295082222155,0.569777765867103,-7.21553459434246));
#29161=CARTESIAN_POINT('Ctrl Pts',(95.4193432675725,0.550984297282275,-7.21403617994727));
#29162=CARTESIAN_POINT('Ctrl Pts',(95.3827879980073,0.478771694850923,-7.2082997182316));
#29163=CARTESIAN_POINT('Ctrl Pts',(95.3599552648316,0.42365813462929,-7.20395848604041));
#29164=CARTESIAN_POINT('Ctrl Pts',(95.3195427015775,0.300448730435618,-7.19444577167821));
#29165=CARTESIAN_POINT('Ctrl Pts',(95.3036831961164,0.232013488983423,-7.18928031076791));
#29166=CARTESIAN_POINT('Ctrl Pts',(95.2926462473488,0.1528203160044,-7.18367589446421));
#29167=CARTESIAN_POINT('Ctrl Pts',(95.2914098320819,0.143054810241082,-7.18299132878215));
#29168=CARTESIAN_POINT('Ctrl Pts',(95.2898554532965,0.129406963909059,-7.1820447388615));
#29169=CARTESIAN_POINT('Ctrl Pts',(95.2894341343718,0.125537136038314,-7.18177746831511));
#29170=CARTESIAN_POINT('Ctrl Pts',(95.2887380323313,0.118834744115188,-7.18131660860916));
#29171=CARTESIAN_POINT('Ctrl Pts',(95.2884543179673,0.116003171342957,-7.18112253853675));
#29172=CARTESIAN_POINT('Ctrl Pts',(95.2878747106748,0.10999919222908,-7.18071241289187));
#29173=CARTESIAN_POINT('Ctrl Pts',(95.2875814222413,0.10682655609912,-7.18049650762431));
#29174=CARTESIAN_POINT('Ctrl Pts',(95.2868813143617,0.0989024760366053,
-7.17995920056615));
#29175=CARTESIAN_POINT('Ctrl Pts',(95.2864904661398,0.0941496165057984,
-7.179638668394));
#29176=CARTESIAN_POINT('Ctrl Pts',(95.2851006452773,0.0758918809506207,
-7.17841361194429));
#29177=CARTESIAN_POINT('Ctrl Pts',(95.284305698751,0.0623719110757795,-7.1775195511536));
#29178=CARTESIAN_POINT('Ctrl Pts',(95.2828493126887,0.0272825526794893,
-7.17522610452706));
#29179=CARTESIAN_POINT('Ctrl Pts',(95.282547079335,0.00570270419554888,
-7.17384199628592));
#29180=CARTESIAN_POINT('Ctrl Pts',(95.2842025494585,-0.117107522713611,
-7.16605448070247));
#29181=CARTESIAN_POINT('Ctrl Pts',(95.2986139016332,-0.217743232586888,
-7.15998149464462));
#29182=CARTESIAN_POINT('Ctrl Pts',(95.3346706671793,-0.347511047007553,
-7.15141632201767));
#29183=CARTESIAN_POINT('Ctrl Pts',(95.3449874073226,-0.379323814872747,
-7.1492584789627));
#29184=CARTESIAN_POINT('Ctrl Pts',(95.3600810426165,-0.419895658609567,
-7.14640748089808));
#29185=CARTESIAN_POINT('Ctrl Pts',(95.3636355121046,-0.429094856590577,
-7.14575434176744));
#29186=CARTESIAN_POINT('Ctrl Pts',(95.3695421689451,-0.443828554419652,
-7.14469688489526));
#29187=CARTESIAN_POINT('Ctrl Pts',(95.3718220003918,-0.449391698741871,
-7.14429497306278));
#29188=CARTESIAN_POINT('Ctrl Pts',(95.3762550846813,-0.459977387230508,
-7.14352503560608));
#29189=CARTESIAN_POINT('Ctrl Pts',(95.3784009005822,-0.465002891080957,
-7.14315726713749));
#29190=CARTESIAN_POINT('Ctrl Pts',(95.3834047900295,-0.476499795760483,
-7.1423106600264));
#29191=CARTESIAN_POINT('Ctrl Pts',(95.3862863311969,-0.48296068876288,-7.14183104041683));
#29192=CARTESIAN_POINT('Ctrl Pts',(95.3954780030865,-0.503080680124973,
-7.14032511902933));
#29193=CARTESIAN_POINT('Ctrl Pts',(95.4019915724351,-0.516644606023258,
-7.13929196806175));
#29194=CARTESIAN_POINT('Ctrl Pts',(95.4177902270503,-0.547990336991621,
-7.13686109665307));
#29195=CARTESIAN_POINT('Ctrl Pts',(95.4272730842841,-0.565666666295478,
-7.13545695361596));
#29196=CARTESIAN_POINT('Ctrl Pts',(95.4636608857215,-0.629524349062002,
-7.1302599023813));
#29197=CARTESIAN_POINT('Ctrl Pts',(95.4932465663937,-0.674097670688097,
-7.12638399706332));
#29198=CARTESIAN_POINT('Ctrl Pts',(95.5740446875582,-0.779504297028057,
-7.11665735681072));
#29199=CARTESIAN_POINT('Ctrl Pts',(95.62858543295,-0.837465206029179,-7.11077792168826));
#29200=CARTESIAN_POINT('Ctrl Pts',(95.6957594850679,-0.895760769046088,
-7.10455068856831));
#29201=CARTESIAN_POINT('Ctrl Pts',(95.7030486728573,-0.901932721639979,
-7.10388709292501));
#29202=CARTESIAN_POINT('Ctrl Pts',(95.7133007831966,-0.910401503095874,
-7.10297142093866));
#29203=CARTESIAN_POINT('Ctrl Pts',(95.7162005663911,-0.912773690484297,
-7.10271435786222));
#29204=CARTESIAN_POINT('Ctrl Pts',(95.7215130223108,-0.917077431853546,
-7.10224700266729));
#29205=CARTESIAN_POINT('Ctrl Pts',(95.7239220718261,-0.919013402527863,
-7.10203640413542));
#29206=CARTESIAN_POINT('Ctrl Pts',(95.728930227221,-0.923005734727604,-7.10160139161262));
#29207=CARTESIAN_POINT('Ctrl Pts',(95.7315304268305,-0.925060636820044,
-7.10137707799624));
#29208=CARTESIAN_POINT('Ctrl Pts',(95.7383558275954,-0.930408008604561,
-7.10079218272046));
#29209=CARTESIAN_POINT('Ctrl Pts',(95.7425949361117,-0.93368272376813,-7.10043281518524));
#29210=CARTESIAN_POINT('Ctrl Pts',(95.7617024237202,-0.948236207503202,
-7.09882963138234));
#29211=CARTESIAN_POINT('Ctrl Pts',(95.7768161991651,-0.959190250880203,
-7.09760633348266));
#29212=CARTESIAN_POINT('Ctrl Pts',(95.8206129299226,-0.989371472369909,
-7.09416694190529));
#29213=CARTESIAN_POINT('Ctrl Pts',(95.8498907613682,-1.00770380980554,-7.09199202535038));
#29214=CARTESIAN_POINT('Ctrl Pts',(95.9479093735551,-1.06323525555173,-7.08496662368879));
#29215=CARTESIAN_POINT('Ctrl Pts',(96.0195458572858,-1.09488582035073,-7.08021051329017));
#29216=CARTESIAN_POINT('Ctrl Pts',(96.1285784333299,-1.13060870515844,-7.07293827403741));
#29217=CARTESIAN_POINT('Ctrl Pts',(96.1638778151523,-1.14037778623842,-7.07058161408795));
#29218=CARTESIAN_POINT('Ctrl Pts',(96.2094865454845,-1.15073899573484,-7.06750332380953));
#29219=CARTESIAN_POINT('Ctrl Pts',(96.2194292591178,-1.15286274079395,-7.06683032951213));
#29220=CARTESIAN_POINT('Ctrl Pts',(96.2353585167992,-1.15605013012008,-7.06574848073897));
#29221=CARTESIAN_POINT('Ctrl Pts',(96.2413281094346,-1.15719663126365,-7.0653422394339));
#29222=CARTESIAN_POINT('Ctrl Pts',(96.2526658383167,-1.15928324431396,-7.06456902719351));
#29223=CARTESIAN_POINT('Ctrl Pts',(96.2580321629237,-1.16023241123785,-7.06420235139753));
#29224=CARTESIAN_POINT('Ctrl Pts',(96.2702574620156,-1.16230735991896,-7.06336531956014));
#29225=CARTESIAN_POINT('Ctrl Pts',(96.2771201501804,-1.1634097248192,-7.06289424406003));
#29226=CARTESIAN_POINT('Ctrl Pts',(96.2982203883794,-1.16660776114289,-7.06144194293551));
#29227=CARTESIAN_POINT('Ctrl Pts',(96.3124864635607,-1.16850321283646,-7.06045454795605));
#29228=CARTESIAN_POINT('Ctrl Pts',(96.3822301989317,-1.17647201107858,-7.05559866299609));
#29229=CARTESIAN_POINT('Ctrl Pts',(96.4380493536092,-1.17885740816322,-7.05161896937105));
#29230=CARTESIAN_POINT('Ctrl Pts',(96.5113505659212,-1.17678158475051,-7.04629107032982));
#29231=CARTESIAN_POINT('Ctrl Pts',(96.5288670947054,-1.17589367120393,-7.04501069102188));
#29232=CARTESIAN_POINT('Ctrl Pts',(96.626849917006,-1.1687301596835,-7.03781801478963));
#29233=CARTESIAN_POINT('Ctrl Pts',(96.706530149574,-1.15458674167189,-7.03183599012591));
#29234=CARTESIAN_POINT('Ctrl Pts',(96.7932187250978,-1.12980960832299,-7.02552511159158));
#29235=CARTESIAN_POINT('Ctrl Pts',(96.8022642197074,-1.12710620113606,-7.02486930687755));
#29236=CARTESIAN_POINT('Ctrl Pts',(96.8148362527548,-1.12318354976671,-7.02396252156958));
#29237=CARTESIAN_POINT('Ctrl Pts',(96.8183906922109,-1.12205596314794,-7.02370667720276));
#29238=CARTESIAN_POINT('Ctrl Pts',(96.8248770695408,-1.11996430974583,-7.0232408359018));
#29239=CARTESIAN_POINT('Ctrl Pts',(96.8278106868398,-1.11900556404084,-7.02303053969552));
#29240=CARTESIAN_POINT('Ctrl Pts',(96.8338945017082,-1.1169907876808,-7.02259527837974));
#29241=CARTESIAN_POINT('Ctrl Pts',(96.8370440404602,-1.11593294599405,-7.02237041927322));
#29242=CARTESIAN_POINT('Ctrl Pts',(96.8452950034731,-1.11312276982819,-7.02178248311324));
#29243=CARTESIAN_POINT('Ctrl Pts',(96.8503890120951,-1.11134866821537,-7.02142064343985));
#29244=CARTESIAN_POINT('Ctrl Pts',(96.8731326856828,-1.10325204894939,-7.01980946886404));
#29245=CARTESIAN_POINT('Ctrl Pts',(96.8906431706415,-1.09654324968982,-7.0185808125437));
#29246=CARTESIAN_POINT('Ctrl Pts',(96.9402778032874,-1.07615457341026,-7.01511183557275));
#29247=CARTESIAN_POINT('Ctrl Pts',(96.9719652400314,-1.06146025342563,-7.01291371710492));
#29248=CARTESIAN_POINT('Ctrl Pts',(97.0965942161623,-0.996787044247089,
-7.00416046050713));
#29249=CARTESIAN_POINT('Ctrl Pts',(97.183271811658,-0.935840105926767,-6.9977733110124));
#29250=CARTESIAN_POINT('Ctrl Pts',(97.2720171310125,-0.853664476248166,
-6.98989117853153));
#29251=CARTESIAN_POINT('Ctrl Pts',(97.2831510134443,-0.842940058212227,
-6.98887530735476));
#29252=CARTESIAN_POINT('Ctrl Pts',(97.2990671687752,-0.826993500780641,
-6.9873809816462));
#29253=CARTESIAN_POINT('Ctrl Pts',(97.3040188384712,-0.821942165673621,
-6.98690991780984));
#29254=CARTESIAN_POINT('Ctrl Pts',(97.3127258588277,-0.81289834267137,-6.98607036457632));
#29255=CARTESIAN_POINT('Ctrl Pts',(97.3164994383877,-0.808923634186177,
-6.98570267085466));
#29256=CARTESIAN_POINT('Ctrl Pts',(97.3243146759316,-0.800575925509163,
-6.98493300926392));
#29257=CARTESIAN_POINT('Ctrl Pts',(97.3283511774271,-0.796198332489722,
-6.98453083874448));
#29258=CARTESIAN_POINT('Ctrl Pts',(97.3382321643194,-0.785317967227464,
-6.98353467796098));
#29259=CARTESIAN_POINT('Ctrl Pts',(97.3440376853467,-0.778780451835088,
-6.98293909623894));
#29260=CARTESIAN_POINT('Ctrl Pts',(97.3692275591161,-0.749770246965699,
-6.98030856743592));
#29261=CARTESIAN_POINT('Ctrl Pts',(97.3878297739134,-0.726635885885746,
-6.97824255253814));
#29262=CARTESIAN_POINT('Ctrl Pts',(97.4367249598435,-0.660888833648281,
-6.9724516504901));
#29263=CARTESIAN_POINT('Ctrl Pts',(97.4650834474865,-0.616927201653601,
-6.96866492238197));
#29264=CARTESIAN_POINT('Ctrl Pts',(97.5298625280332,-0.500128977485876,
-6.95888825038202));
#29265=CARTESIAN_POINT('Ctrl Pts',(97.5618318478151,-0.425128321206344,
-6.95285989921297));
#29266=CARTESIAN_POINT('Ctrl Pts',(97.5885532574293,-0.338576064939547,
-6.94652023167593));
#29267=CARTESIAN_POINT('Ctrl Pts',(97.5911816327146,-0.329692071386415,
-6.94587666624319));
#29268=CARTESIAN_POINT('Ctrl Pts',(97.5947295362783,-0.317158250401129,
-6.94497960275223));
#29269=CARTESIAN_POINT('Ctrl Pts',(97.5957367391065,-0.313533898560549,
-6.94472147644937));
#29270=CARTESIAN_POINT('Ctrl Pts',(97.5975407703799,-0.306919534514355,
-6.94425279702013));
#29271=CARTESIAN_POINT('Ctrl Pts',(97.5983432127486,-0.303931090332096,
-6.94404193126013));
#29272=CARTESIAN_POINT('Ctrl Pts',(97.5999789103354,-0.297742164598787,
-6.94360711950385));
#29273=CARTESIAN_POINT('Ctrl Pts',(97.6008104754472,-0.29454129127137,-6.94338326905021));
#29274=CARTESIAN_POINT('Ctrl Pts',(97.6029457055444,-0.286177734656938,
-6.94280095745395));
#29275=CARTESIAN_POINT('Ctrl Pts',(97.6042278798425,-0.281009566781523,
-6.94244369080399));
#29276=CARTESIAN_POINT('Ctrl Pts',(97.6069648810169,-0.269648153308233,
-6.94166355937552));
#29277=CARTESIAN_POINT('Ctrl Pts',(97.6084046780018,-0.263451417752321,
-6.94124147792089));
#29278=CARTESIAN_POINT('Ctrl Pts',(97.6125689502187,-0.244846245399837,
-6.9399836009899));
#29279=CARTESIAN_POINT('Ctrl Pts',(97.6151430339537,-0.232404699287403,
-6.93915490476511));
#29280=CARTESIAN_POINT('Ctrl Pts',(97.6312300440705,-0.147769664749213,
-6.93358689565391));
#29281=CARTESIAN_POINT('Ctrl Pts',(97.6381662002851,-0.0744864016200065,
-6.92909825428085));
#29282=CARTESIAN_POINT('Ctrl Pts',(97.6382304983754,-0.00103092444165349,
-6.92454738504961));
#29283=CARTESIAN_POINT('Ctrl Pts',(97.6382304987957,-0.00103044418824775,
-6.92454735529594));
#29284=CARTESIAN_POINT('Ctrl Pts',(97.6382908279616,0.0679229729281441,
-6.92027540704751));
#29285=CARTESIAN_POINT('Ctrl Pts',(97.63229585996,0.136742120609072,-6.9159638278707));
#29286=CARTESIAN_POINT('Ctrl Pts',(97.6186126308913,0.2142946587171,-6.91081892651751));
#29287=CARTESIAN_POINT('Ctrl Pts',(97.6167885836402,0.223928198828335,-6.91017491059771));
#29288=CARTESIAN_POINT('Ctrl Pts',(97.6135643146035,0.23986558290601,-6.90910069828434));
#29289=CARTESIAN_POINT('Ctrl Pts',(97.6122321235123,0.246182808429343,-6.9086726053109));
#29290=CARTESIAN_POINT('Ctrl Pts',(97.60973585836,0.257556077200189,-6.90789757002909));
#29291=CARTESIAN_POINT('Ctrl Pts',(97.6085901788517,0.262616020965674,-6.90755121101665));
#29292=CARTESIAN_POINT('Ctrl Pts',(97.6061790235561,0.272947570031992,-6.90684075135015));
#29293=CARTESIAN_POINT('Ctrl Pts',(97.6049105068863,0.278218330422606,-6.90647656218959));
#29294=CARTESIAN_POINT('Ctrl Pts',(97.6020831862839,0.289619414271739,-6.90568492548757));
#29295=CARTESIAN_POINT('Ctrl Pts',(97.6005113012784,0.295746287350625,-6.90525707139467));
#29296=CARTESIAN_POINT('Ctrl Pts',(97.5960696016152,0.312497331416325,-6.90408047169089));
#29297=CARTESIAN_POINT('Ctrl Pts',(97.593100172343,0.323094182481593,-6.90332857222809));
#29298=CARTESIAN_POINT('Ctrl Pts',(97.5751801613336,0.383759049595454,-6.89897913368304));
#29299=CARTESIAN_POINT('Ctrl Pts',(97.5570613007104,0.432822701760297,-6.89528048534449));
#29300=CARTESIAN_POINT('Ctrl Pts',(97.5161816469907,0.524300522489095,-6.88804133905029));
#29301=CARTESIAN_POINT('Ctrl Pts',(97.493959980958,0.566847112124095,-6.88451999508911));
#29302=CARTESIAN_POINT('Ctrl Pts',(97.4390221108619,0.658006278284554,-6.8767106198991));
#29303=CARTESIAN_POINT('Ctrl Pts',(97.4051441630644,0.705781753812096,-6.87243344213195));
#29304=CARTESIAN_POINT('Ctrl Pts',(97.3615984580203,0.758405275480429,-6.86764703812046));
#29305=CARTESIAN_POINT('Ctrl Pts',(97.3552489701487,0.765886108325646,-6.86696480929489));
#29306=CARTESIAN_POINT('Ctrl Pts',(97.3460017082658,0.776509044806948,-6.86599446395726));
#29307=CARTESIAN_POINT('Ctrl Pts',(97.3431793688538,0.779715853866698,-6.86570133129326));
#29308=CARTESIAN_POINT('Ctrl Pts',(97.3382841975529,0.785217218807283,-6.86519819959786));
#29309=CARTESIAN_POINT('Ctrl Pts',(97.3362196815034,0.787519077352361,-6.86498760543505));
#29310=CARTESIAN_POINT('Ctrl Pts',(97.3318730469432,0.792327182174312,-6.86454759450497));
#29311=CARTESIAN_POINT('Ctrl Pts',(97.3295891534876,0.794831731620892,-6.86431831231389));
#29312=CARTESIAN_POINT('Ctrl Pts',(97.3234375702759,0.801519425845047,-6.8637057506998));
#29313=CARTESIAN_POINT('Ctrl Pts',(97.3195502276695,0.80568449029458,-6.86332390311782));
#29314=CARTESIAN_POINT('Ctrl Pts',(97.301937772174,0.824282818984372,-6.86161635946472));
#29315=CARTESIAN_POINT('Ctrl Pts',(97.2878772024976,0.838395672404941,-6.86031385341831));
#29316=CARTESIAN_POINT('Ctrl Pts',(97.2153743632653,0.907566458257483,-6.85385215574387));
#29317=CARTESIAN_POINT('Ctrl Pts',(97.1517641694078,0.956907005852332,-6.84897337898678));
#29318=CARTESIAN_POINT('Ctrl Pts',(97.0467493897519,1.02238574811196,-6.84128454079765));
#29319=CARTESIAN_POINT('Ctrl Pts',(97.0086346080747,1.04331702700504,-6.8385611434389));
#29320=CARTESIAN_POINT('Ctrl Pts',(96.9535335695033,1.06972229523379,-6.83464100862845));
#29321=CARTESIAN_POINT('Ctrl Pts',(96.9374456875861,1.07699176643994,-6.83349861422961));
#29322=CARTESIAN_POINT('Ctrl Pts',(96.9087728354542,1.08917942379276,-6.83146183117773));
#29323=CARTESIAN_POINT('Ctrl Pts',(96.8962550494031,1.09424784293197,-6.8305723976577));
#29324=CARTESIAN_POINT('Ctrl Pts',(96.8775143074176,1.10146335148661,-6.82923911201458));
#29325=CARTESIAN_POINT('Ctrl Pts',(96.8713557408925,1.1037754477876,-6.8288007043033));
#29326=CARTESIAN_POINT('Ctrl Pts',(96.8600571879523,1.10790957590403,-6.82799575732531));
#29327=CARTESIAN_POINT('Ctrl Pts',(96.8549232674718,1.1097477437695,-6.82762975969184));
#29328=CARTESIAN_POINT('Ctrl Pts',(96.8440559650715,1.11355377636021,-6.82685443256345));
#29329=CARTESIAN_POINT('Ctrl Pts',(96.838319802003,1.11551315751356,-6.82644483811882));
#29330=CARTESIAN_POINT('Ctrl Pts',(96.8229971940445,1.12061537122909,-6.82534965653715));
#29331=CARTESIAN_POINT('Ctrl Pts',(96.8133852387631,1.12367939797443,-6.82466153947367));
#29332=CARTESIAN_POINT('Ctrl Pts',(96.7698718858962,1.13693689131066,-6.82154066108701));
#29333=CARTESIAN_POINT('Ctrl Pts',(96.7355638628342,1.14572125106972,-6.81906352414358));
#29334=CARTESIAN_POINT('Ctrl Pts',(96.6146572635333,1.17093498950523,-6.81027280933388));
#29335=CARTESIAN_POINT('Ctrl Pts',(96.5266586168271,1.17918458829314,-6.80374218019794));
#29336=CARTESIAN_POINT('Ctrl Pts',(96.3964666135989,1.17676305530942,-6.79425476426406));
#29337=CARTESIAN_POINT('Ctrl Pts',(96.3544215765119,1.17372115108118,-6.79122345119864));
#29338=CARTESIAN_POINT('Ctrl Pts',(96.3059657839785,1.16758947867422,-6.78782876884236));
#29339=CARTESIAN_POINT('Ctrl Pts',(96.2993130064042,1.16668977302475,-6.78736489481905));
#29340=CARTESIAN_POINT('Ctrl Pts',(96.2890948011554,1.16521881363432,-6.7866561715524));
#29341=CARTESIAN_POINT('Ctrl Pts',(96.285523832206,1.16468798546192,-6.78640920021549));
#29342=CARTESIAN_POINT('Ctrl Pts',(96.2789446103847,1.16367903542043,-6.78595554919555));
#29343=CARTESIAN_POINT('Ctrl Pts',(96.2759357714203,1.1632056643294,-6.78574862185241));
#29344=CARTESIAN_POINT('Ctrl Pts',(96.2690880848778,1.16210110054651,-6.78527888548373));
#29345=CARTESIAN_POINT('Ctrl Pts',(96.2652505025404,1.16146255651345,-6.78501648778175));
#29346=CARTESIAN_POINT('Ctrl Pts',(96.2552291311031,1.15974400521432,-6.78433333055051));
#29347=CARTESIAN_POINT('Ctrl Pts',(96.2490505916633,1.1586335376587,-6.7839141949466));
#29348=CARTESIAN_POINT('Ctrl Pts',(96.202964169312,1.14996949597904,-6.78080118937489));
#29349=CARTESIAN_POINT('Ctrl Pts',(96.1634573741443,1.14040453132776,-6.77820730946662));
#29350=CARTESIAN_POINT('Ctrl Pts',(96.0558335471731,1.10837323839852,-6.77115437793228));
#29351=CARTESIAN_POINT('Ctrl Pts',(95.9891556431021,1.08170410353104,-6.76679192197993));
#29352=CARTESIAN_POINT('Ctrl Pts',(95.9241423110083,1.04854072782659,-6.76222263069734));
#29353=CARTESIAN_POINT('Ctrl Pts',(95.9229714708682,1.04794100655766,-6.76214023561899));
#29354=CARTESIAN_POINT('Ctrl Pts',(95.9218016727113,1.04733934289486,-6.7620578065779));
#29355=CARTESIAN_POINT('Ctrl Pts',(95.9218016806086,1.0473393469567,-6.66223764680097));
#29356=CARTESIAN_POINT('Ctrl Pts',(95.9435181322099,1.05850879486024,-6.66377551141126));
#29357=CARTESIAN_POINT('Ctrl Pts',(95.9655785064204,1.06900103023623,-6.66532772277226));
#29358=CARTESIAN_POINT('Ctrl Pts',(96.0025003733893,1.08517332476905,-6.66792309340538));
#29359=CARTESIAN_POINT('Ctrl Pts',(96.0171764254609,1.09125084906102,-6.66895404657819));
#29360=CARTESIAN_POINT('Ctrl Pts',(96.0436542399985,1.10159334498987,-6.67081606135641));
#29361=CARTESIAN_POINT('Ctrl Pts',(96.0554098791637,1.10597007727781,-6.67164345074486));
#29362=CARTESIAN_POINT('Ctrl Pts',(96.0734388694618,1.11235643499293,-6.67291450491019));
#29363=CARTESIAN_POINT('Ctrl Pts',(96.0796631318412,1.11450266800341,-6.67335369934532));
#29364=CARTESIAN_POINT('Ctrl Pts',(96.0905451866241,1.11815318654723,-6.67412236561389));
#29365=CARTESIAN_POINT('Ctrl Pts',(96.0951950129957,1.11968084765166,-6.67445106721583));
#29366=CARTESIAN_POINT('Ctrl Pts',(96.1057009934111,1.12306009070981,-6.67519439221232));
#29367=CARTESIAN_POINT('Ctrl Pts',(96.11156234348,1.12489492331328,-6.67560954763513));
#29368=CARTESIAN_POINT('Ctrl Pts',(96.1274426587684,1.12973002900543,-6.67673569446181));
#29369=CARTESIAN_POINT('Ctrl Pts',(96.1374874767613,1.13264277063171,-6.67744947357175));
#29370=CARTESIAN_POINT('Ctrl Pts',(96.1865509212101,1.14616419647763,-6.68094390453352));
#29371=CARTESIAN_POINT('Ctrl Pts',(96.2260552812149,1.15489132280347,-6.68378339203293));
#29372=CARTESIAN_POINT('Ctrl Pts',(96.3481913215893,1.17534823930417,-6.69264163076331));
#29373=CARTESIAN_POINT('Ctrl Pts',(96.4316832959287,1.1803477172002,-6.69882464684398));
#29374=CARTESIAN_POINT('Ctrl Pts',(96.5428427901678,1.17519743417564,-6.70692750980104));
#29375=CARTESIAN_POINT('Ctrl Pts',(96.5706424745308,1.17291820978649,-6.70894070607248));
#29376=CARTESIAN_POINT('Ctrl Pts',(96.6091636745739,1.16837808984237,-6.71169136754974));
#29377=CARTESIAN_POINT('Ctrl Pts',(96.6199728173294,1.16695170278519,-6.71245888418601));
#29378=CARTESIAN_POINT('Ctrl Pts',(96.638803733818,1.16420020334963,-6.71378672745948));
#29379=CARTESIAN_POINT('Ctrl Pts',(96.64683435382,1.16294176412217,-6.71435004032614));
#29380=CARTESIAN_POINT('Ctrl Pts',(96.658695020026,1.16095711826751,-6.71517700961791));
#29381=CARTESIAN_POINT('Ctrl Pts',(96.6625353194276,1.16029491117584,-6.71544399049936));
#29382=CARTESIAN_POINT('Ctrl Pts',(96.6690859883181,1.15913182874012,-6.71589798717931));
#29383=CARTESIAN_POINT('Ctrl Pts',(96.6717979657275,1.15864048689156,-6.7160855249842));
#29384=CARTESIAN_POINT('Ctrl Pts',(96.6779378797579,1.15750581418434,-6.71650915109689));
#29385=CARTESIAN_POINT('Ctrl Pts',(96.6813647029323,1.15685677361167,-6.71674491719432));
#29386=CARTESIAN_POINT('Ctrl Pts',(96.6906662181432,1.15505222856155,-6.71738316899787));
#29387=CARTESIAN_POINT('Ctrl Pts',(96.696535161133,1.15386711605725,-6.71778404510473));
#29388=CARTESIAN_POINT('Ctrl Pts',(96.7257802248937,1.14772920002724,-6.71977358708758));
#29389=CARTESIAN_POINT('Ctrl Pts',(96.7490126445444,1.14211018263302,-6.72132844618114));
#29390=CARTESIAN_POINT('Ctrl Pts',(96.8548577064927,1.11307387229661,-6.72836092387237));
#29391=CARTESIAN_POINT('Ctrl Pts',(96.9349295810044,1.0813729462213,-6.73355220565791));
#29392=CARTESIAN_POINT('Ctrl Pts',(97.04341469029,1.02403134812153,-6.74121499626182));
#29393=CARTESIAN_POINT('Ctrl Pts',(97.0751534725957,1.00530061053149,-6.74353963409945));
#29394=CARTESIAN_POINT('Ctrl Pts',(97.1192229152418,0.976424846598278,-6.74693223892321));
#29395=CARTESIAN_POINT('Ctrl Pts',(97.1323076918178,0.967468475297618,-6.74796141245266));
#29396=CARTESIAN_POINT('Ctrl Pts',(97.1553987839183,0.950968542118187,-6.74982049522431));
#29397=CARTESIAN_POINT('Ctrl Pts',(97.1654731798984,0.943524191648493,-6.7506467494412));
#29398=CARTESIAN_POINT('Ctrl Pts',(97.1806557828157,0.931926269874227,-6.75191641833662));
#29399=CARTESIAN_POINT('Ctrl Pts',(97.1858512832153,0.927888053073119,-6.75235537794897));
#29400=CARTESIAN_POINT('Ctrl Pts',(97.1948513662871,0.920770929697331,-6.75312378748024));
#29401=CARTESIAN_POINT('Ctrl Pts',(97.198671139769,0.917711422934184,-6.7534524688929));
#29402=CARTESIAN_POINT('Ctrl Pts',(97.2072433927009,0.910757196069246,-6.75419595276506));
#29403=CARTESIAN_POINT('Ctrl Pts',(97.2119846543876,0.906848937717653,-6.75461128864135));
#29404=CARTESIAN_POINT('Ctrl Pts',(97.2247220388007,0.896180924856015,-6.75573843912593));
#29405=CARTESIAN_POINT('Ctrl Pts',(97.2326587947664,0.889351480380417,-6.75645304995754));
#29406=CARTESIAN_POINT('Ctrl Pts',(97.2709354598514,0.85551641057501,-6.75996094438057));
#29407=CARTESIAN_POINT('Ctrl Pts',(97.2999522443008,0.827062340072261,-6.76281362781111));
#29408=CARTESIAN_POINT('Ctrl Pts',(97.3837875392097,0.735887642268726,-6.77167497483926));
#29409=CARTESIAN_POINT('Ctrl Pts',(97.4334767086992,0.668806815210093,-6.77784611622798));
#29410=CARTESIAN_POINT('Ctrl Pts',(97.4897927612263,0.573051478831407,-6.78593488741303));
#29411=CARTESIAN_POINT('Ctrl Pts',(97.5030572716375,0.548548650099507,-6.78794584345695));
#29412=CARTESIAN_POINT('Ctrl Pts',(97.5202844854446,0.513838700140383,-6.79069376422158));
#29413=CARTESIAN_POINT('Ctrl Pts',(97.5249922963517,0.504013249753029,-6.79146072178625));
#29414=CARTESIAN_POINT('Ctrl Pts',(97.5329715401187,0.486749411169764,-6.79278769582341));
#29415=CARTESIAN_POINT('Ctrl Pts',(97.5363035368953,0.479339989808475,-6.79335069344924));
#29416=CARTESIAN_POINT('Ctrl Pts',(97.5411197535718,0.468326826836095,-6.79417729129723));
#29417=CARTESIAN_POINT('Ctrl Pts',(97.5426631004528,0.464749432334438,-6.79444421179172));
#29418=CARTESIAN_POINT('Ctrl Pts',(97.5452678423514,0.458628450132566,-6.79489814072942));
#29419=CARTESIAN_POINT('Ctrl Pts',(97.5463380932441,0.456088721791253,-6.79508567074725));
#29420=CARTESIAN_POINT('Ctrl Pts',(97.5487427527305,0.450325968673833,-6.79550932642587));
#29421=CARTESIAN_POINT('Ctrl Pts',(97.5500717656045,0.447100754514082,-6.79574512956077));
#29422=CARTESIAN_POINT('Ctrl Pts',(97.5536438077036,0.438321689429858,-6.79638358096444));
#29423=CARTESIAN_POINT('Ctrl Pts',(97.555858868204,0.432756463779058,-6.79678461795352));
#29424=CARTESIAN_POINT('Ctrl Pts',(97.5667090232984,0.404878875773957,-6.79877630092245));
#29425=CARTESIAN_POINT('Ctrl Pts',(97.5747059531034,0.382322224684695,-6.80033305317518));
#29426=CARTESIAN_POINT('Ctrl Pts',(97.5880346056005,0.34074505937641,-6.8031304835891));
#29427=CARTESIAN_POINT('Ctrl Pts',(97.5935855444375,0.32180504350194,-6.80437825465699));
#29428=CARTESIAN_POINT('Ctrl Pts',(97.6149555492005,0.241460998635152,-6.8095936509178));
#29429=CARTESIAN_POINT('Ctrl Pts',(97.6262788359309,0.178971290107049,-6.81346639847084));
#29430=CARTESIAN_POINT('Ctrl Pts',(97.6363068845378,0.0775388148548756,
-6.8198220078009));
#29431=CARTESIAN_POINT('Ctrl Pts',(97.6382135311509,0.0390449728083933,
-6.82224853635611));
#29432=CARTESIAN_POINT('Ctrl Pts',(97.6382415568925,-0.0233515149004739,
-6.82626240700895));
#29433=CARTESIAN_POINT('Ctrl Pts',(97.6375259693824,-0.047225378884949,
-6.82781704811608));
#29434=CARTESIAN_POINT('Ctrl Pts',(97.6355589528823,-0.0797674762297623,
-6.82996991716587));
#29435=CARTESIAN_POINT('Ctrl Pts',(97.6349358924056,-0.0884688906534224,
-6.83054885818288));
#29436=CARTESIAN_POINT('Ctrl Pts',(97.6337880983953,-0.102334403040144,
-6.83147697959983));
#29437=CARTESIAN_POINT('Ctrl Pts',(97.6333257819149,-0.107503457206415,
-6.83182422397345));
#29438=CARTESIAN_POINT('Ctrl Pts',(97.6323036044168,-0.118139442363736,
-6.83254136180633));
#29439=CARTESIAN_POINT('Ctrl Pts',(97.6317396131446,-0.123605839259553,
-6.83291137491555));
#29440=CARTESIAN_POINT('Ctrl Pts',(97.6303376454547,-0.136321790378976,
-6.83377554624475));
#29441=CARTESIAN_POINT('Ctrl Pts',(97.6294705098105,-0.143567835317118,
-6.83427059767699));
#29442=CARTESIAN_POINT('Ctrl Pts',(97.6264517634534,-0.166949402410066,
-6.83587674086363));
#29443=CARTESIAN_POINT('Ctrl Pts',(97.6240330375774,-0.183047901922865,
-6.83699605107244));
#29444=CARTESIAN_POINT('Ctrl Pts',(97.6175248743006,-0.220993873722818,
-6.83966763660328));
#29445=CARTESIAN_POINT('Ctrl Pts',(97.6131492148192,-0.242785288354996,
-6.84122821531472));
#29446=CARTESIAN_POINT('Ctrl Pts',(97.583305604925,-0.372308247967736,-6.85066255182494));
#29447=CARTESIAN_POINT('Ctrl Pts',(97.5433741580206,-0.476114472347658,
-6.85895734332145));
#29448=CARTESIAN_POINT('Ctrl Pts',(97.4779679255668,-0.593617984458168,
-6.86860234599094));
#29449=CARTESIAN_POINT('Ctrl Pts',(97.4657575551305,-0.614069369081318,
-6.87028837375453));
#29450=CARTESIAN_POINT('Ctrl Pts',(97.4497143378922,-0.639177701303956,
-6.87235509738748));
#29451=CARTESIAN_POINT('Ctrl Pts',(97.4464557519938,-0.644192923876767,
-6.87276774073831));
#29452=CARTESIAN_POINT('Ctrl Pts',(97.441237418681,-0.652091990600966,-6.873417123019));
#29453=CARTESIAN_POINT('Ctrl Pts',(97.4393028815496,-0.654992245893617,
-6.87365543678758));
#29454=CARTESIAN_POINT('Ctrl Pts',(97.435815738999,-0.660170212101329,-6.87408064063689));
#29455=CARTESIAN_POINT('Ctrl Pts',(97.4342680208881,-0.662451055070377,
-6.87426783858703));
#29456=CARTESIAN_POINT('Ctrl Pts',(97.4305115351465,-0.667945304155838,
-6.87471856099046));
#29457=CARTESIAN_POINT('Ctrl Pts',(97.4282947996807,-0.671153200783884,
-6.87498155102142));
#29458=CARTESIAN_POINT('Ctrl Pts',(97.421401291663,-0.68102380326286,-6.87579043316972));
#29459=CARTESIAN_POINT('Ctrl Pts',(97.4166712259537,-0.687649248432255,
-6.87633291141048));
#29460=CARTESIAN_POINT('Ctrl Pts',(97.389859097989,-0.72439356673599,-6.87934209876629));
#29461=CARTESIAN_POINT('Ctrl Pts',(97.3664206127203,-0.753500961981441,
-6.88172853690735));
#29462=CARTESIAN_POINT('Ctrl Pts',(97.2894128843905,-0.84033432027858,-6.88902722800703));
#29463=CARTESIAN_POINT('Ctrl Pts',(97.2314181341364,-0.893838065211288,
-6.89380392673516));
#29464=CARTESIAN_POINT('Ctrl Pts',(97.131849080621,-0.968744305876814,-6.90163532587682));
#29465=CARTESIAN_POINT('Ctrl Pts',(97.0936029867845,-0.994161175202824,
-6.90456739568809));
#29466=CARTESIAN_POINT('Ctrl Pts',(97.0447424233536,-1.02266702537903,-6.90828539177868));
#29467=CARTESIAN_POINT('Ctrl Pts',(97.0354372748858,-1.0279272961891,-6.90899216104235));
#29468=CARTESIAN_POINT('Ctrl Pts',(97.0205768317845,-1.03606311167467,-6.91011951414726));
#29469=CARTESIAN_POINT('Ctrl Pts',(97.0150678610423,-1.03902238846291,-6.91053714497291));
#29470=CARTESIAN_POINT('Ctrl Pts',(97.0047358233251,-1.04446691228128,-6.9113199951797));
#29471=CARTESIAN_POINT('Ctrl Pts',(96.9999186237999,-1.04696298520599,-6.91168482436119));
#29472=CARTESIAN_POINT('Ctrl Pts',(96.9891288141714,-1.05245958198956,-6.91250170902271));
#29473=CARTESIAN_POINT('Ctrl Pts',(96.983147600216,-1.05544270597129,-6.91295435191427));
#29474=CARTESIAN_POINT('Ctrl Pts',(96.9654278318999,-1.06409285969387,-6.91429497601245));
#29475=CARTESIAN_POINT('Ctrl Pts',(96.9536205458373,-1.06961595115866,-6.91518782593623));
#29476=CARTESIAN_POINT('Ctrl Pts',(96.9265004072677,-1.08175743667071,-6.91723835317986));
#29477=CARTESIAN_POINT('Ctrl Pts',(96.9111340115599,-1.08824861882579,-6.91840002367127));
#29478=CARTESIAN_POINT('Ctrl Pts',(96.8586552625048,-1.10911497610921,-6.92236761226475));
#29479=CARTESIAN_POINT('Ctrl Pts',(96.8209569187169,-1.12193375296381,-6.92521935593456));
#29480=CARTESIAN_POINT('Ctrl Pts',(96.6996653053471,-1.15643236359103,-6.934373677303));
#29481=CARTESIAN_POINT('Ctrl Pts',(96.6143037399726,-1.17084730419555,-6.94080517792564));
#29482=CARTESIAN_POINT('Ctrl Pts',(96.5086020925552,-1.17692913051396,-6.94835612972556));
#29483=CARTESIAN_POINT('Ctrl Pts',(96.4890437388933,-1.1775661759021,-6.94973497666021));
#29484=CARTESIAN_POINT('Ctrl Pts',(96.4638165574998,-1.17775888098992,-6.95148258865477));
#29485=CARTESIAN_POINT('Ctrl Pts',(96.4581554637986,-1.17776131001634,-6.95187275376299));
#29486=CARTESIAN_POINT('Ctrl Pts',(96.4491132359276,-1.177699991763,-6.95249251379603));
#29487=CARTESIAN_POINT('Ctrl Pts',(96.4457321001787,-1.17766250160362,-6.95272349189297));
#29488=CARTESIAN_POINT('Ctrl Pts',(96.4392567417308,-1.17756281061463,-6.95316431953868));
#29489=CARTESIAN_POINT('Ctrl Pts',(96.4361625658402,-1.17750297509937,-6.95337428823693));
#29490=CARTESIAN_POINT('Ctrl Pts',(96.4287800408916,-1.17733109906063,-6.95387371125276));
#29491=CARTESIAN_POINT('Ctrl Pts',(96.4244919502068,-1.17720782268296,-6.95416255302269));
#29492=CARTESIAN_POINT('Ctrl Pts',(96.4098881010507,-1.17670811156251,-6.95514230554123));
#29493=CARTESIAN_POINT('Ctrl Pts',(96.3995763092994,-1.17621947730991,-6.95582739638931));
#29494=CARTESIAN_POINT('Ctrl Pts',(96.3743905260724,-1.17469390385401,-6.95748717316768));
#29495=CARTESIAN_POINT('Ctrl Pts',(96.3595269261624,-1.17350997325286,-6.95845517505391));
#29496=CARTESIAN_POINT('Ctrl Pts',(96.2988995579458,-1.16752030555357,-6.96237090055341));
#29497=CARTESIAN_POINT('Ctrl Pts',(96.2534107677746,-1.16031668294897,-6.96523362639875));
#29498=CARTESIAN_POINT('Ctrl Pts',(96.1194400056407,-1.13096881069579,-6.97372832373236));
#29499=CARTESIAN_POINT('Ctrl Pts',(96.0329974962076,-1.10120622183265,-6.97931971926822));
#29500=CARTESIAN_POINT('Ctrl Pts',(95.9376018579259,-1.05541867101454,-6.98622221068482));
#29501=CARTESIAN_POINT('Ctrl Pts',(95.9244712063652,-1.04881106005287,-6.98718874841855));
#29502=CARTESIAN_POINT('Ctrl Pts',(95.905243918589,-1.03868012300822,-6.98863036919659));
#29503=CARTESIAN_POINT('Ctrl Pts',(95.8990493543302,-1.03534492744148,-6.98909893745356));
#29504=CARTESIAN_POINT('Ctrl Pts',(95.8880880824478,-1.02931600670457,-6.98993560726436));
#29505=CARTESIAN_POINT('Ctrl Pts',(95.8833095377571,-1.02664414265652,-6.99030293174996));
#29506=CARTESIAN_POINT('Ctrl Pts',(95.8733578288444,-1.02098832895136,-6.99107342155238));
#29507=CARTESIAN_POINT('Ctrl Pts',(95.8681883969793,-1.0179981614062,-6.99147680020582));
#29508=CARTESIAN_POINT('Ctrl Pts',(95.8547007603713,-1.01005896281564,-6.99253767135532));
#29509=CARTESIAN_POINT('Ctrl Pts',(95.8464205764423,-1.00504656332294,-6.99319742075052));
#29510=CARTESIAN_POINT('Ctrl Pts',(95.8081570389825,-0.981234419937012,
-6.99628667569865));
#29511=CARTESIAN_POINT('Ctrl Pts',(95.7789718237791,-0.961193180207256,
-6.99876091674393));
#29512=CARTESIAN_POINT('Ctrl Pts',(95.7014389129711,-0.90264400448064,-7.00567105559041));
#29513=CARTESIAN_POINT('Ctrl Pts',(95.6551523152623,-0.861600454694597,
-7.0101881889309));
#29514=CARTESIAN_POINT('Ctrl Pts',(95.5680027667561,-0.771138540234212,
-7.0194071278191));
#29515=CARTESIAN_POINT('Ctrl Pts',(95.5275117015609,-0.721624500413595,
-7.02409439104554));
#29516=CARTESIAN_POINT('Ctrl Pts',(95.4855573550991,-0.660847048678829,
-7.02927284511133));
#29517=CARTESIAN_POINT('Ctrl Pts',(95.4799874441898,-0.652554472178123,
-7.02996779402803));
#29518=CARTESIAN_POINT('Ctrl Pts',(95.4723718619117,-0.640898562664305,
-7.03092748358191));
#29519=CARTESIAN_POINT('Ctrl Pts',(95.4702367091495,-0.637594606440704,
-7.03119762595653));
#29520=CARTESIAN_POINT('Ctrl Pts',(95.4665800815491,-0.631873628964075,
-7.0316620587793));
#29521=CARTESIAN_POINT('Ctrl Pts',(95.4650507871649,-0.629461683227001,
-7.03185684763986));
#29522=CARTESIAN_POINT('Ctrl Pts',(95.4618407354994,-0.624357954664768,
-7.03226684868743));
#29523=CARTESIAN_POINT('Ctrl Pts',(95.4601620561173,-0.621664897318871,
-7.03248191930135));
#29524=CARTESIAN_POINT('Ctrl Pts',(95.4560197870403,-0.614959351634867,
-7.03301436434572));
#29525=CARTESIAN_POINT('Ctrl Pts',(95.4535693019478,-0.610938758757568,
-7.03333090265751));
#29526=CARTESIAN_POINT('Ctrl Pts',(95.4443936450504,-0.595678772052536,
-7.03452252106524));
#29527=CARTESIAN_POINT('Ctrl Pts',(95.4378317123981,-0.584341666096217,
-7.03538785524774));
#29528=CARTESIAN_POINT('Ctrl Pts',(95.4214407765628,-0.554900735563526,
-7.03759042591352));
#29529=CARTESIAN_POINT('Ctrl Pts',(95.4118948154764,-0.536643762463493,
-7.03891385874727));
#29530=CARTESIAN_POINT('Ctrl Pts',(95.3774462232762,-0.466326513788181,
-7.04388728208573));
#29531=CARTESIAN_POINT('Ctrl Pts',(95.3559013267196,-0.412709686764973,
-7.04743038984246));
#29532=CARTESIAN_POINT('Ctrl Pts',(95.3154698778587,-0.285885369046476,
-7.05567274513202));
#29533=CARTESIAN_POINT('Ctrl Pts',(95.2995219671884,-0.21202083607617,-7.06038223187065));
#29534=CARTESIAN_POINT('Ctrl Pts',(95.2895334610219,-0.126826518984517,
-7.06601187704241));
#29535=CARTESIAN_POINT('Ctrl Pts',(95.2884603447734,-0.116493251282683,
-7.06669766382515));
#29536=CARTESIAN_POINT('Ctrl Pts',(95.2869179760793,-0.0994496693158102,
-7.06783432644692));
#29537=CARTESIAN_POINT('Ctrl Pts',(95.2863692502246,-0.0927469880201546,
-7.06828274301734));
#29538=CARTESIAN_POINT('Ctrl Pts',(95.2854814066951,-0.0806263165939802,
-7.06909633092116));
#29539=CARTESIAN_POINT('Ctrl Pts',(95.2851222846926,-0.0752099454617208,
-7.06946087270627));
#29540=CARTESIAN_POINT('Ctrl Pts',(95.2844318644319,-0.063579372613031,
-7.07024583139685));
#29541=CARTESIAN_POINT('Ctrl Pts',(95.2841123508418,-0.0573646636602585,
-7.0706666015377));
#29542=CARTESIAN_POINT('Ctrl Pts',(95.2833716588476,-0.0403252856444004,
-7.07182406284828));
#29543=CARTESIAN_POINT('Ctrl Pts',(95.2830505617619,-0.0294971056563918,
-7.07256381269156));
#29544=CARTESIAN_POINT('Ctrl Pts',(95.2820333170437,0.0346777292341549,
-7.07697423523189));
#29545=CARTESIAN_POINT('Ctrl Pts',(95.284813404224,0.0880097582886529,-7.08075089277713));
#29546=CARTESIAN_POINT('Ctrl Pts',(95.2969371898862,0.188575961179659,-7.08807211695678));
#29547=CARTESIAN_POINT('Ctrl Pts',(95.3055796823814,0.235791440587897,-7.09159417919729));
#29548=CARTESIAN_POINT('Ctrl Pts',(95.3238379460088,0.309731218146189,-7.09718199086497));
#29549=CARTESIAN_POINT('Ctrl Pts',(95.3315821718537,0.33686553528854,-7.09924791973965));
#29550=CARTESIAN_POINT('Ctrl Pts',(95.3509929565848,0.396650905548326,-7.10380531659571));
#29551=CARTESIAN_POINT('Ctrl Pts',(95.3631426573753,0.429120863504874,-7.10628431940859));
#29552=CARTESIAN_POINT('Ctrl Pts',(95.379081138831,0.466590047760546,-7.10911446708953));
#29553=CARTESIAN_POINT('Ctrl Pts',(95.3814975393095,0.472151064371352,-7.10953368278558));
#29554=CARTESIAN_POINT('Ctrl Pts',(95.3855085750354,0.481190287892778,-7.11021347052416));
#29555=CARTESIAN_POINT('Ctrl Pts',(95.3870773675656,0.484679739987771,-7.11047549234275));
#29556=CARTESIAN_POINT('Ctrl Pts',(95.389924052472,0.490929981392766,-7.11094402181338));
#29557=CARTESIAN_POINT('Ctrl Pts',(95.3911956586952,0.493693512123373,-7.11115089321832));
#29558=CARTESIAN_POINT('Ctrl Pts',(95.3940214942159,0.499772648695421,-7.11160532652717));
#29559=CARTESIAN_POINT('Ctrl Pts',(95.3955804853054,0.503085949335144,-7.11185259679593));
#29560=CARTESIAN_POINT('Ctrl Pts',(95.400146981531,0.51267471541555,-7.11256716902181));
#29561=CARTESIAN_POINT('Ctrl Pts',(95.4031947464796,0.518930995542927,-7.11303210874049));
#29562=CARTESIAN_POINT('Ctrl Pts',(95.4295789089374,0.571893394205202,-7.11696014137991));
#29563=CARTESIAN_POINT('Ctrl Pts',(95.4559451144396,0.617033462149801,-7.12025664880505));
#29564=CARTESIAN_POINT('Ctrl Pts',(95.5318781515408,0.729189328667322,-7.12869343626242));
#29565=CARTESIAN_POINT('Ctrl Pts',(95.585701710694,0.792957202164231,-7.13375744393606));
#29566=CARTESIAN_POINT('Ctrl Pts',(95.6680247354002,0.871811718591976,-7.1410286297561));
#29567=CARTESIAN_POINT('Ctrl Pts',(95.6910777997151,0.892222540414428,-7.14301999628774));
#29568=CARTESIAN_POINT('Ctrl Pts',(95.7223100699347,0.917763797904444,-7.14567895538587));
#29569=CARTESIAN_POINT('Ctrl Pts',(95.7297912070994,0.923731090551799,-7.14631304261169));
#29570=CARTESIAN_POINT('Ctrl Pts',(95.7420389099312,0.933258526762123,-7.14734708613484));
#29571=CARTESIAN_POINT('Ctrl Pts',(95.7467612931565,0.936874960679396,-7.14774482871979));
#29572=CARTESIAN_POINT('Ctrl Pts',(95.755888378535,0.943755490090837,-7.14851184547839));
#29573=CARTESIAN_POINT('Ctrl Pts',(95.7602888849372,0.947024913672375,-7.1488809002435));
#29574=CARTESIAN_POINT('Ctrl Pts',(95.7705273187116,0.954521344673939,-7.14973792370096));
#29575=CARTESIAN_POINT('Ctrl Pts',(95.7763814920068,0.958725684613716,-7.15022674013802));
#29576=CARTESIAN_POINT('Ctrl Pts',(95.7951695847861,0.971959185091832,-7.15179192094793));
#29577=CARTESIAN_POINT('Ctrl Pts',(95.8082459979776,0.980782032735578,-7.1528759287993));
#29578=CARTESIAN_POINT('Ctrl Pts',(95.8394105242881,1.00091030577544,-7.15544822591452));
#29579=CARTESIAN_POINT('Ctrl Pts',(95.8576358909193,1.01199192230355,-7.15694400981839));
#29580=CARTESIAN_POINT('Ctrl Pts',(95.891188954041,1.03116519760778,-7.15968278018666));
#29581=CARTESIAN_POINT('Ctrl Pts',(95.9064096505938,1.03942274704365,-7.16091977633442));
#29582=CARTESIAN_POINT('Ctrl Pts',(95.921801726504,1.04733937056209,-7.16216478479583));
#29583=CARTESIAN_POINT('Origin',(96.460480949577,-7.19464945638997E-16,
0.924367114736168));
#29584=CARTESIAN_POINT('',(95.9218015552897,1.04733928250124,-7.7622548478038));
#29585=CARTESIAN_POINT('',(95.9218016730721,1.04733934308043,-7.66392541087522));
#29586=CARTESIAN_POINT('',(95.9218016730721,1.04733934308042,0.924367114736168));
#29587=CARTESIAN_POINT('Ctrl Pts',(95.9218015552896,1.04733928250123,-7.76225484780379));
#29588=CARTESIAN_POINT('Ctrl Pts',(95.8623558116904,1.01676447480516,-7.75745389936112));
#29589=CARTESIAN_POINT('Ctrl Pts',(95.8056001884861,0.98117324913246,-7.75252362611853));
#29590=CARTESIAN_POINT('Ctrl Pts',(95.7104284735965,0.909529753051495,-7.74380334359668));
#29591=CARTESIAN_POINT('Ctrl Pts',(95.6708304283255,0.87537217593098,-7.74001378553606));
#29592=CARTESIAN_POINT('Ctrl Pts',(95.6286713472776,0.833808301570045,-7.7358960785663));
#29593=CARTESIAN_POINT('Ctrl Pts',(95.6237585763514,0.828878262619539,-7.7354149034486));
#29594=CARTESIAN_POINT('Ctrl Pts',(95.6163278537723,0.821288027268597,-7.7346854488181));
#29595=CARTESIAN_POINT('Ctrl Pts',(95.6137782317822,0.818659258475165,-7.73443485500648));
#29596=CARTESIAN_POINT('Ctrl Pts',(95.6091329451359,0.813824854424591,-7.73397779754325));
#29597=CARTESIAN_POINT('Ctrl Pts',(95.6070335569774,0.811622983199139,-7.73377105779751));
#29598=CARTESIAN_POINT('Ctrl Pts',(95.6023131234428,0.806633549989927,-7.73330578623913));
#29599=CARTESIAN_POINT('Ctrl Pts',(95.5996971140449,0.803841334655844,-7.73304763261966));
#29600=CARTESIAN_POINT('Ctrl Pts',(95.5929705930079,0.796591244776481,-7.73238289354525));
#29601=CARTESIAN_POINT('Ctrl Pts',(95.5888807564069,0.792114219726847,-7.73197779223504));
#29602=CARTESIAN_POINT('Ctrl Pts',(95.5616517694671,0.761841192206451,-7.72927282621328));
#29603=CARTESIAN_POINT('Ctrl Pts',(95.5396238510393,0.735063675310923,-7.72704554617816));
#29604=CARTESIAN_POINT('Ctrl Pts',(95.5018766974373,0.68481207866792,-7.72307426380063));
#29605=CARTESIAN_POINT('Ctrl Pts',(95.4857603702686,0.661671828179948,-7.7213189995572));
#29606=CARTESIAN_POINT('Ctrl Pts',(95.4445239084751,0.597682230029865,-7.71659903347338));
#29607=CARTESIAN_POINT('Ctrl Pts',(95.4210429206934,0.555842828153083,-7.7136512878776));
#29608=CARTESIAN_POINT('Ctrl Pts',(95.3769402612776,0.464633175988972,-7.70731590496983));
#29609=CARTESIAN_POINT('Ctrl Pts',(95.357000226675,0.415058573191055,-7.70392275662391));
#29610=CARTESIAN_POINT('Ctrl Pts',(95.3371404041336,0.354003493066166,-7.69970304477885));
#29611=CARTESIAN_POINT('Ctrl Pts',(95.3339313870623,0.343654658855028,-7.69898659985602));
#29612=CARTESIAN_POINT('Ctrl Pts',(95.3291045948915,0.327293967159561,-7.69785137481006));
#29613=CARTESIAN_POINT('Ctrl Pts',(95.3273908735627,0.32131086818038,-7.69743568607001));
#29614=CARTESIAN_POINT('Ctrl Pts',(95.3242712661299,0.31008400299646,-7.69665453956417));
#29615=CARTESIAN_POINT('Ctrl Pts',(95.3228540544881,0.304843532904559,-7.69628945600205));
#29616=CARTESIAN_POINT('Ctrl Pts',(95.3197623509039,0.293089358644882,-7.69546946736407));
#29617=CARTESIAN_POINT('Ctrl Pts',(95.3181073326422,0.286570775895503,-7.69501395445715));
#29618=CARTESIAN_POINT('Ctrl Pts',(95.3140381142473,0.269947794253929,-7.69385024094827));
#29619=CARTESIAN_POINT('Ctrl Pts',(95.311701655163,0.259825147057946,-7.69313960999478));
#29620=CARTESIAN_POINT('Ctrl Pts',(95.293502274304,0.175926871196835,-7.6872319712601));
#29621=CARTESIAN_POINT('Ctrl Pts',(95.284632574587,0.100827628796701,-7.68181333533136));
#29622=CARTESIAN_POINT('Ctrl Pts',(95.2817578858941,-0.0323856236665279,
-7.67206625033741));
#29623=CARTESIAN_POINT('Ctrl Pts',(95.2847675297353,-0.0901947604395963,
-7.66779664176533));
#29624=CARTESIAN_POINT('Ctrl Pts',(95.2945782898097,-0.167887660780126,
-7.66214169867262));
#29625=CARTESIAN_POINT('Ctrl Pts',(95.2976771504118,-0.18815606035501,-7.66067478824316));
#29626=CARTESIAN_POINT('Ctrl Pts',(95.3036126679399,-0.221181417611749,
-7.65830834490023));
#29627=CARTESIAN_POINT('Ctrl Pts',(95.3061351554409,-0.233989879058172,
-7.65739647204719));
#29628=CARTESIAN_POINT('Ctrl Pts',(95.3098554244798,-0.251352494807781,
-7.65617078305995));
#29629=CARTESIAN_POINT('Ctrl Pts',(95.3108682041788,-0.255944746293492,
-7.65584759672723));
#29630=CARTESIAN_POINT('Ctrl Pts',(95.3126102332335,-0.263624628277087,
-7.65530892385985));
#29631=CARTESIAN_POINT('Ctrl Pts',(95.3133244929625,-0.266715561787505,
-7.65509261604539));
#29632=CARTESIAN_POINT('Ctrl Pts',(95.3147058025516,-0.272584920650193,
-7.65468285522255));
#29633=CARTESIAN_POINT('Ctrl Pts',(95.3153704858758,-0.275363855420494,
-7.65448926651578));
#29634=CARTESIAN_POINT('Ctrl Pts',(95.3169754459565,-0.281967619849792,
-7.65403016537959));
#29635=CARTESIAN_POINT('Ctrl Pts',(95.3179248164491,-0.285790236380545,
-7.65376516146224));
#29636=CARTESIAN_POINT('Ctrl Pts',(95.3213565728594,-0.299317657425676,
-7.65282979058452));
#29637=CARTESIAN_POINT('Ctrl Pts',(95.3239436580247,-0.308995804033067,
-7.65216500767871));
#29638=CARTESIAN_POINT('Ctrl Pts',(95.3440546483653,-0.380557351833379,
-7.64727437673847));
#29639=CARTESIAN_POINT('Ctrl Pts',(95.3665003643921,-0.44095381115291,-7.64328185087216));
#29640=CARTESIAN_POINT('Ctrl Pts',(95.4197954966609,-0.55483219002027,-7.63549953789965));
#29641=CARTESIAN_POINT('Ctrl Pts',(95.4501286307923,-0.608319489865074,
-7.63171932980393));
#29642=CARTESIAN_POINT('Ctrl Pts',(95.5042328763501,-0.688424765656717,
-7.625580045225));
#29643=CARTESIAN_POINT('Ctrl Pts',(95.5252750434112,-0.716748613827844,
-7.62330529138456));
#29644=CARTESIAN_POINT('Ctrl Pts',(95.553663635546,-0.751578949035402,-7.62034464378981));
#29645=CARTESIAN_POINT('Ctrl Pts',(95.5598644549051,-0.758998338619742,
-7.61970404976792));
#29646=CARTESIAN_POINT('Ctrl Pts',(95.5700404585016,-0.77087381413286,-7.61866199740248));
#29647=CARTESIAN_POINT('Ctrl Pts',(95.5739594936044,-0.775377592752606,
-7.61826281759666));
#29648=CARTESIAN_POINT('Ctrl Pts',(95.5815384749185,-0.783954829693693,
-7.61749479895331));
#29649=CARTESIAN_POINT('Ctrl Pts',(95.585192929818,-0.78803294949385,-7.61712619253361));
#29650=CARTESIAN_POINT('Ctrl Pts',(95.5936108264012,-0.797295945090009,
-7.61628092628429));
#29651=CARTESIAN_POINT('Ctrl Pts',(95.5983925512732,-0.802463846099366,
-7.6158035089931));
#29652=CARTESIAN_POINT('Ctrl Pts',(95.6133168484535,-0.818306090214565,
-7.61432156713335));
#29653=CARTESIAN_POINT('Ctrl Pts',(95.6236131450621,-0.828832983937494,
-7.61331054777798));
#29654=CARTESIAN_POINT('Ctrl Pts',(95.698816421333,-0.902890379633603,-7.60600292835653));
#29655=CARTESIAN_POINT('Ctrl Pts',(95.7706717911202,-0.958906205808967,
-7.5993852895564));
#29656=CARTESIAN_POINT('Ctrl Pts',(95.8877120106867,-1.03012958227682,-7.58933030368828));
#29657=CARTESIAN_POINT('Ctrl Pts',(95.9285770109048,-1.05181267972917,-7.58594205587981));
#29658=CARTESIAN_POINT('Ctrl Pts',(95.9842059676899,-1.07725606654963,-7.58156511302202));
#29659=CARTESIAN_POINT('Ctrl Pts',(95.9979169860043,-1.08321425176453,-7.58050457575498));
#29660=CARTESIAN_POINT('Ctrl Pts',(96.0213010971731,-1.09285090271834,-7.57873062670749));
#29661=CARTESIAN_POINT('Ctrl Pts',(96.0309157350125,-1.0966657572051,-7.57801101814121));
#29662=CARTESIAN_POINT('Ctrl Pts',(96.0445909927128,-1.10188431295254,-7.57700246069502));
#29663=CARTESIAN_POINT('Ctrl Pts',(96.0486106222244,-1.10339309869505,-7.57670782434119));
#29664=CARTESIAN_POINT('Ctrl Pts',(96.0555424544591,-1.10595183426817,-7.57620294810431));
#29665=CARTESIAN_POINT('Ctrl Pts',(96.0584506853503,-1.10701233602849,-7.57599210192367));
#29666=CARTESIAN_POINT('Ctrl Pts',(96.064543367787,-1.10920688772061,-7.57555245416719));
#29667=CARTESIAN_POINT('Ctrl Pts',(96.0677285515537,-1.11033870643756,-7.57532378126615));
#29668=CARTESIAN_POINT('Ctrl Pts',(96.076255595299,-1.11332741011944,-7.57471461227414));
#29669=CARTESIAN_POINT('Ctrl Pts',(96.0816061128963,-1.11515958781862,-7.574335520574));
#29670=CARTESIAN_POINT('Ctrl Pts',(96.1054700193082,-1.12313972185915,-7.57265782571121));
#29671=CARTESIAN_POINT('Ctrl Pts',(96.1241224446603,-1.12886609399666,-7.57138143487332));
#29672=CARTESIAN_POINT('Ctrl Pts',(96.2252861281093,-1.15719332151939,-7.56460230885184));
#29673=CARTESIAN_POINT('Ctrl Pts',(96.3099381244624,-1.17121853105755,-7.55942288639653));
#29674=CARTESIAN_POINT('Ctrl Pts',(96.4505528376814,-1.17900424556005,-7.55065428444415));
#29675=CARTESIAN_POINT('Ctrl Pts',(96.5058763561995,-1.17817136094729,-7.5471660186304));
#29676=CARTESIAN_POINT('Ctrl Pts',(96.5752032635571,-1.17223674596182,-7.54262278544775));
#29677=CARTESIAN_POINT('Ctrl Pts',(96.5894496208711,-1.17075499180739,-7.54168023680153));
#29678=CARTESIAN_POINT('Ctrl Pts',(96.610551054602,-1.16817043113566,-7.54026924194545));
#29679=CARTESIAN_POINT('Ctrl Pts',(96.6174294667427,-1.16726618734159,-7.53980694331343));
#29680=CARTESIAN_POINT('Ctrl Pts',(96.6296945976675,-1.16554342973198,-7.53897820654938));
#29681=CARTESIAN_POINT('Ctrl Pts',(96.6350844258278,-1.16474820011479,-7.5386125034827));
#29682=CARTESIAN_POINT('Ctrl Pts',(96.6464831928538,-1.16298549864059,-7.53783577770189));
#29683=CARTESIAN_POINT('Ctrl Pts',(96.6524905198881,-1.16200878958067,-7.53742447621294));
#29684=CARTESIAN_POINT('Ctrl Pts',(96.6685460471911,-1.15927047969631,-7.53631983284869));
#29685=CARTESIAN_POINT('Ctrl Pts',(96.6785791909015,-1.15742484668191,-7.53562388348187));
#29686=CARTESIAN_POINT('Ctrl Pts',(96.7249969849779,-1.14826116216898,-7.53237696637806));
#29687=CARTESIAN_POINT('Ctrl Pts',(96.7610432099318,-1.13935694086453,-7.52977691457013));
#29688=CARTESIAN_POINT('Ctrl Pts',(96.879467093729,-1.10409260668574,-7.52096718048058));
#29689=CARTESIAN_POINT('Ctrl Pts',(96.9593542506177,-1.07037018027013,-7.514559087871));
#29690=CARTESIAN_POINT('Ctrl Pts',(97.0596107332953,-1.01436923821392,-7.50619341250719));
#29691=CARTESIAN_POINT('Ctrl Pts',(97.083895044422,-0.999628196070767,-7.50414192887341));
#29692=CARTESIAN_POINT('Ctrl Pts',(97.1213250061091,-0.975012356557827,
-7.5009639365712));
#29693=CARTESIAN_POINT('Ctrl Pts',(97.1348370543568,-0.965716249038768,
-7.49981329221704));
#29694=CARTESIAN_POINT('Ctrl Pts',(97.152306662886,-0.953151846782232,-7.49832550858258));
#29695=CARTESIAN_POINT('Ctrl Pts',(97.1564425446897,-0.950136159273038,
-7.49797327203306));
#29696=CARTESIAN_POINT('Ctrl Pts',(97.1631815834963,-0.945154759713182,
-7.49739949555798));
#29697=CARTESIAN_POINT('Ctrl Pts',(97.1657964137941,-0.943205066416705,
-7.49717690324461));
#29698=CARTESIAN_POINT('Ctrl Pts',(97.1708984402366,-0.93936776615128,-7.49674271662857));
#29699=CARTESIAN_POINT('Ctrl Pts',(97.1733862777433,-0.937481095572839,
-7.4965310656016));
#29700=CARTESIAN_POINT('Ctrl Pts',(97.1789410007957,-0.933233730354478,
-7.49605857756015));
#29701=CARTESIAN_POINT('Ctrl Pts',(97.1820038409129,-0.930867745169545,
-7.49579810251875));
#29702=CARTESIAN_POINT('Ctrl Pts',(97.192631930154,-0.922573778070909,-7.49489421371316));
#29703=CARTESIAN_POINT('Ctrl Pts',(97.200136480555,-0.916568134041856,-7.49425590606996));
#29704=CARTESIAN_POINT('Ctrl Pts',(97.2651823877418,-0.863194787566515,
-7.48871434044085));
#29705=CARTESIAN_POINT('Ctrl Pts',(97.3181887822631,-0.810549255170093,
-7.48412905434578));
#29706=CARTESIAN_POINT('Ctrl Pts',(97.4176337646367,-0.691017228400199,
-7.47451097721846));
#29707=CARTESIAN_POINT('Ctrl Pts',(97.4628407987864,-0.623633540421259,
-7.46949080904351));
#29708=CARTESIAN_POINT('Ctrl Pts',(97.5069490201436,-0.540530077820964,
-7.46333495666381));
#29709=CARTESIAN_POINT('Ctrl Pts',(97.5129222043343,-0.528805796551455,
-7.46246777314942));
#29710=CARTESIAN_POINT('Ctrl Pts',(97.5216424792608,-0.51095624115618,-7.46114820672977));
#29711=CARTESIAN_POINT('Ctrl Pts',(97.5245358199176,-0.504903260273835,
-7.4607008449404));
#29712=CARTESIAN_POINT('Ctrl Pts',(97.5296760441138,-0.493909274013369,
-7.45988835217087));
#29713=CARTESIAN_POINT('Ctrl Pts',(97.5319408014373,-0.488976794239848,
-7.4595238425127));
#29714=CARTESIAN_POINT('Ctrl Pts',(97.5367340954343,-0.478344136362578,
-7.45873803717769));
#29715=CARTESIAN_POINT('Ctrl Pts',(97.5392516068777,-0.472639199734736,
-7.45831638172234));
#29716=CARTESIAN_POINT('Ctrl Pts',(97.5459296304045,-0.457174779250553,
-7.45717316120706));
#29717=CARTESIAN_POINT('Ctrl Pts',(97.5500036851413,-0.447378825397032,
-7.45644873094879));
#29718=CARTESIAN_POINT('Ctrl Pts',(97.5704997607619,-0.396155492114108,
-7.45265828528396));
#29719=CARTESIAN_POINT('Ctrl Pts',(97.5846911894789,-0.353880478620545,
-7.44951994158513));
#29720=CARTESIAN_POINT('Ctrl Pts',(97.6159489981286,-0.239672984383178,
-7.44101802352181));
#29721=CARTESIAN_POINT('Ctrl Pts',(97.628700611264,-0.166765739178536,-7.43555749908482));
#29722=CARTESIAN_POINT('Ctrl Pts',(97.6370103902116,-0.0620330255118681,
-7.42788722945364));
#29723=CARTESIAN_POINT('Ctrl Pts',(97.6382414144787,-0.0308248451714677,
-7.4256255119171));
#29724=CARTESIAN_POINT('Ctrl Pts',(97.6382250963924,0.0175510471689629,
-7.42218790599012));
#29725=CARTESIAN_POINT('Ctrl Pts',(97.637844546256,0.0347037554939205,-7.42098240564126));
#29726=CARTESIAN_POINT('Ctrl Pts',(97.6368518540831,0.0572334709682163,
-7.41942162953615));
#29727=CARTESIAN_POINT('Ctrl Pts',(97.6365773004606,0.0626222916618255,
-7.41905001739357));
#29728=CARTESIAN_POINT('Ctrl Pts',(97.6360738433497,0.071326371668827,-7.41845274298954));
#29729=CARTESIAN_POINT('Ctrl Pts',(97.6358679307473,0.0746428052391939,
-7.41822586351453));
#29730=CARTESIAN_POINT('Ctrl Pts',(97.6354413540386,0.0810731456158617,
-7.41778736350986));
#29731=CARTESIAN_POINT('Ctrl Pts',(97.6352223426724,0.0841870927961977,
-7.41757566117703));
#29732=CARTESIAN_POINT('Ctrl Pts',(97.6346616197167,0.0917308899732993,
-7.41706428573184));
#29733=CARTESIAN_POINT('Ctrl Pts',(97.634307212413,0.0961598074494911,-7.41676530517044));
#29734=CARTESIAN_POINT('Ctrl Pts',(97.6329645891463,0.111822881555163,-7.41571201637014));
#29735=CARTESIAN_POINT('Ctrl Pts',(97.6318400550919,0.123045157626982,-7.41496476956478));
#29736=CARTESIAN_POINT('Ctrl Pts',(97.6286412735856,0.150924547474556,-7.4131229993358));
#29737=CARTESIAN_POINT('Ctrl Pts',(97.6263717794734,0.167557135799995,-7.41203723029747));
#29738=CARTESIAN_POINT('Ctrl Pts',(97.6148547453488,0.240315055069447,-7.40732273760123));
#29739=CARTESIAN_POINT('Ctrl Pts',(97.601903446648,0.29578006646135,-7.40381818630191));
#29740=CARTESIAN_POINT('Ctrl Pts',(97.5623822618168,0.422722802698419,-7.39559371656221));
#29741=CARTESIAN_POINT('Ctrl Pts',(97.5327915116385,0.492979955074924,-7.3908732136551));
#29742=CARTESIAN_POINT('Ctrl Pts',(97.4892561064338,0.57354839906996,-7.38490577819364));
#29743=CARTESIAN_POINT('Ctrl Pts',(97.4816066152015,0.587059134952063,-7.38388558091821));
#29744=CARTESIAN_POINT('Ctrl Pts',(97.4700803449232,0.60650995837164,-7.38238606427812));
#29745=CARTESIAN_POINT('Ctrl Pts',(97.4664132370991,0.612572851128108,-7.38191420993432));
#29746=CARTESIAN_POINT('Ctrl Pts',(97.4598120728653,0.623267540035415,-7.381073749374));
#29747=CARTESIAN_POINT('Ctrl Pts',(97.4568999359014,0.62791267099355,-7.38070594478892));
#29748=CARTESIAN_POINT('Ctrl Pts',(97.4507605105384,0.637555364912286,-7.37993656028917));
#29749=CARTESIAN_POINT('Ctrl Pts',(97.4475275839824,0.642549135441851,-7.37953478112472));
#29750=CARTESIAN_POINT('Ctrl Pts',(97.4389945306226,0.655513426905098,-7.37848287006844));
#29751=CARTESIAN_POINT('Ctrl Pts',(97.4336349135633,0.663444070094435,-7.37783055100202));
#29752=CARTESIAN_POINT('Ctrl Pts',(97.4087065304904,0.699378612347029,-7.374833415328));
#29753=CARTESIAN_POINT('Ctrl Pts',(97.3880234667278,0.726585621774624,-7.37244707601841));
#29754=CARTESIAN_POINT('Ctrl Pts',(97.3238210633379,0.803823310700079,-7.36531297918666));
#29755=CARTESIAN_POINT('Ctrl Pts',(97.2772302581138,0.851120930213523,-7.36046011495299));
#29756=CARTESIAN_POINT('Ctrl Pts',(97.1807822938679,0.933784072745702,-7.35113798834233));
#29757=CARTESIAN_POINT('Ctrl Pts',(97.1316537720359,0.969698527499502,-7.3466863313735));
#29758=CARTESIAN_POINT('Ctrl Pts',(97.071458208579,1.0069269986169,-7.34172323075003));
#29759=CARTESIAN_POINT('Ctrl Pts',(97.0628807414419,1.01208186371204,-7.34102702647592));
#29760=CARTESIAN_POINT('Ctrl Pts',(97.0508383092989,1.01911174525446,-7.3400658826868));
#29761=CARTESIAN_POINT('Ctrl Pts',(97.0474283576277,1.02107947917315,-7.33979552101594));
#29762=CARTESIAN_POINT('Ctrl Pts',(97.0415270179989,1.02444555263128,-7.33933080287894));
#29763=CARTESIAN_POINT('Ctrl Pts',(97.039040317828,1.0258519784978,-7.33913594672454));
#29764=CARTESIAN_POINT('Ctrl Pts',(97.033781089707,1.02880128246279,-7.33872591184219));
#29765=CARTESIAN_POINT('Ctrl Pts',(97.0310073992268,1.03034203066807,-7.33851087413949));
#29766=CARTESIAN_POINT('Ctrl Pts',(97.024105312229,1.03413963116142,-7.33797869070289));
#29767=CARTESIAN_POINT('Ctrl Pts',(97.0199694987162,1.03638302001118,-7.33766237910681));
#29768=CARTESIAN_POINT('Ctrl Pts',(97.0042937001302,1.04476485493732,-7.33647276251103));
#29769=CARTESIAN_POINT('Ctrl Pts',(96.9926647399576,1.05073610291761,-7.33560916077351));
#29770=CARTESIAN_POINT('Ctrl Pts',(96.9625140858283,1.06558885834615,-7.33341206362287));
#29771=CARTESIAN_POINT('Ctrl Pts',(96.9438546017547,1.0741819666713,-7.33209228504785));
#29772=CARTESIAN_POINT('Ctrl Pts',(96.8718965799324,1.10506515197573,-7.32711812537154));
#29773=CARTESIAN_POINT('Ctrl Pts',(96.8172070537007,1.12391240568597,-7.32357120277021));
#29774=CARTESIAN_POINT('Ctrl Pts',(96.6884212599415,1.15794153465484,-7.31532316964458));
#29775=CARTESIAN_POINT('Ctrl Pts',(96.6138178078214,1.17015852961668,-7.31061190277869));
#29776=CARTESIAN_POINT('Ctrl Pts',(96.528197767502,1.17584753754396,-7.30498023216329));
#29777=CARTESIAN_POINT('Ctrl Pts',(96.5178229966456,1.17639911485073,-7.30429440758684));
#29778=CARTESIAN_POINT('Ctrl Pts',(96.5007223101016,1.17708153028367,-7.30315767469362));
#29779=CARTESIAN_POINT('Ctrl Pts',(96.4940000170793,1.17729213239372,-7.30270922586411));
#29780=CARTESIAN_POINT('Ctrl Pts',(96.4818490600108,1.17756865518606,-7.30189557389904));
#29781=CARTESIAN_POINT('Ctrl Pts',(96.476421005871,1.17765463814315,-7.30153100037028));
#29782=CARTESIAN_POINT('Ctrl Pts',(96.4647693167382,1.17775863617915,-7.30074596679458));
#29783=CARTESIAN_POINT('Ctrl Pts',(96.4585457684928,1.17776485246227,-7.30032515340624));
#29784=CARTESIAN_POINT('Ctrl Pts',(96.4414887046712,1.17764669374707,-7.29916755468797));
#29785=CARTESIAN_POINT('Ctrl Pts',(96.4306567219911,1.1774221598528,-7.29842770984083));
#29786=CARTESIAN_POINT('Ctrl Pts',(96.3664943826372,1.17520620965132,-7.29401605913285));
#29787=CARTESIAN_POINT('Ctrl Pts',(96.3133538030027,1.16974152643362,-7.29023820108482));
#29788=CARTESIAN_POINT('Ctrl Pts',(96.2135222039986,1.15256461326035,-7.28291658145488));
#29789=CARTESIAN_POINT('Ctrl Pts',(96.1668139085357,1.14155728981306,-7.27939540057324));
#29790=CARTESIAN_POINT('Ctrl Pts',(96.0939102860484,1.11960530312535,-7.27380934040356));
#29791=CARTESIAN_POINT('Ctrl Pts',(96.0672113503834,1.11050853330485,-7.27174427099868));
#29792=CARTESIAN_POINT('Ctrl Pts',(96.0084857835527,1.08811589690994,-7.2671874028214));
#29793=CARTESIAN_POINT('Ctrl Pts',(95.9766647592157,1.07434548673394,-7.26470809197181));
#29794=CARTESIAN_POINT('Ctrl Pts',(95.9400412828461,1.05653886952192,-7.26187761570583));
#29795=CARTESIAN_POINT('Ctrl Pts',(95.9346085123334,1.05384534592833,-7.26145836432119));
#29796=CARTESIAN_POINT('Ctrl Pts',(95.9267272622495,1.04986176209182,-7.26085132993787));
#29797=CARTESIAN_POINT('Ctrl Pts',(95.9242622558478,1.0486048975143,-7.26066163643734));
#29798=CARTESIAN_POINT('Ctrl Pts',(95.9218016730718,1.04733934308028,-7.26047246820102));
#29799=CARTESIAN_POINT('',(97.6382304121186,-0.00105003317618258,-7.32539498110769));
#29800=CARTESIAN_POINT('Ctrl Pts',(95.921801726504,1.04733937056209,-7.16216478479583));
#29801=CARTESIAN_POINT('Ctrl Pts',(95.9591974350094,1.06657314690066,-7.16518958624442));
#29802=CARTESIAN_POINT('Ctrl Pts',(95.9976046480664,1.08379451576264,-7.16826302779609));
#29803=CARTESIAN_POINT('Ctrl Pts',(96.1025184098093,1.12423731727004,-7.17651154264819));
#29804=CARTESIAN_POINT('Ctrl Pts',(96.17031902097,1.14361469209607,-7.18169729887447));
#29805=CARTESIAN_POINT('Ctrl Pts',(96.2491066072225,1.15866846873086,-7.18731936563644));
#29806=CARTESIAN_POINT('Ctrl Pts',(96.2587871500516,1.16039276109642,-7.18800317998797));
#29807=CARTESIAN_POINT('Ctrl Pts',(96.2723256823316,1.16262968461514,-7.18894878999018));
#29808=CARTESIAN_POINT('Ctrl Pts',(96.2761660133341,1.16324468341463,-7.18921582109563));
#29809=CARTESIAN_POINT('Ctrl Pts',(96.282820477877,1.16427656144637,-7.18967637140375));
#29810=CARTESIAN_POINT('Ctrl Pts',(96.2856331761037,1.16470228440079,-7.18987037012976));
#29811=CARTESIAN_POINT('Ctrl Pts',(96.2916000298121,1.16558331020396,-7.19028046845593));
#29812=CARTESIAN_POINT('Ctrl Pts',(96.2947545482123,1.16603601080375,-7.19049641712659));
#29813=CARTESIAN_POINT('Ctrl Pts',(96.3026380899499,1.16713472850511,-7.19103404198624));
#29814=CARTESIAN_POINT('Ctrl Pts',(96.307369336814,1.16776482170248,-7.19135484617066));
#29815=CARTESIAN_POINT('Ctrl Pts',(96.3255705739285,1.17007628634915,-7.19258234695495));
#29816=CARTESIAN_POINT('Ctrl Pts',(96.3390660376483,1.17155357682746,-7.19347852595174));
#29817=CARTESIAN_POINT('Ctrl Pts',(96.3741438293579,1.17478069999937,-7.1957787605492));
#29818=CARTESIAN_POINT('Ctrl Pts',(96.3957548727367,1.17616939298684,-7.19716742438219));
#29819=CARTESIAN_POINT('Ctrl Pts',(96.5196859976844,1.18070642880199,-7.20502956792278));
#29820=CARTESIAN_POINT('Ctrl Pts',(96.6220314712868,1.17110053595687,-7.21116672083788));
#29821=CARTESIAN_POINT('Ctrl Pts',(96.7534657819626,1.14118633580097,-7.21974864204908));
#29822=CARTESIAN_POINT('Ctrl Pts',(96.7847679230462,1.13268884921638,-7.22184330644841));
#29823=CARTESIAN_POINT('Ctrl Pts',(96.824970971947,1.11997191619762,-7.22462111372228));
#29824=CARTESIAN_POINT('Ctrl Pts',(96.8342271881816,1.11691710042995,-7.22526677972755));
#29825=CARTESIAN_POINT('Ctrl Pts',(96.8491056710481,1.1118011199322,-7.22631503660085));
#29826=CARTESIAN_POINT('Ctrl Pts',(96.8547521274066,1.1098113085187,-7.22671529761028));
#29827=CARTESIAN_POINT('Ctrl Pts',(96.8655286333175,1.1059210475786,-7.22748401734929));
#29828=CARTESIAN_POINT('Ctrl Pts',(96.8706611054725,1.10402772952428,-7.2278522335152));
#29829=CARTESIAN_POINT('Ctrl Pts',(96.8820576079503,1.09973323403487,-7.22867462880464));
#29830=CARTESIAN_POINT('Ctrl Pts',(96.8883146478405,1.09731417029696,-7.22912938893054));
#29831=CARTESIAN_POINT('Ctrl Pts',(96.9077542326644,1.08960699927538,-7.23055258095497));
#29832=CARTESIAN_POINT('Ctrl Pts',(96.9208615922565,1.08413395663274,-7.23152710457075));
#29833=CARTESIAN_POINT('Ctrl Pts',(96.9510925451723,1.07086378541808,-7.23381063586987));
#29834=CARTESIAN_POINT('Ctrl Pts',(96.9681342656382,1.06289088205631,-7.23512522789101));
#29835=CARTESIAN_POINT('Ctrl Pts',(97.0280365758891,1.03309655741813,-7.23984508616663));
#29836=CARTESIAN_POINT('Ctrl Pts',(97.0697395585445,1.00906439763026,-7.2433175154822));
#29837=CARTESIAN_POINT('Ctrl Pts',(97.1709907925111,0.942147163313296,-7.2521827165742));
#29838=CARTESIAN_POINT('Ctrl Pts',(97.22822477813,0.896122516800112,-7.2576160465742));
#29839=CARTESIAN_POINT('Ctrl Pts',(97.2951699905241,0.831137604939691,-7.26427421868002));
#29840=CARTESIAN_POINT('Ctrl Pts',(97.3091722573297,0.816834556961828,-7.26568529166555));
#29841=CARTESIAN_POINT('Ctrl Pts',(97.3266907615216,0.798002622476429,-7.26746729384109));
#29842=CARTESIAN_POINT('Ctrl Pts',(97.3305470454988,0.793796331445133,-7.26786063360503));
#29843=CARTESIAN_POINT('Ctrl Pts',(97.3366462279603,0.787045721925327,-7.26848424106066));
#29844=CARTESIAN_POINT('Ctrl Pts',(97.3389089112597,0.784519521946573,-7.26871592110936));
#29845=CARTESIAN_POINT('Ctrl Pts',(97.3432129821596,0.779672222969465,-7.26915720298308));
#29846=CARTESIAN_POINT('Ctrl Pts',(97.345256168005,0.777352834745229,-7.26936693010767));
#29847=CARTESIAN_POINT('Ctrl Pts',(97.350097796024,0.771812886475229,-7.26986455851786));
#29848=CARTESIAN_POINT('Ctrl Pts',(97.35288794527,0.768585077048926,-7.27015185927811));
#29849=CARTESIAN_POINT('Ctrl Pts',(97.362016261522,0.757908175426811,-7.27109381882598));
#29850=CARTESIAN_POINT('Ctrl Pts',(97.3682793829589,0.750395056415769,-7.27174336064407));
#29851=CARTESIAN_POINT('Ctrl Pts',(97.4154394840695,0.692367945131401,-7.27666721329326));
#29852=CARTESIAN_POINT('Ctrl Pts',(97.4521910511448,0.63861767252533,-7.28070108974733));
#29853=CARTESIAN_POINT('Ctrl Pts',(97.5068147296403,0.54254182391545,-7.28754150059198));
#29854=CARTESIAN_POINT('Ctrl Pts',(97.526994660201,0.501711418860703,-7.29034667458858));
#29855=CARTESIAN_POINT('Ctrl Pts',(97.563711822864,0.415129839834728,-7.29624541427028));
#29856=CARTESIAN_POINT('Ctrl Pts',(97.5798798595034,0.369318792195161,-7.29934051304164));
#29857=CARTESIAN_POINT('Ctrl Pts',(97.5961430672416,0.312224297856886,-7.30324119576074));
#29858=CARTESIAN_POINT('Ctrl Pts',(97.5989672688397,0.301763725041129,-7.30395745700501));
#29859=CARTESIAN_POINT('Ctrl Pts',(97.6032013897438,0.285174647001968,-7.30509656698941));
#29860=CARTESIAN_POINT('Ctrl Pts',(97.6047072851678,0.279071091346675,-7.30551635624563));
#29861=CARTESIAN_POINT('Ctrl Pts',(97.6074210590021,0.267680512804017,-7.30630117707449));
#29862=CARTESIAN_POINT('Ctrl Pts',(97.6086414290489,0.262396614380233,-7.30666580107502));
#29863=CARTESIAN_POINT('Ctrl Pts',(97.6109602119369,0.252030870645167,-7.30738227873806));
#29864=CARTESIAN_POINT('Ctrl Pts',(97.6120615531454,0.246949802320305,-7.30773403034554));
#29865=CARTESIAN_POINT('Ctrl Pts',(97.6144636450787,0.235502072818314,-7.30852783677025));
#29866=CARTESIAN_POINT('Ctrl Pts',(97.6157454101175,0.229131645776193,-7.30897047856181));
#29867=CARTESIAN_POINT('Ctrl Pts',(97.6188481042354,0.213022875997737,-7.31009218523653));
#29868=CARTESIAN_POINT('Ctrl Pts',(97.620598965071,0.203271715843115,-7.31077340664094));
#29869=CARTESIAN_POINT('Ctrl Pts',(97.6329375460311,0.129192640195376,-7.31596632696674));
#29870=CARTESIAN_POINT('Ctrl Pts',(97.6382886189501,0.0641194517159614,
-7.32063848889019));
#29871=CARTESIAN_POINT('Ctrl Pts',(97.6382304809295,-0.00105066599438048,
-7.32539490694684));
#29872=CARTESIAN_POINT('Ctrl Pts',(97.638230481486,-0.00105004197394352,
-7.32539486140295));
#29873=CARTESIAN_POINT('Ctrl Pts',(97.638157620742,-0.0827722104236852,
-7.33135932450499));
#29874=CARTESIAN_POINT('Ctrl Pts',(97.6295793538412,-0.164269445791813,
-7.33743351708362));
#29875=CARTESIAN_POINT('Ctrl Pts',(97.610523462441,-0.254166306561867,-7.34393779875387));
#29876=CARTESIAN_POINT('Ctrl Pts',(97.6082879512948,-0.264078388432546,
-7.34465193898493));
#29877=CARTESIAN_POINT('Ctrl Pts',(97.6046581051944,-0.279254958818313,
-7.34573949217641));
#29878=CARTESIAN_POINT('Ctrl Pts',(97.6033551261193,-0.284540532751324,
-7.34611715363922));
#29879=CARTESIAN_POINT('Ctrl Pts',(97.6008571483418,-0.294379596564185,
-7.34681787358606));
#29880=CARTESIAN_POINT('Ctrl Pts',(97.5996714113404,-0.298935302869374,
-7.34714140085036));
#29881=CARTESIAN_POINT('Ctrl Pts',(97.5976407119398,-0.306549842746858,
-7.347680469905));
#29882=CARTESIAN_POINT('Ctrl Pts',(97.5968106548838,-0.309612552776908,
-7.34789683566885));
#29883=CARTESIAN_POINT('Ctrl Pts',(97.5952099831903,-0.315425490058207,
-7.34830657298591));
#29884=CARTESIAN_POINT('Ctrl Pts',(97.5944417290941,-0.318176319770466,
-7.34850008106393));
#29885=CARTESIAN_POINT('Ctrl Pts',(97.5925913664677,-0.32470994203855,-7.34895882277975));
#29886=CARTESIAN_POINT('Ctrl Pts',(97.5915002855447,-0.3284901905073,-7.34922354965856));
#29887=CARTESIAN_POINT('Ctrl Pts',(97.5875710231533,-0.341852147389928,
-7.35015704847638));
#29888=CARTESIAN_POINT('Ctrl Pts',(97.5846297642654,-0.351403448008432,
-7.35082026511642));
#29889=CARTESIAN_POINT('Ctrl Pts',(97.5620452483513,-0.421555926547498,
-7.35566937701087));
#29890=CARTESIAN_POINT('Ctrl Pts',(97.5376327908623,-0.480519891455983,
-7.35962630864354));
#29891=CARTESIAN_POINT('Ctrl Pts',(97.4836892790883,-0.585759495725363,
-7.36694691844554));
#29892=CARTESIAN_POINT('Ctrl Pts',(97.4554713634781,-0.632505505260704,
-7.37030526359025));
#29893=CARTESIAN_POINT('Ctrl Pts',(97.4001217422688,-0.711275037832558,
-7.3763807779452));
#29894=CARTESIAN_POINT('Ctrl Pts',(97.3743302486744,-0.74412087238454,-7.37905823658713));
#29895=CARTESIAN_POINT('Ctrl Pts',(97.3404058631544,-0.782894019470938,
-7.38244875230918));
#29896=CARTESIAN_POINT('Ctrl Pts',(97.3338681322983,-0.790180814025435,
-7.38309658342121));
#29897=CARTESIAN_POINT('Ctrl Pts',(97.3237278757249,-0.801203297629566,
-7.38409348163802));
#29898=CARTESIAN_POINT('Ctrl Pts',(97.3201901267464,-0.804998204268755,
-7.38443984738119));
#29899=CARTESIAN_POINT('Ctrl Pts',(97.313265587889,-0.812328376056222,-7.38511511266905));
#29900=CARTESIAN_POINT('Ctrl Pts',(97.30988159626,-0.81586614715012,-7.38544388964002));
#29901=CARTESIAN_POINT('Ctrl Pts',(97.3022092642363,-0.823787662643767,
-7.38618664145084));
#29902=CARTESIAN_POINT('Ctrl Pts',(97.2979085713053,-0.82815919045536,-7.38660114328146));
#29903=CARTESIAN_POINT('Ctrl Pts',(97.2862120990038,-0.839864039181051,
-7.38772365624678));
#29904=CARTESIAN_POINT('Ctrl Pts',(97.2787530072162,-0.847133025592625,
-7.38843442434006));
#29905=CARTESIAN_POINT('Ctrl Pts',(97.2423415226478,-0.881686894131928,
-7.39188079997064));
#29906=CARTESIAN_POINT('Ctrl Pts',(97.212118608622,-0.907589075905287,-7.39467325356153));
#29907=CARTESIAN_POINT('Ctrl Pts',(97.1057980421773,-0.989751887259648,
-7.40427882677055));
#29908=CARTESIAN_POINT('Ctrl Pts',(97.024255105031,-1.0383633716278,-7.41132757327188));
#29909=CARTESIAN_POINT('Ctrl Pts',(96.9185086385123,-1.08524223256013,-7.41968734711519));
#29910=CARTESIAN_POINT('Ctrl Pts',(96.8989961616024,-1.09327241939852,-7.42119812811534));
#29911=CARTESIAN_POINT('Ctrl Pts',(96.8669058572911,-1.10548137299237,-7.42362080027618));
#29912=CARTESIAN_POINT('Ctrl Pts',(96.8544551886515,-1.10997955266591,-7.42454592111846));
#29913=CARTESIAN_POINT('Ctrl Pts',(96.8374090132999,-1.11581501108063,-7.42578999034491));
#29914=CARTESIAN_POINT('Ctrl Pts',(96.8328778510732,-1.11733542587152,-7.42611854108084));
#29915=CARTESIAN_POINT('Ctrl Pts',(96.8253088424273,-1.1198240197441,-7.426663652408));
#29916=CARTESIAN_POINT('Ctrl Pts',(96.822276139186,-1.12080750715113,-7.42688107565991));
#29917=CARTESIAN_POINT('Ctrl Pts',(96.8165309419425,-1.12264489115577,-7.42729104866585));
#29918=CARTESIAN_POINT('Ctrl Pts',(96.8138192926112,-1.1235012970534,-7.42748374621271));
#29919=CARTESIAN_POINT('Ctrl Pts',(96.8073957968243,-1.12550443961412,-7.42793837752827));
#29920=CARTESIAN_POINT('Ctrl Pts',(96.803681297167,-1.12664265732642,-7.4281998259278));
#29921=CARTESIAN_POINT('Ctrl Pts',(96.7905723515356,-1.13058872553943,-7.42911763244383));
#29922=CARTESIAN_POINT('Ctrl Pts',(96.7811482311819,-1.13329771456478,-7.42976864605399));
#29923=CARTESIAN_POINT('Ctrl Pts',(96.7031736702421,-1.15466113281394,-7.43509117624486));
#29924=CARTESIAN_POINT('Ctrl Pts',(96.6330883105678,-1.16719818577864,-7.43947526903408));
#29925=CARTESIAN_POINT('Ctrl Pts',(96.5035800790976,-1.17843564929446,-7.44751619979219));
#29926=CARTESIAN_POINT('Ctrl Pts',(96.44457251753,-1.17911593092873,-7.45115801567501));
#29927=CARTESIAN_POINT('Ctrl Pts',(96.3645746375355,-1.17403060157308,-7.45626716080015));
#29928=CARTESIAN_POINT('Ctrl Pts',(96.3434264095497,-1.1721109282954,-7.45763366360753));
#29929=CARTESIAN_POINT('Ctrl Pts',(96.3067312214503,-1.16777703170361,-7.46004064338165));
#29930=CARTESIAN_POINT('Ctrl Pts',(96.2911590356336,-1.16562096166176,-7.46107340279646));
#29931=CARTESIAN_POINT('Ctrl Pts',(96.268526703433,-1.16202428432297,-7.46259309967684));
#29932=CARTESIAN_POINT('Ctrl Pts',(96.2614288063174,-1.16082949238368,-7.46307239636197));
#29933=CARTESIAN_POINT('Ctrl Pts',(96.2489462960017,-1.15861045713583,-7.46392025091268));
#29934=CARTESIAN_POINT('Ctrl Pts',(96.2435569969662,-1.15761353572798,-7.46428794331594));
#29935=CARTESIAN_POINT('Ctrl Pts',(96.2323294911441,-1.15545549720831,-7.46505745802665));
#29936=CARTESIAN_POINT('Ctrl Pts',(96.2264927493763,-1.15428766515915,-7.46545948198795));
#29937=CARTESIAN_POINT('Ctrl Pts',(96.2112766513671,-1.15112303333598,-7.46651285182607));
#29938=CARTESIAN_POINT('Ctrl Pts',(96.2019125478508,-1.14905586997392,-7.4671663964536));
#29939=CARTESIAN_POINT('Ctrl Pts',(96.1624157983958,-1.13982956473642,-7.46994609190785));
#29940=CARTESIAN_POINT('Ctrl Pts',(96.1325489171274,-1.1315982267196,-7.47210568749937));
#29941=CARTESIAN_POINT('Ctrl Pts',(96.0239005324763,-1.09699208501677,-7.4801811728874));
#29942=CARTESIAN_POINT('Ctrl Pts',(95.947654416635,-1.06348469239176,-7.48630334749115));
#29943=CARTESIAN_POINT('Ctrl Pts',(95.8303154980595,-0.996346338643619,
-7.49619936972193));
#29944=CARTESIAN_POINT('Ctrl Pts',(95.7868168949102,-0.967467086651361,
-7.49998273243608));
#29945=CARTESIAN_POINT('Ctrl Pts',(95.739843511886,-0.93157133641251,-7.5040945736259));
#29946=CARTESIAN_POINT('Ctrl Pts',(95.7343525980531,-0.92729773772543,-7.50457561350047));
#29947=CARTESIAN_POINT('Ctrl Pts',(95.726030341534,-0.920701239751516,-7.50530489311694));
#29948=CARTESIAN_POINT('Ctrl Pts',(95.7231715390142,-0.918413470364259,
-7.50555544572017));
#29949=CARTESIAN_POINT('Ctrl Pts',(95.7179571203013,-0.914200568654421,
-7.5060124443317));
#29950=CARTESIAN_POINT('Ctrl Pts',(95.71559828447,-0.91227963500244,-7.50621916624076));
#29951=CARTESIAN_POINT('Ctrl Pts',(95.7102894388488,-0.907922022309581,
-7.50668441614867));
#29952=CARTESIAN_POINT('Ctrl Pts',(95.7073438423781,-0.905480093738512,
-7.5069425658723));
#29953=CARTESIAN_POINT('Ctrl Pts',(95.6997606455557,-0.899130943647556,
-7.5076073271905));
#29954=CARTESIAN_POINT('Ctrl Pts',(95.6951411585998,-0.89520212407097,-7.5080124543006));
#29955=CARTESIAN_POINT('Ctrl Pts',(95.6643153242603,-0.868572080151798,
-7.51071865403968));
#29956=CARTESIAN_POINT('Ctrl Pts',(95.6390893606961,-0.84475648876388,-7.51294706388831));
#29957=CARTESIAN_POINT('Ctrl Pts',(95.5952711707043,-0.799566222936112,
-7.51692435876652));
#29958=CARTESIAN_POINT('Ctrl Pts',(95.5763297994118,-0.778569824341681,
-7.51868439317666));
#29959=CARTESIAN_POINT('Ctrl Pts',(95.5272295965055,-0.720037140619252,
-7.52342119575347));
#29960=CARTESIAN_POINT('Ctrl Pts',(95.4985875214946,-0.681302068870754,
-7.52638096158948));
#29961=CARTESIAN_POINT('Ctrl Pts',(95.4434939262649,-0.596366595909807,
-7.53271290005684));
#29962=CARTESIAN_POINT('Ctrl Pts',(95.4176422416363,-0.549910972917084,
-7.53608964263101));
#29963=CARTESIAN_POINT('Ctrl Pts',(95.3904034647755,-0.492083678644121,
-7.54029090448739));
#29964=CARTESIAN_POINT('Ctrl Pts',(95.3859273309835,-0.482230938757396,
-7.54100649707373));
#29965=CARTESIAN_POINT('Ctrl Pts',(95.3790930756971,-0.466619784912922,
-7.5421406529871));
#29966=CARTESIAN_POINT('Ctrl Pts',(95.3766436574041,-0.460901810625772,
-7.54255613447892));
#29967=CARTESIAN_POINT('Ctrl Pts',(95.3721417316361,-0.450158058904509,
-7.54333706074196));
#29968=CARTESIAN_POINT('Ctrl Pts',(95.3700784450415,-0.445136953889366,
-7.54370213276935));
#29969=CARTESIAN_POINT('Ctrl Pts',(95.365535696516,-0.433860838211755,-7.54452231733685));
#29970=CARTESIAN_POINT('Ctrl Pts',(95.3630749933896,-0.427598524565747,
-7.54497803939264));
#29971=CARTESIAN_POINT('Ctrl Pts',(95.3569478850125,-0.411604166266832,
-7.54614271775527));
#29972=CARTESIAN_POINT('Ctrl Pts',(95.3533565415494,-0.401844182991244,
-7.54685411167661));
#29973=CARTESIAN_POINT('Ctrl Pts',(95.3249289675635,-0.321313089346457,
-7.55273104885834));
#29974=CARTESIAN_POINT('Ctrl Pts',(95.3067804238525,-0.248378113446867,
-7.55811532245824));
#29975=CARTESIAN_POINT('Ctrl Pts',(95.2872919586694,-0.118087669317124,
-7.56775092128684));
#29976=CARTESIAN_POINT('Ctrl Pts',(95.2829642828051,-0.0614150673103769,
-7.57194274071615));
#29977=CARTESIAN_POINT('Ctrl Pts',(95.2826555066454,0.0167799672035462,
-7.57759659982393));
#29978=CARTESIAN_POINT('Ctrl Pts',(95.2831558334285,0.0382102534638454,
-7.57913210938997));
#29979=CARTESIAN_POINT('Ctrl Pts',(95.2849228949759,0.0730747710711165,
-7.58159604245247));
#29980=CARTESIAN_POINT('Ctrl Pts',(95.2858360048942,0.0865214109962014,
-7.58253802065525));
#29981=CARTESIAN_POINT('Ctrl Pts',(95.2873836960152,0.10469265036322,-7.58379715924895));
#29982=CARTESIAN_POINT('Ctrl Pts',(95.2878163849017,0.109432801584641,-7.58412434257435));
#29983=CARTESIAN_POINT('Ctrl Pts',(95.2885864635311,0.117339311282526,-7.58466780720895));
#29984=CARTESIAN_POINT('Ctrl Pts',(95.2889079742152,0.120507114021598,-7.58488494061709));
#29985=CARTESIAN_POINT('Ctrl Pts',(95.2895412808636,0.126504780577694,-7.58529483964327));
#29986=CARTESIAN_POINT('Ctrl Pts',(95.2898504964252,0.129334874909668,-7.58548775002663));
#29987=CARTESIAN_POINT('Ctrl Pts',(95.2906074015932,0.136037270219565,-7.58594346932322));
#29988=CARTESIAN_POINT('Ctrl Pts',(95.2910640630389,0.139908554822893,-7.58620578721081));
#29989=CARTESIAN_POINT('Ctrl Pts',(95.2927368306378,0.15350849710487,-7.58712436331314));
#29990=CARTESIAN_POINT('Ctrl Pts',(95.2940552266629,0.163224490437702,-7.58777528712605));
#29991=CARTESIAN_POINT('Ctrl Pts',(95.3058338955376,0.242577520562612,-7.59305630224015));
#29992=CARTESIAN_POINT('Ctrl Pts',(95.3224005554039,0.311174301414529,-7.59740421450017));
#29993=CARTESIAN_POINT('Ctrl Pts',(95.3640468312999,0.434109420209981,-7.60543313266074));
#29994=CARTESIAN_POINT('Ctrl Pts',(95.3873149324483,0.488807534187662,-7.60910009493874));
#29995=CARTESIAN_POINT('Ctrl Pts',(95.4244084299881,0.560449221728249,-7.61424133277476));
#29996=CARTESIAN_POINT('Ctrl Pts',(95.4347228311029,0.579111212913541,-7.61561328863156));
#29997=CARTESIAN_POINT('Ctrl Pts',(95.4535375380097,0.611071766647473,-7.61802900246984));
#29998=CARTESIAN_POINT('Ctrl Pts',(95.4618093112538,0.62449872592867,-7.61906496358505));
#29999=CARTESIAN_POINT('Ctrl Pts',(95.4742503221216,0.643813753243735,-7.62058850518528));
#30000=CARTESIAN_POINT('Ctrl Pts',(95.4782082387301,0.6498363771467,-7.621068388979));
#30001=CARTESIAN_POINT('Ctrl Pts',(95.485273734165,0.660375652247995,-7.62191691462782));
#30002=CARTESIAN_POINT('Ctrl Pts',(95.4883580718981,0.664907680836141,-7.62228468649131));
#30003=CARTESIAN_POINT('Ctrl Pts',(95.4948548926377,0.674312067393965,-7.6230540034452));
#30004=CARTESIAN_POINT('Ctrl Pts',(95.4982728665639,0.679180424349913,-7.62345574775843));
#30005=CARTESIAN_POINT('Ctrl Pts',(95.5072862127381,0.691813890705781,-7.62450756864363));
#30006=CARTESIAN_POINT('Ctrl Pts',(95.5129395254003,0.699536922402434,-7.62515983203001));
#30007=CARTESIAN_POINT('Ctrl Pts',(95.5371777233368,0.731815952960126,-7.62792612289781));
#30008=CARTESIAN_POINT('Ctrl Pts',(95.5566263823996,0.755705006370475,-7.63007319188216));
#30009=CARTESIAN_POINT('Ctrl Pts',(95.6320125178234,0.841224955868691,-7.63814539601335));
#30010=CARTESIAN_POINT('Ctrl Pts',(95.6934930493862,0.897633303007338,-7.64427850865171));
#30011=CARTESIAN_POINT('Ctrl Pts',(95.8023740553451,0.978118584368847,-7.65419014178745));
#30012=CARTESIAN_POINT('Ctrl Pts',(95.8463786458702,1.00633012099548,-7.6579779348895));
#30013=CARTESIAN_POINT('Ctrl Pts',(95.8982099163185,1.0348887725285,-7.66209394762261));
#30014=CARTESIAN_POINT('Ctrl Pts',(95.9043345337815,1.03819297647297,-7.66257506274894));
#30015=CARTESIAN_POINT('Ctrl Pts',(95.9137261276896,1.04315273805798,-7.66330443239969));
#30016=CARTESIAN_POINT('Ctrl Pts',(95.9169720073122,1.04484759691054,-7.66355500063715));
#30017=CARTESIAN_POINT('Ctrl Pts',(95.9207508843772,1.04679838957602,-7.66384491542143));
#30018=CARTESIAN_POINT('Ctrl Pts',(95.9212761773124,1.04706906422808,-7.66388517556795));
#30019=CARTESIAN_POINT('Ctrl Pts',(95.9218016730721,1.04733934308044,-7.66392541087522));
#30020=CARTESIAN_POINT('Origin',(96.460480949577,-7.19464945638997E-16,
0.924367114736168));
#30021=CARTESIAN_POINT('',(95.9218015205746,1.0473392646462,-8.26212858994183));
#30022=CARTESIAN_POINT('',(95.9218018246468,1.04733942104002,-8.16230712347375));
#30023=CARTESIAN_POINT('',(95.9218016730721,1.04733934308042,0.924367114736168));
#30024=CARTESIAN_POINT('',(97.6382307576569,0.000672359933839044,-7.92526064390542));
#30025=CARTESIAN_POINT('Ctrl Pts',(95.9218015205746,1.04733926464621,-8.26212858994183));
#30026=CARTESIAN_POINT('Ctrl Pts',(95.882681846614,1.02721878951153,-8.25936245837624));
#30027=CARTESIAN_POINT('Ctrl Pts',(95.8447008289881,1.00491246711868,-8.25655020994838));
#30028=CARTESIAN_POINT('Ctrl Pts',(95.7993899953988,0.974762406621344,-8.25297826354386));
#30029=CARTESIAN_POINT('Ctrl Pts',(95.7908173484039,0.968893001898539,-8.25229243871632));
#30030=CARTESIAN_POINT('Ctrl Pts',(95.7768249461735,0.959038458591712,-8.25115570549246));
#30031=CARTESIAN_POINT('Ctrl Pts',(95.7713595746905,0.955118853113391,-8.25070725658608));
#30032=CARTESIAN_POINT('Ctrl Pts',(95.7615439012237,0.94795123095032,-8.24989360453923));
#30033=CARTESIAN_POINT('Ctrl Pts',(95.7571818866182,0.94471951402355,-8.24952903100594));
#30034=CARTESIAN_POINT('Ctrl Pts',(95.7478675076307,0.937718442569192,-8.2487439974839));
#30035=CARTESIAN_POINT('Ctrl Pts',(95.7429223851959,0.933939772840843,-8.24832318415447));
#30036=CARTESIAN_POINT('Ctrl Pts',(95.729451335272,0.923476119660658,-8.24716558576631));
#30037=CARTESIAN_POINT('Ctrl Pts',(95.7209875163982,0.916712544510815,-8.24642574119306));
#30038=CARTESIAN_POINT('Ctrl Pts',(95.6713914557111,0.875945701237547,-8.24201409666496));
#30039=CARTESIAN_POINT('Ctrl Pts',(95.6325214570363,0.839300128391896,-8.23823624487958));
#30040=CARTESIAN_POINT('Ctrl Pts',(95.5637003315537,0.76496950178014,-8.23091462754437));
#30041=CARTESIAN_POINT('Ctrl Pts',(95.5333069540389,0.727833610568228,-8.2273934423024));
#30042=CARTESIAN_POINT('Ctrl Pts',(95.4887689216743,0.666082444684675,-8.22180737492187));
#30043=CARTESIAN_POINT('Ctrl Pts',(95.473100983738,0.64262818596326,-8.21974230271395));
#30044=CARTESIAN_POINT('Ctrl Pts',(95.4400879169729,0.589146750712411,-8.21518543217378));
#30045=CARTESIAN_POINT('Ctrl Pts',(95.423194530971,0.55886779862607,-8.21270612170247));
#30046=CARTESIAN_POINT('Ctrl Pts',(95.4049419280051,0.522464547557197,-8.20987564580925));
#30047=CARTESIAN_POINT('Ctrl Pts',(95.4022659697706,0.51702310383408,-8.20945639443925));
#30048=CARTESIAN_POINT('Ctrl Pts',(95.3979701946385,0.508114748190687,-8.208776548753));
#30049=CARTESIAN_POINT('Ctrl Pts',(95.3963250765105,0.504660262500222,-8.20851450443043));
#30050=CARTESIAN_POINT('Ctrl Pts',(95.3934021177061,0.498444665722067,-8.20804593414983));
#30051=CARTESIAN_POINT('Ctrl Pts',(95.3921181180113,0.495686573332658,-8.2078390443837));
#30052=CARTESIAN_POINT('Ctrl Pts',(95.3893121035893,0.48959756571323,-8.20738456835387));
#30053=CARTESIAN_POINT('Ctrl Pts',(95.3877949290369,0.486264511574047,-8.2071372737954));
#30054=CARTESIAN_POINT('Ctrl Pts',(95.3834395744818,0.476576725492688,-8.20642262318772));
#30055=CARTESIAN_POINT('Ctrl Pts',(95.38064208494,0.470203712391128,-8.20595762994692));
#30056=CARTESIAN_POINT('Ctrl Pts',(95.3573317243991,0.415794497655136,-8.20202815120875));
#30057=CARTESIAN_POINT('Ctrl Pts',(95.3399760945923,0.366460931705132,-8.1987303848441));
#30058=CARTESIAN_POINT('Ctrl Pts',(95.3036000738901,0.23591528754517,-8.19028896714968));
#30059=CARTESIAN_POINT('Ctrl Pts',(95.2898192555901,0.153558411476834,-8.18522162110159));
#30060=CARTESIAN_POINT('Ctrl Pts',(95.2830021057068,0.0397759502831907,
-8.17795051953922));
#30061=CARTESIAN_POINT('Ctrl Pts',(95.2823653890387,0.00905682395242783,
-8.17596322049056));
#30062=CARTESIAN_POINT('Ctrl Pts',(95.2831057553097,-0.0312116579043044,
-8.17330889172885));
#30063=CARTESIAN_POINT('Ctrl Pts',(95.2833979960099,-0.0407704209231531,
-8.17267521516017));
#30064=CARTESIAN_POINT('Ctrl Pts',(95.284060713067,-0.0562659482092893,
-8.17164165295492));
#30065=CARTESIAN_POINT('Ctrl Pts',(95.2843598209786,-0.0622054536819052,
-8.17124397679849));
#30066=CARTESIAN_POINT('Ctrl Pts',(95.2850211371898,-0.0736162789259981,
-8.17047695843129));
#30067=CARTESIAN_POINT('Ctrl Pts',(95.2853765976744,-0.0790878464458857,
-8.17010783472231));
#30068=CARTESIAN_POINT('Ctrl Pts',(95.2862880061383,-0.0917496681503411,
-8.16925045795215));
#30069=CARTESIAN_POINT('Ctrl Pts',(95.286871810717,-0.0989376329198813,
-8.16876135523244));
#30070=CARTESIAN_POINT('Ctrl Pts',(95.2889447249378,-0.121849923252953,
-8.16719444909374));
#30071=CARTESIAN_POINT('Ctrl Pts',(95.2906840942086,-0.137549280856266,
-8.16610897898886));
#30072=CARTESIAN_POINT('Ctrl Pts',(95.2955176631305,-0.174390393026171,
-8.16353261927663));
#30073=CARTESIAN_POINT('Ctrl Pts',(95.2988724329037,-0.195491748269196,
-8.16203420334519));
#30074=CARTESIAN_POINT('Ctrl Pts',(95.3137501292293,-0.275050671341572,
-8.1562977324833));
#30075=CARTESIAN_POINT('Ctrl Pts',(95.329127828755,-0.332690736736164,-8.1519564923183));
#30076=CARTESIAN_POINT('Ctrl Pts',(95.3719464291284,-0.455084718884924,
-8.14244378150568));
#30077=CARTESIAN_POINT('Ctrl Pts',(95.4009595206696,-0.519062251917712,
-8.13727833250891));
#30078=CARTESIAN_POINT('Ctrl Pts',(95.4403418686973,-0.588649468377628,
-8.13167392612265));
#30079=CARTESIAN_POINT('Ctrl Pts',(95.4452971304245,-0.597154728753573,
-8.13098935956052));
#30080=CARTESIAN_POINT('Ctrl Pts',(95.4523602057575,-0.608935777177968,
-8.13004276880873));
#30081=CARTESIAN_POINT('Ctrl Pts',(95.4543783503521,-0.612264465534613,
-8.12977549829468));
#30082=CARTESIAN_POINT('Ctrl Pts',(95.4579003810507,-0.618009194217589,
-8.12931463862833));
#30083=CARTESIAN_POINT('Ctrl Pts',(95.4593965733118,-0.620429877231171,
-8.12912056856425));
#30084=CARTESIAN_POINT('Ctrl Pts',(95.4625864982447,-0.625549260893683,
-8.12871044291798));
#30085=CARTESIAN_POINT('Ctrl Pts',(95.4642824385231,-0.628246560585122,
-8.12849453764082));
#30086=CARTESIAN_POINT('Ctrl Pts',(95.468544014674,-0.634963716069903,-8.12795723052745));
#30087=CARTESIAN_POINT('Ctrl Pts',(95.4711231919266,-0.638974986108999,
-8.12763669830973));
#30088=CARTESIAN_POINT('Ctrl Pts',(95.4811195011341,-0.65431612449475,-8.12641164147063));
#30089=CARTESIAN_POINT('Ctrl Pts',(95.4887078012383,-0.665533939221011,
-8.12551758034506));
#30090=CARTESIAN_POINT('Ctrl Pts',(95.5088840504445,-0.694279448018501,
-8.12322413265107));
#30091=CARTESIAN_POINT('Ctrl Pts',(95.5217635598996,-0.711597067387305,
-8.12184002369523));
#30092=CARTESIAN_POINT('Ctrl Pts',(95.5977405522421,-0.808099058412,-8.11405249659541));
#30093=CARTESIAN_POINT('Ctrl Pts',(95.6703644292126,-0.879240053469003,
-8.10797950064297));
#30094=CARTESIAN_POINT('Ctrl Pts',(95.7778849940188,-0.960351742938887,
-8.09941432605921));
#30095=CARTESIAN_POINT('Ctrl Pts',(95.805416671247,-0.979338133418017,-8.09725649336949));
#30096=CARTESIAN_POINT('Ctrl Pts',(95.8420661468472,-1.00237490534565,-8.09440550694393));
#30097=CARTESIAN_POINT('Ctrl Pts',(95.8504809491419,-1.00751789506175,-8.09375236865836));
#30098=CARTESIAN_POINT('Ctrl Pts',(95.8641280266139,-1.01562512771406,-8.09269491282443));
#30099=CARTESIAN_POINT('Ctrl Pts',(95.8693202675426,-1.01865610218649,-8.09229300117623));
#30100=CARTESIAN_POINT('Ctrl Pts',(95.8792755942964,-1.02436578324012,-8.09152306385312));
#30101=CARTESIAN_POINT('Ctrl Pts',(95.8840345747372,-1.02705136097872,-8.09115529533236));
#30102=CARTESIAN_POINT('Ctrl Pts',(95.8949970879321,-1.03313750833258,-8.09030868778497));
#30103=CARTESIAN_POINT('Ctrl Pts',(95.901212865204,-1.03651546777072,-8.08982906778885));
#30104=CARTESIAN_POINT('Ctrl Pts',(95.9207428057527,-1.04690218442485,-8.0883231439486));
#30105=CARTESIAN_POINT('Ctrl Pts',(95.9341606346707,-1.05371169561501,-8.08728999088254));
#30106=CARTESIAN_POINT('Ctrl Pts',(95.9657610881423,-1.0689946740104,-8.08485911367879));
#30107=CARTESIAN_POINT('Ctrl Pts',(95.9840366153707,-1.07726415922205,-8.08345496690317));
#30108=CARTESIAN_POINT('Ctrl Pts',(96.0517501768846,-1.10584371683332,-8.07825789507965));
#30109=CARTESIAN_POINT('Ctrl Pts',(96.1023390567273,-1.12324727066319,-8.07438197218799));
#30110=CARTESIAN_POINT('Ctrl Pts',(96.2305726227726,-1.15781617635916,-8.06465534113248));
#30111=CARTESIAN_POINT('Ctrl Pts',(96.3091135989226,-1.17067757658251,-8.0587759345803));
#30112=CARTESIAN_POINT('Ctrl Pts',(96.3978885825564,-1.17612434281129,-8.05254872506534));
#30113=CARTESIAN_POINT('Ctrl Pts',(96.4074282834039,-1.17659326163005,-8.05188512750123));
#30114=CARTESIAN_POINT('Ctrl Pts',(96.4207168330286,-1.17708449694094,-8.05096945332527));
#30115=CARTESIAN_POINT('Ctrl Pts',(96.4244613648939,-1.17720503243364,-8.05071238994967));
#30116=CARTESIAN_POINT('Ctrl Pts',(96.4312957886264,-1.17739238995755,-8.05024503438272));
#30117=CARTESIAN_POINT('Ctrl Pts',(96.4343854888847,-1.17746492149759,-8.05003443577605));
#30118=CARTESIAN_POINT('Ctrl Pts',(96.4407889780288,-1.17759002711593,-8.04959942331176));
#30119=CARTESIAN_POINT('Ctrl Pts',(96.4441027480469,-1.17764077753261,-8.04937510982734));
#30120=CARTESIAN_POINT('Ctrl Pts',(96.4527728713507,-1.17773695692433,-8.04879021528799));
#30121=CARTESIAN_POINT('Ctrl Pts',(96.4581294728761,-1.17775983436876,-8.0484308483514));
#30122=CARTESIAN_POINT('Ctrl Pts',(96.4821480357246,-1.17769854689708,-8.04682767123812));
#30123=CARTESIAN_POINT('Ctrl Pts',(96.5008074190952,-1.17720737372872,-8.04560437921946));
#30124=CARTESIAN_POINT('Ctrl Pts',(96.5539292613146,-1.17454433195946,-8.0421650100875));
#30125=CARTESIAN_POINT('Ctrl Pts',(96.5883200204505,-1.17130034575865,-8.03999010945456));
#30126=CARTESIAN_POINT('Ctrl Pts',(96.7001935469232,-1.15576052322287,-8.03294652260264));
#30127=CARTESIAN_POINT('Ctrl Pts',(96.7765919773321,-1.1372414935333,-8.02817300690954));
#30128=CARTESIAN_POINT('Ctrl Pts',(96.8848907960461,-1.0992240030229,-8.02089624246755));
#30129=CARTESIAN_POINT('Ctrl Pts',(96.9186193751852,-1.08559933091248,-8.018555153531));
#30130=CARTESIAN_POINT('Ctrl Pts',(96.9608821034556,-1.06620667203889,-8.01549456926928));
#30131=CARTESIAN_POINT('Ctrl Pts',(96.9700473755437,-1.06185687796953,-8.01482300070829));
#30132=CARTESIAN_POINT('Ctrl Pts',(96.9846082800733,-1.05471441465971,-8.01374290367239));
#30133=CARTESIAN_POINT('Ctrl Pts',(96.9900406150765,-1.05199739229978,-8.01333697325192));
#30134=CARTESIAN_POINT('Ctrl Pts',(97.0002107789363,-1.04681197529418,-8.01257128177804));
#30135=CARTESIAN_POINT('Ctrl Pts',(97.004953318899,-1.04435311928142,-8.01221185882702));
#30136=CARTESIAN_POINT('Ctrl Pts',(97.0137129758967,-1.03973563142965,-8.0115435174496));
#30137=CARTESIAN_POINT('Ctrl Pts',(97.0177346168637,-1.03758575910388,-8.0112349108547));
#30138=CARTESIAN_POINT('Ctrl Pts',(97.0274203983783,-1.03233541970745,-8.01048733093199));
#30139=CARTESIAN_POINT('Ctrl Pts',(97.033071671341,-1.02921164969092,-8.01004754452365));
#30140=CARTESIAN_POINT('Ctrl Pts',(97.0472406054713,-1.02122688259445,-8.00893566694788));
#30141=CARTESIAN_POINT('Ctrl Pts',(97.0557236336438,-1.01630574953466,-8.00826147434284));
#30142=CARTESIAN_POINT('Ctrl Pts',(97.0798381379711,-1.0019110772545,-8.00632008186966));
#30143=CARTESIAN_POINT('Ctrl Pts',(97.0953112850696,-0.99217917532878,-8.00504393221268));
#30144=CARTESIAN_POINT('Ctrl Pts',(97.1488365689114,-0.956749502199679,
-8.00052014805598));
#30145=CARTESIAN_POINT('Ctrl Pts',(97.1856036031758,-0.929192889135423,
-7.99721133302771));
#30146=CARTESIAN_POINT('Ctrl Pts',(97.2724299281134,-0.855819507330814,
-7.98891915041526));
#30147=CARTESIAN_POINT('Ctrl Pts',(97.3203218699485,-0.80768925115512,-7.98389915104469));
#30148=CARTESIAN_POINT('Ctrl Pts',(97.3815158761386,-0.734541518744345,
-7.97702980782797));
#30149=CARTESIAN_POINT('Ctrl Pts',(97.3984749759291,-0.712758066103191,
-7.97506838108668));
#30150=CARTESIAN_POINT('Ctrl Pts',(97.4183180867831,-0.685333598737634,
-7.97271843286279));
#30151=CARTESIAN_POINT('Ctrl Pts',(97.4219414803578,-0.680240968336361,
-7.97228692665625));
#30152=CARTESIAN_POINT('Ctrl Pts',(97.4275579999866,-0.672212487577854,
-7.9716145560675));
#30153=CARTESIAN_POINT('Ctrl Pts',(97.4295786270648,-0.669296154336314,
-7.97137193213941));
#30154=CARTESIAN_POINT('Ctrl Pts',(97.4332970930069,-0.663877216469327,
-7.97092415019197));
#30155=CARTESIAN_POINT('Ctrl Pts',(97.4349984661246,-0.661377212879593,
-7.97071876641029));
#30156=CARTESIAN_POINT('Ctrl Pts',(97.4389061118847,-0.655587486987043,
-7.97024584804853));
#30157=CARTESIAN_POINT('Ctrl Pts',(97.4411054357761,-0.652293162265798,
-7.96997877282884));
#30158=CARTESIAN_POINT('Ctrl Pts',(97.4479511871981,-0.641926165725371,
-7.96914438775376));
#30159=CARTESIAN_POINT('Ctrl Pts',(97.4525381589471,-0.634814284570565,
-7.96858080896662));
#30160=CARTESIAN_POINT('Ctrl Pts',(97.4631690587488,-0.617934891994223,
-7.96726230295342));
#30161=CARTESIAN_POINT('Ctrl Pts',(97.4691476438505,-0.608127039652732,
-7.96651099676791));
#30162=CARTESIAN_POINT('Ctrl Pts',(97.4903188745895,-0.572224239362974,
-7.96380812365564));
#30163=CARTESIAN_POINT('Ctrl Pts',(97.5046509938826,-0.545633493795853,
-7.96189557052363));
#30164=CARTESIAN_POINT('Ctrl Pts',(97.5558766097704,-0.441164320400889,
-7.95460803341234));
#30165=CARTESIAN_POINT('Ctrl Pts',(97.5852041854912,-0.359882674271186,
-7.94938736772712));
#30166=CARTESIAN_POINT('Ctrl Pts',(97.6134975550974,-0.242568601285419,
-7.94172654504229));
#30167=CARTESIAN_POINT('Ctrl Pts',(97.6201112343303,-0.208672169309545,
-7.93950201758299));
#30168=CARTESIAN_POINT('Ctrl Pts',(97.62675719429,-0.164321264077293,-7.93655143866693));
#30169=CARTESIAN_POINT('Ctrl Pts',(97.6281534480907,-0.154086605225606,
-7.93586787151051));
#30170=CARTESIAN_POINT('Ctrl Pts',(97.6301615643288,-0.137766846607678,
-7.93477303215731));
#30171=CARTESIAN_POINT('Ctrl Pts',(97.6308609824075,-0.131692903840552,
-7.93436448635546));
#30172=CARTESIAN_POINT('Ctrl Pts',(97.6320815070449,-0.120314595326233,
-7.93359704290566));
#30173=CARTESIAN_POINT('Ctrl Pts',(97.6326139634476,-0.115011583338101,
-7.93323850777708));
#30174=CARTESIAN_POINT('Ctrl Pts',(97.6335993547528,-0.104478821721182,
-7.93252461309413));
#30175=CARTESIAN_POINT('Ctrl Pts',(97.6340533559106,-0.0992492937059147,
-7.93216929534758));
#30176=CARTESIAN_POINT('Ctrl Pts',(97.6350048828449,-0.0873675624448035,
-7.93135995466523));
#30177=CARTESIAN_POINT('Ctrl Pts',(97.6354808770979,-0.0807138645901476,
-7.93090527670038));
#30178=CARTESIAN_POINT('Ctrl Pts',(97.6374679059321,-0.0491759301201907,
-7.92874301648142));
#30179=CARTESIAN_POINT('Ctrl Pts',(97.6382449876383,-0.0242538099230699,
-7.92701314135852));
#30180=CARTESIAN_POINT('Ctrl Pts',(97.6382307576569,0.000672359933839044,
-7.92526064390542));
#30181=CARTESIAN_POINT('Ctrl Pts',(97.6382307583967,0.000671062669383031,
-7.92526073511286));
#30182=CARTESIAN_POINT('Ctrl Pts',(97.6381788678385,0.0917416851970525,
-7.91885778732613));
#30183=CARTESIAN_POINT('Ctrl Pts',(97.6275636890022,0.182492453302888,-7.91214600970138));
#30184=CARTESIAN_POINT('Ctrl Pts',(97.5947290699091,0.321306745803253,-7.90170620881246));
#30185=CARTESIAN_POINT('Ctrl Pts',(97.5795656154965,0.370685317609632,-7.89796480067282));
#30186=CARTESIAN_POINT('Ctrl Pts',(97.5587390848017,0.42540851181193,-7.89389245952835));
#30187=CARTESIAN_POINT('Ctrl Pts',(97.5562103528544,0.431880092304319,-7.89341211582663));
#30188=CARTESIAN_POINT('Ctrl Pts',(97.5522624328536,0.441725760558389,-7.89268365600119));
#30189=CARTESIAN_POINT('Ctrl Pts',(97.5508845945892,0.445116104657489,-7.89243323497917));
#30190=CARTESIAN_POINT('Ctrl Pts',(97.5483323484103,0.451313253910075,-7.89197634301844));
#30191=CARTESIAN_POINT('Ctrl Pts',(97.547162863573,0.454121941042803,-7.89176959733242));
#30192=CARTESIAN_POINT('Ctrl Pts',(97.5444969317415,0.460455290347638,-7.8913041262469));
#30193=CARTESIAN_POINT('Ctrl Pts',(97.5429941715983,0.463977207610486,-7.89104578054566));
#30194=CARTESIAN_POINT('Ctrl Pts',(97.5390635449132,0.473066096652275,-7.89038021109147));
#30195=CARTESIAN_POINT('Ctrl Pts',(97.5366097107556,0.478621813088558,-7.88997447766068));
#30196=CARTESIAN_POINT('Ctrl Pts',(97.5197690095781,0.515966438396092,-7.88725304740198));
#30197=CARTESIAN_POINT('Ctrl Pts',(97.5040170461905,0.547124747641917,-7.88501095298144));
#30198=CARTESIAN_POINT('Ctrl Pts',(97.4422110397586,0.656968198972049,-7.87704906693644));
#30199=CARTESIAN_POINT('Ctrl Pts',(97.3884507087036,0.730940934143778,-7.87155206831638));
#30200=CARTESIAN_POINT('Ctrl Pts',(97.3089018822944,0.817292297682451,-7.86412814048908));
#30201=CARTESIAN_POINT('Ctrl Pts',(97.2904678529663,0.836006206917915,-7.86244966789188));
#30202=CARTESIAN_POINT('Ctrl Pts',(97.2622801296232,0.862770042867849,-7.85992857271642));
#30203=CARTESIAN_POINT('Ctrl Pts',(97.2529970444156,0.871304936576174,-7.85910519891827));
#30204=CARTESIAN_POINT('Ctrl Pts',(97.2378989691732,0.884745225689368,-7.8577756137069));
#30205=CARTESIAN_POINT('Ctrl Pts',(97.2321702316626,0.889746334120657,-7.85727326266728));
#30206=CARTESIAN_POINT('Ctrl Pts',(97.221211058643,0.899128080513568,-7.85631598703616));
#30207=CARTESIAN_POINT('Ctrl Pts',(97.2159901884433,0.903519446784354,-7.85586151772605));
#30208=CARTESIAN_POINT('Ctrl Pts',(97.2106885287038,0.907900685006797,-7.85540148842156));
#30209=CARTESIAN_POINT('Ctrl Pts',(97.2106455029646,0.907936235897516,-7.8553977551405));
#30210=CARTESIAN_POINT('Ctrl Pts',(97.2105558175339,0.908010329579029,-7.85538997346799));
#30211=CARTESIAN_POINT('Ctrl Pts',(97.2105091571299,0.908048872053512,-7.8553859250318));
#30212=CARTESIAN_POINT('Ctrl Pts',(97.2104117953303,0.90812928232232,-7.85537747778543));
#30213=CARTESIAN_POINT('Ctrl Pts',(97.2103610934887,0.908171149393383,-7.85537307895715));
#30214=CARTESIAN_POINT('Ctrl Pts',(97.2102551803057,0.908258592340649,-7.85536389034314));
#30215=CARTESIAN_POINT('Ctrl Pts',(97.2101999683967,0.908304167361049,-7.85535910053311));
#30216=CARTESIAN_POINT('Ctrl Pts',(97.2061063390936,0.911682652084415,-7.8550039768909));
#30217=CARTESIAN_POINT('Ctrl Pts',(97.2020458007649,0.914988551609131,-7.8546525760926));
#30218=CARTESIAN_POINT('Ctrl Pts',(97.1932846170847,0.922024868644866,-7.85389611600036));
#30219=CARTESIAN_POINT('Ctrl Pts',(97.1885772516971,0.925746642474763,-7.85349072866336));
#30220=CARTESIAN_POINT('Ctrl Pts',(97.1760998555832,0.935457580731893,-7.85241884138715));
#30221=CARTESIAN_POINT('Ctrl Pts',(97.1682832163167,0.941385810963418,-7.85174999845019));
#30222=CARTESIAN_POINT('Ctrl Pts',(97.1338660660346,0.966817192450627,-7.84881577862293));
#30223=CARTESIAN_POINT('Ctrl Pts',(97.1065292658109,0.98529396814419,-7.84651216950563));
#30224=CARTESIAN_POINT('Ctrl Pts',(96.9918347383923,1.05598859796899,-7.836948411576));
#30225=CARTESIAN_POINT('Ctrl Pts',(96.8986633753071,1.09792529657191,-7.82936131017581));
#30226=CARTESIAN_POINT('Ctrl Pts',(96.7806017521716,1.13361576901222,-7.82044134353543));
#30227=CARTESIAN_POINT('Ctrl Pts',(96.7597471231105,1.13929886813824,-7.81889264964768));
#30228=CARTESIAN_POINT('Ctrl Pts',(96.7255741137713,1.14760814458412,-7.81641003465013));
#30229=CARTESIAN_POINT('Ctrl Pts',(96.7123464609499,1.15058360964401,-7.81546232043411));
#30230=CARTESIAN_POINT('Ctrl Pts',(96.6943978749204,1.15429662326251,-7.81419680258446));
#30231=CARTESIAN_POINT('Ctrl Pts',(96.6897201245905,1.15523470560876,-7.81386884959797));
#30232=CARTESIAN_POINT('Ctrl Pts',(96.681908648989,1.15675191388651,-7.81332444525744));
#30233=CARTESIAN_POINT('Ctrl Pts',(96.678778086775,1.15734678336254,-7.81310713593988));
#30234=CARTESIAN_POINT('Ctrl Pts',(96.6728476068142,1.15844877380885,-7.81269716094467));
#30235=CARTESIAN_POINT('Ctrl Pts',(96.67004820822,1.15895846482445,-7.81250434883756));
#30236=CARTESIAN_POINT('Ctrl Pts',(96.6634161166412,1.16014116488754,-7.8120491777055));
#30237=CARTESIAN_POINT('Ctrl Pts',(96.6595818514943,1.16080533958989,-7.81178730673393));
#30238=CARTESIAN_POINT('Ctrl Pts',(96.6460368055927,1.16308253606897,-7.81086650454938));
#30239=CARTESIAN_POINT('Ctrl Pts',(96.6363088437271,1.16459285958177,-7.81021296366014));
#30240=CARTESIAN_POINT('Ctrl Pts',(96.5571348415205,1.1758703641614,-7.80494855049348));
#30241=CARTESIAN_POINT('Ctrl Pts',(96.4869523569598,1.17954019898972,-7.80061738570189));
#30242=CARTESIAN_POINT('Ctrl Pts',(96.3573388014611,1.17473550103533,-7.79259425294203));
#30243=CARTESIAN_POINT('Ctrl Pts',(96.2980822458911,1.16801875081837,-7.7889159212225));
#30244=CARTESIAN_POINT('Ctrl Pts',(96.2186095145754,1.15284409237539,-7.78376015977628));
#30245=CARTESIAN_POINT('Ctrl Pts',(96.1977428977383,1.14826822940311,-7.78238572714134));
#30246=CARTESIAN_POINT('Ctrl Pts',(96.1616851223464,1.1393267797889,-7.77996603116743));
#30247=CARTESIAN_POINT('Ctrl Pts',(96.1464357464839,1.13521805374715,-7.77892860056521));
#30248=CARTESIAN_POINT('Ctrl Pts',(96.1243503821836,1.1287884238588,-7.77740326998126));
#30249=CARTESIAN_POINT('Ctrl Pts',(96.1174453984027,1.12670922199922,-7.77692309221318));
#30250=CARTESIAN_POINT('Ctrl Pts',(96.1053246085734,1.12293770970135,-7.77607420382506));
#30251=CARTESIAN_POINT('Ctrl Pts',(96.1001006641551,1.12127212333614,-7.77570636529627));
#30252=CARTESIAN_POINT('Ctrl Pts',(96.0892351813118,1.11772403189962,-7.77493706397254));
#30253=CARTESIAN_POINT('Ctrl Pts',(96.0835959035028,1.11583515437995,-7.7745354029575));
#30254=CARTESIAN_POINT('Ctrl Pts',(96.0689257800281,1.11079749764821,-7.7734841463847));
#30255=CARTESIAN_POINT('Ctrl Pts',(96.0599187092887,1.10758133510916,-7.77283236868855));
#30256=CARTESIAN_POINT('Ctrl Pts',(96.0221448556305,1.09357236743689,-7.77007148455463));
#30257=CARTESIAN_POINT('Ctrl Pts',(95.9937692854553,1.08176660022033,-7.76792950014785));
#30258=CARTESIAN_POINT('Ctrl Pts',(95.9510389526017,1.06199420098715,-7.76459595846739));
#30259=CARTESIAN_POINT('Ctrl Pts',(95.9363398230804,1.05481676894557,-7.76342898525895));
#30260=CARTESIAN_POINT('Ctrl Pts',(95.9218015552896,1.04733928250123,-7.76225484780379));
#30261=CARTESIAN_POINT('Ctrl Pts',(95.9218016730721,1.04733934308044,-7.66392541087522));
#30262=CARTESIAN_POINT('Ctrl Pts',(95.923981392874,1.04846044093055,-7.66409230412672));
#30263=CARTESIAN_POINT('Ctrl Pts',(95.9261646025136,1.04957472918492,-7.66425876593663));
#30264=CARTESIAN_POINT('Ctrl Pts',(95.9317643886838,1.05241080267926,-7.6646839675234));
#30265=CARTESIAN_POINT('Ctrl Pts',(95.9351858978763,1.05412276754204,-7.6649420999066));
#30266=CARTESIAN_POINT('Ctrl Pts',(95.944051180343,1.05850466115847,-7.66560678627251));
#30267=CARTESIAN_POINT('Ctrl Pts',(95.9495074184012,1.0611493196062,-7.66601185632826));
#30268=CARTESIAN_POINT('Ctrl Pts',(95.9862798530973,1.07862365387436,-7.66871657412019));
#30269=CARTESIAN_POINT('Ctrl Pts',(96.018220186207,1.09210878084112,-7.67094365038082));
#30270=CARTESIAN_POINT('Ctrl Pts',(96.0771503032242,1.11397842592764,-7.67491543705369));
#30271=CARTESIAN_POINT('Ctrl Pts',(96.1039335913543,1.12283766412314,-7.67667138336449));
#30272=CARTESIAN_POINT('Ctrl Pts',(96.1770424663697,1.14414010667485,-7.68139279936664));
#30273=CARTESIAN_POINT('Ctrl Pts',(96.2238502174275,1.15472930241282,-7.68434131347457));
#30274=CARTESIAN_POINT('Ctrl Pts',(96.3238411505766,1.17101331010402,-7.69067649809304));
#30275=CARTESIAN_POINT('Ctrl Pts',(96.3770253976349,1.17600029435913,-7.69406862072802));
#30276=CARTESIAN_POINT('Ctrl Pts',(96.4411899657492,1.1776418308785,-7.6982871419761));
#30277=CARTESIAN_POINT('Ctrl Pts',(96.4520227688403,1.17776944700149,-7.69900349607877));
#30278=CARTESIAN_POINT('Ctrl Pts',(96.4690785456704,1.17773505944926,-7.70013858705303));
#30279=CARTESIAN_POINT('Ctrl Pts',(96.4753012878662,1.17767319065209,-7.70055423341445));
#30280=CARTESIAN_POINT('Ctrl Pts',(96.4869505466649,1.17746502665234,-7.70133530583461));
#30281=CARTESIAN_POINT('Ctrl Pts',(96.4923771303507,1.17733052305712,-7.70170035780464));
#30282=CARTESIAN_POINT('Ctrl Pts',(96.5045240580543,1.17694540726014,-7.70252028234999));
#30283=CARTESIAN_POINT('Ctrl Pts',(96.5112435305895,1.17667474018992,-7.70297576270701));
#30284=CARTESIAN_POINT('Ctrl Pts',(96.5283359003427,1.17583956405077,-7.70413940511488));
#30285=CARTESIAN_POINT('Ctrl Pts',(96.5387041420007,1.17519534330095,-7.70484999732243));
#30286=CARTESIAN_POINT('Ctrl Pts',(96.6243336689131,1.16873665653123,-7.71075922872014));
#30287=CARTESIAN_POINT('Ctrl Pts',(96.698870871402,1.15583711950869,-7.71617964687596));
#30288=CARTESIAN_POINT('Ctrl Pts',(96.8274458155472,1.12061534841979,-7.7259317615011));
#30289=CARTESIAN_POINT('Ctrl Pts',(96.882041191241,1.10123984115792,-7.73020463661731));
#30290=CARTESIAN_POINT('Ctrl Pts',(96.9537164314812,1.06968796768564,-7.73585944498116));
#30291=CARTESIAN_POINT('Ctrl Pts',(96.9722236550819,1.06095857194982,-7.73732331876027));
#30292=CARTESIAN_POINT('Ctrl Pts',(97.0021344371959,1.04588548132331,-7.73968541400261));
#30293=CARTESIAN_POINT('Ctrl Pts',(97.0136762307433,1.03982688791344,-7.74059592323309));
#30294=CARTESIAN_POINT('Ctrl Pts',(97.0292399282159,1.0313245719447,-7.74182007589355));
#30295=CARTESIAN_POINT('Ctrl Pts',(97.0333507758058,1.02904679804116,-7.74214306064631));
#30296=CARTESIAN_POINT('Ctrl Pts',(97.0402128531085,1.02519073401116,-7.74268147839931));
#30297=CARTESIAN_POINT('Ctrl Pts',(97.0429715059819,1.02362584646643,-7.74289773121208));
#30298=CARTESIAN_POINT('Ctrl Pts',(97.0482035591064,1.02062988484212,-7.74330744919929));
#30299=CARTESIAN_POINT('Ctrl Pts',(97.0506781178956,1.01920092746069,-7.74350104965702));
#30300=CARTESIAN_POINT('Ctrl Pts',(97.0565522982165,1.01578025856189,-7.74396025449424));
#30301=CARTESIAN_POINT('Ctrl Pts',(97.0599472012252,1.01378044989703,-7.74422534970025));
#30302=CARTESIAN_POINT('Ctrl Pts',(97.0719456412569,1.00663127700011,-7.74516144565428));
#30303=CARTESIAN_POINT('Ctrl Pts',(97.0804936776347,1.00138895061651,-7.74582685074794));
#30304=CARTESIAN_POINT('Ctrl Pts',(97.1395304446723,0.964137153080263,-7.75041955431513));
#30305=CARTESIAN_POINT('Ctrl Pts',(97.1875914875447,0.928429196611734,-7.75414603620714));
#30306=CARTESIAN_POINT('Ctrl Pts',(97.2833176830194,0.845294428741272,-7.76200156674863));
#30307=CARTESIAN_POINT('Ctrl Pts',(97.3300547112697,0.797134767390442,-7.76611449751116));
#30308=CARTESIAN_POINT('Ctrl Pts',(97.3941867288306,0.718657966222643,-7.77255740664575));
#30309=CARTESIAN_POINT('Ctrl Pts',(97.4147534228625,0.691114645895845,-7.77477522796733));
#30310=CARTESIAN_POINT('Ctrl Pts',(97.4394811072968,0.654786760845278,-7.77767124484812));
#30311=CARTESIAN_POINT('Ctrl Pts',(97.4447796286538,0.646794490101691,-7.77830660638022));
#30312=CARTESIAN_POINT('Ctrl Pts',(97.4532080207281,0.633737686267731,-7.77934221371402));
#30313=CARTESIAN_POINT('Ctrl Pts',(97.4563981888518,0.628712448665733,-7.77974023313545));
#30314=CARTESIAN_POINT('Ctrl Pts',(97.4624523569862,0.619014054877953,-7.78050743141556));
#30315=CARTESIAN_POINT('Ctrl Pts',(97.4653221036924,0.614344654616672,-7.78087638828942));
#30316=CARTESIAN_POINT('Ctrl Pts',(97.4718222383855,0.603600809592548,-7.78172446047449));
#30317=CARTESIAN_POINT('Ctrl Pts',(97.4754306490261,0.597513383611834,-7.7822043509442));
#30318=CARTESIAN_POINT('Ctrl Pts',(97.4867553406637,0.578009916324859,-7.78374012593532));
#30319=CARTESIAN_POINT('Ctrl Pts',(97.4942618576207,0.564474608690195,-7.78480336821043));
#30320=CARTESIAN_POINT('Ctrl Pts',(97.5385074194192,0.480849366789827,-7.79135988224784));
#30321=CARTESIAN_POINT('Ctrl Pts',(97.5683654796724,0.40736333352814,-7.79708871814974));
#30322=CARTESIAN_POINT('Ctrl Pts',(97.6059753545198,0.279125989572298,-7.80688944562775));
#30323=CARTESIAN_POINT('Ctrl Pts',(97.6176700059914,0.22579363957247,-7.81090600405515));
#30324=CARTESIAN_POINT('Ctrl Pts',(97.6280210618544,0.155609559437917,-7.81599592808213));
#30325=CARTESIAN_POINT('Ctrl Pts',(97.6300756242715,0.139329114946114,-7.81716285249217));
#30326=CARTESIAN_POINT('Ctrl Pts',(97.6329475763833,0.111982270537919,-7.81909455767893));
#30327=CARTESIAN_POINT('Ctrl Pts',(97.6339499796347,0.100937989160873,-7.81986696237905));
#30328=CARTESIAN_POINT('Ctrl Pts',(97.6351330921114,0.0854803105500236,
-7.82093575569451));
#30329=CARTESIAN_POINT('Ctrl Pts',(97.6354451638727,0.0810779633869377,
-7.82123875898059));
#30330=CARTESIAN_POINT('Ctrl Pts',(97.6359353436993,0.0735645232211535,
-7.82175340623233));
#30331=CARTESIAN_POINT('Ctrl Pts',(97.6361258629712,0.0704543133286296,
-7.82196571891625));
#30332=CARTESIAN_POINT('Ctrl Pts',(97.6364710750203,0.064426864369362,-7.82237572313969));
#30333=CARTESIAN_POINT('Ctrl Pts',(97.6366272600685,0.0615097779286169,
-7.8225735003458));
#30334=CARTESIAN_POINT('Ctrl Pts',(97.6370231344539,0.0535622265020901,
-7.82311064072549));
#30335=CARTESIAN_POINT('Ctrl Pts',(97.6372414179168,0.0485306844431066,
-7.8234488461278));
#30336=CARTESIAN_POINT('Ctrl Pts',(97.637957227386,0.0291625846617524,-7.82474411053741));
#30337=CARTESIAN_POINT('Ctrl Pts',(97.6382251109924,0.0148181076439342,
-7.82568950209409));
#30338=CARTESIAN_POINT('Ctrl Pts',(97.6382404784862,-0.0235631149471175,
-7.82819039740362));
#30339=CARTESIAN_POINT('Ctrl Pts',(97.6375143748193,-0.0475940345359999,
-7.82972620866432));
#30340=CARTESIAN_POINT('Ctrl Pts',(97.6327832013468,-0.125287048562484,
-7.83464160347656));
#30341=CARTESIAN_POINT('Ctrl Pts',(97.6258373578872,-0.178701947925456,
-7.83794595302156));
#30342=CARTESIAN_POINT('Ctrl Pts',(97.6007545329808,-0.303844985852653,
-7.84585154403032));
#30343=CARTESIAN_POINT('Ctrl Pts',(97.5794736190406,-0.374698412701719,
-7.85046793662601));
#30344=CARTESIAN_POINT('Ctrl Pts',(97.5477790168846,-0.452754685395738,
-7.85599649562586));
#30345=CARTESIAN_POINT('Ctrl Pts',(97.5437261244805,-0.462367572432125,
-7.85668510301689));
#30346=CARTESIAN_POINT('Ctrl Pts',(97.5368461327927,-0.478098796804973,
-7.85782547647642));
#30347=CARTESIAN_POINT('Ctrl Pts',(97.5340932087621,-0.48424908973175,-7.85827475498668));
#30348=CARTESIAN_POINT('Ctrl Pts',(97.5290271529877,-0.495311568997524,
-7.85908926490367));
#30349=CARTESIAN_POINT('Ctrl Pts',(97.5267325255483,-0.50023206040703,-7.85945386019599));
#30350=CARTESIAN_POINT('Ctrl Pts',(97.521739050489,-0.510749363739677,-7.86023822072937));
#30351=CARTESIAN_POINT('Ctrl Pts',(97.5190297785611,-0.516341014654776,
-7.86065833417033));
#30352=CARTESIAN_POINT('Ctrl Pts',(97.5114954458012,-0.531582533612204,
-7.86181212282035));
#30353=CARTESIAN_POINT('Ctrl Pts',(97.5065819321537,-0.541187751284302,
-7.8625488243611));
#30354=CARTESIAN_POINT('Ctrl Pts',(97.4770272598079,-0.597056186318608,
-7.86689159600093));
#30355=CARTESIAN_POINT('Ctrl Pts',(97.4494551542298,-0.641693939673995,
-7.87059978908286));
#30356=CARTESIAN_POINT('Ctrl Pts',(97.3736237896031,-0.747907263960275,
-7.88002573071777));
#30357=CARTESIAN_POINT('Ctrl Pts',(97.3220345654406,-0.806795777735824,
-7.88582339340791));
#30358=CARTESIAN_POINT('Ctrl Pts',(97.2402882546581,-0.883255588928051,
-7.8939333980572));
#30359=CARTESIAN_POINT('Ctrl Pts',(97.2145904897262,-0.905295055001402,
-7.89635247591214));
#30360=CARTESIAN_POINT('Ctrl Pts',(97.1832346826081,-0.929923902702669,
-7.8991234977911));
#30361=CARTESIAN_POINT('Ctrl Pts',(97.1784639431013,-0.933612257977767,
-7.89954039139932));
#30362=CARTESIAN_POINT('Ctrl Pts',(97.170628310543,-0.939574557225028,-7.90021718085949));
#30363=CARTESIAN_POINT('Ctrl Pts',(97.1675803930718,-0.94187047990306,-7.90047850593111));
#30364=CARTESIAN_POINT('Ctrl Pts',(97.162082953424,-0.945969842204705,-7.90094630844021));
#30365=CARTESIAN_POINT('Ctrl Pts',(97.1596375638603,-0.947778636336309,
-7.90115314436538));
#30366=CARTESIAN_POINT('Ctrl Pts',(97.1542258818935,-0.951749180392414,
-7.90160811688304));
#30367=CARTESIAN_POINT('Ctrl Pts',(97.1512564779503,-0.953906548782637,
-7.9018559572103));
#30368=CARTESIAN_POINT('Ctrl Pts',(97.1425945762482,-0.960138044451458,
-7.90257384813418));
#30369=CARTESIAN_POINT('Ctrl Pts',(97.1368756616,-0.964175431919296,-7.90304150269117));
#30370=CARTESIAN_POINT('Ctrl Pts',(97.0861931324487,-0.999282924268112,
-7.90713390707167));
#30371=CARTESIAN_POINT('Ctrl Pts',(97.0391470314475,-1.02724354803441,-7.91057601267292));
#30372=CARTESIAN_POINT('Ctrl Pts',(96.9102390934021,-1.09217829912979,-7.91955466080026));
#30373=CARTESIAN_POINT('Ctrl Pts',(96.8258164937886,-1.12323857126121,-7.92501210942893));
#30374=CARTESIAN_POINT('Ctrl Pts',(96.7157084209652,-1.15000578251797,-7.93230372389437));
#30375=CARTESIAN_POINT('Ctrl Pts',(96.6925665164683,-1.15489849320668,-7.93384366748186));
#30376=CARTESIAN_POINT('Ctrl Pts',(96.6607406382336,-1.1606320079399,-7.93597932178633));
#30377=CARTESIAN_POINT('Ctrl Pts',(96.6521704588125,-1.16207819276933,-7.93655615219706));
#30378=CARTESIAN_POINT('Ctrl Pts',(96.6384647125157,-1.1642352476759,-7.9374817464514));
#30379=CARTESIAN_POINT('Ctrl Pts',(96.6333389866055,-1.16500730872376,-7.93782859379942));
#30380=CARTESIAN_POINT('Ctrl Pts',(96.6227658495484,-1.16652857157378,-7.9385455581791));
#30381=CARTESIAN_POINT('Ctrl Pts',(96.6173179630493,-1.16727350972342,-7.93891579873738));
#30382=CARTESIAN_POINT('Ctrl Pts',(96.6046073473807,-1.1689209572902,-7.93978162148022));
#30383=CARTESIAN_POINT('Ctrl Pts',(96.5973410917316,-1.16979396486757,-7.94027810737867));
#30384=CARTESIAN_POINT('Ctrl Pts',(96.5737710898679,-1.17240318486601,-7.94189377898199));
#30385=CARTESIAN_POINT('Ctrl Pts',(96.5574397270239,-1.17386661608748,-7.94302131999425));
#30386=CARTESIAN_POINT('Ctrl Pts',(96.5187024889696,-1.17652394634718,-7.9457161908674));
#30387=CARTESIAN_POINT('Ctrl Pts',(96.4962832048433,-1.17741939404442,-7.94729202062163));
#30388=CARTESIAN_POINT('Ctrl Pts',(96.4087629222459,-1.17841317164145,-7.95350675958483));
#30389=CARTESIAN_POINT('Ctrl Pts',(96.3437299466168,-1.17375458646104,-7.95826892214971));
#30390=CARTESIAN_POINT('Ctrl Pts',(96.2773912255896,-1.1634334708004,-7.96319621355617));
#30391=CARTESIAN_POINT('Ctrl Pts',(96.2753608873686,-1.16311214015841,-7.96334707517624));
#30392=CARTESIAN_POINT('Ctrl Pts',(96.2138408374906,-1.15321052920601,-7.96791989695895));
#30393=CARTESIAN_POINT('Ctrl Pts',(96.155166685269,-1.13908319271317,-7.9723333659338));
#30394=CARTESIAN_POINT('Ctrl Pts',(96.0882896217135,-1.11743866191224,-7.97726264357549));
#30395=CARTESIAN_POINT('Ctrl Pts',(96.0787918472646,-1.11423022462396,-7.9779601054315));
#30396=CARTESIAN_POINT('Ctrl Pts',(96.0656198009241,-1.10959238300891,-7.97892267819898));
#30397=CARTESIAN_POINT('Ctrl Pts',(96.0619103105781,-1.1082653247258,-7.97919323199774));
#30398=CARTESIAN_POINT('Ctrl Pts',(96.0555219677818,-1.10594369208253,-7.97965817941775));
#30399=CARTESIAN_POINT('Ctrl Pts',(96.052839976488,-1.10495794693614,-7.97985307395861));
#30400=CARTESIAN_POINT('Ctrl Pts',(96.0471886032513,-1.10285745155562,-7.98026306879484));
#30401=CARTESIAN_POINT('Ctrl Pts',(96.0442200884078,-1.10174044941557,-7.98047802873518));
#30402=CARTESIAN_POINT('Ctrl Pts',(96.0368637933656,-1.09893842355254,-7.98100981441349));
#30403=CARTESIAN_POINT('Ctrl Pts',(96.0324814597836,-1.09723907713851,-7.98132580858024));
#30404=CARTESIAN_POINT('Ctrl Pts',(96.0159818528589,-1.09072709730348,-7.98251291855449));
#30405=CARTESIAN_POINT('Ctrl Pts',(96.0039340740785,-1.08573939457892,-7.98337438319121));
#30406=CARTESIAN_POINT('Ctrl Pts',(95.9731932581564,-1.07241067677955,-7.98556480544839));
#30407=CARTESIAN_POINT('Ctrl Pts',(95.9546297974243,-1.06378036505403,-7.98688015028496));
#30408=CARTESIAN_POINT('Ctrl Pts',(95.8845037051856,-1.02892701597441,-7.9918552458824));
#30409=CARTESIAN_POINT('Ctrl Pts',(95.8346714612259,-0.999401760449134,
-7.99540683162181));
#30410=CARTESIAN_POINT('Ctrl Pts',(95.7252821882188,-0.923186988955485,
-8.00366198635098));
#30411=CARTESIAN_POINT('Ctrl Pts',(95.6676555304831,-0.874195105200194,
-8.00837561357045));
#30412=CARTESIAN_POINT('Ctrl Pts',(95.6078818816454,-0.812574807312045,
-8.01400988825543));
#30413=CARTESIAN_POINT('Ctrl Pts',(95.6007477014007,-0.805022806449267,
-8.01469567892419));
#30414=CARTESIAN_POINT('Ctrl Pts',(95.5891613991801,-0.792428249643242,
-8.01583234665886));
#30415=CARTESIAN_POINT('Ctrl Pts',(95.5846508168138,-0.787440070819168,
-8.01628076441739));
#30416=CARTESIAN_POINT('Ctrl Pts',(95.5765771155062,-0.778356307117406,
-8.01709435359027));
#30417=CARTESIAN_POINT('Ctrl Pts',(95.5729990976729,-0.774274169509924,
-8.0174588954474));
#30418=CARTESIAN_POINT('Ctrl Pts',(95.565380121745,-0.765459532008716,-8.01824385330516));
#30419=CARTESIAN_POINT('Ctrl Pts',(95.5613482118395,-0.760719465040718,
-8.01866462253414));
#30420=CARTESIAN_POINT('Ctrl Pts',(95.5504010775743,-0.747640980844114,
-8.01982207874377));
#30421=CARTESIAN_POINT('Ctrl Pts',(95.5435631797032,-0.739238932524814,
-8.02056182435269));
#30422=CARTESIAN_POINT('Ctrl Pts',(95.5037412679311,-0.688905224362348,
-8.02497215138119));
#30423=CARTESIAN_POINT('Ctrl Pts',(95.4735260474554,-0.644871905957608,
-8.02874871213888));
#30424=CARTESIAN_POINT('Ctrl Pts',(95.4220126954558,-0.557654685753922,
-8.03606990122398));
#30425=CARTESIAN_POINT('Ctrl Pts',(95.4001694423836,-0.514911776524459,
-8.0395920312369));
#30426=CARTESIAN_POINT('Ctrl Pts',(95.3697136831079,-0.445103973447315,
-8.04517995291811));
#30427=CARTESIAN_POINT('Ctrl Pts',(95.3593658798564,-0.418851374801232,
-8.04724592331202));
#30428=CARTESIAN_POINT('Ctrl Pts',(95.3384308940089,-0.359582001908917,
-8.05180335635843));
#30429=CARTESIAN_POINT('Ctrl Pts',(95.3283373680479,-0.326415302427263,
-8.05428235473442));
#30430=CARTESIAN_POINT('Ctrl Pts',(95.3182127567085,-0.286975955233544,
-8.05711249804184));
#30431=CARTESIAN_POINT('Ctrl Pts',(95.3167504999801,-0.281091596912665,
-8.05753171356749));
#30432=CARTESIAN_POINT('Ctrl Pts',(95.3144397687624,-0.271476170337992,
-8.05821150108607));
#30433=CARTESIAN_POINT('Ctrl Pts',(95.3135639393123,-0.267751884754611,
-8.05847352285367));
#30434=CARTESIAN_POINT('Ctrl Pts',(95.3120243031907,-0.261058705927105,
-8.05894205227142));
#30435=CARTESIAN_POINT('Ctrl Pts',(95.3113538388309,-0.258091457737228,
-8.05914892367343));
#30436=CARTESIAN_POINT('Ctrl Pts',(95.309901671687,-0.251546805998029,-8.05960335702116));
#30437=CARTESIAN_POINT('Ctrl Pts',(95.3091251511017,-0.247968337789584,
-8.05985062733141));
#30438=CARTESIAN_POINT('Ctrl Pts',(95.3069213459685,-0.237578889177517,
-8.06056519979769));
#30439=CARTESIAN_POINT('Ctrl Pts',(95.305537690475,-0.230758665475385,-8.0610301397131));
#30440=CARTESIAN_POINT('Ctrl Pts',(95.2942875463215,-0.172667411780121,
-8.06495818342253));
#30441=CARTESIAN_POINT('Ctrl Pts',(95.2877787524103,-0.120797812134772,
-8.06825470066511));
#30442=CARTESIAN_POINT('Ctrl Pts',(95.2798825823654,0.0144152596926865,
-8.07669152404167));
#30443=CARTESIAN_POINT('Ctrl Pts',(95.2838495873202,0.0977678340915831,
-8.08175555754729));
#30444=CARTESIAN_POINT('Ctrl Pts',(95.3012726004469,0.210424564021685,-8.08902674324303));
#30445=CARTESIAN_POINT('Ctrl Pts',(95.3071673398022,0.240644875148239,-8.09101807885458));
#30446=CARTESIAN_POINT('Ctrl Pts',(95.316437071813,0.279911130639541,-8.09367700250467));
#30447=CARTESIAN_POINT('Ctrl Pts',(95.3187490843432,0.289197120202337,-8.09431108635793));
#30448=CARTESIAN_POINT('Ctrl Pts',(95.3226812400735,0.304207598564376,-8.09534512574232));
#30449=CARTESIAN_POINT('Ctrl Pts',(95.3242320828442,0.309949919541177,-8.09574286759459));
#30450=CARTESIAN_POINT('Ctrl Pts',(95.3272957451871,0.320961693719857,-8.09650988387517));
#30451=CARTESIAN_POINT('Ctrl Pts',(95.3288019944376,0.326232826421337,-8.09687893890141));
#30452=CARTESIAN_POINT('Ctrl Pts',(95.3323736130768,0.33840929047697,-8.09773596435205));
#30453=CARTESIAN_POINT('Ctrl Pts',(95.3344656624178,0.345306501001488,-8.09822478253417));
#30454=CARTESIAN_POINT('Ctrl Pts',(95.3413376921524,0.367235950547476,-8.0997899747078));
#30455=CARTESIAN_POINT('Ctrl Pts',(95.3463562418367,0.382191009621324,-8.10087399233418));
#30456=CARTESIAN_POINT('Ctrl Pts',(95.3588632736023,0.417119191439609,-8.10344631681161));
#30457=CARTESIAN_POINT('Ctrl Pts',(95.3665968033818,0.43699805579233,-8.10494211851914));
#30458=CARTESIAN_POINT('Ctrl Pts',(95.3978969844965,0.511408642158896,-8.11066317469452));
#30459=CARTESIAN_POINT('Ctrl Pts',(95.425035493879,0.56433568359023,-8.11499100548655));
#30460=CARTESIAN_POINT('Ctrl Pts',(95.4927894191806,0.674995981601999,-8.12450980863772));
#30461=CARTESIAN_POINT('Ctrl Pts',(95.5348399948096,0.731598988080648,-8.12969542746935));
#30462=CARTESIAN_POINT('Ctrl Pts',(95.5882422964497,0.791448966555949,-8.13531737553614));
#30463=CARTESIAN_POINT('Ctrl Pts',(95.5948801799698,0.798703360492994,-8.13600119577185));
#30464=CARTESIAN_POINT('Ctrl Pts',(95.6042695696886,0.808710245520468,-8.13694681263806));
#30465=CARTESIAN_POINT('Ctrl Pts',(95.6069448196807,0.811533279844901,-8.13721384481675));
#30466=CARTESIAN_POINT('Ctrl Pts',(95.6116009832352,0.816398161134206,-8.13767439646127));
#30467=CARTESIAN_POINT('Ctrl Pts',(95.6135753805651,0.818446157285428,-8.13786839545716));
#30468=CARTESIAN_POINT('Ctrl Pts',(95.6177772947821,0.82277321799582,-8.13827849373416));
#30469=CARTESIAN_POINT('Ctrl Pts',(95.6200066818052,0.825050437114664,-8.13849444208905));
#30470=CARTESIAN_POINT('Ctrl Pts',(95.6255980343187,0.830715571304896,-8.13903206510085));
#30471=CARTESIAN_POINT('Ctrl Pts',(95.6289714460034,0.834092195153589,-8.13935286776616));
#30472=CARTESIAN_POINT('Ctrl Pts',(95.6420173842216,0.84699274662755,-8.14058035559939));
#30473=CARTESIAN_POINT('Ctrl Pts',(95.6518342031193,0.856370129662178,-8.14147652344846));
#30474=CARTESIAN_POINT('Ctrl Pts',(95.6777227524703,0.88025756435866,-8.14377672248058));
#30475=CARTESIAN_POINT('Ctrl Pts',(95.6940368270737,0.894498349035152,-8.1451653624917));
#30476=CARTESIAN_POINT('Ctrl Pts',(95.7759368057593,0.962103074910108,-8.15189801471611));
#30477=CARTESIAN_POINT('Ctrl Pts',(95.8467046785975,1.00871463130525,-8.15700823768759));
#30478=CARTESIAN_POINT('Ctrl Pts',(95.9218018246467,1.04733942103997,-8.16230712347374));
#30479=CARTESIAN_POINT('Origin',(96.460480949577,-7.19464945638997E-16,
0.924367114736168));
#30480=CARTESIAN_POINT('',(95.9218016730721,1.04733934308043,-8.76046578184569));
#30481=CARTESIAN_POINT('',(95.921801762405,1.04733938902714,-8.66210246100831));
#30482=CARTESIAN_POINT('',(95.9218016730721,1.04733934308042,0.924367114736168));
#30483=CARTESIAN_POINT('Ctrl Pts',(95.9218016730721,1.04733934308043,-8.76046578184569));
#30484=CARTESIAN_POINT('Ctrl Pts',(95.9211842780576,1.04702179757625,-8.76041879885222));
#30485=CARTESIAN_POINT('Ctrl Pts',(95.9205671622309,1.04670370532963,-8.76037184943281));
#30486=CARTESIAN_POINT('Ctrl Pts',(95.9165307298097,1.04461860740334,-8.76006484091161));
#30487=CARTESIAN_POINT('Ctrl Pts',(95.913119753472,1.04283536502668,-8.75980577226046));
#30488=CARTESIAN_POINT('Ctrl Pts',(95.9013312091185,1.03659859431538,-8.75891147927471));
#30489=CARTESIAN_POINT('Ctrl Pts',(95.8929984894525,1.03206043884117,-8.75828121998423));
#30490=CARTESIAN_POINT('Ctrl Pts',(95.8181144841698,0.990095988105696,-8.75262590390221));
#30491=CARTESIAN_POINT('Ctrl Pts',(95.7552852822633,0.946375818399088,-8.74793572478132));
#30492=CARTESIAN_POINT('Ctrl Pts',(95.6623524818714,0.86727796028939,-8.74038626992124));
#30493=CARTESIAN_POINT('Ctrl Pts',(95.6293319022418,0.835685977619807,-8.73755738925862));
#30494=CARTESIAN_POINT('Ctrl Pts',(95.5715688439873,0.773603423845097,-8.73219260237199));
#30495=CARTESIAN_POINT('Ctrl Pts',(95.5463551035912,0.74363998872754,-8.72967626963997));
#30496=CARTESIAN_POINT('Ctrl Pts',(95.5166424333765,0.704530742097177,-8.72644233250801));
#30497=CARTESIAN_POINT('Ctrl Pts',(95.5107050311602,0.696505854939194,-8.72578134450696));
#30498=CARTESIAN_POINT('Ctrl Pts',(95.5013409497965,0.683507122522943,-8.72471424646144));
#30499=CARTESIAN_POINT('Ctrl Pts',(95.4978491887168,0.678580589470841,-8.7243106234197));
#30500=CARTESIAN_POINT('Ctrl Pts',(95.4912736773382,0.669150294930611,-8.72353942360661));
#30501=CARTESIAN_POINT('Ctrl Pts',(95.4881830407352,0.664651509069659,-8.72317211916705));
#30502=CARTESIAN_POINT('Ctrl Pts',(95.481187067939,0.654314822800542,-8.72232945364582));
#30503=CARTESIAN_POINT('Ctrl Pts',(95.4773024916593,0.648463191044452,-8.72185333684939));
#30504=CARTESIAN_POINT('Ctrl Pts',(95.46540918291,0.630194852233414,-8.72036954512109));
#30505=CARTESIAN_POINT('Ctrl Pts',(95.4575818680362,0.617662343407645,-8.7193553059623));
#30506=CARTESIAN_POINT('Ctrl Pts',(95.4025190146929,0.525692724165228,-8.71193540965759));
#30507=CARTESIAN_POINT('Ctrl Pts',(95.3645522209929,0.441101013695717,-8.70519592273347));
#30508=CARTESIAN_POINT('Ctrl Pts',(95.3181402789188,0.293354257713818,-8.69383120564699));
#30509=CARTESIAN_POINT('Ctrl Pts',(95.3041862876573,0.232343001431131,-8.68925602295264));
#30510=CARTESIAN_POINT('Ctrl Pts',(95.2939073356206,0.162090760520949,-8.68429738906492));
#30511=CARTESIAN_POINT('Ctrl Pts',(95.2927670840496,0.153661153550667,-8.68370747849889));
#30512=CARTESIAN_POINT('Ctrl Pts',(95.2912288159413,0.141280799914897,-8.68284923397529));
#30513=CARTESIAN_POINT('Ctrl Pts',(95.29075931823,0.137339443536495,-8.68257721416311));
#30514=CARTESIAN_POINT('Ctrl Pts',(95.2899671444323,0.130390352626268,-8.68209982383404));
#30515=CARTESIAN_POINT('Ctrl Pts',(95.2896361196581,0.127383661070721,-8.68189400279479));
#30516=CARTESIAN_POINT('Ctrl Pts',(95.2889425785984,0.120853036245441,-8.68144856056237));
#30517=CARTESIAN_POINT('Ctrl Pts',(95.2885843746164,0.117328723975617,-8.68120917777893));
#30518=CARTESIAN_POINT('Ctrl Pts',(95.2876404947567,0.107606179763843,-8.68055142589863));
#30519=CARTESIAN_POINT('Ctrl Pts',(95.2870880453752,0.101404728403375,-8.68013483393737));
#30520=CARTESIAN_POINT('Ctrl Pts',(95.2843838722493,0.0680596538361094,
-8.67790926236002));
#30521=CARTESIAN_POINT('Ctrl Pts',(95.2831245786215,0.0408496400342891,
-8.67614445703815));
#30522=CARTESIAN_POINT('Ctrl Pts',(95.2815696192174,-0.0936205332582201,
-8.66756895531445));
#30523=CARTESIAN_POINT('Ctrl Pts',(95.2949818918721,-0.200529130520746,
-8.66116360281169));
#30524=CARTESIAN_POINT('Ctrl Pts',(95.3283571361453,-0.325382365659745,
-8.65293680430483));
#30525=CARTESIAN_POINT('Ctrl Pts',(95.3346252602013,-0.346448973402391,
-8.65152396327156));
#30526=CARTESIAN_POINT('Ctrl Pts',(95.3465126448089,-0.382661965703558,
-8.64904286503726));
#30527=CARTESIAN_POINT('Ctrl Pts',(95.3518610343859,-0.397891199686078,
-8.6479830132691));
#30528=CARTESIAN_POINT('Ctrl Pts',(95.3600711271452,-0.419816853374509,
-8.64643078797672));
#30529=CARTESIAN_POINT('Ctrl Pts',(95.3626847787278,-0.426604654199901,
-8.64594653449259));
#30530=CARTESIAN_POINT('Ctrl Pts',(95.3673820050107,-0.438474542000598,
-8.64509297021063));
#30531=CARTESIAN_POINT('Ctrl Pts',(95.3694385899896,-0.443567125065877,
-8.64472456303101));
#30532=CARTESIAN_POINT('Ctrl Pts',(95.3737859137832,-0.454118939286172,
-8.64395654959733));
#30533=CARTESIAN_POINT('Ctrl Pts',(95.3760823431109,-0.459575643312554,
-8.64355676161306));
#30534=CARTESIAN_POINT('Ctrl Pts',(95.382146985966,-0.473687701068225,-8.64251588640876));
#30535=CARTESIAN_POINT('Ctrl Pts',(95.3859782342551,-0.482315333563207,
-8.64187269636415));
#30536=CARTESIAN_POINT('Ctrl Pts',(95.4022214265444,-0.51773924100463,-8.63920285196703));
#30537=CARTESIAN_POINT('Ctrl Pts',(95.415534380345,-0.544108022986234,-8.63714599639503));
#30538=CARTESIAN_POINT('Ctrl Pts',(95.4755117863384,-0.65256758896969,-8.62838312584974));
#30539=CARTESIAN_POINT('Ctrl Pts',(95.5309659408508,-0.729387289474188,
-8.62138758773002));
#30540=CARTESIAN_POINT('Ctrl Pts',(95.6147579853023,-0.820181837635842,
-8.6123813906755));
#30541=CARTESIAN_POINT('Ctrl Pts',(95.6353273565597,-0.840872971823087,
-8.61027283586771));
#30542=CARTESIAN_POINT('Ctrl Pts',(95.6648514106568,-0.868443881140002,
-8.60740581393572));
#30543=CARTESIAN_POINT('Ctrl Pts',(95.6731673572244,-0.875989991812716,
-8.60661476688659));
#30544=CARTESIAN_POINT('Ctrl Pts',(95.6878278629858,-0.888915869348591,
-8.60525039694788));
#30545=CARTESIAN_POINT('Ctrl Pts',(95.6941237391187,-0.894349400822565,
-8.60467387062112));
#30546=CARTESIAN_POINT('Ctrl Pts',(95.7034814761785,-0.902254026976828,
-8.60383133774801));
#30547=CARTESIAN_POINT('Ctrl Pts',(95.7064988447006,-0.904777054623755,
-8.60356182935913));
#30548=CARTESIAN_POINT('Ctrl Pts',(95.7118777212156,-0.909229105266357,
-8.6030853037642));
#30549=CARTESIAN_POINT('Ctrl Pts',(95.7142341411626,-0.911164124103672,
-8.60287786672912));
#30550=CARTESIAN_POINT('Ctrl Pts',(95.7193724395717,-0.91535023030522,-8.6024284177829));
#30551=CARTESIAN_POINT('Ctrl Pts',(95.7221570763296,-0.917597802290566,
-8.6021866518989));
#30552=CARTESIAN_POINT('Ctrl Pts',(95.7299385245949,-0.923820108665626,
-8.601515931548));
#30553=CARTESIAN_POINT('Ctrl Pts',(95.7349575691058,-0.927767027203849,
-8.60108886982957));
#30554=CARTESIAN_POINT('Ctrl Pts',(95.7635872130698,-0.949906625424945,
-8.59868250325961));
#30555=CARTESIAN_POINT('Ctrl Pts',(95.7878518124206,-0.967240331875523,
-8.59675632405785));
#30556=CARTESIAN_POINT('Ctrl Pts',(95.8680069556926,-1.02002300960022,-8.59065703546099));
#30557=CARTESIAN_POINT('Ctrl Pts',(95.9262346484818,-1.05169118227962,-8.58661386465318));
#30558=CARTESIAN_POINT('Ctrl Pts',(96.03923721859,-1.10132960663053,-8.57895404146153));
#30559=CARTESIAN_POINT('Ctrl Pts',(96.0932613484339,-1.1205007344467,-8.57536398091351));
#30560=CARTESIAN_POINT('Ctrl Pts',(96.1659300215136,-1.14046613070225,-8.57047341649828));
#30561=CARTESIAN_POINT('Ctrl Pts',(96.1835060987019,-1.14486161582736,-8.56928644051504));
#30562=CARTESIAN_POINT('Ctrl Pts',(96.2086004523608,-1.15052562382111,-8.56758257635424));
#30563=CARTESIAN_POINT('Ctrl Pts',(96.2160410040387,-1.15212937834259,-8.56707625195697));
#30564=CARTESIAN_POINT('Ctrl Pts',(96.2289302135854,-1.15477707416851,-8.566196972238));
#30565=CARTESIAN_POINT('Ctrl Pts',(96.2343717297784,-1.15585485822996,-8.56582509395023));
#30566=CARTESIAN_POINT('Ctrl Pts',(96.2448390772497,-1.15785134925287,-8.56510837616905));
#30567=CARTESIAN_POINT('Ctrl Pts',(96.2498636817537,-1.15877587528674,-8.56476372875672));
#30568=CARTESIAN_POINT('Ctrl Pts',(96.2617368480116,-1.16088076033953,-8.56394782681518));
#30569=CARTESIAN_POINT('Ctrl Pts',(96.2685900935064,-1.16203324109228,-8.56347571063541));
#30570=CARTESIAN_POINT('Ctrl Pts',(96.289118600927,-1.16529888102834,-8.56205780835957));
#30571=CARTESIAN_POINT('Ctrl Pts',(96.3028209119581,-1.16723169122311,-8.56110647160767));
#30572=CARTESIAN_POINT('Ctrl Pts',(96.3987508623386,-1.17904337428846,-8.55440947349797));
#30573=CARTESIAN_POINT('Ctrl Pts',(96.4817718175587,-1.18046425580085,-8.54840142969621));
#30574=CARTESIAN_POINT('Ctrl Pts',(96.5912543825941,-1.17078131615757,-8.54033712234632));
#30575=CARTESIAN_POINT('Ctrl Pts',(96.6181790593375,-1.16745960028257,-8.53834480689025));
#30576=CARTESIAN_POINT('Ctrl Pts',(96.6871408678306,-1.15652231572469,-8.53324499413282));
#30577=CARTESIAN_POINT('Ctrl Pts',(96.7289260181774,-1.14754371656134,-8.53015731660019));
#30578=CARTESIAN_POINT('Ctrl Pts',(96.7791962291346,-1.13384471562949,-8.52651067663623));
#30579=CARTESIAN_POINT('Ctrl Pts',(96.7882281126902,-1.13126702396626,-8.52585828241797));
#30580=CARTESIAN_POINT('Ctrl Pts',(96.8011868413537,-1.12740038181003,-8.52492719540668));
#30581=CARTESIAN_POINT('Ctrl Pts',(96.8051389760955,-1.12619846015263,-8.52464390170203));
#30582=CARTESIAN_POINT('Ctrl Pts',(96.8120181768897,-1.12406675575666,-8.52415205640604));
#30583=CARTESIAN_POINT('Ctrl Pts',(96.8149480460406,-1.12314628254219,-8.52394298260227));
#30584=CARTESIAN_POINT('Ctrl Pts',(96.8211684247907,-1.12116526836502,-8.52349998822256));
#30585=CARTESIAN_POINT('Ctrl Pts',(96.8244578888169,-1.1201016928115,-8.52326624386522));
#30586=CARTESIAN_POINT('Ctrl Pts',(96.8334472900785,-1.11715138602034,-8.52262877348939));
#30587=CARTESIAN_POINT('Ctrl Pts',(96.8391376545662,-1.11523549709474,-8.52222668750093));
#30588=CARTESIAN_POINT('Ctrl Pts',(96.866786812288,-1.10569027770406,-8.52027885394045));
#30589=CARTESIAN_POINT('Ctrl Pts',(96.8885327351065,-1.09745491291875,-8.51876500485213));
#30590=CARTESIAN_POINT('Ctrl Pts',(97.0128510821649,-1.04611628294192,-8.51013841814316));
#30591=CARTESIAN_POINT('Ctrl Pts',(97.1091498410261,-0.989295292884637,
-8.50351572056958));
#30592=CARTESIAN_POINT('Ctrl Pts',(97.2134379046955,-0.905895424642369,
-8.49501942527079));
#30593=CARTESIAN_POINT('Ctrl Pts',(97.2304261337612,-0.891501552738335,
-8.49358874200812));
#30594=CARTESIAN_POINT('Ctrl Pts',(97.2591285801648,-0.865749810891562,
-8.49107918161947));
#30595=CARTESIAN_POINT('Ctrl Pts',(97.271033824083,-0.854613812469825,-8.49000898352595));
#30596=CARTESIAN_POINT('Ctrl Pts',(97.2879317579071,-0.838136947522117,
-8.48844436315807));
#30597=CARTESIAN_POINT('Ctrl Pts',(97.2931122175869,-0.832990726556178,
-8.48795824783972));
#30598=CARTESIAN_POINT('Ctrl Pts',(97.3021076615307,-0.823886977371597,
-8.48710253898842));
#30599=CARTESIAN_POINT('Ctrl Pts',(97.3059434567362,-0.81995025519821,-8.48673386352082));
#30600=CARTESIAN_POINT('Ctrl Pts',(97.3133466633373,-0.812245075770864,
-8.48601480464279));
#30601=CARTESIAN_POINT('Ctrl Pts',(97.3169170074563,-0.808479601537116,
-8.48566455895368));
#30602=CARTESIAN_POINT('Ctrl Pts',(97.3264192367563,-0.798324469961256,
-8.48472296446376));
#30603=CARTESIAN_POINT('Ctrl Pts',(97.3323051522515,-0.79189243530133,-8.48412970254977));
#30604=CARTESIAN_POINT('Ctrl Pts',(97.354017975294,-0.767629510259118,-8.48190287322368));
#30605=CARTESIAN_POINT('Ctrl Pts',(97.3693727601446,-0.749385759080339,
-8.48025027865178));
#30606=CARTESIAN_POINT('Ctrl Pts',(97.4466517714443,-0.65169560283316,-8.47150611531008));
#30607=CARTESIAN_POINT('Ctrl Pts',(97.4987420384819,-0.565019850578628,
-8.46404776293676));
#30608=CARTESIAN_POINT('Ctrl Pts',(97.5511168404512,-0.445527834110276,
-8.45453284245056));
#30609=CARTESIAN_POINT('Ctrl Pts',(97.5620326663222,-0.417810663962877,
-8.45237863494645));
#30610=CARTESIAN_POINT('Ctrl Pts',(97.5756528823295,-0.378967236935836,
-8.44945613081243));
#30611=CARTESIAN_POINT('Ctrl Pts',(97.5792632684749,-0.36817217512048,-8.44865401945114));
#30612=CARTESIAN_POINT('Ctrl Pts',(97.5852662903431,-0.349318788476043,
-8.44727252384054));
#30613=CARTESIAN_POINT('Ctrl Pts',(97.5877301632562,-0.34128419113304,-8.44668983145004));
#30614=CARTESIAN_POINT('Ctrl Pts',(97.5912254298325,-0.329435249380985,
-8.44584005543365));
#30615=CARTESIAN_POINT('Ctrl Pts',(97.5923239030641,-0.325641202774733,
-8.44556938571883));
#30616=CARTESIAN_POINT('Ctrl Pts',(97.5942293624012,-0.318933750328886,
-8.4450934785937));
#30617=CARTESIAN_POINT('Ctrl Pts',(97.5950442422032,-0.316022683446636,
-8.44488780066328));
#30618=CARTESIAN_POINT('Ctrl Pts',(97.5967931533119,-0.309680931238853,
-8.44444163282195));
#30619=CARTESIAN_POINT('Ctrl Pts',(97.5977228635654,-0.306249136220512,
-8.44420138866213));
#30620=CARTESIAN_POINT('Ctrl Pts',(97.6002524912478,-0.296741255344784,
-8.44353895765058));
#30621=CARTESIAN_POINT('Ctrl Pts',(97.6018193779372,-0.290656388325064,
-8.4431185892707));
#30622=CARTESIAN_POINT('Ctrl Pts',(97.6101275723764,-0.257288717246765,
-8.44083146265122));
#30623=CARTESIAN_POINT('Ctrl Pts',(97.6159399941321,-0.229781476355569,
-8.43901182200827));
#30624=CARTESIAN_POINT('Ctrl Pts',(97.6323279481588,-0.135691566786816,
-8.43292874612855));
#30625=CARTESIAN_POINT('Ctrl Pts',(97.638172637943,-0.0684185474167267,
-8.42881073112888));
#30626=CARTESIAN_POINT('Ctrl Pts',(97.638288928963,0.0670203470091355,-8.42040720520913));
#30627=CARTESIAN_POINT('Ctrl Pts',(97.6324528730179,0.134919763600495,-8.41613413550818));
#30628=CARTESIAN_POINT('Ctrl Pts',(97.6190047976249,0.212193473866689,-8.41098671423547));
#30629=CARTESIAN_POINT('Ctrl Pts',(97.6170827189339,0.222431815812507,-8.41029908822471));
#30630=CARTESIAN_POINT('Ctrl Pts',(97.6136949506509,0.239244388044,-8.40915998524878));
#30631=CARTESIAN_POINT('Ctrl Pts',(97.6123081999403,0.245834073396765,-8.40871098582325));
#30632=CARTESIAN_POINT('Ctrl Pts',(97.6097014358219,0.257714598887316,-8.40789674518727));
#30633=CARTESIAN_POINT('Ctrl Pts',(97.6085011927426,0.263009619749616,-8.40753213777826));
#30634=CARTESIAN_POINT('Ctrl Pts',(97.6058480309298,0.274350083908236,-8.40674748774043));
#30635=CARTESIAN_POINT('Ctrl Pts',(97.6043837704946,0.280392677017655,-8.40632709499444));
#30636=CARTESIAN_POINT('Ctrl Pts',(97.6002437938077,0.296904851152215,-8.40517184912718));
#30637=CARTESIAN_POINT('Ctrl Pts',(97.5974717792407,0.307349428983304,-8.40443395722813));
#30638=CARTESIAN_POINT('Ctrl Pts',(97.5803208595963,0.36856166670961,-8.40006592030178));
#30639=CARTESIAN_POINT('Ctrl Pts',(97.562689114698,0.418347773561824,-8.39633222311502));
#30640=CARTESIAN_POINT('Ctrl Pts',(97.509522427056,0.541509408494223,-8.3866407084649));
#30641=CARTESIAN_POINT('Ctrl Pts',(97.4696048715636,0.6126894090522,-8.38059031032449));
#30642=CARTESIAN_POINT('Ctrl Pts',(97.4050826419625,0.704097088389595,-8.3725078247273));
#30643=CARTESIAN_POINT('Ctrl Pts',(97.3865334626102,0.728321473055659,-8.37033421998128));
#30644=CARTESIAN_POINT('Ctrl Pts',(97.3629628493765,0.75674483211,-8.36776944691956));
#30645=CARTESIAN_POINT('Ctrl Pts',(97.3588221728985,0.761655677787649,-8.36732578461432));
#30646=CARTESIAN_POINT('Ctrl Pts',(97.3523067567127,0.769255912953854,-8.36663864084424));
#30647=CARTESIAN_POINT('Ctrl Pts',(97.3499596327205,0.771968654146624,-8.36639327630558));
#30648=CARTESIAN_POINT('Ctrl Pts',(97.3455951780672,0.776966637785597,-8.36594109026902));
#30649=CARTESIAN_POINT('Ctrl Pts',(97.3435813735682,0.779254769130043,-8.36573403386395));
#30650=CARTESIAN_POINT('Ctrl Pts',(97.3389566729847,0.784468508441572,-8.36526211197091));
#30651=CARTESIAN_POINT('Ctrl Pts',(97.3363400316248,0.787388917153487,-8.36499767366084));
#30652=CARTESIAN_POINT('Ctrl Pts',(97.3281709839798,0.796415203079632,-8.3641798511745));
#30653=CARTESIAN_POINT('Ctrl Pts',(97.3225688064215,0.802475985936705,-8.3636299902638));
#30654=CARTESIAN_POINT('Ctrl Pts',(97.2820552915367,0.845392049097954,-8.35972685056704));
#30655=CARTESIAN_POINT('Ctrl Pts',(97.2448524988876,0.880019713295745,-8.35652509977306));
#30656=CARTESIAN_POINT('Ctrl Pts',(97.1398571894401,0.965780820581755,-8.34808344016331));
#30657=CARTESIAN_POINT('Ctrl Pts',(97.068591409239,1.01216887893699,-8.3429237716438));
#30658=CARTESIAN_POINT('Ctrl Pts',(96.9671112961228,1.06360745098873,-8.33565167848363));
#30659=CARTESIAN_POINT('Ctrl Pts',(96.9407860016459,1.07575181089376,-8.33377362916025));
#30660=CARTESIAN_POINT('Ctrl Pts',(96.9053929096018,1.09052108054632,-8.33124500271943));
#30661=CARTESIAN_POINT('Ctrl Pts',(96.8967020705501,1.09402650998677,-8.33062384178089));
#30662=CARTESIAN_POINT('Ctrl Pts',(96.8824679795996,1.09957122616767,-8.32960563061935));
#30663=CARTESIAN_POINT('Ctrl Pts',(96.8769494743406,1.10167322771075,-8.32921066703086));
#30664=CARTESIAN_POINT('Ctrl Pts',(96.8662633344815,1.10565181803414,-8.32844534035056));
#30665=CARTESIAN_POINT('Ctrl Pts',(96.8610978990314,1.1075339022676,-8.32807517003289));
#30666=CARTESIAN_POINT('Ctrl Pts',(96.8490341189216,1.11183403883277,-8.32721001601538));
#30667=CARTESIAN_POINT('Ctrl Pts',(96.8421261257348,1.11422414740502,-8.32671413318425));
#30668=CARTESIAN_POINT('Ctrl Pts',(96.819701613168,1.12174984229938,-8.32510261706217));
#30669=CARTESIAN_POINT('Ctrl Pts',(96.8041009091444,1.12662658888919,-8.32397868889354));
#30670=CARTESIAN_POINT('Ctrl Pts',(96.7669469884363,1.13739735591256,-8.32129407832577));
#30671=CARTESIAN_POINT('Ctrl Pts',(96.7453181829567,1.14300560672248,-8.31972498347182));
#30672=CARTESIAN_POINT('Ctrl Pts',(96.6605834513324,1.16242257878544,-8.31355345120968));
#30673=CARTESIAN_POINT('Ctrl Pts',(96.5965489616525,1.17164459404734,-8.30882966436784));
#30674=CARTESIAN_POINT('Ctrl Pts',(96.4691981810892,1.17940197167777,-8.29946576974513));
#30675=CARTESIAN_POINT('Ctrl Pts',(96.4060950144904,1.17818025902253,-8.29484277039885));
#30676=CARTESIAN_POINT('Ctrl Pts',(96.3334283030631,1.1709196655273,-8.28972179981462));
#30677=CARTESIAN_POINT('Ctrl Pts',(96.323481788128,1.16979762540815,-8.28902543102294));
#30678=CARTESIAN_POINT('Ctrl Pts',(96.3096438828062,1.1680576800051,-8.28806409847642));
#30679=CARTESIAN_POINT('Ctrl Pts',(96.305739797882,1.16754689054268,-8.28779370987133));
#30680=CARTESIAN_POINT('Ctrl Pts',(96.2990073946744,1.16663169662121,-8.28732895804583));
#30681=CARTESIAN_POINT('Ctrl Pts',(96.2961778819051,1.16623656557837,-8.28713409497307));
#30682=CARTESIAN_POINT('Ctrl Pts',(96.2902091667988,1.16538090286236,-8.28672406049733));
#30683=CARTESIAN_POINT('Ctrl Pts',(96.2870703361303,1.16491797494558,-8.28650903003984));
#30684=CARTESIAN_POINT('Ctrl Pts',(96.279282138397,1.16373716305372,-8.28597688976864));
#30685=CARTESIAN_POINT('Ctrl Pts',(96.2746350666321,1.16300408576626,-8.28566061379496));
#30686=CARTESIAN_POINT('Ctrl Pts',(96.2570975170206,1.1601297284631,-8.28447129234524));
#30687=CARTESIAN_POINT('Ctrl Pts',(96.2442380221496,1.15780172687388,-8.2836079439286));
#30688=CARTESIAN_POINT('Ctrl Pts',(96.211281539951,1.1512672099253,-8.28141164209038));
#30689=CARTESIAN_POINT('Ctrl Pts',(96.1912504127016,1.1467482515924,-8.28009239301039));
#30690=CARTESIAN_POINT('Ctrl Pts',(96.1153409310211,1.1275243779895,-8.27511812391382));
#30691=CARTESIAN_POINT('Ctrl Pts',(96.0604515700358,1.10923854495724,-8.2715706463311));
#30692=CARTESIAN_POINT('Ctrl Pts',(95.9781481430738,1.07491196548991,-8.26604898326986));
#30693=CARTESIAN_POINT('Ctrl Pts',(95.9496855826237,1.06168091221913,-8.26410025730001));
#30694=CARTESIAN_POINT('Ctrl Pts',(95.9218015205746,1.04733926464621,-8.26212858994183));
#30695=CARTESIAN_POINT('',(97.6382305443328,0.000598681062270171,-8.32477232136367));
#30696=CARTESIAN_POINT('Ctrl Pts',(95.9218018246467,1.04733942103997,-8.16230712347374));
#30697=CARTESIAN_POINT('Ctrl Pts',(95.9376213785056,1.05547590789257,-8.16342335775821));
#30698=CARTESIAN_POINT('Ctrl Pts',(95.9536330940809,1.06325799827498,-8.16454713565674));
#30699=CARTESIAN_POINT('Ctrl Pts',(95.9993064571837,1.08418854436589,-8.1677457616158));
#30700=CARTESIAN_POINT('Ctrl Pts',(96.0293304725305,1.09647420555693,-8.16984076206555));
#30701=CARTESIAN_POINT('Ctrl Pts',(96.0689874993574,1.11082084931101,-8.17261895661093));
#30702=CARTESIAN_POINT('Ctrl Pts',(96.0781944250211,1.11402292821804,-8.17326466054049));
#30703=CARTESIAN_POINT('Ctrl Pts',(96.0931184993395,1.11900658447433,-8.17431296398046));
#30704=CARTESIAN_POINT('Ctrl Pts',(96.0988114706818,1.12085953256381,-8.17471323324801));
#30705=CARTESIAN_POINT('Ctrl Pts',(96.1097329183442,1.12432237715949,-8.17548195875513));
#30706=CARTESIAN_POINT('Ctrl Pts',(96.1149589818321,1.12593941101157,-8.17585017235612));
#30707=CARTESIAN_POINT('Ctrl Pts',(96.1270159411701,1.12957819471921,-8.17670061075007));
#30708=CARTESIAN_POINT('Ctrl Pts',(96.1338542365482,1.13157447668932,-8.17718364132761));
#30709=CARTESIAN_POINT('Ctrl Pts',(96.1554494191646,1.13766663184967,-8.17871144984711));
#30710=CARTESIAN_POINT('Ctrl Pts',(96.1702678110726,1.14153663793594,-8.17976336547231));
#30711=CARTESIAN_POINT('Ctrl Pts',(96.2051113702321,1.14991418852876,-8.18224621418645));
#30712=CARTESIAN_POINT('Ctrl Pts',(96.2251867630577,1.15418924843768,-8.18368395328458));
#30713=CARTESIAN_POINT('Ctrl Pts',(96.2999933746522,1.1680866102826,-8.18906859257534));
#30714=CARTESIAN_POINT('Ctrl Pts',(96.3552681436596,1.17435583488003,-8.19310523061123));
#30715=CARTESIAN_POINT('Ctrl Pts',(96.4868476555972,1.17991420171222,-8.2027574443861));
#30716=CARTESIAN_POINT('Ctrl Pts',(96.5630604304775,1.17574320280996,-8.20838698803029));
#30717=CARTESIAN_POINT('Ctrl Pts',(96.6477295567153,1.16280832750164,-8.21438606753708));
#30718=CARTESIAN_POINT('Ctrl Pts',(96.6570998995637,1.1612606297152,-8.21504621847737));
#30719=CARTESIAN_POINT('Ctrl Pts',(96.6702417737039,1.15892634951521,-8.21596583650769));
#30720=CARTESIAN_POINT('Ctrl Pts',(96.6740294316017,1.15823440365383,-8.2162301506444));
#30721=CARTESIAN_POINT('Ctrl Pts',(96.6808769345714,1.15694873980231,-8.21670658284306));
#30722=CARTESIAN_POINT('Ctrl Pts',(96.6839379406715,1.15636142735559,-8.2169190496742));
#30723=CARTESIAN_POINT('Ctrl Pts',(96.6902045659298,1.15513324279914,-8.21735292706584));
#30724=CARTESIAN_POINT('Ctrl Pts',(96.6934099036018,1.15449116565154,-8.21757426899638));
#30725=CARTESIAN_POINT('Ctrl Pts',(96.701660562451,1.15280267445468,-8.21814260448124));
#30726=CARTESIAN_POINT('Ctrl Pts',(96.706701830934,1.15173646808278,-8.21848850757027));
#30727=CARTESIAN_POINT('Ctrl Pts',(96.7280597979011,1.14707270586781,-8.21994883013858));
#30728=CARTESIAN_POINT('Ctrl Pts',(96.7443068691964,1.14316103401756,-8.22104695234132));
#30729=CARTESIAN_POINT('Ctrl Pts',(96.7886996680762,1.13146805901097,-8.22402604699274));
#30730=CARTESIAN_POINT('Ctrl Pts',(96.8166489027617,1.12298358140763,-8.22587789398752));
#30731=CARTESIAN_POINT('Ctrl Pts',(96.9310258042014,1.08356174976196,-8.23346407644181));
#30732=CARTESIAN_POINT('Ctrl Pts',(97.014000519188,1.04361631120548,-8.23901238498897));
#30733=CARTESIAN_POINT('Ctrl Pts',(97.1181634727909,0.977520428472241,-8.24687328584309));
#30734=CARTESIAN_POINT('Ctrl Pts',(97.144136534596,0.959534916780235,-8.24891487487024));
#30735=CARTESIAN_POINT('Ctrl Pts',(97.1770996325259,0.934690752812255,-8.25163438835768));
#30736=CARTESIAN_POINT('Ctrl Pts',(97.1847727488286,0.928757514339493,-8.25227694135909));
#30737=CARTESIAN_POINT('Ctrl Pts',(97.1970538391894,0.91901640792623,-8.25332137609325));
#30738=CARTESIAN_POINT('Ctrl Pts',(97.201707743476,0.915266965168827,-8.25372095942066));
#30739=CARTESIAN_POINT('Ctrl Pts',(97.2103866369195,0.908165160879373,-8.25447340853585));
#30740=CARTESIAN_POINT('Ctrl Pts',(97.21441820407,0.904821039825654,-8.25482593955127));
#30741=CARTESIAN_POINT('Ctrl Pts',(97.2184747229205,0.901410287225249,-8.255183740089));
#30742=CARTESIAN_POINT('Ctrl Pts',(97.2185221684086,0.901370388295164,-8.255187925393));
#30743=CARTESIAN_POINT('Ctrl Pts',(97.2186131797962,0.9012938406779,-8.25519595459592));
#30744=CARTESIAN_POINT('Ctrl Pts',(97.2186567461433,0.901257192616039,-8.25519979846698));
#30745=CARTESIAN_POINT('Ctrl Pts',(97.2187403893975,0.901186821456293,-8.25520717903109));
#30746=CARTESIAN_POINT('Ctrl Pts',(97.218780466728,0.90115309883054,-8.25521071570583));
#30747=CARTESIAN_POINT('Ctrl Pts',(97.2240497492897,0.896718718985027,-8.2556757505796));
#30748=CARTESIAN_POINT('Ctrl Pts',(97.2292404544705,0.892272712292352,-8.25613907959916));
#30749=CARTESIAN_POINT('Ctrl Pts',(97.2401289638164,0.882780810148187,-8.2571222766092));
#30750=CARTESIAN_POINT('Ctrl Pts',(97.2458171210067,0.877724374734772,-8.25764256447768));
#30751=CARTESIAN_POINT('Ctrl Pts',(97.2608102664443,0.864133932322353,-8.25903203219213));
#30752=CARTESIAN_POINT('Ctrl Pts',(97.2700274946725,0.855505019569865,-8.25990509755621));
#30753=CARTESIAN_POINT('Ctrl Pts',(97.2980199134487,0.828441799380065,-8.2626162295607));
#30754=CARTESIAN_POINT('Ctrl Pts',(97.3163164459866,0.809526254503011,-8.26447381892073));
#30755=CARTESIAN_POINT('Ctrl Pts',(97.3953994078684,0.722087977457959,-8.27289646660675));
#30756=CARTESIAN_POINT('Ctrl Pts',(97.4486996239311,0.64722820615961,-8.27970909160612));
#30757=CARTESIAN_POINT('Ctrl Pts',(97.5093456169397,0.536807066780993,-8.28884125681446));
#30758=CARTESIAN_POINT('Ctrl Pts',(97.5245813818428,0.505934456595152,-8.29130250206012));
#30759=CARTESIAN_POINT('Ctrl Pts',(97.5408830509369,0.468895515912719,-8.29411514053513));
#30760=CARTESIAN_POINT('Ctrl Pts',(97.5432788478144,0.46333618560343,-8.2945336730474));
#30761=CARTESIAN_POINT('Ctrl Pts',(97.5471175739887,0.454236197606946,-8.29521257879922));
#30762=CARTESIAN_POINT('Ctrl Pts',(97.5485862794652,0.450706632784188,-8.2954743957543));
#30763=CARTESIAN_POINT('Ctrl Pts',(97.5511927632089,0.444355775744889,-8.29594271117344));
#30764=CARTESIAN_POINT('Ctrl Pts',(97.5523368172484,0.441537179297196,-8.29614957184232));
#30765=CARTESIAN_POINT('Ctrl Pts',(97.5548348966612,0.43531359645602,-8.29660416233487));
#30766=CARTESIAN_POINT('Ctrl Pts',(97.5561839592968,0.431906707707123,-8.29685159916921));
#30767=CARTESIAN_POINT('Ctrl Pts',(97.5600532922032,0.422000377830806,-8.29756714038691));
#30768=CARTESIAN_POINT('Ctrl Pts',(97.5625318400079,0.415484652260095,-8.29803287268604));
#30769=CARTESIAN_POINT('Ctrl Pts',(97.5833160763188,0.359351239590522,-8.30200638201027));
#30770=CARTESIAN_POINT('Ctrl Pts',(97.5983207980556,0.30856770415855,-8.30534320794276));
#30771=CARTESIAN_POINT('Ctrl Pts',(97.628674876271,0.172784145315577,-8.31400656589799));
#30772=CARTESIAN_POINT('Ctrl Pts',(97.6381868702256,0.0868239361698437,
-8.31925247929609));
#30773=CARTESIAN_POINT('Ctrl Pts',(97.6382307967427,0.000600001017636307,
-8.32477179780212));
#30774=CARTESIAN_POINT('Ctrl Pts',(97.6382307974286,0.000598653194140394,
-8.32477188407827));
#30775=CARTESIAN_POINT('Ctrl Pts',(97.6382392206163,-0.0159725571986599,
-8.32583263163235));
#30776=CARTESIAN_POINT('Ctrl Pts',(97.6378979026431,-0.0325416332374212,
-8.32690186388278));
#30777=CARTESIAN_POINT('Ctrl Pts',(97.6367128128061,-0.0609447856470732,
-8.32875333490612));
#30778=CARTESIAN_POINT('Ctrl Pts',(97.6360396297213,-0.0727834900835447,
-8.32953058173302));
#30779=CARTESIAN_POINT('Ctrl Pts',(97.6347089373993,-0.0912586028483084,
-8.33075321158656));
#30780=CARTESIAN_POINT('Ctrl Pts',(97.6341736078574,-0.0979032219807065,
-8.33119489236586));
#30781=CARTESIAN_POINT('Ctrl Pts',(97.633116109985,-0.109769667460043,-8.33198735939884));
#30782=CARTESIAN_POINT('Ctrl Pts',(97.6326153903691,-0.114993262975679,
-8.33233747966645));
#30783=CARTESIAN_POINT('Ctrl Pts',(97.6315356383286,-0.1255165293268,-8.33304548240145));
#30784=CARTESIAN_POINT('Ctrl Pts',(97.6309554970805,-0.130815959395499,
-8.33340339119062));
#30785=CARTESIAN_POINT('Ctrl Pts',(97.6296324605646,-0.142187290451245,
-8.33417439734584));
#30786=CARTESIAN_POINT('Ctrl Pts',(97.628878201172,-0.148257685264711,-8.33458783818055));
#30787=CARTESIAN_POINT('Ctrl Pts',(97.6267212323564,-0.164577266213844,
-8.33570445639677));
#30788=CARTESIAN_POINT('Ctrl Pts',(97.6252307472846,-0.174814103076982,
-8.33641034116554));
#30789=CARTESIAN_POINT('Ctrl Pts',(97.6176480683421,-0.222479970214684,
-8.33972357386405));
#30790=CARTESIAN_POINT('Ctrl Pts',(97.6098858946794,-0.259616637683789,
-8.34238221654071));
#30791=CARTESIAN_POINT('Ctrl Pts',(97.5750158959795,-0.393756554545006,
-8.35227324131233));
#30792=CARTESIAN_POINT('Ctrl Pts',(97.5372986198312,-0.487536874375286,
-8.35979328114584));
#30793=CARTESIAN_POINT('Ctrl Pts',(97.4790480813285,-0.591574945361573,
-8.36837896019924));
#30794=CARTESIAN_POINT('Ctrl Pts',(97.4695933649293,-0.607562448508005,
-8.36970418491041));
#30795=CARTESIAN_POINT('Ctrl Pts',(97.4533341308031,-0.633628616101496,
-8.37186705020228));
#30796=CARTESIAN_POINT('Ctrl Pts',(97.4467448336499,-0.643837124172231,
-8.37271467999996));
#30797=CARTESIAN_POINT('Ctrl Pts',(97.4374587663522,-0.657746401694128,
-8.37386847899008));
#30798=CARTESIAN_POINT('Ctrl Pts',(97.4348969081134,-0.661535732143874,
-8.37418269431734));
#30799=CARTESIAN_POINT('Ctrl Pts',(97.4305356649558,-0.667906288813469,
-8.37471062264048));
#30800=CARTESIAN_POINT('Ctrl Pts',(97.428747911615,-0.670495378472053,-8.37492508866309));
#30801=CARTESIAN_POINT('Ctrl Pts',(97.4253024255865,-0.675442736868094,
-8.37533467902837));
#30802=CARTESIAN_POINT('Ctrl Pts',(97.4236463876081,-0.677802117725618,
-8.37552991785086));
#30803=CARTESIAN_POINT('Ctrl Pts',(97.4191879243562,-0.684104817828945,
-8.37605128460905));
#30804=CARTESIAN_POINT('Ctrl Pts',(97.4163697997968,-0.688037043567038,
-8.37637637124131));
#30805=CARTESIAN_POINT('Ctrl Pts',(97.405903430926,-0.702452693990141,-8.37756789149714));
#30806=CARTESIAN_POINT('Ctrl Pts',(97.3981059801271,-0.712827322481144,
-8.37842490051302));
#30807=CARTESIAN_POINT('Ctrl Pts',(97.3204164942796,-0.812713158967548,
-8.38669419186976));
#30808=CARTESIAN_POINT('Ctrl Pts',(97.238088213149,-0.891810683197873,-8.39343675762738));
#30809=CARTESIAN_POINT('Ctrl Pts',(97.1228414963137,-0.974250060021788,
-8.40237357785148));
#30810=CARTESIAN_POINT('Ctrl Pts',(97.0994104536838,-0.989774516967249,
-8.40416523485624));
#30811=CARTESIAN_POINT('Ctrl Pts',(97.0641821565468,-1.0113428722489,-8.40684059241589));
#30812=CARTESIAN_POINT('Ctrl Pts',(97.0528015696989,-1.01805000561974,-8.40770211824817));
#30813=CARTESIAN_POINT('Ctrl Pts',(97.0319632719575,-1.02986332979704,-8.40927642913202));
#30814=CARTESIAN_POINT('Ctrl Pts',(97.0225438004328,-1.03503423231993,-8.4099869085273));
#30815=CARTESIAN_POINT('Ctrl Pts',(97.0076350180766,-1.04295501235957,-8.41111031068038));
#30816=CARTESIAN_POINT('Ctrl Pts',(97.0021925532073,-1.04579217274279,-8.41152017771205));
#30817=CARTESIAN_POINT('Ctrl Pts',(96.9966573556901,-1.04862287328072,-8.41193686312558));
#30818=CARTESIAN_POINT('Ctrl Pts',(96.9965864609357,-1.04865911979573,-8.41194220000072));
#30819=CARTESIAN_POINT('Ctrl Pts',(96.9964209083942,-1.04874374102696,-8.41195466254078));
#30820=CARTESIAN_POINT('Ctrl Pts',(96.9963262477872,-1.0487921100896,-8.41196178839662));
#30821=CARTESIAN_POINT('Ctrl Pts',(96.9961053615563,-1.0489049393915,-8.41197841614494));
#30822=CARTESIAN_POINT('Ctrl Pts',(96.9959791307749,-1.04896938969725,-8.41198791838805));
#30823=CARTESIAN_POINT('Ctrl Pts',(96.9956848752093,-1.04911956233236,-8.41201006879238));
#30824=CARTESIAN_POINT('Ctrl Pts',(96.9955168415815,-1.04920526702239,-8.41202271755359));
#30825=CARTESIAN_POINT('Ctrl Pts',(96.9908003906001,-1.05160944098781,-8.41237774505554));
#30826=CARTESIAN_POINT('Ctrl Pts',(96.9862370290952,-1.05389832021191,-8.41272114002119));
#30827=CARTESIAN_POINT('Ctrl Pts',(96.9756273597883,-1.059133833904,-8.41351934926885));
#30828=CARTESIAN_POINT('Ctrl Pts',(96.9695704528358,-1.06205846190355,-8.4139749066734));
#30829=CARTESIAN_POINT('Ctrl Pts',(96.9540926268301,-1.06936923610807,-8.41513887929156));
#30830=CARTESIAN_POINT('Ctrl Pts',(96.9446382613142,-1.0736827914018,-8.41584972703787));
#30831=CARTESIAN_POINT('Ctrl Pts',(96.8660674157879,-1.10828197788786,-8.42175754354924));
#30832=CARTESIAN_POINT('Ctrl Pts',(96.7942566176936,-1.13198023258078,-8.42717612754659));
#30833=CARTESIAN_POINT('Ctrl Pts',(96.6642970988846,-1.16142022136874,-8.43692382029308));
#30834=CARTESIAN_POINT('Ctrl Pts',(96.6070433823238,-1.17002463992289,-8.44119411273427));
#30835=CARTESIAN_POINT('Ctrl Pts',(96.52895620662,-1.17593625296761,-8.44684903970999));
#30836=CARTESIAN_POINT('Ctrl Pts',(96.508485818296,-1.17694968628901,-8.44831532663428));
#30837=CARTESIAN_POINT('Ctrl Pts',(96.4749530420315,-1.17773337046574,-8.45068086426726));
#30838=CARTESIAN_POINT('Ctrl Pts',(96.4619029600606,-1.1778214408856,-8.45159244455721));
#30839=CARTESIAN_POINT('Ctrl Pts',(96.4441520343127,-1.17764618392891,-8.45281779036776));
#30840=CARTESIAN_POINT('Ctrl Pts',(96.43945083449,-1.17757161316871,-8.45314092004508));
#30841=CARTESIAN_POINT('Ctrl Pts',(96.4315789125318,-1.17739959063944,-8.45367951175966));
#30842=CARTESIAN_POINT('Ctrl Pts',(96.4284079498098,-1.17731747937758,-8.45389579472045));
#30843=CARTESIAN_POINT('Ctrl Pts',(96.4223814925994,-1.1771370594775,-8.45430551774925));
#30844=CARTESIAN_POINT('Ctrl Pts',(96.4195259719922,-1.1770411699135,-8.45449909343269));
#30845=CARTESIAN_POINT('Ctrl Pts',(96.4127349759271,-1.176788382249,-8.45495817417184));
#30846=CARTESIAN_POINT('Ctrl Pts',(96.4087998515414,-1.17662213127505,-8.45522317070103));
#30847=CARTESIAN_POINT('Ctrl Pts',(96.3948590583756,-1.17596308779483,-8.45615857024002));
#30848=CARTESIAN_POINT('Ctrl Pts',(96.384858585929,-1.17536236578321,-8.45682338843237));
#30849=CARTESIAN_POINT('Ctrl Pts',(96.3155119626332,-1.17030796927137,-8.46139799979149));
#30850=CARTESIAN_POINT('Ctrl Pts',(96.2565625723474,-1.16148864254912,-8.46510876878153));
#30851=CARTESIAN_POINT('Ctrl Pts',(96.1330059625051,-1.13330116666639,-8.47296146268175));
#30852=CARTESIAN_POINT('Ctrl Pts',(96.068888917809,-1.11277423120893,-8.47708672042868));
#30853=CARTESIAN_POINT('Ctrl Pts',(95.9751094120417,-1.07363599069651,-8.48354641586234));
#30854=CARTESIAN_POINT('Ctrl Pts',(95.9439442028268,-1.05899443342629,-8.48576789680546));
#30855=CARTESIAN_POINT('Ctrl Pts',(95.9049702986871,-1.03855429685316,-8.48866806842902));
#30856=CARTESIAN_POINT('Ctrl Pts',(95.8965287162861,-1.03399467135022,-8.48930376882515));
#30857=CARTESIAN_POINT('Ctrl Pts',(95.8829407577058,-1.02643939570379,-8.4903397920286));
#30858=CARTESIAN_POINT('Ctrl Pts',(95.8777596271705,-1.02350689518473,-8.49073788508202));
#30859=CARTESIAN_POINT('Ctrl Pts',(95.8678521795802,-1.01779970449294,-8.49150513188693));
#30860=CARTESIAN_POINT('Ctrl Pts',(95.8631225493015,-1.01503105241784,-8.49187406296975));
#30861=CARTESIAN_POINT('Ctrl Pts',(95.8523325665774,-1.00861323100451,-8.49272194315122));
#30862=CARTESIAN_POINT('Ctrl Pts',(95.8462854736071,-1.00494229636424,-8.49320166622082));
#30863=CARTESIAN_POINT('Ctrl Pts',(95.8271264802143,-0.99307416147238,-8.49473635058312));
#30864=CARTESIAN_POINT('Ctrl Pts',(95.814143246543,-0.984673401847484,-8.49579865488929));
#30865=CARTESIAN_POINT('Ctrl Pts',(95.7352913549769,-0.931421076440506,
-8.50239248583097));
#30866=CARTESIAN_POINT('Ctrl Pts',(95.6739613913848,-0.880243095976197,
-8.50816324845082));
#30867=CARTESIAN_POINT('Ctrl Pts',(95.5858991665516,-0.790156366322242,
-8.5174029828112));
#30868=CARTESIAN_POINT('Ctrl Pts',(95.5555031009311,-0.755152790578475,
-8.52081160964979));
#30869=CARTESIAN_POINT('Ctrl Pts',(95.5143762584434,-0.701730808254361,
-8.5256841105564));
#30870=CARTESIAN_POINT('Ctrl Pts',(95.5019564887557,-0.684668663603472,
-8.52719514758669));
#30871=CARTESIAN_POINT('Ctrl Pts',(95.4824510421254,-0.656300345233046,
-8.52962437156156));
#30872=CARTESIAN_POINT('Ctrl Pts',(95.4750874342494,-0.645191677327805,
-8.5305556744556));
#30873=CARTESIAN_POINT('Ctrl Pts',(95.4653624018703,-0.629965555754765,
-8.53180296083662));
#30874=CARTESIAN_POINT('Ctrl Pts',(95.4628352965825,-0.625955811873396,
-8.53212873354624));
#30875=CARTESIAN_POINT('Ctrl Pts',(95.4586532710032,-0.61923055156973,-8.5326705009611));
#30876=CARTESIAN_POINT('Ctrl Pts',(95.4569850417627,-0.61652342802353,-8.53288733689324));
#30877=CARTESIAN_POINT('Ctrl Pts',(95.4538422470899,-0.611376896545914,
-8.53329716717314));
#30878=CARTESIAN_POINT('Ctrl Pts',(95.4523655440753,-0.608938844717003,
-8.53349030313241));
#30879=CARTESIAN_POINT('Ctrl Pts',(95.4488832289914,-0.603142119974017,
-8.53394716861775));
#30880=CARTESIAN_POINT('Ctrl Pts',(95.4468854549054,-0.59977874207513,-8.53421040115479));
#30881=CARTESIAN_POINT('Ctrl Pts',(95.4399124979376,-0.587904987854958,
-8.53513342793279));
#30882=CARTESIAN_POINT('Ctrl Pts',(95.4350272745504,-0.579341881095869,
-8.53578782797955));
#30883=CARTESIAN_POINT('Ctrl Pts',(95.3967842589272,-0.510307554410845,
-8.54098224062719));
#30884=CARTESIAN_POINT('Ctrl Pts',(95.36869213472,-0.44706180687142,-8.54525141769817));
#30885=CARTESIAN_POINT('Ctrl Pts',(95.3449414061817,-0.37773568272148,-8.5497847485548));
#30886=CARTESIAN_POINT('Ctrl Pts',(95.34360083012,-0.373753284475691,-8.55004464719236));
#30887=CARTESIAN_POINT('Ctrl Pts',(95.3243124592721,-0.315423496565407,
-8.55384477511811));
#30888=CARTESIAN_POINT('Ctrl Pts',(95.310329465387,-0.259849444097576,-8.55738671506793));
#30889=CARTESIAN_POINT('Ctrl Pts',(95.2968346320253,-0.182915999438662,
-8.56236816534095));
#30890=CARTESIAN_POINT('Ctrl Pts',(95.2937749494476,-0.162259198428188,
-8.56371265947386));
#30891=CARTESIAN_POINT('Ctrl Pts',(95.2894011079331,-0.1261265244011,-8.56608435046378));
#30892=CARTESIAN_POINT('Ctrl Pts',(95.287840940841,-0.110685451145692,-8.56710414537149));
#30893=CARTESIAN_POINT('Ctrl Pts',(95.286007407231,-0.0880808904912756,
-8.56860826421662));
#30894=CARTESIAN_POINT('Ctrl Pts',(95.2854935643887,-0.0809381603499936,
-8.5690851717157));
#30895=CARTESIAN_POINT('Ctrl Pts',(95.284701828785,-0.068326452183756,-8.56993030137004));
#30896=CARTESIAN_POINT('Ctrl Pts',(95.284396876667,-0.0628593404331867,
-8.57029767646876));
#30897=CARTESIAN_POINT('Ctrl Pts',(95.2838391923939,-0.0514282886749231,
-8.57106802598894));
#30898=CARTESIAN_POINT('Ctrl Pts',(95.2835936565079,-0.0454641702217535,
-8.57147121209585));
#30899=CARTESIAN_POINT('Ctrl Pts',(95.2830692914335,-0.0298376782038799,
-8.57253101724502));
#30900=CARTESIAN_POINT('Ctrl Pts',(95.2828640671068,-0.0201734537291122,
-8.5731898848881));
#30901=CARTESIAN_POINT('Ctrl Pts',(95.2824952750901,0.0211594125294026,
-8.57602314687485));
#30902=CARTESIAN_POINT('Ctrl Pts',(95.2834901153434,0.0528225255822563,
-8.57823261008795));
#30903=CARTESIAN_POINT('Ctrl Pts',(95.2923559830223,0.176215314340497,-8.5870009905925));
#30904=CARTESIAN_POINT('Ctrl Pts',(95.3096931054212,0.266928711875819,-8.59382194027456));
#30905=CARTESIAN_POINT('Ctrl Pts',(95.3461421143299,0.382342066056478,-8.60264342910261));
#30906=CARTESIAN_POINT('Ctrl Pts',(95.3558972987908,0.40967264824717,-8.60474035401363));
#30907=CARTESIAN_POINT('Ctrl Pts',(95.3728194965996,0.452066766911041,-8.60797972913013));
#30908=CARTESIAN_POINT('Ctrl Pts',(95.3793136272116,0.467385375310766,-8.60914736039707));
#30909=CARTESIAN_POINT('Ctrl Pts',(95.3882384258373,0.487255065858787,-8.61065350251444));
#30910=CARTESIAN_POINT('Ctrl Pts',(95.3903770900645,0.491934204160688,-8.6110075659273));
#30911=CARTESIAN_POINT('Ctrl Pts',(95.3939240041136,0.499561827048202,-8.61158354419316));
#30912=CARTESIAN_POINT('Ctrl Pts',(95.3953139559845,0.502518669685959,-8.61180652669242));
#30913=CARTESIAN_POINT('Ctrl Pts',(95.398054403159,0.508285960691424,-8.61224081945136));
#30914=CARTESIAN_POINT('Ctrl Pts',(95.3994037794112,0.511096882861558,-8.61245219050216));
#30915=CARTESIAN_POINT('Ctrl Pts',(95.402446304048,0.517370863497887,-8.61292337208669));
#30916=CARTESIAN_POINT('Ctrl Pts',(95.4041453393494,0.520831067755723,-8.61318282702259));
#30917=CARTESIAN_POINT('Ctrl Pts',(95.4101003838315,0.532809917757184,-8.61407982287164));
#30918=CARTESIAN_POINT('Ctrl Pts',(95.4144428308351,0.541285515805737,-8.61471235892664));
#30919=CARTESIAN_POINT('Ctrl Pts',(95.4542031382021,0.616623835850128,-8.62032407155302));
#30920=CARTESIAN_POINT('Ctrl Pts',(95.4958900581477,0.67999095751371,-8.62497471224905));
#30921=CARTESIAN_POINT('Ctrl Pts',(95.5784303611809,0.782434427210256,-8.63311283983266));
#30922=CARTESIAN_POINT('Ctrl Pts',(95.6165353063062,0.823390541596666,-8.63657465287442));
#30923=CARTESIAN_POINT('Ctrl Pts',(95.6724613362659,0.875525040333735,-8.64145330767545));
#30924=CARTESIAN_POINT('Ctrl Pts',(95.6878870509317,0.889166801479525,-8.64277972748967));
#30925=CARTESIAN_POINT('Ctrl Pts',(95.7154252675029,0.912262466272874,-8.64512239240248));
#30926=CARTESIAN_POINT('Ctrl Pts',(95.7273801088304,0.921896902424378,-8.64613148934295));
#30927=CARTESIAN_POINT('Ctrl Pts',(95.7451580267079,0.935659674561807,-8.64762274174136));
#30928=CARTESIAN_POINT('Ctrl Pts',(95.7508360468243,0.939973413900392,-8.64809766340276));
#30929=CARTESIAN_POINT('Ctrl Pts',(95.7609394249046,0.947505490666184,-8.64894053586588));
#30930=CARTESIAN_POINT('Ctrl Pts',(95.7653487345696,0.950745077042163,-8.6493076548794));
#30931=CARTESIAN_POINT('Ctrl Pts',(95.7746269416008,0.957462868727021,-8.65007873618765));
#30932=CARTESIAN_POINT('Ctrl Pts',(95.7795000809177,0.960934919487381,-8.65048291868082));
#30933=CARTESIAN_POINT('Ctrl Pts',(95.7923683063355,0.969956325422524,-8.65154823968423));
#30934=CARTESIAN_POINT('Ctrl Pts',(95.8004059495252,0.975443879336585,-8.65221166985895));
#30935=CARTESIAN_POINT('Ctrl Pts',(95.8353978852335,0.998703449836975,-8.65509214989827));
#30936=CARTESIAN_POINT('Ctrl Pts',(95.8630063518476,1.01546106633469,-8.65734573735509));
#30937=CARTESIAN_POINT('Ctrl Pts',(95.9013687031556,1.0366396328609,-8.66045379444873));
#30938=CARTESIAN_POINT('Ctrl Pts',(95.9115484421861,1.04206578788199,-8.6612763282379));
#30939=CARTESIAN_POINT('Ctrl Pts',(95.921801762405,1.04733938902713,-8.66210246100831));
#30940=CARTESIAN_POINT('Origin',(96.460480949577,-7.19464945638997E-16,
0.924367114736168));
#30941=CARTESIAN_POINT('',(95.9218016185417,1.04733931503377,-9.26219012624909));
#30942=CARTESIAN_POINT('',(95.9218016730733,1.04733934308104,-9.16391269549479));
#30943=CARTESIAN_POINT('',(95.9218016730721,1.04733934308042,0.924367114736168));
#30944=CARTESIAN_POINT('',(97.6382311976804,0.000311627330674785,-8.92336529225763));
#30945=CARTESIAN_POINT('Ctrl Pts',(95.9218016185417,1.04733931503376,-9.26219012624909));
#30946=CARTESIAN_POINT('Ctrl Pts',(95.8332784251477,1.00180907100097,-9.25501416132673));
#30947=CARTESIAN_POINT('Ctrl Pts',(95.7508631399599,0.945229306744171,-9.24755876670025));
#30948=CARTESIAN_POINT('Ctrl Pts',(95.6635171965987,0.86732228481971,-9.23923800564499));
#30949=CARTESIAN_POINT('Ctrl Pts',(95.6507616381096,0.855426142460901,-9.23801205511989));
#30950=CARTESIAN_POINT('Ctrl Pts',(95.6343871797205,0.83946031424405,-9.23642906382491));
#30951=CARTESIAN_POINT('Ctrl Pts',(95.6305263087149,0.835643364573313,-9.23605512220094));
#30952=CARTESIAN_POINT('Ctrl Pts',(95.6243399411904,0.829442201897154,-9.23545502250654));
#30953=CARTESIAN_POINT('Ctrl Pts',(95.6219979779109,0.827074639387784,-9.23522762682557));
#30954=CARTESIAN_POINT('Ctrl Pts',(95.6174828636359,0.822471282382071,-9.23478886182069));
#30955=CARTESIAN_POINT('Ctrl Pts',(95.6153085170151,0.820236760164353,-9.23457740587272));
#30956=CARTESIAN_POINT('Ctrl Pts',(95.610071736312,0.814812117809688,-9.2340676684695));
#30957=CARTESIAN_POINT('Ctrl Pts',(95.6070183058351,0.811613291314616,-9.23377006855282));
#30958=CARTESIAN_POINT('Ctrl Pts',(95.5963341544147,0.800293417965915,-9.23272705236595));
#30959=CARTESIAN_POINT('Ctrl Pts',(95.5888004600422,0.792081046873416,-9.23198851643698));
#30960=CARTESIAN_POINT('Ctrl Pts',(95.5703933134886,0.771434918124074,-9.23017257084104));
#30961=CARTESIAN_POINT('Ctrl Pts',(95.5596624405256,0.758876738002787,-9.22910360267678));
#30962=CARTESIAN_POINT('Ctrl Pts',(95.5142318550548,0.70338781346771,-9.22451117616927));
#30963=CARTESIAN_POINT('Ctrl Pts',(95.4823079087213,0.658270608994931,-9.22110546872755));
#30964=CARTESIAN_POINT('Ctrl Pts',(95.4130661535855,0.544187317139664,-9.21285082608394));
#30965=CARTESIAN_POINT('Ctrl Pts',(95.3792394750312,0.473426349609431,-9.20800302113732));
#30966=CARTESIAN_POINT('Ctrl Pts',(95.3474189686693,0.385263793617961,-9.20189512861979));
#30967=CARTESIAN_POINT('Ctrl Pts',(95.342446799899,0.370587058396515,-9.20087685596749));
#30968=CARTESIAN_POINT('Ctrl Pts',(95.3356267486446,0.349067642520101,-9.19937964886737));
#30969=CARTESIAN_POINT('Ctrl Pts',(95.3335486392436,0.342299220968954,-9.19890814633734));
#30970=CARTESIAN_POINT('Ctrl Pts',(95.3299701140216,0.330258023865242,-9.19806809013768));
#30971=CARTESIAN_POINT('Ctrl Pts',(95.3284452343853,0.32499269135528,-9.1977003354521));
#30972=CARTESIAN_POINT('Ctrl Pts',(95.3253415942028,0.313989053433054,-9.19693082963369));
#30973=CARTESIAN_POINT('Ctrl Pts',(95.3237694649128,0.308249055451559,-9.19652887774416));
#30974=CARTESIAN_POINT('Ctrl Pts',(95.3197795457139,0.293235754425902,-9.1954760083271));
#30975=CARTESIAN_POINT('Ctrl Pts',(95.3174313588221,0.283944579297801,-9.19482289623396));
#30976=CARTESIAN_POINT('Ctrl Pts',(95.3072009027109,0.241280090969467,-9.19181613537016));
#30977=CARTESIAN_POINT('Ctrl Pts',(95.3006658508474,0.207604123923289,-9.18942063446428));
#30978=CARTESIAN_POINT('Ctrl Pts',(95.2857668404014,0.107684458492103,-9.18224382992015));
#30979=CARTESIAN_POINT('Ctrl Pts',(95.2815537781544,0.0409644271714967,
-9.17735578153224));
#30980=CARTESIAN_POINT('Ctrl Pts',(95.2843263917638,-0.0858425006856801,
-9.16804775771988));
#30981=CARTESIAN_POINT('Ctrl Pts',(95.2902396280184,-0.145757237615887,
-9.16364524380017));
#30982=CARTESIAN_POINT('Ctrl Pts',(95.3024488669829,-0.214842747839243,
-9.15872543845992));
#30983=CARTESIAN_POINT('Ctrl Pts',(95.3043210274542,-0.224699714615762,
-9.15802740159081));
#30984=CARTESIAN_POINT('Ctrl Pts',(95.307103818103,-0.23839418593838,-9.15706415567521));
#30985=CARTESIAN_POINT('Ctrl Pts',(95.3079080405473,-0.242252524822921,
-9.15679349441877));
#30986=CARTESIAN_POINT('Ctrl Pts',(95.3093288295732,-0.248901640744811,
-9.15632840163204));
#30987=CARTESIAN_POINT('Ctrl Pts',(95.309936207762,-0.251694313963008,-9.15613346858606));
#30988=CARTESIAN_POINT('Ctrl Pts',(95.3112390682229,-0.257581481905566,
-9.15572343796251));
#30989=CARTESIAN_POINT('Ctrl Pts',(95.3119368959619,-0.260675428491912,
-9.15550848052399));
#30990=CARTESIAN_POINT('Ctrl Pts',(95.3136995903661,-0.268346151201486,
-9.15497677600476));
#30991=CARTESIAN_POINT('Ctrl Pts',(95.3147793796356,-0.272919506809456,
-9.1546608597584));
#30992=CARTESIAN_POINT('Ctrl Pts',(95.3189559007996,-0.290147101585245,
-9.15347451595903));
#30993=CARTESIAN_POINT('Ctrl Pts',(95.3222352798843,-0.302756680496362,
-9.15261372299451));
#30994=CARTESIAN_POINT('Ctrl Pts',(95.3311966315269,-0.335007371820055,
-9.15042543884504));
#30995=CARTESIAN_POINT('Ctrl Pts',(95.3371821602943,-0.354560205331172,
-9.14911152636124));
#30996=CARTESIAN_POINT('Ctrl Pts',(95.3620467297682,-0.428818907265126,
-9.14413615180968));
#30997=CARTESIAN_POINT('Ctrl Pts',(95.3844393162725,-0.482264035663483,
-9.1405830800919));
#30998=CARTESIAN_POINT('Ctrl Pts',(95.4448872518983,-0.601134383103912,
-9.13232576128364));
#30999=CARTESIAN_POINT('Ctrl Pts',(95.4854873975158,-0.664965014217853,
-9.12761148916091));
#31000=CARTESIAN_POINT('Ctrl Pts',(95.538302413555,-0.732659367047439,-9.12197645673039));
#31001=CARTESIAN_POINT('Ctrl Pts',(95.544801117809,-0.740765438529941,-9.12129062762627));
#31002=CARTESIAN_POINT('Ctrl Pts',(95.555682023743,-0.753975596535628,-9.12015388854749));
#31003=CARTESIAN_POINT('Ctrl Pts',(95.5600023147449,-0.759130108362933,
-9.11970543810132));
#31004=CARTESIAN_POINT('Ctrl Pts',(95.5678891868428,-0.768377823073261,
-9.11889178407716));
#31005=CARTESIAN_POINT('Ctrl Pts',(95.5714403968185,-0.77248393365631,-9.11852721011585));
#31006=CARTESIAN_POINT('Ctrl Pts',(95.5791234004798,-0.781244306060536,
-9.1177421765769));
#31007=CARTESIAN_POINT('Ctrl Pts',(95.5832639370711,-0.785890644750674,
-9.11732136366434));
#31008=CARTESIAN_POINT('Ctrl Pts',(95.5947128477063,-0.798534929345098,
-9.11616376877424));
#31009=CARTESIAN_POINT('Ctrl Pts',(95.6020949093263,-0.806465022122779,
-9.11542392732011));
#31010=CARTESIAN_POINT('Ctrl Pts',(95.6464821035948,-0.852847502169106,
-9.11101236205437));
#31011=CARTESIAN_POINT('Ctrl Pts',(95.6859514661125,-0.888845086902073,
-9.1072345911344));
#31012=CARTESIAN_POINT('Ctrl Pts',(95.7652559284584,-0.951869766641753,
-9.09991300930379));
#31013=CARTESIAN_POINT('Ctrl Pts',(95.8045768963787,-0.979379049581392,
-9.09639177378336));
#31014=CARTESIAN_POINT('Ctrl Pts',(95.8695093277414,-1.01913819128113,-9.09080562642547));
#31015=CARTESIAN_POINT('Ctrl Pts',(95.8940778211517,-1.03299453091597,-9.08874052508318));
#31016=CARTESIAN_POINT('Ctrl Pts',(95.9498950387495,-1.06188410789788,-9.08418363042193));
#31017=CARTESIAN_POINT('Ctrl Pts',(95.9813607684307,-1.07644794516997,-9.08170432428314));
#31018=CARTESIAN_POINT('Ctrl Pts',(96.0190358030001,-1.09190567912478,-9.07887385225048));
#31019=CARTESIAN_POINT('Ctrl Pts',(96.0246634113963,-1.09416402190214,-9.07845460074052));
#31020=CARTESIAN_POINT('Ctrl Pts',(96.0338701310051,-1.09777634843818,-9.07777475470072));
#31021=CARTESIAN_POINT('Ctrl Pts',(96.0374387577416,-1.0991564978109,-9.07751271016649));
#31022=CARTESIAN_POINT('Ctrl Pts',(96.043856932835,-1.1016028081397,-9.07704413952237));
#31023=CARTESIAN_POINT('Ctrl Pts',(96.0467039351538,-1.10267533807656,-9.07683724960353));
#31024=CARTESIAN_POINT('Ctrl Pts',(96.0529870685079,-1.10501457450796,-9.07638277326989));
#31025=CARTESIAN_POINT('Ctrl Pts',(96.0564249676695,-1.10627629341864,-9.0761354785603));
#31026=CARTESIAN_POINT('Ctrl Pts',(96.0664133977201,-1.1098893024343,-9.07542082715038));
#31027=CARTESIAN_POINT('Ctrl Pts',(96.0729790918501,-1.1121986401365,-9.07495583326609));
#31028=CARTESIAN_POINT('Ctrl Pts',(96.1289905470844,-1.13134320341494,-9.07102631995454));
#31029=CARTESIAN_POINT('Ctrl Pts',(96.1794921087499,-1.14493234273633,-9.06772852293112));
#31030=CARTESIAN_POINT('Ctrl Pts',(96.312409385237,-1.1713686081228,-9.05928699315287));
#31031=CARTESIAN_POINT('Ctrl Pts',(96.3955718663988,-1.17890458442218,-9.05421956648677));
#31032=CARTESIAN_POINT('Ctrl Pts',(96.5095442979045,-1.17712838993749,-9.04694846659041));
#31033=CARTESIAN_POINT('Ctrl Pts',(96.5402225146593,-1.17544863241202,-9.04496126539066));
#31034=CARTESIAN_POINT('Ctrl Pts',(96.5803190218028,-1.17167629870942,-9.04230704886361));
#31035=CARTESIAN_POINT('Ctrl Pts',(96.5898284265352,-1.17066465473783,-9.04167338303666));
#31036=CARTESIAN_POINT('Ctrl Pts',(96.6052297671665,-1.16883626277116,-9.04063983406126));
#31037=CARTESIAN_POINT('Ctrl Pts',(96.6111298136731,-1.16809047034655,-9.04024216028685));
#31038=CARTESIAN_POINT('Ctrl Pts',(96.6224583441052,-1.16657123693149,-9.03947514356716));
#31039=CARTESIAN_POINT('Ctrl Pts',(96.6278875834212,-1.16580450521287,-9.03910601910244));
#31040=CARTESIAN_POINT('Ctrl Pts',(96.6404448233589,-1.16394161163298,-9.03824863620056));
#31041=CARTESIAN_POINT('Ctrl Pts',(96.6475684418948,-1.16281784359028,-9.03775952806478));
#31042=CARTESIAN_POINT('Ctrl Pts',(96.6702599122193,-1.15902430091659,-9.03619258634598));
#31043=CARTESIAN_POINT('Ctrl Pts',(96.6857840071798,-1.15610684349203,-9.03510708558295));
#31044=CARTESIAN_POINT('Ctrl Pts',(96.7221573549886,-1.14851075738763,-9.03253064001181));
#31045=CARTESIAN_POINT('Ctrl Pts',(96.7429466835705,-1.1435753196859,-9.0310321681964));
#31046=CARTESIAN_POINT('Ctrl Pts',(96.8211627608579,-1.12274375100132,-9.02529536512948));
#31047=CARTESIAN_POINT('Ctrl Pts',(96.8774837088491,-1.10306489479191,-9.02095383538607));
#31048=CARTESIAN_POINT('Ctrl Pts',(96.9962989981343,-1.05114576597485,-9.01144141500817));
#31049=CARTESIAN_POINT('Ctrl Pts',(97.0579015001254,-1.01739808530671,-9.00627656180522));
#31050=CARTESIAN_POINT('Ctrl Pts',(97.1242927047042,-0.972905603992704,
-9.00067475197841));
#31051=CARTESIAN_POINT('Ctrl Pts',(97.1323763299039,-0.967340671148337,
-8.99999222008305));
#31052=CARTESIAN_POINT('Ctrl Pts',(97.1435779716884,-0.959421057888762,
-8.99904678457792));
#31053=CARTESIAN_POINT('Ctrl Pts',(97.1467549973599,-0.957151106337928,
-8.99877868051539));
#31054=CARTESIAN_POINT('Ctrl Pts',(97.1522303069411,-0.953197778031151,
-8.99831678201743));
#31055=CARTESIAN_POINT('Ctrl Pts',(97.1545338560112,-0.951521802676203,
-8.99812250161839));
#31056=CARTESIAN_POINT('Ctrl Pts',(97.1593343201527,-0.94800245839582,-8.99771777073918));
#31057=CARTESIAN_POINT('Ctrl Pts',(97.1618300733611,-0.946157545923668,
-8.9975074324903));
#31058=CARTESIAN_POINT('Ctrl Pts',(97.1678524781998,-0.941668736802228,
-8.99699999122045));
#31059=CARTESIAN_POINT('Ctrl Pts',(97.1713716780376,-0.939014836468964,
-8.9967035655622));
#31060=CARTESIAN_POINT('Ctrl Pts',(97.1790357241446,-0.933167441947189,
-8.99605802801546));
#31061=CARTESIAN_POINT('Ctrl Pts',(97.1831743781743,-0.929965939927039,
-8.99570944004017));
#31062=CARTESIAN_POINT('Ctrl Pts',(97.1948426707389,-0.920814863777414,
-8.99472623318917));
#31063=CARTESIAN_POINT('Ctrl Pts',(97.2023213017794,-0.914800555213958,
-8.99409556215138));
#31064=CARTESIAN_POINT('Ctrl Pts',(97.2929932359935,-0.840038988469825,
-8.98643137536576));
#31065=CARTESIAN_POINT('Ctrl Pts',(97.3664388077481,-0.76025586850915,-8.97999646387024));
#31066=CARTESIAN_POINT('Ctrl Pts',(97.4540863476987,-0.633985087939889,
-8.97033442780474));
#31067=CARTESIAN_POINT('Ctrl Pts',(97.477962422791,-0.594911333428827,-8.96741037220426));
#31068=CARTESIAN_POINT('Ctrl Pts',(97.5045333345108,-0.545127309715428,
-8.96370132341083));
#31069=CARTESIAN_POINT('Ctrl Pts',(97.5094344125026,-0.535635871324302,
-8.96299500506957));
#31070=CARTESIAN_POINT('Ctrl Pts',(97.5169983466645,-0.520485487562804,
-8.96186818838862));
#31071=CARTESIAN_POINT('Ctrl Pts',(97.5197464772194,-0.514869587875632,
-8.96145063788746));
#31072=CARTESIAN_POINT('Ctrl Pts',(97.5247958486115,-0.504339469967128,
-8.9606678244623));
#31073=CARTESIAN_POINT('Ctrl Pts',(97.52710810395,-0.499430693029835,-8.96030295086229));
#31074=CARTESIAN_POINT('Ctrl Pts',(97.5321939444214,-0.488437337636629,
-8.95948581864335));
#31075=CARTESIAN_POINT('Ctrl Pts',(97.5349497784742,-0.482344802663101,
-8.95903297133037));
#31076=CARTESIAN_POINT('Ctrl Pts',(97.5429294590955,-0.464295736129671,
-8.95769125082671));
#31077=CARTESIAN_POINT('Ctrl Pts',(97.5480065195336,-0.452275819960613,
-8.95679749733693));
#31078=CARTESIAN_POINT('Ctrl Pts',(97.5789173118845,-0.375563045826508,
-8.95108988856989));
#31079=CARTESIAN_POINT('Ctrl Pts',(97.5991639724754,-0.308780551613872,
-8.94609295436767));
#31080=CARTESIAN_POINT('Ctrl Pts',(97.6299280764564,-0.16137194007726,-8.9350904266245));
#31081=CARTESIAN_POINT('Ctrl Pts',(97.638252237779,-0.0806385399990132,
-8.929079197479));
#31082=CARTESIAN_POINT('Ctrl Pts',(97.6382309086937,0.000310323435185096,
-8.92336488290745));
#31083=CARTESIAN_POINT('Ctrl Pts',(97.6382309083588,0.000311592030453068,
-8.92336479335523));
#31084=CARTESIAN_POINT('Ctrl Pts',(97.6382276895883,0.0124778426499294,
-8.9225059580564));
#31085=CARTESIAN_POINT('Ctrl Pts',(97.6380359531211,0.0246439812452245,
-8.92165456740108));
#31086=CARTESIAN_POINT('Ctrl Pts',(97.6375296113348,0.0408386007025197,
-8.92053300477536));
#31087=CARTESIAN_POINT('Ctrl Pts',(97.6373827885247,0.0448709939316155,
-8.92025471094953));
#31088=CARTESIAN_POINT('Ctrl Pts',(97.6370893274945,0.0519324893646293,
-8.91976915610684));
#31089=CARTESIAN_POINT('Ctrl Pts',(97.6369517093267,0.0549618996042393,
-8.91956142878702));
#31090=CARTESIAN_POINT('Ctrl Pts',(97.636657125303,0.0609374264415622,-8.91915286931953));
#31091=CARTESIAN_POINT('Ctrl Pts',(97.6365007874133,0.0638835510311558,
-8.91895200686091));
#31092=CARTESIAN_POINT('Ctrl Pts',(97.6361389968834,0.0702492204367553,
-8.9185192649837));
#31093=CARTESIAN_POINT('Ctrl Pts',(97.6359296948163,0.0736684819833694,
-8.91828759858531));
#31094=CARTESIAN_POINT('Ctrl Pts',(97.6353218691996,0.0829350650225935,
-8.91766174528768));
#31095=CARTESIAN_POINT('Ctrl Pts',(97.6348946066744,0.0887804988577374,
-8.91726909985336));
#31096=CARTESIAN_POINT('Ctrl Pts',(97.6326888707052,0.116146122393434,-8.91543995848173));
#31097=CARTESIAN_POINT('Ctrl Pts',(97.6303622920809,0.137619466719396,-8.91403086391976));
#31098=CARTESIAN_POINT('Ctrl Pts',(97.6187467021329,0.222861201831005,-8.90849877630197));
#31099=CARTESIAN_POINT('Ctrl Pts',(97.6048218237422,0.285888264249353,-8.90454185578871));
#31100=CARTESIAN_POINT('Ctrl Pts',(97.5634371774038,0.419920242698919,-8.89586072487024));
#31101=CARTESIAN_POINT('Ctrl Pts',(97.5341231161294,0.490036592359137,-8.89113791524995));
#31102=CARTESIAN_POINT('Ctrl Pts',(97.4920792842694,0.568393992170254,-8.8853190825196));
#31103=CARTESIAN_POINT('Ctrl Pts',(97.4856901193522,0.579838762393659,-8.88445518669768));
#31104=CARTESIAN_POINT('Ctrl Pts',(97.4757490374506,0.596967876397367,-8.88313962084845));
#31105=CARTESIAN_POINT('Ctrl Pts',(97.4723372783363,0.602732695763284,-8.88269292527567));
#31106=CARTESIAN_POINT('Ctrl Pts',(97.4660728559163,0.613114533831275,-8.88188114088289));
#31107=CARTESIAN_POINT('Ctrl Pts',(97.4632370853661,0.61774156744024,-8.88151666830515));
#31108=CARTESIAN_POINT('Ctrl Pts',(97.4570703848893,0.627649216240995,-8.88073038011151));
#31109=CARTESIAN_POINT('Ctrl Pts',(97.4537292535835,0.632923253816214,-8.88030820072308));
#31110=CARTESIAN_POINT('Ctrl Pts',(97.4445797007711,0.647115115993269,-8.87916216788381));
#31111=CARTESIAN_POINT('Ctrl Pts',(97.4386921939768,0.655981001165737,-8.87843542538287));
#31112=CARTESIAN_POINT('Ctrl Pts',(97.4072312126746,0.701991967803485,-8.87460575947559));
#31113=CARTESIAN_POINT('Ctrl Pts',(97.3796630547364,0.737720903967526,-8.87142867429431));
#31114=CARTESIAN_POINT('Ctrl Pts',(97.2791439462794,0.853590358476638,-8.86040950179982));
#31115=CARTESIAN_POINT('Ctrl Pts',(97.1972327732983,0.925213385596874,-8.85227200437735));
#31116=CARTESIAN_POINT('Ctrl Pts',(97.0985135410843,0.990002638551259,-8.84392264336416));
#31117=CARTESIAN_POINT('Ctrl Pts',(97.0902659467377,0.99526965372209,-8.84323545128999));
#31118=CARTESIAN_POINT('Ctrl Pts',(97.0774484045568,1.00323195139268,-8.84218443958758));
#31119=CARTESIAN_POINT('Ctrl Pts',(97.0729244866847,1.00600005227844,-8.84181669158475));
#31120=CARTESIAN_POINT('Ctrl Pts',(97.0644822237792,1.0110876588527,-8.84113656880563));
#31121=CARTESIAN_POINT('Ctrl Pts',(97.060568847061,1.01341517165003,-8.84082372806416));
#31122=CARTESIAN_POINT('Ctrl Pts',(97.0539597647108,1.01729426972501,-8.84029958641083));
#31123=CARTESIAN_POINT('Ctrl Pts',(97.051271263729,1.01885795902174,-8.84008753116873));
#31124=CARTESIAN_POINT('Ctrl Pts',(97.0461022073597,1.02183705202581,-8.83968208750244));
#31125=CARTESIAN_POINT('Ctrl Pts',(97.0436226540505,1.02325410891238,-8.83948859078269));
#31126=CARTESIAN_POINT('Ctrl Pts',(97.0377160768376,1.02660125638527,-8.8390299511251));
#31127=CARTESIAN_POINT('Ctrl Pts',(97.0342844636194,1.02852324238589,-8.8387653142942));
#31128=CARTESIAN_POINT('Ctrl Pts',(97.0221083623426,1.03526295500918,-8.83783252987749));
#31129=CARTESIAN_POINT('Ctrl Pts',(97.0133120188657,1.03998680846358,-8.83716992620203));
#31130=CARTESIAN_POINT('Ctrl Pts',(96.9539772956563,1.07088540751493,-8.8327681510595));
#31131=CARTESIAN_POINT('Ctrl Pts',(96.9016525248316,1.09348226976643,-8.8292107009021));
#31132=CARTESIAN_POINT('Ctrl Pts',(96.7825310760637,1.13497545290733,-8.82138807095433));
#31133=CARTESIAN_POINT('Ctrl Pts',(96.715293193805,1.15193564854449,-8.81714607711188));
#31134=CARTESIAN_POINT('Ctrl Pts',(96.6240770276374,1.16656261123013,-8.81127695664107));
#31135=CARTESIAN_POINT('Ctrl Pts',(96.6010952461265,1.16955526613333,-8.80978976997621));
#31136=CARTESIAN_POINT('Ctrl Pts',(96.56132016922,1.17354544884839,-8.80719032863235));
#31137=CARTESIAN_POINT('Ctrl Pts',(96.5445658886967,1.17486473510556,-8.80608765129259));
#31138=CARTESIAN_POINT('Ctrl Pts',(96.5204114854098,1.17624742758363,-8.80448418320723));
#31139=CARTESIAN_POINT('Ctrl Pts',(96.5130295297029,1.1766003240665,-8.80399229991763));
#31140=CARTESIAN_POINT('Ctrl Pts',(96.5001387082074,1.17709502048667,-8.80312991557893));
#31141=CARTESIAN_POINT('Ctrl Pts',(96.4946312029094,1.17726767708703,-8.80276037754926));
#31142=CARTESIAN_POINT('Ctrl Pts',(96.4832508565428,1.17754451872483,-8.80199444203392));
#31143=CARTESIAN_POINT('Ctrl Pts',(96.4773780527988,1.17764342990208,-8.80159789217506));
#31144=CARTESIAN_POINT('Ctrl Pts',(96.4622802390568,1.17778475362582,-8.80057500305499));
#31145=CARTESIAN_POINT('Ctrl Pts',(96.453055171937,1.17776271495903,-8.79994669585846));
#31146=CARTESIAN_POINT('Ctrl Pts',(96.4160964373965,1.17724019093933,-8.79741567913715));
#31147=CARTESIAN_POINT('Ctrl Pts',(96.3883860345321,1.1758684252349,-8.79548656255368));
#31148=CARTESIAN_POINT('Ctrl Pts',(96.2646127433491,1.16534980695569,-8.78672288011929));
#31149=CARTESIAN_POINT('Ctrl Pts',(96.1698511337788,1.14539668457812,-8.77957436320877));
#31150=CARTESIAN_POINT('Ctrl Pts',(96.0509117732827,1.1046289492316,-8.77040832924488));
#31151=CARTESIAN_POINT('Ctrl Pts',(96.0235809783956,1.0941072481382,-8.76829155837132));
#31152=CARTESIAN_POINT('Ctrl Pts',(95.9812832004364,1.07598548108368,-8.76502541241066));
#31153=CARTESIAN_POINT('Ctrl Pts',(95.9660386378216,1.06906599881069,-8.76385039570325));
#31154=CARTESIAN_POINT('Ctrl Pts',(95.9462971708132,1.05959270031176,-8.76233625385094));
#31155=CARTESIAN_POINT('Ctrl Pts',(95.941663089498,1.05733139526956,-8.76198137666944));
#31156=CARTESIAN_POINT('Ctrl Pts',(95.9341146724985,1.05358639762704,-8.76140439909831));
#31157=CARTESIAN_POINT('Ctrl Pts',(95.9311914618543,1.05212090263434,-8.76118122435437));
#31158=CARTESIAN_POINT('Ctrl Pts',(95.9261134092303,1.0495485992528,-8.76079404995843));
#31159=CARTESIAN_POINT('Ctrl Pts',(95.9239558417446,1.04844729918809,-8.76062971140502));
#31160=CARTESIAN_POINT('Ctrl Pts',(95.9218016730721,1.04733934308043,-8.76046578184569));
#31161=CARTESIAN_POINT('Ctrl Pts',(95.921801762405,1.04733938902713,-8.66210246100831));
#31162=CARTESIAN_POINT('Ctrl Pts',(96.0026452746676,1.08891971908056,-8.66861620224818));
#31163=CARTESIAN_POINT('Ctrl Pts',(96.0880613387606,1.12101445553017,-8.67538701849297));
#31164=CARTESIAN_POINT('Ctrl Pts',(96.1973600557611,1.1481862295067,-8.68353275506134));
#31165=CARTESIAN_POINT('Ctrl Pts',(96.2185218236774,1.15283134845987,-8.68508516595406));
#31166=CARTESIAN_POINT('Ctrl Pts',(96.2531391665135,1.15943470315772,-8.68757302155445));
#31167=CARTESIAN_POINT('Ctrl Pts',(96.266521185894,1.16174829267295,-8.68852232754309));
#31168=CARTESIAN_POINT('Ctrl Pts',(96.2846579683376,1.16456177497881,-8.68978959231629));
#31169=CARTESIAN_POINT('Ctrl Pts',(96.2893795233907,1.16526484217128,-8.69011773593559));
#31170=CARTESIAN_POINT('Ctrl Pts',(96.2972602562689,1.16638939640873,-8.6906623568494));
#31171=CARTESIAN_POINT('Ctrl Pts',(96.3004170587716,1.16682679535453,-8.69087969365735));
#31172=CARTESIAN_POINT('Ctrl Pts',(96.3063948843866,1.16763035190628,-8.69128964389267));
#31173=CARTESIAN_POINT('Ctrl Pts',(96.309215516796,1.1679991110707,-8.69148240421451));
#31174=CARTESIAN_POINT('Ctrl Pts',(96.3158952565737,1.16884779267269,-8.69193735710874));
#31175=CARTESIAN_POINT('Ctrl Pts',(96.3197554893138,1.16931883203664,-8.69219906264013));
#31176=CARTESIAN_POINT('Ctrl Pts',(96.3333724455114,1.17091201264814,-8.69311818073018));
#31177=CARTESIAN_POINT('Ctrl Pts',(96.3431411238883,1.17193126671885,-8.69377023082555));
#31178=CARTESIAN_POINT('Ctrl Pts',(96.4231719686491,1.17927083242644,-8.69906081889157));
#31179=CARTESIAN_POINT('Ctrl Pts',(96.4938691601936,1.17938952544481,-8.70341612414954));
#31180=CARTESIAN_POINT('Ctrl Pts',(96.6232038990814,1.16795964666036,-8.71144754105458));
#31181=CARTESIAN_POINT('Ctrl Pts',(96.6817658415168,1.1582922052049,-8.71510942033331));
#31182=CARTESIAN_POINT('Ctrl Pts',(96.7600454756172,1.13921461501162,-8.7202441729295));
#31183=CARTESIAN_POINT('Ctrl Pts',(96.7806002045575,1.13361035000759,-8.72161502937965));
#31184=CARTESIAN_POINT('Ctrl Pts',(96.8160771968344,1.12289569042697,-8.72402898261375));
#31185=CARTESIAN_POINT('Ctrl Pts',(96.8310700204213,1.11803717517318,-8.72506429855792));
#31186=CARTESIAN_POINT('Ctrl Pts',(96.8527683615087,1.11052130090468,-8.72658706548817));
#31187=CARTESIAN_POINT('Ctrl Pts',(96.8595545184739,1.10810074274621,-8.72706683106561));
#31188=CARTESIAN_POINT('Ctrl Pts',(96.8714639462168,1.10372917362666,-8.72791522153835));
#31189=CARTESIAN_POINT('Ctrl Pts',(96.876596650974,1.10180435357681,-8.72828297735421));
#31190=CARTESIAN_POINT('Ctrl Pts',(96.8872713451955,1.09771599874422,-8.72905233389177));
#31191=CARTESIAN_POINT('Ctrl Pts',(96.8928107401524,1.09554616773264,-8.7294541343246));
#31192=CARTESIAN_POINT('Ctrl Pts',(96.9072217739639,1.08977491832561,-8.73050626607426));
#31193=CARTESIAN_POINT('Ctrl Pts',(96.9160662032585,1.0861071788856,-8.73115878659929));
#31194=CARTESIAN_POINT('Ctrl Pts',(96.953197770417,1.0701755653839,-8.73392776786964));
#31195=CARTESIAN_POINT('Ctrl Pts',(96.9810400775148,1.05691224719204,-8.73607735087099));
#31196=CARTESIAN_POINT('Ctrl Pts',(97.0819626491045,1.00387986758731,-8.74415021342976));
#31197=CARTESIAN_POINT('Ctrl Pts',(97.1512834224217,0.957498228828896,-8.7502811304991));
#31198=CARTESIAN_POINT('Ctrl Pts',(97.2552030990649,0.870767548907848,-8.76018962993834));
#31199=CARTESIAN_POINT('Ctrl Pts',(97.2930132780533,0.834691945012636,-8.76397653379108));
#31200=CARTESIAN_POINT('Ctrl Pts',(97.3330129195074,0.791095092138699,-8.76809170927561));
#31201=CARTESIAN_POINT('Ctrl Pts',(97.3376718568838,0.785925951567453,-8.76857280931927));
#31202=CARTESIAN_POINT('Ctrl Pts',(97.3447120756631,0.777974154780736,-8.76930216092445));
#31203=CARTESIAN_POINT('Ctrl Pts',(97.3471265506215,0.775221290285062,-8.76955272602837));
#31204=CARTESIAN_POINT('Ctrl Pts',(97.3515234101857,0.770160794970356,-8.77000973662444));
#31205=CARTESIAN_POINT('Ctrl Pts',(97.3535097008062,0.76785673575338,-8.77021645811504));
#31206=CARTESIAN_POINT('Ctrl Pts',(97.3579739539885,0.762637533034789,-8.77068169363572));
#31207=CARTESIAN_POINT('Ctrl Pts',(97.3604466542095,0.759717994573912,-8.77093982949921));
#31208=CARTESIAN_POINT('Ctrl Pts',(97.3668012330325,0.752140525536331,-8.77160453089989));
#31209=CARTESIAN_POINT('Ctrl Pts',(97.3706615049553,0.747464505368721,-8.77200961239814));
#31210=CARTESIAN_POINT('Ctrl Pts',(97.3963404878921,0.715865134402268,-8.7747146272142));
#31211=CARTESIAN_POINT('Ctrl Pts',(97.4170001286997,0.688017101278722,-8.77694197076325));
#31212=CARTESIAN_POINT('Ctrl Pts',(97.4521644223828,0.635965151452648,-8.78091117087153));
#31213=CARTESIAN_POINT('Ctrl Pts',(97.4670844960221,0.612076142840339,-8.78266435391822));
#31214=CARTESIAN_POINT('Ctrl Pts',(97.5050231779529,0.546185502445568,-8.78737858818703));
#31215=CARTESIAN_POINT('Ctrl Pts',(97.5263594562209,0.503279234907906,-8.79032268798985));
#31216=CARTESIAN_POINT('Ctrl Pts',(97.5658709742785,0.409959225388626,-8.79665941474394));
#31217=CARTESIAN_POINT('Ctrl Pts',(97.5833376457288,0.359368087666697,-8.80005784508494));
#31218=CARTESIAN_POINT('Ctrl Pts',(97.600138935057,0.297308263386022,-8.80428344482528));
#31219=CARTESIAN_POINT('Ctrl Pts',(97.6028265324198,0.286808444625609,-8.80500010931137));
#31220=CARTESIAN_POINT('Ctrl Pts',(97.6068287985501,0.270222891142982,-8.80613558140108));
#31221=CARTESIAN_POINT('Ctrl Pts',(97.6082408179135,0.264161094544596,-8.80655129495597));
#31222=CARTESIAN_POINT('Ctrl Pts',(97.610794211434,0.252792260657839,-8.80733242701998));
#31223=CARTESIAN_POINT('Ctrl Pts',(97.6119470757702,0.247487951207393,-8.80769747089252));
#31224=CARTESIAN_POINT('Ctrl Pts',(97.6144457408349,0.235596113074426,-8.8085172898266));
#31225=CARTESIAN_POINT('Ctrl Pts',(97.6157718721288,0.229004692063425,-8.80897267196527));
#31226=CARTESIAN_POINT('Ctrl Pts',(97.6190022366783,0.2122058076789,-8.81013589345186));
#31227=CARTESIAN_POINT('Ctrl Pts',(97.620828016972,0.201984030810402,-8.81084615992917));
#31228=CARTESIAN_POINT('Ctrl Pts',(97.6330339133282,0.128010272761377,-8.81600535362275));
#31229=CARTESIAN_POINT('Ctrl Pts',(97.6382873521505,0.0635346200625748,
-8.82061337127098));
#31230=CARTESIAN_POINT('Ctrl Pts',(97.6381857070302,-0.0518979240526905,
-8.82901867298229));
#31231=CARTESIAN_POINT('Ctrl Pts',(97.6348463079867,-0.102702002495823,
-8.83276932423325));
#31232=CARTESIAN_POINT('Ctrl Pts',(97.6221331347851,-0.199651755711864,
-8.83991300674831));
#31233=CARTESIAN_POINT('Ctrl Pts',(97.6132571065783,-0.245773838948051,
-8.84330439417029));
#31234=CARTESIAN_POINT('Ctrl Pts',(97.6000755396993,-0.297421981170072,
-8.8470129608494));
#31235=CARTESIAN_POINT('Ctrl Pts',(97.5984496763939,-0.303583342707689,
-8.84745387802189));
#31236=CARTESIAN_POINT('Ctrl Pts',(97.595743393164,-0.313511721550963,-8.84816162059654));
#31237=CARTESIAN_POINT('Ctrl Pts',(97.5946940656155,-0.317286974029813,
-8.84843009375209));
#31238=CARTESIAN_POINT('Ctrl Pts',(97.592795103803,-0.323989207806551,-8.84890548276808));
#31239=CARTESIAN_POINT('Ctrl Pts',(97.5919529295628,-0.326918200587228,
-8.84911281083175));
#31240=CARTESIAN_POINT('Ctrl Pts',(97.5900943410519,-0.333288952834766,
-8.84956282566048));
#31241=CARTESIAN_POINT('Ctrl Pts',(97.5890735615615,-0.336729353213197,
-8.84980526064934));
#31242=CARTESIAN_POINT('Ctrl Pts',(97.5861271996069,-0.346495753401351,
-8.85049194277615));
#31243=CARTESIAN_POINT('Ctrl Pts',(97.5841640073638,-0.352810399453397,
-8.85093410273578));
#31244=CARTESIAN_POINT('Ctrl Pts',(97.5702126224545,-0.396387231014497,
-8.85397490603897));
#31245=CARTESIAN_POINT('Ctrl Pts',(97.5564250981301,-0.433052362258197,
-8.85648037560189));
#31246=CARTESIAN_POINT('Ctrl Pts',(97.5097107399221,-0.540667867192817,
-8.86386262415609));
#31247=CARTESIAN_POINT('Ctrl Pts',(97.4715252860834,-0.609093588533009,
-8.86860707027188));
#31248=CARTESIAN_POINT('Ctrl Pts',(97.3999750429592,-0.711796911411264,
-8.87646733590535));
#31249=CARTESIAN_POINT('Ctrl Pts',(97.3708276890198,-0.748713577394931,
-8.8794678433591));
#31250=CARTESIAN_POINT('Ctrl Pts',(97.3324001863698,-0.791812798322973,
-8.88326254688917));
#31251=CARTESIAN_POINT('Ctrl Pts',(97.3251355717588,-0.799739354371371,
-8.88397340470888));
#31252=CARTESIAN_POINT('Ctrl Pts',(97.3134659407791,-0.812127423533355,
-8.88510582237831));
#31253=CARTESIAN_POINT('Ctrl Pts',(97.3091319569148,-0.816655259246756,
-8.88552438355297));
#31254=CARTESIAN_POINT('Ctrl Pts',(97.3013583782963,-0.824647830939835,
-8.88627171676063));
#31255=CARTESIAN_POINT('Ctrl Pts',(97.2979329665957,-0.82812620606204,-8.88659987326107));
#31256=CARTESIAN_POINT('Ctrl Pts',(97.2899486553138,-0.836133771616152,
-8.88736218769851));
#31257=CARTESIAN_POINT('Ctrl Pts',(97.2853741495215,-0.840647110716185,
-8.88779702256677));
#31258=CARTESIAN_POINT('Ctrl Pts',(97.2723060671461,-0.853331083643872,
-8.88903398477828));
#31259=CARTESIAN_POINT('Ctrl Pts',(97.2637266657072,-0.861411784139035,
-8.88983990832325));
#31260=CARTESIAN_POINT('Ctrl Pts',(97.1936635394484,-0.925445433698404,
-8.8963746517436));
#31261=CARTESIAN_POINT('Ctrl Pts',(97.126545887193,-0.974863275694764,-8.90237486083419));
#31262=CARTESIAN_POINT('Ctrl Pts',(96.9903447759414,-1.05447304683196,-8.91394057979042));
#31263=CARTESIAN_POINT('Ctrl Pts',(96.922446900855,-1.08593665415552,-8.91945601027064));
#31264=CARTESIAN_POINT('Ctrl Pts',(96.842967863557,-1.11395286756346,-8.92535992027495));
#31265=CARTESIAN_POINT('Ctrl Pts',(96.833874452062,-1.11703381215986,-8.92602741084338));
#31266=CARTESIAN_POINT('Ctrl Pts',(96.8210655382787,-1.12119970544098,-8.92695550341283));
#31267=CARTESIAN_POINT('Ctrl Pts',(96.8173811112285,-1.12237796697934,-8.92722106710744));
#31268=CARTESIAN_POINT('Ctrl Pts',(96.8107130433086,-1.1244742268811,-8.9276990784321));
#31269=CARTESIAN_POINT('Ctrl Pts',(96.8077314367788,-1.12539855443997,-8.92791188208985));
#31270=CARTESIAN_POINT('Ctrl Pts',(96.8016266293524,-1.12726453332523,-8.92834563196215));
#31271=CARTESIAN_POINT('Ctrl Pts',(96.798503135777,-1.12820508118679,-8.92856651470408));
#31272=CARTESIAN_POINT('Ctrl Pts',(96.7904663083689,-1.13058876171693,-8.92913227078558));
#31273=CARTESIAN_POINT('Ctrl Pts',(96.7855473337465,-1.13201286804066,-8.92947607253095));
#31274=CARTESIAN_POINT('Ctrl Pts',(96.7648154269111,-1.13786874069433,-8.93091532125131));
#31275=CARTESIAN_POINT('Ctrl Pts',(96.7489191217967,-1.14200185305585,-8.93199504986969));
#31276=CARTESIAN_POINT('Ctrl Pts',(96.7052540704864,-1.15238494866848,-8.93490924530784));
#31277=CARTESIAN_POINT('Ctrl Pts',(96.677336012989,-1.15796332289593,-8.93671610637991));
#31278=CARTESIAN_POINT('Ctrl Pts',(96.5634931877829,-1.17644811160953,-8.9439547395685));
#31279=CARTESIAN_POINT('Ctrl Pts',(96.4764689390601,-1.1808414794972,-8.94921309518676));
#31280=CARTESIAN_POINT('Ctrl Pts',(96.3531593540693,-1.17342275468991,-8.95704253774371));
#31281=CARTESIAN_POINT('Ctrl Pts',(96.3166932962594,-1.16951425198565,-8.95940223384516));
#31282=CARTESIAN_POINT('Ctrl Pts',(96.2704201922636,-1.16235769593161,-8.96248394779818));
#31283=CARTESIAN_POINT('Ctrl Pts',(96.2603898597982,-1.16067310209854,-8.96315719026119));
#31284=CARTESIAN_POINT('Ctrl Pts',(96.2444011709794,-1.15777439442056,-8.96423932142411));
#31285=CARTESIAN_POINT('Ctrl Pts',(96.2384280708523,-1.15664365117532,-8.96464559415983));
#31286=CARTESIAN_POINT('Ctrl Pts',(96.2271182292784,-1.15441179582903,-8.96541879096145));
#31287=CARTESIAN_POINT('Ctrl Pts',(96.2217798369081,-1.15331978682177,-8.96578541936212));
#31288=CARTESIAN_POINT('Ctrl Pts',(96.209651848317,-1.15075110357181,-8.96662223763662));
#31289=CARTESIAN_POINT('Ctrl Pts',(96.2028674087887,-1.14925132170226,-8.96709314594343));
#31290=CARTESIAN_POINT('Ctrl Pts',(96.1820837443378,-1.14446356151313,-8.96854453698026));
#31291=CARTESIAN_POINT('Ctrl Pts',(96.1681315890108,-1.14097925799956,-8.96953117834694));
#31292=CARTESIAN_POINT('Ctrl Pts',(96.1004376446571,-1.12275077657516,-8.97438059094485));
#31293=CARTESIAN_POINT('Ctrl Pts',(96.047732075131,-1.10446242725119,-8.97835422834948));
#31294=CARTESIAN_POINT('Ctrl Pts',(95.9533692625956,-1.06401942127327,-8.98581298357337));
#31295=CARTESIAN_POINT('Ctrl Pts',(95.9113592283587,-1.04295956951831,-8.98926897422103));
#31296=CARTESIAN_POINT('Ctrl Pts',(95.8231962375153,-0.991956469866126,
-8.99673154841249));
#31297=CARTESIAN_POINT('Ctrl Pts',(95.7776470957344,-0.961170537998989,
-9.00072390880263));
#31298=CARTESIAN_POINT('Ctrl Pts',(95.7293417335712,-0.92334820751348,-9.00499318991353));
#31299=CARTESIAN_POINT('Ctrl Pts',(95.7243078949355,-0.919339819495835,
-9.0054385021301));
#31300=CARTESIAN_POINT('Ctrl Pts',(95.716247524516,-0.912812779271459,-9.0061518914059));
#31301=CARTESIAN_POINT('Ctrl Pts',(95.713200411131,-0.910319921218946,-9.00642165760369));
#31302=CARTESIAN_POINT('Ctrl Pts',(95.7078155141216,-0.905869252183274,
-9.00689844664392));
#31303=CARTESIAN_POINT('Ctrl Pts',(95.705472771868,-0.90391759144402,-9.00710589134667));
#31304=CARTESIAN_POINT('Ctrl Pts',(95.7003995353483,-0.899657761856323,
-9.00755513339919));
#31305=CARTESIAN_POINT('Ctrl Pts',(95.6976719574077,-0.897346247020134,
-9.00779668637519));
#31306=CARTESIAN_POINT('Ctrl Pts',(95.6899772717571,-0.890764866611322,
-9.00847832761034));
#31307=CARTESIAN_POINT('Ctrl Pts',(95.685035103162,-0.886465853405737,-9.00891637670522));
#31308=CARTESIAN_POINT('Ctrl Pts',(95.6520568623407,-0.857292418303717,
-9.01184309335455));
#31309=CARTESIAN_POINT('Ctrl Pts',(95.6251829805327,-0.831130390173551,
-9.01424641764324));
#31310=CARTESIAN_POINT('Ctrl Pts',(95.5636988577416,-0.765274172404805,
-9.01992516067165));
#31311=CARTESIAN_POINT('Ctrl Pts',(95.5304130895609,-0.724456286997456,
-9.02315645332247));
#31312=CARTESIAN_POINT('Ctrl Pts',(95.4577096039204,-0.621994394564452,
-9.03093980649257));
#31313=CARTESIAN_POINT('Ctrl Pts',(95.4210881083236,-0.558648222203954,
-9.03550849996856));
#31314=CARTESIAN_POINT('Ctrl Pts',(95.386197010051,-0.482823429841529,-9.04098566184126));
#31315=CARTESIAN_POINT('Ctrl Pts',(95.3819519172179,-0.473264790652232,
-9.04167599163561));
#31316=CARTESIAN_POINT('Ctrl Pts',(95.3751789246654,-0.457449549611166,
-9.04281863079031));
#31317=CARTESIAN_POINT('Ctrl Pts',(95.3725764357243,-0.451225377475119,
-9.04326843524873));
#31318=CARTESIAN_POINT('Ctrl Pts',(95.3679760934093,-0.439951912217908,
-9.04408350902235));
#31319=CARTESIAN_POINT('Ctrl Pts',(95.3659593992626,-0.434910473575024,
-9.04444813821783));
#31320=CARTESIAN_POINT('Ctrl Pts',(95.3617119734176,-0.424075860306241,
-9.04523213973406));
#31321=CARTESIAN_POINT('Ctrl Pts',(95.3594920473265,-0.418278654535147,
-9.04565185721066));
#31322=CARTESIAN_POINT('Ctrl Pts',(95.3535489632979,-0.40238348462306,-9.04680343263187));
#31323=CARTESIAN_POINT('Ctrl Pts',(95.349918303695,-0.39225181604212,-9.04753829748996));
#31324=CARTESIAN_POINT('Ctrl Pts',(95.3296008541513,-0.333009770201912,
-9.05184133235174));
#31325=CARTESIAN_POINT('Ctrl Pts',(95.3160363395497,-0.282896575225514,
-9.05550939519109));
#31326=CARTESIAN_POINT('Ctrl Pts',(95.291379816098,-0.160212360778678,-9.06454386764575));
#31327=CARTESIAN_POINT('Ctrl Pts',(95.2836782018558,-0.0871763788865241,
-9.06997315389065));
#31328=CARTESIAN_POINT('Ctrl Pts',(95.2825938975948,0.0046540075335601,
-9.07665259779763));
#31329=CARTESIAN_POINT('Ctrl Pts',(95.2828135099476,0.0232169289674477,
-9.07799447330159));
#31330=CARTESIAN_POINT('Ctrl Pts',(95.2842545183918,0.0638244603832813,
-9.08090230399666));
#31331=CARTESIAN_POINT('Ctrl Pts',(95.2856571515968,0.0858567077776324,
-9.08246216078433));
#31332=CARTESIAN_POINT('Ctrl Pts',(95.2882186663797,0.113714676535725,-9.08440165798949));
#31333=CARTESIAN_POINT('Ctrl Pts',(95.2888031843305,0.119587233140062,-9.08480865167357));
#31334=CARTESIAN_POINT('Ctrl Pts',(95.2897976628285,0.128870086636871,-9.08544879429877));
#31335=CARTESIAN_POINT('Ctrl Pts',(95.290178431839,0.132283312783194,-9.08568348380922));
#31336=CARTESIAN_POINT('Ctrl Pts',(95.290928640726,0.138751312871955,-9.08612685445825));
#31337=CARTESIAN_POINT('Ctrl Pts',(95.2912951180347,0.141806281616544,-9.08633568297616));
#31338=CARTESIAN_POINT('Ctrl Pts',(95.2921869840546,0.149002336107572,-9.08682625900769));
#31339=CARTESIAN_POINT('Ctrl Pts',(95.2927224212851,0.15314211363836,-9.08710744963118));
#31340=CARTESIAN_POINT('Ctrl Pts',(95.2945673128121,0.16683344497711,-9.08803427043197));
#31341=CARTESIAN_POINT('Ctrl Pts',(95.2959720762489,0.176372065257464,-9.0886748968747));
#31342=CARTESIAN_POINT('Ctrl Pts',(95.3046118192007,0.230424255908912,-9.09228172881294));
#31343=CARTESIAN_POINT('Ctrl Pts',(95.314282469017,0.274515485252917,-9.09513427424002));
#31344=CARTESIAN_POINT('Ctrl Pts',(95.3300461253124,0.330739571111064,-9.09877817154008));
#31345=CARTESIAN_POINT('Ctrl Pts',(95.3338488197845,0.343469953300518,-9.09960360304719));
#31346=CARTESIAN_POINT('Ctrl Pts',(95.3666718678334,0.446935783694662,-9.10633365250383));
#31347=CARTESIAN_POINT('Ctrl Pts',(95.4063835015753,0.533897345921919,-9.11216097206476));
#31348=CARTESIAN_POINT('Ctrl Pts',(95.4636995518088,0.62748055799282,-9.11932437364334));
#31349=CARTESIAN_POINT('Ctrl Pts',(95.4714942850816,0.639695515979718,-9.12027770664394));
#31350=CARTESIAN_POINT('Ctrl Pts',(95.4833687995423,0.657567850032197,-9.12170171611157));
#31351=CARTESIAN_POINT('Ctrl Pts',(95.4872768641221,0.663338100593111,-9.12216607465751));
#31352=CARTESIAN_POINT('Ctrl Pts',(95.4943326955004,0.67355944827148,-9.12299707094115));
#31353=CARTESIAN_POINT('Ctrl Pts',(95.4974606153455,0.678024050726204,-9.12336295772801));
#31354=CARTESIAN_POINT('Ctrl Pts',(95.5041352036542,0.687411586742202,-9.12413857113665));
#31355=CARTESIAN_POINT('Ctrl Pts',(95.5076891354094,0.692329135463135,-9.12454856621731));
#31356=CARTESIAN_POINT('Ctrl Pts',(95.517269665803,0.705372155491361,-9.12564607069554));
#31357=CARTESIAN_POINT('Ctrl Pts',(95.5233631154638,0.713447655751167,-9.12633612932253));
#31358=CARTESIAN_POINT('Ctrl Pts',(95.5546588761258,0.753830432212282,-9.12984155859137));
#31359=CARTESIAN_POINT('Ctrl Pts',(95.58142815977,0.784881806145456,-9.13271783672671));
#31360=CARTESIAN_POINT('Ctrl Pts',(95.6787011198604,0.886484168771322,-9.14277850183074));
#31361=CARTESIAN_POINT('Ctrl Pts',(95.7564981755249,0.94944129940154,-9.15022718970229));
#31362=CARTESIAN_POINT('Ctrl Pts',(95.8632688936181,1.01543122228265,-9.15925078542189));
#31363=CARTESIAN_POINT('Ctrl Pts',(95.8856933115311,1.02829091681967,-9.1610842947984));
#31364=CARTESIAN_POINT('Ctrl Pts',(95.9129354082631,1.04274343654859,-9.16322435212941));
#31365=CARTESIAN_POINT('Ctrl Pts',(95.9173612125742,1.0450554758084,-9.16356934140438));
#31366=CARTESIAN_POINT('Ctrl Pts',(95.9218016730733,1.04733934308103,-9.1639126954948));
#31367=CARTESIAN_POINT('Origin',(96.460480949577,-7.19464945638997E-16,
0.924367114736168));
#31368=CARTESIAN_POINT('',(95.9218016501122,1.04733933127144,-9.76219702307975));
#31369=CARTESIAN_POINT('',(95.9218016730721,1.04733934308042,-9.66286811608663));
#31370=CARTESIAN_POINT('',(95.9218016730721,1.04733934308042,0.924367114736168));
#31371=CARTESIAN_POINT('Ctrl Pts',(95.9218016501122,1.04733933127145,-9.76219702307975));
#31372=CARTESIAN_POINT('Ctrl Pts',(95.8859551904519,1.02890237850787,-9.75965259857021));
#31373=CARTESIAN_POINT('Ctrl Pts',(95.8510742174078,1.00863488510987,-9.75706685301096));
#31374=CARTESIAN_POINT('Ctrl Pts',(95.8082201404791,0.980697856469402,-9.75370467124793));
#31375=CARTESIAN_POINT('Ctrl Pts',(95.7992262958196,0.974656205474092,-9.75298824003682));
#31376=CARTESIAN_POINT('Ctrl Pts',(95.7851994043365,0.964950067071735,-9.75185302554793));
#31377=CARTESIAN_POINT('Ctrl Pts',(95.7801097237193,0.961368186389378,-9.75143733331187));
#31378=CARTESIAN_POINT('Ctrl Pts',(95.7706339977982,0.9545866740277,-9.75065617333148));
#31379=CARTESIAN_POINT('Ctrl Pts',(95.7662412058318,0.951396716214778,-9.75029107974152));
#31380=CARTESIAN_POINT('Ctrl Pts',(95.7564559991169,0.944187040075249,-9.74947105952465));
#31381=CARTESIAN_POINT('Ctrl Pts',(95.7510756834141,0.940151297724262,-9.74901552497651));
#31382=CARTESIAN_POINT('Ctrl Pts',(95.737472929536,0.929764703474581,-9.74785173960773));
#31383=CARTESIAN_POINT('Ctrl Pts',(95.7292995630512,0.923350837376153,-9.74714105803139));
#31384=CARTESIAN_POINT('Ctrl Pts',(95.6624215877496,0.869425032570293,-9.74122918043905));
#31385=CARTESIAN_POINT('Ctrl Pts',(95.6083377002103,0.816484307829847,-9.73580597333349));
#31386=CARTESIAN_POINT('Ctrl Pts',(95.5223932718477,0.714450945155771,-9.72604671231284));
#31387=CARTESIAN_POINT('Ctrl Pts',(95.4884028671743,0.667467678364804,-9.7217694792751));
#31388=CARTESIAN_POINT('Ctrl Pts',(95.44729189965,0.600799206543354,-9.71611408146137));
#31389=CARTESIAN_POINT('Ctrl Pts',(95.4370306462928,0.583147762462043,-9.71465352815616));
#31390=CARTESIAN_POINT('Ctrl Pts',(95.4209874716981,0.553821011983468,-9.71229615852173));
#31391=CARTESIAN_POINT('Ctrl Pts',(95.4149313973869,0.542301182802119,-9.71138711082909));
#31392=CARTESIAN_POINT('Ctrl Pts',(95.4069508619269,0.526489769144039,-9.71016458051316));
#31393=CARTESIAN_POINT('Ctrl Pts',(95.4048595770507,0.522284062884356,-9.70984178698023));
#31394=CARTESIAN_POINT('Ctrl Pts',(95.4013986043073,0.515218112832308,-9.70930359446622));
#31395=CARTESIAN_POINT('Ctrl Pts',(95.4000152249072,0.51236468011977,-9.70908737710467));
#31396=CARTESIAN_POINT('Ctrl Pts',(95.3974069812261,0.506928957773521,-9.7086776614679));
#31397=CARTESIAN_POINT('Ctrl Pts',(95.3961799689023,0.504347750459011,-9.70848402831789));
#31398=CARTESIAN_POINT('Ctrl Pts',(95.3932829018368,0.49819567350931,-9.70802465654521));
#31399=CARTESIAN_POINT('Ctrl Pts',(95.391621341949,0.494620806772807,-9.70775942803424));
#31400=CARTESIAN_POINT('Ctrl Pts',(95.385792224421,0.481912840934746,-9.70682238729961));
#31401=CARTESIAN_POINT('Ctrl Pts',(95.381723382299,0.472734565796525,-9.70615618611606));
#31402=CARTESIAN_POINT('Ctrl Pts',(95.3541720295892,0.40837692421404,-9.70155047877698));
#31403=CARTESIAN_POINT('Ctrl Pts',(95.3348135389338,0.351519378942257,-9.69781304091315));
#31404=CARTESIAN_POINT('Ctrl Pts',(95.3032170928488,0.228697882328771,-9.68995593415588));
#31405=CARTESIAN_POINT('Ctrl Pts',(95.2921061103653,0.162671419829283,-9.68585200399263));
#31406=CARTESIAN_POINT('Ctrl Pts',(95.2838558549581,0.0618564476482338,
-9.6794213451601));
#31407=CARTESIAN_POINT('Ctrl Pts',(95.2825533035396,0.0275490047474106,
-9.67720620339286));
#31408=CARTESIAN_POINT('Ctrl Pts',(95.2828054225735,-0.0163490089426878,
-9.67431322973995));
#31409=CARTESIAN_POINT('Ctrl Pts',(95.2829774790101,-0.0259326989281477,
-9.67367812195108));
#31410=CARTESIAN_POINT('Ctrl Pts',(95.2834459430347,-0.0414617368867229,
-9.6726428293934));
#31411=CARTESIAN_POINT('Ctrl Pts',(95.2836704837632,-0.0474089401186523,
-9.67224486872131));
#31412=CARTESIAN_POINT('Ctrl Pts',(95.2841883834959,-0.0588294355572201,
-9.67147771624354));
#31413=CARTESIAN_POINT('Ctrl Pts',(95.2844748954074,-0.0643028951119048,
-9.67110874594469));
#31414=CARTESIAN_POINT('Ctrl Pts',(95.2852189348757,-0.0768398338296617,
-9.67026054729053));
#31415=CARTESIAN_POINT('Ctrl Pts',(95.2857019521605,-0.0839015298191893,
-9.66978054286784));
#31416=CARTESIAN_POINT('Ctrl Pts',(95.2874445843107,-0.106398155289384,
-9.66824400479199));
#31417=CARTESIAN_POINT('Ctrl Pts',(95.288944940145,-0.121812235576373,-9.66718010226665));
#31418=CARTESIAN_POINT('Ctrl Pts',(95.2999177011923,-0.215368901695882,
-9.66065196487231));
#31419=CARTESIAN_POINT('Ctrl Pts',(95.3168991471132,-0.292416437063511,
-9.65495490582798));
#31420=CARTESIAN_POINT('Ctrl Pts',(95.3560870521407,-0.411848393887781,
-9.64573718168791));
#31421=CARTESIAN_POINT('Ctrl Pts',(95.3734046135435,-0.455598816334138,
-9.64227655404078));
#31422=CARTESIAN_POINT('Ctrl Pts',(95.4022832226942,-0.517459655926531,
-9.63734150021458));
#31423=CARTESIAN_POINT('Ctrl Pts',(95.4117955220666,-0.536475449482421,
-9.63581878476946));
#31424=CARTESIAN_POINT('Ctrl Pts',(95.4281338964913,-0.567039786626174,
-9.633372990048));
#31425=CARTESIAN_POINT('Ctrl Pts',(95.434651383726,-0.578747179305988,-9.63243658481255));
#31426=CARTESIAN_POINT('Ctrl Pts',(95.4437480526257,-0.594450866877249,
-9.63118363540933));
#31427=CARTESIAN_POINT('Ctrl Pts',(95.446153424185,-0.598545979893881,-9.63085718962409));
#31428=CARTESIAN_POINT('Ctrl Pts',(95.4502115924571,-0.605360233479817,
-9.63031461401684));
#31429=CARTESIAN_POINT('Ctrl Pts',(95.4518507333845,-0.608087390053742,
-9.63009763767671));
#31430=CARTESIAN_POINT('Ctrl Pts',(95.454978473789,-0.613243793507612,-9.62968775809024));
#31431=CARTESIAN_POINT('Ctrl Pts',(95.4564648645179,-0.615674329880191,
-9.62949471180154));
#31432=CARTESIAN_POINT('Ctrl Pts',(95.4600097988215,-0.621424004043693,
-9.62903835213527));
#31433=CARTESIAN_POINT('Ctrl Pts',(95.4620760778907,-0.624738368892867,
-9.62877553296718));
#31434=CARTESIAN_POINT('Ctrl Pts',(95.4693951447811,-0.636349284878479,
-9.62785546428633));
#31435=CARTESIAN_POINT('Ctrl Pts',(95.4747353395464,-0.644590639520166,
-9.62720356349149));
#31436=CARTESIAN_POINT('Ctrl Pts',(95.518938404173,-0.710973510562911,-9.62195374949609));
#31437=CARTESIAN_POINT('Ctrl Pts',(95.5628117749466,-0.765622922601538,
-9.61763392512529));
#31438=CARTESIAN_POINT('Ctrl Pts',(95.6526389221856,-0.859097719116934,
-9.60961459335801));
#31439=CARTESIAN_POINT('Ctrl Pts',(95.6972050010947,-0.898925358209768,
-9.6059284605526));
#31440=CARTESIAN_POINT('Ctrl Pts',(95.761578133085,-0.948202145616376,-9.60076273497721));
#31441=CARTESIAN_POINT('Ctrl Pts',(95.7789105813841,-0.960736283753483,
-9.59938660352113));
#31442=CARTESIAN_POINT('Ctrl Pts',(95.8096307771272,-0.981702095110454,
-9.59696417698904));
#31443=CARTESIAN_POINT('Ctrl Pts',(95.822865199314,-0.990348962262571,-9.59592573904913));
#31444=CARTESIAN_POINT('Ctrl Pts',(95.8423867953013,-1.00255011061876,-9.59439918537191));
#31445=CARTESIAN_POINT('Ctrl Pts',(95.8485393284822,-1.0063173238857,-9.59391880907546));
#31446=CARTESIAN_POINT('Ctrl Pts',(95.859428753683,-1.01284815812958,-9.59306967845667));
#31447=CARTESIAN_POINT('Ctrl Pts',(95.8641511086371,-1.01563568895872,-9.59270179762273));
#31448=CARTESIAN_POINT('Ctrl Pts',(95.874034436112,-1.02137696677683,-9.59193251505349));
#31449=CARTESIAN_POINT('Ctrl Pts',(95.8791986449019,-1.02432480271343,-9.59153091580406));
#31450=CARTESIAN_POINT('Ctrl Pts',(95.892722240761,-1.03190914605693,-9.59048005983638));
#31451=CARTESIAN_POINT('Ctrl Pts',(95.901116002572,-1.03648313246012,-9.58982862435961));
#31452=CARTESIAN_POINT('Ctrl Pts',(95.9366764927274,-1.05530323395806,-9.58707149231913));
#31453=CARTESIAN_POINT('Ctrl Pts',(95.9643365492331,-1.06858619715539,-9.58493303263459));
#31454=CARTESIAN_POINT('Ctrl Pts',(96.0689309243904,-1.11387794247038,-9.57686364034604));
#31455=CARTESIAN_POINT('Ctrl Pts',(96.1486695586333,-1.13877379048116,-9.57072363283565));
#31456=CARTESIAN_POINT('Ctrl Pts',(96.2815894238688,-1.16525631087155,-9.56080220974697));
#31457=CARTESIAN_POINT('Ctrl Pts',(96.33345483736,-1.17204527172996,-9.55701168976383));
#31458=CARTESIAN_POINT('Ctrl Pts',(96.3925511677265,-1.17580995510247,-9.55289304259375));
#31459=CARTESIAN_POINT('Ctrl Pts',(96.3995012063141,-1.17619087844943,-9.55241183030035));
#31460=CARTESIAN_POINT('Ctrl Pts',(96.4101128557629,-1.17667817605298,-9.55168232025463));
#31461=CARTESIAN_POINT('Ctrl Pts',(96.4137721177493,-1.17682911283672,-9.55143170803378));
#31462=CARTESIAN_POINT('Ctrl Pts',(96.4204725206237,-1.17707418828228,-9.55097462377396));
#31463=CARTESIAN_POINT('Ctrl Pts',(96.4235133340026,-1.17717361291988,-9.55076787555905));
#31464=CARTESIAN_POINT('Ctrl Pts',(96.4303792334441,-1.17737147453957,-9.55030259045109));
#31465=CARTESIAN_POINT('Ctrl Pts',(96.4342044362904,-1.17746305600493,-9.55004443172208));
#31466=CARTESIAN_POINT('Ctrl Pts',(96.4440927691344,-1.17765158665202,-9.54937967669437));
#31467=CARTESIAN_POINT('Ctrl Pts',(96.4501564133056,-1.17772035720364,-9.54897456460657));
#31468=CARTESIAN_POINT('Ctrl Pts',(96.4908761042343,-1.1778676604155,-9.54626940342467));
#31469=CARTESIAN_POINT('Ctrl Pts',(96.5255241434315,-1.17646333535691,-9.54404194948902));
#31470=CARTESIAN_POINT('Ctrl Pts',(96.5881484456094,-1.17114923716987,-9.54007068966371));
#31471=CARTESIAN_POINT('Ctrl Pts',(96.6161402226448,-1.16775846669995,-9.53831561173425));
#31472=CARTESIAN_POINT('Ctrl Pts',(96.6913337700111,-1.15589782805985,-9.53359578930069));
#31473=CARTESIAN_POINT('Ctrl Pts',(96.7381822487611,-1.14554559493261,-9.53064800233047));
#31474=CARTESIAN_POINT('Ctrl Pts',(96.8355895263926,-1.11769304590989,-9.52431269752399));
#31475=CARTESIAN_POINT('Ctrl Pts',(96.8858468571973,-1.09954851988977,-9.52091967414613));
#31476=CARTESIAN_POINT('Ctrl Pts',(96.9446142311109,-1.07369801028633,-9.51670010441911));
#31477=CARTESIAN_POINT('Ctrl Pts',(96.9544708171645,-1.06919897564376,-9.51598366696585));
#31478=CARTESIAN_POINT('Ctrl Pts',(96.9698892185514,-1.06190254354049,-9.51484845148636));
#31479=CARTESIAN_POINT('Ctrl Pts',(96.9754934853382,-1.05919586572956,-9.51443276475589));
#31480=CARTESIAN_POINT('Ctrl Pts',(96.9859455307391,-1.05404530620512,-9.51365162066659));
#31481=CARTESIAN_POINT('Ctrl Pts',(96.9907983938131,-1.05161206736982,-9.51328653749921));
#31482=CARTESIAN_POINT('Ctrl Pts',(97.0016252260918,-1.04608946353732,-9.51246654799852));
#31483=CARTESIAN_POINT('Ctrl Pts',(97.0075898638776,-1.04298232313767,-9.51201103382089));
#31484=CARTESIAN_POINT('Ctrl Pts',(97.0226995506075,-1.03494600459869,-9.51084731390792));
#31485=CARTESIAN_POINT('Ctrl Pts',(97.0318064318337,-1.02994668265892,-9.51013667776087));
#31486=CARTESIAN_POINT('Ctrl Pts',(97.1065147089747,-0.987639029854072,
-9.50422858454984));
#31487=CARTESIAN_POINT('Ctrl Pts',(97.1684449873345,-0.944231704060049,
-9.49880945708824));
#31488=CARTESIAN_POINT('Ctrl Pts',(97.2697365825046,-0.857638245867293,
-9.48906112779236));
#31489=CARTESIAN_POINT('Ctrl Pts',(97.3108586993011,-0.81688186071571,-9.48479076685285));
#31490=CARTESIAN_POINT('Ctrl Pts',(97.3622755606574,-0.757813587199519,
-9.47913573117237));
#31491=CARTESIAN_POINT('Ctrl Pts',(97.3753245597906,-0.742008235792204,
-9.47766940251814));
#31492=CARTESIAN_POINT('Ctrl Pts',(97.3959976894294,-0.715593302520383,
-9.47530379049061));
#31493=CARTESIAN_POINT('Ctrl Pts',(97.4038692637876,-0.705183571225206,
-9.4743921769645));
#31494=CARTESIAN_POINT('Ctrl Pts',(97.4143398134915,-0.690847623066946,
-9.47316677951444));
#31495=CARTESIAN_POINT('Ctrl Pts',(97.4170903339025,-0.687033957145837,
-9.47284363073537));
#31496=CARTESIAN_POINT('Ctrl Pts',(97.4216581523541,-0.680619945372944,
-9.47230500493844));
#31497=CARTESIAN_POINT('Ctrl Pts',(97.4234878936372,-0.678028577309876,
-9.47208870690451));
#31498=CARTESIAN_POINT('Ctrl Pts',(97.4269458266491,-0.673089049200456,
-9.47167895283645));
#31499=CARTESIAN_POINT('Ctrl Pts',(97.4285759733574,-0.670742314262643,
-9.4714853611806));
#31500=CARTESIAN_POINT('Ctrl Pts',(97.4324329809438,-0.66514646985121,-9.47102623864534));
#31501=CARTESIAN_POINT('Ctrl Pts',(97.4346521321528,-0.661892049942476,
-9.47076121641535));
#31502=CARTESIAN_POINT('Ctrl Pts',(97.442457819903,-0.650320589331951,-9.46982570428204));
#31503=CARTESIAN_POINT('Ctrl Pts',(97.4479547003819,-0.641943183283677,
-9.46916080076482));
#31504=CARTESIAN_POINT('Ctrl Pts',(97.4871209619809,-0.580558859525506,
-9.46437011267051));
#31505=CARTESIAN_POINT('Ctrl Pts',(97.5166144735962,-0.524997485779002,
-9.46046650915653));
#31506=CARTESIAN_POINT('Ctrl Pts',(97.5672262681078,-0.407922157811988,
-9.45256963243796));
#31507=CARTESIAN_POINT('Ctrl Pts',(97.5879695640729,-0.346488785834593,
-9.44858816834218));
#31508=CARTESIAN_POINT('Ctrl Pts',(97.6089473610301,-0.261954743813344,
-9.44304743214294));
#31509=CARTESIAN_POINT('Ctrl Pts',(97.6137149089239,-0.240097331154344,
-9.44161021404495));
#31510=CARTESIAN_POINT('Ctrl Pts',(97.6208867666266,-0.202042142555787,
-9.4390902408425));
#31511=CARTESIAN_POINT('Ctrl Pts',(97.6235810768083,-0.185905188569885,
-9.43801626633463));
#31512=CARTESIAN_POINT('Ctrl Pts',(97.6269920582106,-0.162481897634714,
-9.43644712753011));
#31513=CARTESIAN_POINT('Ctrl Pts',(97.6279783664016,-0.155236307944396,
-9.43596033906931));
#31514=CARTESIAN_POINT('Ctrl Pts',(97.6295879339619,-0.14252771489406,-9.43510385717476));
#31515=CARTESIAN_POINT('Ctrl Pts',(97.6302405347156,-0.137068602094876,
-9.43473508707107));
#31516=CARTESIAN_POINT('Ctrl Pts',(97.6315146219413,-0.125738058193731,
-9.43396782133301));
#31517=CARTESIAN_POINT('Ctrl Pts',(97.6321302267512,-0.119866134497164,
-9.43356915395697));
#31518=CARTESIAN_POINT('Ctrl Pts',(97.6336081332065,-0.104668014213329,
-9.43253448221552));
#31519=CARTESIAN_POINT('Ctrl Pts',(97.6344033685614,-0.095335867280265,
-9.43189642183917));
#31520=CARTESIAN_POINT('Ctrl Pts',(97.6372002648836,-0.0571332458221609,
-9.42927262217701));
#31521=CARTESIAN_POINT('Ctrl Pts',(97.6382486527104,-0.0282053345403859,
-9.42725795700893));
#31522=CARTESIAN_POINT('Ctrl Pts',(97.6381988360772,0.0521916868471752,
-9.42157768963717));
#31523=CARTESIAN_POINT('Ctrl Pts',(97.6347940729209,0.103590782919541,-9.41785139203066));
#31524=CARTESIAN_POINT('Ctrl Pts',(97.617189254572,0.236546808710548,-9.40803746655624));
#31525=CARTESIAN_POINT('Ctrl Pts',(97.597740096058,0.317130997477428,-9.40190418519218));
#31526=CARTESIAN_POINT('Ctrl Pts',(97.566910878893,0.403724255026715,-9.39547326972626));
#31527=CARTESIAN_POINT('Ctrl Pts',(97.5637088862815,0.412393738420563,-9.39483150476054));
#31528=CARTESIAN_POINT('Ctrl Pts',(97.5589536710704,0.424816697425107,-9.39391577835899));
#31529=CARTESIAN_POINT('Ctrl Pts',(97.5574826602829,0.428600973186868,-9.39363735470494));
#31530=CARTESIAN_POINT('Ctrl Pts',(97.5548646214973,0.435234273324378,-9.39315033390435));
#31531=CARTESIAN_POINT('Ctrl Pts',(97.5537259769176,0.438086526974744,-9.39294125456747));
#31532=CARTESIAN_POINT('Ctrl Pts',(97.5512820076479,0.444139688565794,-9.39249827890143));
#31533=CARTESIAN_POINT('Ctrl Pts',(97.5499737392852,0.447339326680638,-9.39226455858095));
#31534=CARTESIAN_POINT('Ctrl Pts',(97.5463552794594,0.456078973178444,-9.39162722522645));
#31535=CARTESIAN_POINT('Ctrl Pts',(97.5440167554704,0.46160724777128,-9.39122525102946));
#31536=CARTESIAN_POINT('Ctrl Pts',(97.5310437962972,0.491633481092809,-9.38904709874659));
#31537=CARTESIAN_POINT('Ctrl Pts',(97.5196198101522,0.515784273382338,-9.38731380062034));
#31538=CARTESIAN_POINT('Ctrl Pts',(97.4779256047128,0.596687933488769,-9.38150232586648));
#31539=CARTESIAN_POINT('Ctrl Pts',(97.4438337871889,0.65134362304228,-9.37756291412851));
#31540=CARTESIAN_POINT('Ctrl Pts',(97.3618095508863,0.761608451092322,-9.36904914138031));
#31541=CARTESIAN_POINT('Ctrl Pts',(97.3128099496039,0.816072218763233,-9.36447494702547));
#31542=CARTESIAN_POINT('Ctrl Pts',(97.251406931976,0.872720003483838,-9.35899267628131));
#31543=CARTESIAN_POINT('Ctrl Pts',(97.2436379240827,0.879698389241347,-9.35830337965559));
#31544=CARTESIAN_POINT('Ctrl Pts',(97.2307022953402,0.891010434065669,-9.35716207731774));
#31545=CARTESIAN_POINT('Ctrl Pts',(97.2255893216783,0.895404763697256,-9.35671256590973));
#31546=CARTESIAN_POINT('Ctrl Pts',(97.216290696226,0.903258641847561,-9.35589777458998));
#31547=CARTESIAN_POINT('Ctrl Pts',(97.212118281935,0.906733624677735,-9.35553313236064));
#31548=CARTESIAN_POINT('Ctrl Pts',(97.2031213655216,0.914121908489025,-9.35474882671488));
#31549=CARTESIAN_POINT('Ctrl Pts',(97.198289651343,0.918026126001126,-9.35432881613633));
#31550=CARTESIAN_POINT('Ctrl Pts',(97.1849889965757,0.928600757789876,-9.35317571529104));
#31551=CARTESIAN_POINT('Ctrl Pts',(97.1764591749049,0.935193266119392,-9.35243960515133));
#31552=CARTESIAN_POINT('Ctrl Pts',(97.1260842532683,0.973033766220799,-9.34811064298131));
#31553=CARTESIAN_POINT('Ctrl Pts',(97.0822942394661,1.0015834035715,-9.34441645064773));
#31554=CARTESIAN_POINT('Ctrl Pts',(96.9701811969145,1.06448524508665,-9.33513283559314));
#31555=CARTESIAN_POINT('Ctrl Pts',(96.9001331014893,1.09527535787211,-9.32947001769076));
#31556=CARTESIAN_POINT('Ctrl Pts',(96.8117530641047,1.12426916652382,-9.32272075086632));
#31557=CARTESIAN_POINT('Ctrl Pts',(96.7957956035911,1.12913125212418,-9.32151783558619));
#31558=CARTESIAN_POINT('Ctrl Pts',(96.7597762500007,1.13927500221777,-9.31884466599141));
#31559=CARTESIAN_POINT('Ctrl Pts',(96.7396663000653,1.14436920415061,-9.31738100904247));
#31560=CARTESIAN_POINT('Ctrl Pts',(96.7137941241155,1.15020036733815,-9.31554308650517));
#31561=CARTESIAN_POINT('Ctrl Pts',(96.7081479578379,1.15142933168303,-9.31514471604512));
#31562=CARTESIAN_POINT('Ctrl Pts',(96.6991581583803,1.15331689608347,-9.31451499968291));
#31563=CARTESIAN_POINT('Ctrl Pts',(96.6958204075905,1.154002605301,-9.31428219479942));
#31564=CARTESIAN_POINT('Ctrl Pts',(96.6894543824504,1.15528167621914,-9.31384013008019));
#31565=CARTESIAN_POINT('Ctrl Pts',(96.6864267743582,1.15587761845616,-9.31363073920797));
#31566=CARTESIAN_POINT('Ctrl Pts',(96.6792415155632,1.15726262571735,-9.31313575933227));
#31567=CARTESIAN_POINT('Ctrl Pts',(96.6750819006015,1.15804119240724,-9.31285075672145));
#31568=CARTESIAN_POINT('Ctrl Pts',(96.6611036303633,1.16057964089917,-9.31189792231971));
#31569=CARTESIAN_POINT('Ctrl Pts',(96.6512665132075,1.16223725969956,-9.31123548693794));
#31570=CARTESIAN_POINT('Ctrl Pts',(96.6273321931131,1.16595826453804,-9.30964079295392));
#31571=CARTESIAN_POINT('Ctrl Pts',(96.6132160358401,1.16789128088837,-9.30871455268559));
#31572=CARTESIAN_POINT('Ctrl Pts',(96.5567626493365,1.17458066438581,-9.30505483216197));
#31573=CARTESIAN_POINT('Ctrl Pts',(96.514213441249,1.17729489988081,-9.30239524977197));
#31574=CARTESIAN_POINT('Ctrl Pts',(96.3750715147137,1.1786095131862,-9.29376481014584));
#31575=CARTESIAN_POINT('Ctrl Pts',(96.2788007321574,1.16764951072788,-9.28786478668805));
#31576=CARTESIAN_POINT('Ctrl Pts',(96.1709999593411,1.14170998014678,-9.28062537908701));
#31577=CARTESIAN_POINT('Ctrl Pts',(96.1571133216392,1.13809884269981,-9.2796811969285));
#31578=CARTESIAN_POINT('Ctrl Pts',(96.1366106696226,1.13236535692382,-9.27826822661105));
#31579=CARTESIAN_POINT('Ctrl Pts',(96.1299415331896,1.13043661943327,-9.27780561166113));
#31580=CARTESIAN_POINT('Ctrl Pts',(96.1180693220419,1.12688909319762,-9.27697652457454));
#31581=CARTESIAN_POINT('Ctrl Pts',(96.1128596526335,1.12529293219493,-9.27661078991669));
#31582=CARTESIAN_POINT('Ctrl Pts',(96.1018572937299,1.12183828775926,-9.27583422535463));
#31583=CARTESIAN_POINT('Ctrl Pts',(96.0960675702115,1.11997096255215,-9.27542311823925));
#31584=CARTESIAN_POINT('Ctrl Pts',(96.080620552989,1.11485646919493,-9.27431955173233));
#31585=CARTESIAN_POINT('Ctrl Pts',(96.0709906764101,1.11152875968215,-9.27362449371967));
#31586=CARTESIAN_POINT('Ctrl Pts',(96.0218915104046,1.09384561913521,-9.27004328299704));
#31587=CARTESIAN_POINT('Ctrl Pts',(95.9831717603254,1.07751293683962,-9.26709298075929));
#31588=CARTESIAN_POINT('Ctrl Pts',(95.9374941354851,1.05529964700024,-9.26345652482644));
#31589=CARTESIAN_POINT('Ctrl Pts',(95.9296240398814,1.05136263071937,-9.26282423601162));
#31590=CARTESIAN_POINT('Ctrl Pts',(95.9218016185417,1.04733931503376,-9.26219012624909));
#31591=CARTESIAN_POINT('',(97.6382309056894,0.000321523407826734,-9.32563288532119));
#31592=CARTESIAN_POINT('Ctrl Pts',(95.9218016730733,1.04733934308103,-9.1639126954948));
#31593=CARTESIAN_POINT('Ctrl Pts',(95.922814848987,1.04786045104073,-9.16399103829153));
#31594=CARTESIAN_POINT('Ctrl Pts',(95.9238287879189,1.04838009233506,-9.16406929595243));
#31595=CARTESIAN_POINT('Ctrl Pts',(95.9279792234048,1.05049958171471,-9.16438904021808));
#31596=CARTESIAN_POINT('Ctrl Pts',(95.9311221772002,1.05208685501054,-9.16462978372474));
#31597=CARTESIAN_POINT('Ctrl Pts',(95.936732942886,1.05488892929961,-9.16505703168365));
#31598=CARTESIAN_POINT('Ctrl Pts',(95.939197888489,1.05610917908104,-9.16524386338441));
#31599=CARTESIAN_POINT('Ctrl Pts',(95.9451213194579,1.0590157307738,-9.16569077717861));
#31600=CARTESIAN_POINT('Ctrl Pts',(95.9485838179442,1.06069373245005,-9.16595035026591));
#31601=CARTESIAN_POINT('Ctrl Pts',(95.9591582030892,1.06575446814968,-9.16673820088793));
#31602=CARTESIAN_POINT('Ctrl Pts',(95.9662960244338,1.06908294838597,-9.16726331563224));
#31603=CARTESIAN_POINT('Ctrl Pts',(95.9829965585636,1.07666766646834,-9.16847765797699));
#31604=CARTESIAN_POINT('Ctrl Pts',(95.9925838192388,1.08086858579362,-9.16916399532946));
#31605=CARTESIAN_POINT('Ctrl Pts',(96.0263765587037,1.09514187831299,-9.17154994191645));
#31606=CARTESIAN_POINT('Ctrl Pts',(96.0508624790331,1.10453395101049,-9.17321972048688));
#31607=CARTESIAN_POINT('Ctrl Pts',(96.1492301884765,1.13854309227748,-9.17977139358815));
#31608=CARTESIAN_POINT('Ctrl Pts',(96.2251598181554,1.15662533032439,-9.18449776961288));
#31609=CARTESIAN_POINT('Ctrl Pts',(96.3495170094827,1.17347794025397,-9.19237453603823));
#31610=CARTESIAN_POINT('Ctrl Pts',(96.3970527609507,1.17700447016527,-9.19541367264068));
#31611=CARTESIAN_POINT('Ctrl Pts',(96.4554530408275,1.17778865940993,-9.19925166261787));
#31612=CARTESIAN_POINT('Ctrl Pts',(96.4662395141318,1.17778530829299,-9.19996476278667));
#31613=CARTESIAN_POINT('Ctrl Pts',(96.4832990891366,1.17754565848997,-9.20109995777827));
#31614=CARTESIAN_POINT('Ctrl Pts',(96.4895731338883,1.1774073583786,-9.2015190287545));
#31615=CARTESIAN_POINT('Ctrl Pts',(96.5012670021924,1.17705606397813,-9.20230318961481));
#31616=CARTESIAN_POINT('Ctrl Pts',(96.5066870626377,1.17685575720505,-9.20266787769109));
#31617=CARTESIAN_POINT('Ctrl Pts',(96.5187542795268,1.17632630391864,-9.2034826555472));
#31618=CARTESIAN_POINT('Ctrl Pts',(96.5254003765902,1.17597823922385,-9.20393331850885));
#31619=CARTESIAN_POINT('Ctrl Pts',(96.5449123104133,1.17479046615917,-9.2052622224221));
#31620=CARTESIAN_POINT('Ctrl Pts',(96.5577673745231,1.17379581814988,-9.20614520439128));
#31621=CARTESIAN_POINT('Ctrl Pts',(96.5869802357034,1.17105233426194,-9.20816949999865));
#31622=CARTESIAN_POINT('Ctrl Pts',(96.6033226237227,1.16917143692625,-9.20931466270758));
#31623=CARTESIAN_POINT('Ctrl Pts',(96.6582174266742,1.1616853477804,-9.21320510040282));
#31624=CARTESIAN_POINT('Ctrl Pts',(96.696526756446,1.15451046970759,-9.21599425470878));
#31625=CARTESIAN_POINT('Ctrl Pts',(96.778019076342,1.13502219176143,-9.22207222122691));
#31626=CARTESIAN_POINT('Ctrl Pts',(96.8209983638215,1.12211084362784,-9.22536839884872));
#31627=CARTESIAN_POINT('Ctrl Pts',(96.9193232450497,1.08633963104154,-9.23304227804842));
#31628=CARTESIAN_POINT('Ctrl Pts',(96.9738802387444,1.06164631933635,-9.23740504343882));
#31629=CARTESIAN_POINT('Ctrl Pts',(97.0319255438538,1.02984796581947,-9.24200988958387));
#31630=CARTESIAN_POINT('Ctrl Pts',(97.0374954285506,1.02673757726301,-9.24245131555883));
#31631=CARTESIAN_POINT('Ctrl Pts',(97.0464471546272,1.02164281368668,-9.24315971210766));
#31632=CARTESIAN_POINT('Ctrl Pts',(97.0498447510446,1.01968659050402,-9.24342833520348));
#31633=CARTESIAN_POINT('Ctrl Pts',(97.055817845369,1.01620765294511,-9.24390006398209));
#31634=CARTESIAN_POINT('Ctrl Pts',(97.0583973770067,1.01469205176521,-9.24410360732617));
#31635=CARTESIAN_POINT('Ctrl Pts',(97.0639634191068,1.0113931332502,-9.24454241270291));
#31636=CARTESIAN_POINT('Ctrl Pts',(97.0669478183563,1.00960640790023,-9.2447774539566));
#31637=CARTESIAN_POINT('Ctrl Pts',(97.0731460440199,1.00585820066837,-9.24526520495842));
#31638=CARTESIAN_POINT('Ctrl Pts',(97.0763584744495,1.00389447309009,-9.24551777177673));
#31639=CARTESIAN_POINT('Ctrl Pts',(97.084565964538,0.998823089156785,-9.24616262672578));
#31640=CARTESIAN_POINT('Ctrl Pts',(97.0895473255119,0.995693309879872,-9.24655359487434));
#31641=CARTESIAN_POINT('Ctrl Pts',(97.1040763463914,0.986412194474156,-9.24769335394931));
#31642=CARTESIAN_POINT('Ctrl Pts',(97.1135589961314,0.980159751339093,-9.24843651446852));
#31643=CARTESIAN_POINT('Ctrl Pts',(97.1474892275136,0.957076568149981,-9.25109870094033));
#31644=CARTESIAN_POINT('Ctrl Pts',(97.1713903370831,0.939459431143961,-9.25297995838663));
#31645=CARTESIAN_POINT('Ctrl Pts',(97.2731280256641,0.858361431341868,-9.26113372196366));
#31646=CARTESIAN_POINT('Ctrl Pts',(97.3433228603323,0.785983443176158,-9.26719052002289));
#31647=CARTESIAN_POINT('Ctrl Pts',(97.4179664287171,0.686222210637065,-9.27520244793632));
#31648=CARTESIAN_POINT('Ctrl Pts',(97.4318476498015,0.666427767296901,-9.27677565144272));
#31649=CARTESIAN_POINT('Ctrl Pts',(97.4499181195329,0.63889432496033,-9.27895024457551));
#31650=CARTESIAN_POINT('Ctrl Pts',(97.4546448548664,0.631514049183242,-9.27953182557908));
#31651=CARTESIAN_POINT('Ctrl Pts',(97.4620427518038,0.619674133616652,-9.28046310977286));
#31652=CARTESIAN_POINT('Ctrl Pts',(97.4647675785383,0.615248275882033,-9.28081085240701));
#31653=CARTESIAN_POINT('Ctrl Pts',(97.4703110390121,0.606109239880254,-9.28152821811447));
#31654=CARTESIAN_POINT('Ctrl Pts',(97.4731261761087,0.601394100092953,-9.28189795603467));
#31655=CARTESIAN_POINT('Ctrl Pts',(97.4795923950988,0.59038954088573,-9.28276010586785));
#31656=CARTESIAN_POINT('Ctrl Pts',(97.4832183708644,0.584085705503281,-9.28325339813373));
#31657=CARTESIAN_POINT('Ctrl Pts',(97.4947006076781,0.563688824558587,-9.28484790831653));
#31658=CARTESIAN_POINT('Ctrl Pts',(97.5023254307736,0.549468310679476,-9.2859571791848));
#31659=CARTESIAN_POINT('Ctrl Pts',(97.5196359476891,0.515527215968371,-9.28860043245823));
#31660=CARTESIAN_POINT('Ctrl Pts',(97.5290664365317,0.495683942702836,-9.29014248266009));
#31661=CARTESIAN_POINT('Ctrl Pts',(97.5430286305111,0.46405239273454,-9.29259559516936));
#31662=CARTESIAN_POINT('Ctrl Pts',(97.5479353973612,0.452434427257455,-9.29349553308035));
#31663=CARTESIAN_POINT('Ctrl Pts',(97.5916981364443,0.343988444268873,-9.30188403299866));
#31664=CARTESIAN_POINT('Ctrl Pts',(97.6177087725841,0.242489700997993,-9.30970477735835));
#31665=CARTESIAN_POINT('Ctrl Pts',(97.6322371076608,0.12016086300608,-9.3184813902564));
#31666=CARTESIAN_POINT('Ctrl Pts',(97.6340120284564,0.101370767593353,-9.31981018525258));
#31667=CARTESIAN_POINT('Ctrl Pts',(97.6357258832803,0.0769776311818763,
-9.32150367281578));
#31668=CARTESIAN_POINT('Ctrl Pts',(97.6360774700598,0.0714075207628335,
-9.321888248877));
#31669=CARTESIAN_POINT('Ctrl Pts',(97.6365774784201,0.0624766447800458,
-9.32250123347332));
#31670=CARTESIAN_POINT('Ctrl Pts',(97.6367511153154,0.0591174611465136,
-9.32273097436978));
#31671=CARTESIAN_POINT('Ctrl Pts',(97.6370484999609,0.0528429352808183,
-9.32315850962415));
#31672=CARTESIAN_POINT('Ctrl Pts',(97.6371758069143,0.0499278411504255,
-9.32335649199225));
#31673=CARTESIAN_POINT('Ctrl Pts',(97.6374145460375,0.0439517227946099,
-9.32376108715971));
#31674=CARTESIAN_POINT('Ctrl Pts',(97.6375248733501,0.0408906645931219,
-9.32396764019607));
#31675=CARTESIAN_POINT('Ctrl Pts',(97.6378027476884,0.0322439599734504,
-9.32454924827992));
#31676=CARTESIAN_POINT('Ctrl Pts',(97.6379424881039,0.0266574109352865,
-9.32492283818597));
#31677=CARTESIAN_POINT('Ctrl Pts',(97.6381657953044,0.0141771713317196,
-9.32575298202203));
#31678=CARTESIAN_POINT('Ctrl Pts',(97.6382286077225,0.00728328496665232,
-9.32620850998168));
#31679=CARTESIAN_POINT('Ctrl Pts',(97.6382308853076,0.000389084372464196,
-9.32666138302753));
#31680=CARTESIAN_POINT('Ctrl Pts',(97.6382309056894,0.000321523407826734,
-9.3256328853212));
#31681=CARTESIAN_POINT('Ctrl Pts',(97.6382435761352,-0.0460907022632928,
-9.32878688556136));
#31682=CARTESIAN_POINT('Ctrl Pts',(97.6355084800378,-0.0926118624646665,
-9.33194088580153));
#31683=CARTESIAN_POINT('Ctrl Pts',(97.630013099911,-0.138887047038513,-9.3350948860417));
#31684=CARTESIAN_POINT('Ctrl Pts',(97.6245255048694,-0.185096675409236,
-9.33824441813588));
#31685=CARTESIAN_POINT('Ctrl Pts',(97.6162854232476,-0.231060459664611,
-9.34139395023005));
#31686=CARTESIAN_POINT('Ctrl Pts',(97.6053323074263,-0.276424367469098,
-9.34454348232423));
#31687=CARTESIAN_POINT('Ctrl Pts',(97.5943897069927,-0.321744724279503,
-9.34768999075355));
#31688=CARTESIAN_POINT('Ctrl Pts',(97.580739357164,-0.366465795608954,-9.35083649918288));
#31689=CARTESIAN_POINT('Ctrl Pts',(97.5644720036866,-0.410242385603896,
-9.3539830076122));
#31690=CARTESIAN_POINT('Ctrl Pts',(97.5482128406558,-0.453996934531981,
-9.35712793180661));
#31691=CARTESIAN_POINT('Ctrl Pts',(97.5293394803747,-0.496807413645105,
-9.36027285600101));
#31692=CARTESIAN_POINT('Ctrl Pts',(97.5079920405549,-0.538345220818771,
-9.36341778019541));
#31693=CARTESIAN_POINT('Ctrl Pts',(97.4866293822363,-0.579912640117923,
-9.36656494639285));
#31694=CARTESIAN_POINT('Ctrl Pts',(97.4627893710122,-0.620205065273235,
-9.36971211259029));
#31695=CARTESIAN_POINT('Ctrl Pts',(97.4366588202512,-0.658917162704153,
-9.37285927878773));
#31696=CARTESIAN_POINT('Ctrl Pts',(97.4105207063682,-0.697640464809353,
-9.37600735588834));
#31697=CARTESIAN_POINT('Ctrl Pts',(97.3820910706567,-0.734782072069771,
-9.37915543298895));
#31698=CARTESIAN_POINT('Ctrl Pts',(97.3515987835877,-0.770067573923226,
-9.38230351008955));
#31699=CARTESIAN_POINT('Ctrl Pts',(97.3210452391043,-0.805423962509669,
-9.38545791151287));
#31700=CARTESIAN_POINT('Ctrl Pts',(97.2884211566196,-0.838916383833414,
-9.38861231293619));
#31701=CARTESIAN_POINT('Ctrl Pts',(97.2539931952205,-0.870306485391062,
-9.39176671435952));
#31702=CARTESIAN_POINT('Ctrl Pts',(97.2204727647251,-0.900869134898895,
-9.39483796485964));
#31703=CARTESIAN_POINT('Ctrl Pts',(97.1852428631882,-0.929438738903102,
-9.39790921535977));
#31704=CARTESIAN_POINT('Ctrl Pts',(97.1485766766973,-0.955834364740461,
-9.4009804658599));
#31705=CARTESIAN_POINT('Ctrl Pts',(97.1092791289799,-0.984124281558804,
-9.40427212568688));
#31706=CARTESIAN_POINT('Ctrl Pts',(97.0681436983917,-1.0100517204561,-9.40756378551386));
#31707=CARTESIAN_POINT('Ctrl Pts',(97.0254881052638,-1.03337407385842,-9.41085544534085));
#31708=CARTESIAN_POINT('Ctrl Pts',(96.9843815618015,-1.05584946954454,-9.41402756763054));
#31709=CARTESIAN_POINT('Ctrl Pts',(96.9418639163497,-1.07590545553094,-9.41719968992023));
#31710=CARTESIAN_POINT('Ctrl Pts',(96.8982506177933,-1.09336763263313,-9.42037181220992));
#31711=CARTESIAN_POINT('Ctrl Pts',(96.8546806647558,-1.11081245477359,-9.42354078185372));
#31712=CARTESIAN_POINT('Ctrl Pts',(96.8100177291949,-1.12566836392258,-9.42670975149752));
#31713=CARTESIAN_POINT('Ctrl Pts',(96.7645997277354,-1.13780790613858,-9.42987872114132));
#31714=CARTESIAN_POINT('Ctrl Pts',(96.719206867905,-1.14994072837884,-9.43304593656748));
#31715=CARTESIAN_POINT('Ctrl Pts',(96.6730603079208,-1.15936001857546,-9.43621315199364));
#31716=CARTESIAN_POINT('Ctrl Pts',(96.626513111044,-1.16598815768369,-9.4393803674198));
#31717=CARTESIAN_POINT('Ctrl Pts',(96.5799711876462,-1.17261554586911,-9.44254722402212));
#31718=CARTESIAN_POINT('Ctrl Pts',(96.5330292694809,-1.17645233430959,-9.44571408062444));
#31719=CARTESIAN_POINT('Ctrl Pts',(96.4860478852236,-1.17747246010327,-9.44888093722676));
#31720=CARTESIAN_POINT('Ctrl Pts',(96.4390189437089,-1.17849361852691,-9.45205099950334));
#31721=CARTESIAN_POINT('Ctrl Pts',(96.3919510147601,-1.17669241495227,-9.45522106177993));
#31722=CARTESIAN_POINT('Ctrl Pts',(96.3452049779548,-1.17209492485317,-9.45839112405651));
#31723=CARTESIAN_POINT('Ctrl Pts',(96.2984304480075,-1.16749463244296,-9.4615631185832));
#31724=CARTESIAN_POINT('Ctrl Pts',(96.2519787513863,-1.1600947496835,-9.46473511310989));
#31725=CARTESIAN_POINT('Ctrl Pts',(96.2062023526948,-1.14997280736007,-9.46790710763658));
#31726=CARTESIAN_POINT('Ctrl Pts',(96.1603436706197,-1.13983267077747,-9.47108480384469));
#31727=CARTESIAN_POINT('Ctrl Pts',(96.1151632425546,-1.12696087008998,-9.47426250005281));
#31728=CARTESIAN_POINT('Ctrl Pts',(96.0709982369142,-1.11148471831006,-9.47744019626092));
#31729=CARTESIAN_POINT('Ctrl Pts',(96.0592304063825,-1.10736107496876,-9.47828689807644));
#31730=CARTESIAN_POINT('Ctrl Pts',(96.0475345487335,-1.10305279343504,-9.47913359989196));
#31731=CARTESIAN_POINT('Ctrl Pts',(96.0359167648909,-1.09856284097989,-9.47998030170748));
#31732=CARTESIAN_POINT('Ctrl Pts',(95.9907511686297,-1.0811075859529,-9.48327196153446));
#31733=CARTESIAN_POINT('Ctrl Pts',(95.946560001052,-1.06082220612803,-9.48656362136144));
#31734=CARTESIAN_POINT('Ctrl Pts',(95.9037200530682,-1.03784024137568,-9.48985528118843));
#31735=CARTESIAN_POINT('Ctrl Pts',(95.8624358103002,-1.0156928519232,-9.49302740650142));
#31736=CARTESIAN_POINT('Ctrl Pts',(95.8224068712118,-0.991041666390307,
-9.49619953181442));
#31737=CARTESIAN_POINT('Ctrl Pts',(95.7839516601953,-0.964055591295815,
-9.49937165712742));
#31738=CARTESIAN_POINT('Ctrl Pts',(95.7455346679984,-0.937096336387842,
-9.50254062981476));
#31739=CARTESIAN_POINT('Ctrl Pts',(95.7086887626404,-0.907807103671446,
-9.5057096025021));
#31740=CARTESIAN_POINT('Ctrl Pts',(95.6737053268424,-0.876401267668292,
-9.50887857518945));
#31741=CARTESIAN_POINT('Ctrl Pts',(95.638741256333,-0.845012816552093,-9.51204579367315));
#31742=CARTESIAN_POINT('Ctrl Pts',(95.6056380273375,-0.811510454951653,
-9.51521301215685));
#31743=CARTESIAN_POINT('Ctrl Pts',(95.5746535605387,-0.776147472668386,
-9.51838023064056));
#31744=CARTESIAN_POINT('Ctrl Pts',(95.5436726039884,-0.740788496678367,
-9.5215470903082));
#31745=CARTESIAN_POINT('Ctrl Pts',(95.5148102987333,-0.703569739044834,
-9.52471394997584));
#31746=CARTESIAN_POINT('Ctrl Pts',(95.4882854648538,-0.664778912108246,
-9.52788080964348));
#31747=CARTESIAN_POINT('Ctrl Pts',(95.4617337811362,-0.625948819047436,
-9.53105087497377));
#31748=CARTESIAN_POINT('Ctrl Pts',(95.4375246036784,-0.585543943478989,
-9.53422094030406));
#31749=CARTESIAN_POINT('Ctrl Pts',(95.415833276992,-0.543880779824758,-9.53739100563435));
#31750=CARTESIAN_POINT('Ctrl Pts',(95.394128728814,-0.502192221266026,-9.54056300321124));
#31751=CARTESIAN_POINT('Ctrl Pts',(95.3749453127051,-0.459244357691733,
-9.54373500078813));
#31752=CARTESIAN_POINT('Ctrl Pts',(95.3584106800634,-0.415374750742292,
-9.54690699836502));
#31753=CARTESIAN_POINT('Ctrl Pts',(95.3418463265242,-0.371426288452221,
-9.55008469758746));
#31754=CARTESIAN_POINT('Ctrl Pts',(95.3279404156537,-0.326553310719913,
-9.55326239680991));
#31755=CARTESIAN_POINT('Ctrl Pts',(95.3167705471221,-0.281107769043174,
-9.55644009603235));
#31756=CARTESIAN_POINT('Ctrl Pts',(95.3137943969909,-0.268999054026411,
-9.55728677653992));
#31757=CARTESIAN_POINT('Ctrl Pts',(95.311012202266,-0.25684973474927,-9.55813345704749));
#31758=CARTESIAN_POINT('Ctrl Pts',(95.3084248112407,-0.2446665416881,-9.55898013755506));
#31759=CARTESIAN_POINT('Ctrl Pts',(95.298365749979,-0.197301653982104,-9.56227179738204));
#31760=CARTESIAN_POINT('Ctrl Pts',(95.2912094176885,-0.14920650195639,-9.56556345720902));
#31761=CARTESIAN_POINT('Ctrl Pts',(95.2870498501539,-0.100769625416666,
-9.568855117036));
#31762=CARTESIAN_POINT('Ctrl Pts',(95.2830413499848,-0.0540918815927246,
-9.5720272302096));
#31763=CARTESIAN_POINT('Ctrl Pts',(95.2818157192262,-0.00709742288570371,
-9.57519934338319));
#31764=CARTESIAN_POINT('Ctrl Pts',(95.2834054806813,0.0398547741674446,
-9.57837145655678));
#31765=CARTESIAN_POINT('Ctrl Pts',(95.2849936621503,0.0867603077308272,
-9.58154041712241));
#31766=CARTESIAN_POINT('Ctrl Pts',(95.2893916789986,0.133623107969756,-9.58470937768803));
#31767=CARTESIAN_POINT('Ctrl Pts',(95.2965800354207,0.180082549199591,-9.58787833825366));
#31768=CARTESIAN_POINT('Ctrl Pts',(95.3037644127641,0.226516273037512,-9.59104554465697));
#31769=CARTESIAN_POINT('Ctrl Pts',(95.3137359849105,0.27254653004219,-9.59421275106028));
#31770=CARTESIAN_POINT('Ctrl Pts',(95.3264235423979,0.317818910265401,-9.59737995746359));
#31771=CARTESIAN_POINT('Ctrl Pts',(95.3391096627594,0.363086162463311,-9.60054680511584));
#31772=CARTESIAN_POINT('Ctrl Pts',(95.3545110052593,0.407595172278291,-9.6037136527681));
#31773=CARTESIAN_POINT('Ctrl Pts',(95.3725061662152,0.451005469222867,-9.60688050042035));
#31774=CARTESIAN_POINT('Ctrl Pts',(95.3905195439408,0.494459711058102,-9.61005055391968));
#31775=CARTESIAN_POINT('Ctrl Pts',(95.4111317638302,0.536812505535616,-9.61322060741901));
#31776=CARTESIAN_POINT('Ctrl Pts',(95.4341735615615,0.577744067736523,-9.61639066091834));
#31777=CARTESIAN_POINT('Ctrl Pts',(95.4572294046774,0.618700580227455,-9.61956264675912));
#31778=CARTESIAN_POINT('Ctrl Pts',(95.4827174703621,0.658233667833045,-9.6227346325999));
#31779=CARTESIAN_POINT('Ctrl Pts',(95.5104247906683,0.696051978963926,-9.62590661844068));
#31780=CARTESIAN_POINT('Ctrl Pts',(95.5381819171211,0.733938271564354,-9.62908430618227));
#31781=CARTESIAN_POINT('Ctrl Pts',(95.5681658979538,0.770103212244596,-9.63226199392386));
#31782=CARTESIAN_POINT('Ctrl Pts',(95.600124365354,0.804289506635592,-9.63543968166545));
#31783=CARTESIAN_POINT('Ctrl Pts',(95.608640393073,0.81339918724068,-9.63628644557784));
#31784=CARTESIAN_POINT('Ctrl Pts',(95.6172964320316,0.822368583475186,-9.63713320949022));
#31785=CARTESIAN_POINT('Ctrl Pts',(95.6260873072049,0.83119330607807,-9.63797997340261));
#31786=CARTESIAN_POINT('Ctrl Pts',(95.659076697028,0.864309714659412,-9.64115761206124));
#31787=CARTESIAN_POINT('Ctrl Pts',(95.6941138831242,0.895532572162974,-9.64433525071987));
#31788=CARTESIAN_POINT('Ctrl Pts',(95.7309530449706,0.92459942618441,-9.6475128893785));
#31789=CARTESIAN_POINT('Ctrl Pts',(95.7677301303009,0.953617300562,-9.65068517349791));
#31790=CARTESIAN_POINT('Ctrl Pts',(95.8063027412018,0.980486026979274,-9.65385745761732));
#31791=CARTESIAN_POINT('Ctrl Pts',(95.8463891762519,1.00498077416159,-9.65702974173673));
#31792=CARTESIAN_POINT('Ctrl Pts',(95.8709813003456,1.02000774928669,-9.65897586652003));
#31793=CARTESIAN_POINT('Ctrl Pts',(95.8961424522912,1.03414200586854,-9.66092199130333));
#31794=CARTESIAN_POINT('Ctrl Pts',(95.9218016730721,1.04733934308042,-9.66286811608663));
#31795=CARTESIAN_POINT('Origin',(96.460480949577,-7.19464945638997E-16,
0.924367114736168));
#31796=CARTESIAN_POINT('',(95.9218016730721,1.04733934308042,-10.2615611054409));
#31797=CARTESIAN_POINT('',(95.9218016730734,1.04733934308113,-10.1620395986893));
#31798=CARTESIAN_POINT('',(95.9218016730721,1.04733934308042,0.924367114736168));
#31799=CARTESIAN_POINT('',(97.6382305095403,-0.0010180895773768,-9.92436711477234));
#31800=CARTESIAN_POINT('Ctrl Pts',(97.6382305095403,-0.0010180895773768,
-9.92436711477234));
#31801=CARTESIAN_POINT('Ctrl Pts',(97.6381806027097,-0.0587514649425388,
-9.92826204859388));
#31802=CARTESIAN_POINT('Ctrl Pts',(97.6338815978861,-0.116299884304691,
-9.93215698241542));
#31803=CARTESIAN_POINT('Ctrl Pts',(97.625438007886,-0.173118788108036,-9.93605191623696));
#31804=CARTESIAN_POINT('Ctrl Pts',(97.6175259493788,-0.226360891431494,
-9.93970166051365));
#31805=CARTESIAN_POINT('Ctrl Pts',(97.6059752679963,-0.278962733452268,
-9.94335140479035));
#31806=CARTESIAN_POINT('Ctrl Pts',(97.5909097147114,-0.33049337278781,-9.94700114906704));
#31807=CARTESIAN_POINT('Ctrl Pts',(97.5773222760419,-0.376968227599609,
-9.95029280889402));
#31808=CARTESIAN_POINT('Ctrl Pts',(97.5608328375572,-0.422710422349559,
-9.953584468721));
#31809=CARTESIAN_POINT('Ctrl Pts',(97.5415427327874,-0.46733337499266,-9.95687612854798));
#31810=CARTESIAN_POINT('Ctrl Pts',(97.5229495237563,-0.510344229312774,
-9.96004887021799));
#31811=CARTESIAN_POINT('Ctrl Pts',(97.5017548078627,-0.552314770916328,
-9.96322161188801));
#31812=CARTESIAN_POINT('Ctrl Pts',(97.4781001221503,-0.592913384999275,
-9.96639435355802));
#31813=CARTESIAN_POINT('Ctrl Pts',(97.4544689782401,-0.633471594210228,
-9.96956393762711));
#31814=CARTESIAN_POINT('Ctrl Pts',(97.428382989555,-0.672660098913267,-9.97273352169621));
#31815=CARTESIAN_POINT('Ctrl Pts',(97.4000302804033,-0.710170484773801,
-9.9759031057653));
#31816=CARTESIAN_POINT('Ctrl Pts',(97.3716933177888,-0.747660038103485,
-9.97907092950972));
#31817=CARTESIAN_POINT('Ctrl Pts',(97.3410924639987,-0.783472874921223,
-9.98223875325413));
#31818=CARTESIAN_POINT('Ctrl Pts',(97.3084584366074,-0.817330559804014,
-9.98540657699855));
#31819=CARTESIAN_POINT('Ctrl Pts',(97.2758281805692,-0.851184331921751,
-9.98857403465325));
#31820=CARTESIAN_POINT('Ctrl Pts',(97.2411656054994,-0.883083001074866,
-9.99174149230796));
#31821=CARTESIAN_POINT('Ctrl Pts',(97.2047390264875,-0.912784189966875,
-9.99490894996267));
#31822=CARTESIAN_POINT('Ctrl Pts',(97.1682757546935,-0.942515297102116,
-9.9980795982226));
#31823=CARTESIAN_POINT('Ctrl Pts',(97.1300453672153,-0.970044155835744,
-10.0012502464825));
#31824=CARTESIAN_POINT('Ctrl Pts',(97.0903485259946,-0.995169281417913,
-10.0044208947425));
#31825=CARTESIAN_POINT('Ctrl Pts',(97.0506275949758,-1.02030965403694,-10.0075934670919));
#31826=CARTESIAN_POINT('Ctrl Pts',(97.0094389274154,-1.04304312138544,-10.0107660394414));
#31827=CARTESIAN_POINT('Ctrl Pts',(96.9671082056204,-1.06321394175111,-10.0139386117908));
#31828=CARTESIAN_POINT('Ctrl Pts',(96.9247016427121,-1.0834209008219,-10.0171168682253));
#31829=CARTESIAN_POINT('Ctrl Pts',(96.8811494611521,-1.10105584820427,-10.0202951246597));
#31830=CARTESIAN_POINT('Ctrl Pts',(96.8367959098715,-1.11601169938247,-10.0234733810941));
#31831=CARTESIAN_POINT('Ctrl Pts',(96.8250380789157,-1.11997639589215,-10.0243159157009));
#31832=CARTESIAN_POINT('Ctrl Pts',(96.813223998895,-1.12375309656353,-10.0251584503078));
#31833=CARTESIAN_POINT('Ctrl Pts',(96.8013602062103,-1.12734040772835,-10.0260009849146));
#31834=CARTESIAN_POINT('Ctrl Pts',(96.7550100985012,-1.14135550924732,-10.0292926447416));
#31835=CARTESIAN_POINT('Ctrl Pts',(96.707688119695,-1.15253944277112,-10.0325843045686));
#31836=CARTESIAN_POINT('Ctrl Pts',(96.6597734620364,-1.16076593548296,-10.0358759643956));
#31837=CARTESIAN_POINT('Ctrl Pts',(96.6135890375894,-1.16869536354693,-10.039048759987));
#31838=CARTESIAN_POINT('Ctrl Pts',(96.5668546157832,-1.1738772039746,-10.0422215555784));
#31839=CARTESIAN_POINT('Ctrl Pts',(96.5199253123462,-1.17624888107703,-10.0453943511699));
#31840=CARTESIAN_POINT('Ctrl Pts',(96.4730425246999,-1.17861820740015,-10.0485640019225));
#31841=CARTESIAN_POINT('Ctrl Pts',(96.4259657918948,-1.17818285547166,-10.0517336526751));
#31842=CARTESIAN_POINT('Ctrl Pts',(96.3790562392596,-1.17493194656105,-10.0549033034277));
#31843=CARTESIAN_POINT('Ctrl Pts',(96.3321725541524,-1.17168283031254,-10.0580712063267));
#31844=CARTESIAN_POINT('Ctrl Pts',(96.285456421646,-1.16562127115218,-10.0612391092258));
#31845=CARTESIAN_POINT('Ctrl Pts',(96.2392671177305,-1.15678844353658,-10.0644070121248));
#31846=CARTESIAN_POINT('Ctrl Pts',(96.193082973705,-1.14795660265201,-10.0675745611317));
#31847=CARTESIAN_POINT('Ctrl Pts',(96.1474260881076,-1.13635421467634,-10.0707421101386));
#31848=CARTESIAN_POINT('Ctrl Pts',(96.1026460672863,-1.12207364264383,-10.0739096591455));
#31849=CARTESIAN_POINT('Ctrl Pts',(96.0578206994124,-1.10777860921001,-10.0770804158109));
#31850=CARTESIAN_POINT('Ctrl Pts',(96.0138744993386,-1.09080015153705,-10.0802511724763));
#31851=CARTESIAN_POINT('Ctrl Pts',(95.9711404885939,-1.07128006410314,-10.0834219291416));
#31852=CARTESIAN_POINT('Ctrl Pts',(95.928380410353,-1.05174806953027,-10.0865946199499));
#31853=CARTESIAN_POINT('Ctrl Pts',(95.8868344850825,-1.02967162166471,-10.0897673107583));
#31854=CARTESIAN_POINT('Ctrl Pts',(95.8468110831302,-1.00523845803628,-10.0929400015666));
#31855=CARTESIAN_POINT('Ctrl Pts',(95.806715808977,-0.980761418446299,-10.0961183897485));
#31856=CARTESIAN_POINT('Ctrl Pts',(95.7681489670769,-0.953919541638821,
-10.0992967779304));
#31857=CARTESIAN_POINT('Ctrl Pts',(95.7313883121002,-0.924942694699029,
-10.1024751661123));
#31858=CARTESIAN_POINT('Ctrl Pts',(95.7216512258934,-0.917267367454935,
-10.1033170509956));
#31859=CARTESIAN_POINT('Ctrl Pts',(95.7120406676856,-0.909442456523787,
-10.1041589358789));
#31860=CARTESIAN_POINT('Ctrl Pts',(95.7025613640735,-0.901472664261251,
-10.1050008207622));
#31861=CARTESIAN_POINT('Ctrl Pts',(95.6654985262603,-0.87031181847344,-10.1082924805892));
#31862=CARTESIAN_POINT('Ctrl Pts',(95.6302740501501,-0.836788696719137,
-10.1115841404162));
#31863=CARTESIAN_POINT('Ctrl Pts',(95.5972018514032,-0.801151834021637,
-10.1148758002431));
#31864=CARTESIAN_POINT('Ctrl Pts',(95.5653691687261,-0.766850608677182,
-10.1180440916396));
#31865=CARTESIAN_POINT('Ctrl Pts',(95.5355307066674,-0.730591736558892,
-10.1212123830361));
#31866=CARTESIAN_POINT('Ctrl Pts',(95.5079326300622,-0.692637539763356,
-10.1243806744326));
#31867=CARTESIAN_POINT('Ctrl Pts',(95.4803619930838,-0.654721079257014,
-10.127545815728));
#31868=CARTESIAN_POINT('Ctrl Pts',(95.4550276605997,-0.615113080019186,
-10.1307109570233));
#31869=CARTESIAN_POINT('Ctrl Pts',(95.432135823626,-0.574109192081777,-10.1338760983186));
#31870=CARTESIAN_POINT('Ctrl Pts',(95.409256602328,-0.533127901358906,-10.1370394953067));
#31871=CARTESIAN_POINT('Ctrl Pts',(95.3888174824896,-0.490752732971964,
-10.1402028922948));
#31872=CARTESIAN_POINT('Ctrl Pts',(95.3709800685385,-0.447306262773352,
-10.1433662892829));
#31873=CARTESIAN_POINT('Ctrl Pts',(95.3531445804579,-0.403864483404788,
-10.1465293447253));
#31874=CARTESIAN_POINT('Ctrl Pts',(95.3379104508013,-0.359352149587515,
-10.1496924001676));
#31875=CARTESIAN_POINT('Ctrl Pts',(95.325391134186,-0.314111721359853,-10.15285545561));
#31876=CARTESIAN_POINT('Ctrl Pts',(95.3128589183797,-0.268824679970558,
-10.1560217700846));
#31877=CARTESIAN_POINT('Ctrl Pts',(95.3030472442471,-0.222808587547782,
-10.1591880845592));
#31878=CARTESIAN_POINT('Ctrl Pts',(95.296019103629,-0.176419023439901,-10.1623543990338));
#31879=CARTESIAN_POINT('Ctrl Pts',(95.2889866142775,-0.130000755317308,
-10.1655226726977));
#31880=CARTESIAN_POINT('Ctrl Pts',(95.2847411354154,-0.0832091126481367,
-10.1686909463616));
#31881=CARTESIAN_POINT('Ctrl Pts',(95.2832937069446,-0.036404097071164,
-10.1718592200254));
#31882=CARTESIAN_POINT('Ctrl Pts',(95.281843638736,0.0104862788335729,-10.1750332718068));
#31883=CARTESIAN_POINT('Ctrl Pts',(95.2832017799413,0.0573895182780501,
-10.1782073235882));
#31884=CARTESIAN_POINT('Ctrl Pts',(95.2873271589674,0.103948285595506,-10.1813813753695));
#31885=CARTESIAN_POINT('Ctrl Pts',(95.2884619364942,0.116755313142996,-10.1822544691163));
#31886=CARTESIAN_POINT('Ctrl Pts',(95.2898057970335,0.129536330417853,-10.183127562863));
#31887=CARTESIAN_POINT('Ctrl Pts',(95.2913572126147,0.142284047494008,-10.1840006566098));
#31888=CARTESIAN_POINT('Ctrl Pts',(95.2970996509865,0.189468683626648,-10.1872323419777));
#31889=CARTESIAN_POINT('Ctrl Pts',(95.3057158572815,0.23640975042499,-10.1904640273457));
#31890=CARTESIAN_POINT('Ctrl Pts',(95.3171708708936,0.282731544899127,-10.1936957127137));
#31891=CARTESIAN_POINT('Ctrl Pts',(95.3284350764437,0.328281749558332,-10.1968735673624));
#31892=CARTESIAN_POINT('Ctrl Pts',(95.3424441166781,0.373232591477927,-10.200051422011));
#31893=CARTESIAN_POINT('Ctrl Pts',(95.3591127838168,0.417232819838045,-10.2032292766597));
#31894=CARTESIAN_POINT('Ctrl Pts',(95.3757644930239,0.461188284399328,-10.2064038983059));
#31895=CARTESIAN_POINT('Ctrl Pts',(95.3950702767673,0.504194532880133,-10.2095785199522));
#31896=CARTESIAN_POINT('Ctrl Pts',(95.4168951568967,0.5459155207683,-10.2127531415984));
#31897=CARTESIAN_POINT('Ctrl Pts',(95.4387073502604,0.587612256317345,-10.2159259178425));
#31898=CARTESIAN_POINT('Ctrl Pts',(95.463035481669,0.628024720293765,-10.2190986940865));
#31899=CARTESIAN_POINT('Ctrl Pts',(95.4896976141636,0.666839394594824,-10.2222714703306));
#31900=CARTESIAN_POINT('Ctrl Pts',(95.5172115161952,0.706894073129085,-10.2255456065898));
#31901=CARTESIAN_POINT('Ctrl Pts',(95.5472108300608,0.745246560407001,-10.228819742849));
#31902=CARTESIAN_POINT('Ctrl Pts',(95.5794474925356,0.781584998623714,-10.2320938791082));
#31903=CARTESIAN_POINT('Ctrl Pts',(95.6107103637616,0.816825740912519,-10.2352691116661));
#31904=CARTESIAN_POINT('Ctrl Pts',(95.6440768495125,0.850172045732689,-10.238444344224));
#31905=CARTESIAN_POINT('Ctrl Pts',(95.6792821897892,0.881375947145148,-10.2416195767818));
#31906=CARTESIAN_POINT('Ctrl Pts',(95.7161324198789,0.914037780199677,-10.2449431648917));
#31907=CARTESIAN_POINT('Ctrl Pts',(95.7549970966545,0.944351592302617,-10.2482667530015));
#31908=CARTESIAN_POINT('Ctrl Pts',(95.7955356627768,0.972081698244651,-10.2515903411114));
#31909=CARTESIAN_POINT('Ctrl Pts',(95.8360742288991,0.999811804186684,-10.2549139292212));
#31910=CARTESIAN_POINT('Ctrl Pts',(95.8782860580672,1.02495790561954,-10.258237517331));
#31911=CARTESIAN_POINT('Ctrl Pts',(95.9218016730721,1.04733934308042,-10.2615611054409));
#31912=CARTESIAN_POINT('Ctrl Pts',(97.6382305277127,-0.000996845613527347,
-9.92470885738545));
#31913=CARTESIAN_POINT('Ctrl Pts',(97.6382801538142,0.0576352226910313,
-9.92106407212053));
#31914=CARTESIAN_POINT('Ctrl Pts',(97.6339515452507,0.116183996103659,-9.91737201317258));
#31915=CARTESIAN_POINT('Ctrl Pts',(97.6238067638071,0.184031654702508,-9.91289245550959));
#31916=CARTESIAN_POINT('Ctrl Pts',(97.6222061158262,0.193879417203326,-9.91223740586212));
#31917=CARTESIAN_POINT('Ctrl Pts',(97.6193519863662,0.210132245002773,-9.91114761288391));
#31918=CARTESIAN_POINT('Ctrl Pts',(97.6181700119439,0.216549468599535,-9.91071506970433));
#31919=CARTESIAN_POINT('Ctrl Pts',(97.6159496139914,0.228066461839842,-9.90993456331032));
#31920=CARTESIAN_POINT('Ctrl Pts',(97.6149305902757,0.23316983313823,-9.90958721204438));
#31921=CARTESIAN_POINT('Ctrl Pts',(97.612781071909,0.243575201327294,-9.90887584716385));
#31922=CARTESIAN_POINT('Ctrl Pts',(97.6116477269105,0.248876474805634,-9.90851175165997));
#31923=CARTESIAN_POINT('Ctrl Pts',(97.6091280253929,0.260276926404082,-9.90772506175124));
#31924=CARTESIAN_POINT('Ctrl Pts',(97.6077296053299,0.266373239017963,-9.9073020952274));
#31925=CARTESIAN_POINT('Ctrl Pts',(97.6038060038904,0.282873650352228,-9.90615091679084));
#31926=CARTESIAN_POINT('Ctrl Pts',(97.6011874598654,0.293254712049666,-9.90541976628536));
#31927=CARTESIAN_POINT('Ctrl Pts',(97.5865027625952,0.348295873656591,-9.90150522238407));
#31928=CARTESIAN_POINT('Ctrl Pts',(97.5719561322038,0.392246196541245,-9.89824351155558));
#31929=CARTESIAN_POINT('Ctrl Pts',(97.5366792409662,0.480951256307829,-9.89137881289994));
#31930=CARTESIAN_POINT('Ctrl Pts',(97.5156464724481,0.525492147390015,-9.88777371580748));
#31931=CARTESIAN_POINT('Ctrl Pts',(97.4705037390419,0.60738098579193,-9.88091039758668));
#31932=CARTESIAN_POINT('Ctrl Pts',(97.4469431123053,0.644942230630121,-9.87765930526512));
#31933=CARTESIAN_POINT('Ctrl Pts',(97.4063947070613,0.702145596063801,-9.87262071329951));
#31934=CARTESIAN_POINT('Ctrl Pts',(97.3907787047892,0.722708512700614,-9.87079041578914));
#31935=CARTESIAN_POINT('Ctrl Pts',(97.3707439113849,0.747363259811054,-9.8685875323534));
#31936=CARTESIAN_POINT('Ctrl Pts',(97.3669545463751,0.751954868190861,-9.86817691037815));
#31937=CARTESIAN_POINT('Ctrl Pts',(97.3609182142219,0.75915720110132,-9.86753249685616));
#31938=CARTESIAN_POINT('Ctrl Pts',(97.3586943954495,0.761787063403281,-9.86729712777962));
#31939=CARTESIAN_POINT('Ctrl Pts',(97.3544644337586,0.766745092457972,-9.86685332409398));
#31940=CARTESIAN_POINT('Ctrl Pts',(97.3524607296352,0.769075145214535,-9.86664473566317));
#31941=CARTESIAN_POINT('Ctrl Pts',(97.3477769109046,0.774478901664052,-9.86616088602439));
#31942=CARTESIAN_POINT('Ctrl Pts',(97.3450899226037,0.777546563358099,-9.86588612819152));
#31943=CARTESIAN_POINT('Ctrl Pts',(97.3361954144138,0.787595395004082,-9.86498558587274));
#31944=CARTESIAN_POINT('Ctrl Pts',(97.3299205775717,0.79451688268189,-9.86436448864603));
#31945=CARTESIAN_POINT('Ctrl Pts',(97.2679616180738,0.861247814878739,-9.85835974938475));
#31946=CARTESIAN_POINT('Ctrl Pts',(97.2062692065016,0.915192176240851,-9.85336299830011));
#31947=CARTESIAN_POINT('Ctrl Pts',(97.0969737343874,0.992309519403442,-9.84508316506271));
#31948=CARTESIAN_POINT('Ctrl Pts',(97.0525303908639,1.01944990511408,-9.84184905581689));
#31949=CARTESIAN_POINT('Ctrl Pts',(96.9889517237128,1.05271236413513,-9.83726348600444));
#31950=CARTESIAN_POINT('Ctrl Pts',(96.9712354578083,1.06142095652103,-9.8359902521145));
#31951=CARTESIAN_POINT('Ctrl Pts',(96.9399081945275,1.07585421641041,-9.83374015045288));
#31952=CARTESIAN_POINT('Ctrl Pts',(96.9263926018372,1.0817758912957,-9.83276982234651));
#31953=CARTESIAN_POINT('Ctrl Pts',(96.9064821015594,1.09005706697645,-9.83133925015582));
#31954=CARTESIAN_POINT('Ctrl Pts',(96.9001719515042,1.09261761673607,-9.83088570534459));
#31955=CARTESIAN_POINT('Ctrl Pts',(96.8887371588211,1.09714256089942,-9.83006336162246));
#31956=CARTESIAN_POINT('Ctrl Pts',(96.883620281411,1.09912614554078,-9.82969521096513));
#31957=CARTESIAN_POINT('Ctrl Pts',(96.8729364203986,1.103182139054,-9.82892608882737));
#31958=CARTESIAN_POINT('Ctrl Pts',(96.8673672593067,1.10524833230617,-9.82852492460978));
#31959=CARTESIAN_POINT('Ctrl Pts',(96.8528274858839,1.11051789247242,-9.82747681654377));
#31960=CARTESIAN_POINT('Ctrl Pts',(96.8438333698294,1.11365466222764,-9.8268277167494));
#31961=CARTESIAN_POINT('Ctrl Pts',(96.8060362470582,1.12632458584874,-9.82409612623462));
#31962=CARTESIAN_POINT('Ctrl Pts',(96.7769107040048,1.13485129356437,-9.82198164721496));
#31963=CARTESIAN_POINT('Ctrl Pts',(96.6664565976677,1.16260491853207,-9.81392200863383));
#31964=CARTESIAN_POINT('Ctrl Pts',(96.5834940684395,1.17428296453015,-9.8077649385387));
#31965=CARTESIAN_POINT('Ctrl Pts',(96.4477045517467,1.17884292769989,-9.79781929621551));
#31966=CARTESIAN_POINT('Ctrl Pts',(96.3953347810975,1.17711136635979,-9.79402209813135));
#31967=CARTESIAN_POINT('Ctrl Pts',(96.3363194618872,1.17120770129634,-9.78989694955664));
#31968=CARTESIAN_POINT('Ctrl Pts',(96.3293964913265,1.17045308546199,-9.7894154967316));
#31969=CARTESIAN_POINT('Ctrl Pts',(96.3188416492059,1.16920776426879,-9.78868563083916));
#31970=CARTESIAN_POINT('Ctrl Pts',(96.315204843989,1.16876145620009,-9.78843490215801));
#31971=CARTESIAN_POINT('Ctrl Pts',(96.308551238925,1.16791339028995,-9.78797764555098));
#31972=CARTESIAN_POINT('Ctrl Pts',(96.3055339004876,1.16751691064055,-9.78777084096204));
#31973=CARTESIAN_POINT('Ctrl Pts',(96.2987258050736,1.16659546546901,-9.78730546124991));
#31974=CARTESIAN_POINT('Ctrl Pts',(96.2949360477026,1.16606371752286,-9.78704726413025));
#31975=CARTESIAN_POINT('Ctrl Pts',(96.2851469566983,1.16464150575536,-9.7863823947235));
#31976=CARTESIAN_POINT('Ctrl Pts',(96.2791516997647,1.1637231427491,-9.78597720705927));
#31977=CARTESIAN_POINT('Ctrl Pts',(96.2389314744389,1.15724377140681,-9.78327080496709));
#31978=CARTESIAN_POINT('Ctrl Pts',(96.2049558135718,1.15021942579944,-9.78104224921283));
#31979=CARTESIAN_POINT('Ctrl Pts',(96.144034545726,1.134790700971,-9.77707133712284));
#31980=CARTESIAN_POINT('Ctrl Pts',(96.1169884396967,1.12689896503417,-9.77531763904385));
#31981=CARTESIAN_POINT('Ctrl Pts',(96.0447474830146,1.10297701717483,-9.77059927321858));
#31982=CARTESIAN_POINT('Ctrl Pts',(96.0002077029332,1.08514564095304,-9.76765156992421));
#31983=CARTESIAN_POINT('Ctrl Pts',(95.9450885397877,1.05907310395355,-9.76383858890257));
#31984=CARTESIAN_POINT('Ctrl Pts',(95.933394606705,1.05330195059611,-9.76301990498141));
#31985=CARTESIAN_POINT('Ctrl Pts',(95.9218016501122,1.04733933127145,-9.76219702307975));
#31986=CARTESIAN_POINT('',(97.6382307323089,0.000715384519801949,-9.8256328852061));
#31987=CARTESIAN_POINT('Ctrl Pts',(95.9218016730721,1.04733934308042,-9.66286811608663));
#31988=CARTESIAN_POINT('Ctrl Pts',(95.9635682821251,1.06882121225243,-9.66603590647616));
#31989=CARTESIAN_POINT('Ctrl Pts',(96.0066556356306,1.08781817527742,-9.6692036968657));
#31990=CARTESIAN_POINT('Ctrl Pts',(96.0507368574096,1.10417609167826,-9.67237148725523));
#31991=CARTESIAN_POINT('Ctrl Pts',(96.0948048958174,1.12052911591698,-9.67553833025368));
#31992=CARTESIAN_POINT('Ctrl Pts',(96.1398656906136,1.13424446519297,-9.67870517325213));
#31993=CARTESIAN_POINT('Ctrl Pts',(96.1855734795076,1.14521654956608,-9.68187201625059));
#31994=CARTESIAN_POINT('Ctrl Pts',(96.2313214648289,1.15619828302968,-9.68504164423989));
#31995=CARTESIAN_POINT('Ctrl Pts',(96.2777170379303,1.16443180029753,-9.6882112722292));
#31996=CARTESIAN_POINT('Ctrl Pts',(96.3244022900723,1.16986224014941,-9.69138090021851));
#31997=CARTESIAN_POINT('Ctrl Pts',(96.3711082203464,1.17529508528663,-9.69455193211983));
#31998=CARTESIAN_POINT('Ctrl Pts',(96.418103527799,1.17792234517528,-9.69772296402114));
#31999=CARTESIAN_POINT('Ctrl Pts',(96.4650268891008,1.1777412266427,-9.70089399592246));
#32000=CARTESIAN_POINT('Ctrl Pts',(96.5120406832511,1.17755975905019,-9.70407113918151));
#32001=CARTESIAN_POINT('Ctrl Pts',(96.5589816965096,1.1745591380844,-9.70724828244057));
#32002=CARTESIAN_POINT('Ctrl Pts',(96.6054919617845,1.16878863308921,-9.71042542569963));
#32003=CARTESIAN_POINT('Ctrl Pts',(96.6374752134872,1.16482048729125,-9.71261022021648));
#32004=CARTESIAN_POINT('Ctrl Pts',(96.6692548903594,1.15954362425323,-9.71479501473333));
#32005=CARTESIAN_POINT('Ctrl Pts',(96.7007181266502,1.15298792762625,-9.71697980925018));
#32006=CARTESIAN_POINT('Ctrl Pts',(96.7481213355683,1.14311096983527,-9.72027146907716));
#32007=CARTESIAN_POINT('Ctrl Pts',(96.795023380856,1.13028308657472,-9.72356312890414));
#32008=CARTESIAN_POINT('Ctrl Pts',(96.841030772512,1.11457475961201,-9.72685478873112));
#32009=CARTESIAN_POINT('Ctrl Pts',(96.8853676900685,1.09943678346448,-9.73002693227416));
#32010=CARTESIAN_POINT('Ctrl Pts',(96.9288732279279,1.08162415454859,-9.73319907581719));
#32011=CARTESIAN_POINT('Ctrl Pts',(96.9712057273268,1.06125174388191,-9.73637121936022));
#32012=CARTESIAN_POINT('Ctrl Pts',(97.0134961557979,1.04089957974523,-9.73954021036031));
#32013=CARTESIAN_POINT('Ctrl Pts',(97.0546153529805,1.01799290967789,-9.7427092013604));
#32014=CARTESIAN_POINT('Ctrl Pts',(97.0942411095978,0.99269487863614,-9.74587819236049));
#32015=CARTESIAN_POINT('Ctrl Pts',(97.1338449318395,0.967410851024522,-9.74904542920256));
#32016=CARTESIAN_POINT('Ctrl Pts',(97.1719564818968,0.939738384116108,-9.75221266604463));
#32017=CARTESIAN_POINT('Ctrl Pts',(97.2082800752212,0.909885448936166,-9.7553799028867));
#32018=CARTESIAN_POINT('Ctrl Pts',(97.2445995535471,0.880035895711941,-9.75854678092135));
#32019=CARTESIAN_POINT('Ctrl Pts',(97.2791310481007,0.848006720107118,-9.761713658956));
#32020=CARTESIAN_POINT('Ctrl Pts',(97.3116118558093,0.814046216720059,-9.76488053699065));
#32021=CARTESIAN_POINT('Ctrl Pts',(97.3441255408362,0.780051338255487,-9.76805062056311));
#32022=CARTESIAN_POINT('Ctrl Pts',(97.3745840125977,0.744121636176582,-9.77122070413557));
#32023=CARTESIAN_POINT('Ctrl Pts',(97.4027627835324,0.706540874895221,-9.77439078770804));
#32024=CARTESIAN_POINT('Ctrl Pts',(97.4309587296713,0.66893720781536,-9.77756280347381));
#32025=CARTESIAN_POINT('Ctrl Pts',(97.4568719028352,0.629680944506121,-9.78073481923959));
#32026=CARTESIAN_POINT('Ctrl Pts',(97.4803214470516,0.589084393114236,-9.78390683500536));
#32027=CARTESIAN_POINT('Ctrl Pts',(97.5038131395076,0.548414873431017,-9.78708455215617));
#32028=CARTESIAN_POINT('Ctrl Pts',(97.5248321236364,0.506400759705283,-9.79026226930698));
#32029=CARTESIAN_POINT('Ctrl Pts',(97.5432445882813,0.463376699025593,-9.79343998645779));
#32030=CARTESIAN_POINT('Ctrl Pts',(97.5481497211905,0.451914966987065,-9.79428653933777));
#32031=CARTESIAN_POINT('Ctrl Pts',(97.5528701407934,0.440381647634523,-9.79513309221775));
#32032=CARTESIAN_POINT('Ctrl Pts',(97.5574039162688,0.428783240862008,-9.79597964509773));
#32033=CARTESIAN_POINT('Ctrl Pts',(97.5766340932484,0.379588167985355,-9.79957033056353));
#32034=CARTESIAN_POINT('Ctrl Pts',(97.5925738799491,0.329038825425604,-9.80316101602933));
#32035=CARTESIAN_POINT('Ctrl Pts',(97.6050574650756,0.277560196478159,-9.80675170149513));
#32036=CARTESIAN_POINT('Ctrl Pts',(97.6174476028956,0.22646691670523,-9.81031550847352));
#32037=CARTESIAN_POINT('Ctrl Pts',(97.6264329545018,0.174458471699299,-9.81387931545191));
#32038=CARTESIAN_POINT('Ctrl Pts',(97.6318980705591,0.121971271904094,-9.8174431224303));
#32039=CARTESIAN_POINT('Ctrl Pts',(97.6360844181291,0.0817654173506131,
-9.82017304335557));
#32040=CARTESIAN_POINT('Ctrl Pts',(97.6382060932456,0.0412790962920784,
-9.82290296428083));
#32041=CARTESIAN_POINT('Ctrl Pts',(97.6382307323089,0.000715384519801949,
-9.8256328852061));
#32042=CARTESIAN_POINT('Ctrl Pts',(95.9218016730735,1.04733934308113,-10.1620395986893));
#32043=CARTESIAN_POINT('Ctrl Pts',(95.888261773431,1.03008872703891,-10.1593489153631));
#32044=CARTESIAN_POINT('Ctrl Pts',(95.8555669796334,1.01123548773281,-10.1567049044136));
#32045=CARTESIAN_POINT('Ctrl Pts',(95.8152007394698,0.985298798942619,-10.1534117848218));
#32046=CARTESIAN_POINT('Ctrl Pts',(95.8066439065627,0.979641467820415,-10.1527119137219));
#32047=CARTESIAN_POINT('Ctrl Pts',(95.7931180721235,0.970442712425622,-10.1516024355852));
#32048=CARTESIAN_POINT('Ctrl Pts',(95.7881009549726,0.966973326194928,-10.1511901840541));
#32049=CARTESIAN_POINT('Ctrl Pts',(95.7791000189668,0.960645162991395,-10.1504491972815));
#32050=CARTESIAN_POINT('Ctrl Pts',(95.7751067001287,0.957800209444742,-10.1501199537778));
#32051=CARTESIAN_POINT('Ctrl Pts',(95.7657386763271,0.951037575232609,-10.1493463161735));
#32052=CARTESIAN_POINT('Ctrl Pts',(95.7603791214077,0.947099112546189,-10.1489027235269));
#32053=CARTESIAN_POINT('Ctrl Pts',(95.7447527531734,0.935410961680217,-10.1476062117876));
#32054=CARTESIAN_POINT('Ctrl Pts',(95.7345789796638,0.92753806905986,-10.1467580444287));
#32055=CARTESIAN_POINT('Ctrl Pts',(95.7117338453776,0.909253385134437,-10.1448423971243));
#32056=CARTESIAN_POINT('Ctrl Pts',(95.6991467431417,0.898740346372868,-10.1437789092505));
#32057=CARTESIAN_POINT('Ctrl Pts',(95.6575631723686,0.862508015541709,-10.1402313511631));
#32058=CARTESIAN_POINT('Ctrl Pts',(95.6296165622779,0.835620584606594,-10.1377903359856));
#32059=CARTESIAN_POINT('Ctrl Pts',(95.5598933337758,0.761576684689437,-10.1314499105702));
#32060=CARTESIAN_POINT('Ctrl Pts',(95.5204864392328,0.712367189311339,-10.1276048056369));
#32061=CARTESIAN_POINT('Ctrl Pts',(95.4796709869745,0.652076839046914,-10.1230383661827));
#32062=CARTESIAN_POINT('Ctrl Pts',(95.4742434635255,0.643838489605852,-10.1224171507759));
#32063=CARTESIAN_POINT('Ctrl Pts',(95.4511054372985,0.607738466445831,-10.1197026822154));
#32064=CARTESIAN_POINT('Ctrl Pts',(95.4344690216764,0.579209847484569,-10.1175772682531));
#32065=CARTESIAN_POINT('Ctrl Pts',(95.4162608407933,0.544734070495049,-10.1149863272038));
#32066=CARTESIAN_POINT('Ctrl Pts',(95.4135077266959,0.539423683243594,-10.1145866235292));
#32067=CARTESIAN_POINT('Ctrl Pts',(95.4090715302349,0.530704949517532,-10.1139289987079));
#32068=CARTESIAN_POINT('Ctrl Pts',(95.4073642468499,0.527308941652815,-10.113672509593));
#32069=CARTESIAN_POINT('Ctrl Pts',(95.4043211380382,0.521182076564831,-10.1132090510234));
#32070=CARTESIAN_POINT('Ctrl Pts',(95.4029794111144,0.518454241117204,-10.1130024474001));
#32071=CARTESIAN_POINT('Ctrl Pts',(95.4000367101134,0.512412550330849,-10.1125442644445));
#32072=CARTESIAN_POINT('Ctrl Pts',(95.398440721472,0.509096414939712,-10.1122923984972));
#32073=CARTESIAN_POINT('Ctrl Pts',(95.3938304133719,0.499401117595293,-10.1115550329371));
#32074=CARTESIAN_POINT('Ctrl Pts',(95.3908579078187,0.493002418947527,-10.1110671402633));
#32075=CARTESIAN_POINT('Ctrl Pts',(95.3635579726657,0.432826586599409,-10.1064697672331));
#32076=CARTESIAN_POINT('Ctrl Pts',(95.343250749446,0.377324657832871,-10.1021662847394));
#32077=CARTESIAN_POINT('Ctrl Pts',(95.3002693628489,0.225362255868542,-10.090584592765));
#32078=CARTESIAN_POINT('Ctrl Pts',(95.2854404327732,0.127148103675182,-10.083342344266));
#32079=CARTESIAN_POINT('Ctrl Pts',(95.2827266604897,0.0139346068543939,
-10.0755098723727));
#32080=CARTESIAN_POINT('Ctrl Pts',(95.2826442712784,-0.000359380236713434,
-10.0745292631217));
#32081=CARTESIAN_POINT('Ctrl Pts',(95.2829082815413,-0.0215794457754825,
-10.0730851979032));
#32082=CARTESIAN_POINT('Ctrl Pts',(95.2830555977114,-0.0285062330002688,
-10.0726156634369));
#32083=CARTESIAN_POINT('Ctrl Pts',(95.2834277714089,-0.0408717785347733,
-10.0717806325756));
#32084=CARTESIAN_POINT('Ctrl Pts',(95.283629225366,-0.0463109862119375,
-10.0714144253475));
#32085=CARTESIAN_POINT('Ctrl Pts',(95.2841356235354,-0.0578249888279326,
-10.0706414539736));
#32086=CARTESIAN_POINT('Ctrl Pts',(95.2844499354126,-0.0638992292770024,
-10.0702349898058));
#32087=CARTESIAN_POINT('Ctrl Pts',(95.2854172200213,-0.0801518116237249,
-10.0691507884375));
#32088=CARTESIAN_POINT('Ctrl Pts',(95.2861553823033,-0.0903247152776928,
-10.068475690877));
#32089=CARTESIAN_POINT('Ctrl Pts',(95.2906289953621,-0.142566142722666,
-10.0650251361004));
#32090=CARTESIAN_POINT('Ctrl Pts',(95.2964933534475,-0.184423914363375,
-10.0623163953557));
#32091=CARTESIAN_POINT('Ctrl Pts',(95.3258637503889,-0.334719792393613,
-10.0526567048008));
#32092=CARTESIAN_POINT('Ctrl Pts',(95.3623944572716,-0.439992172540652,
-10.046062538312));
#32093=CARTESIAN_POINT('Ctrl Pts',(95.4200956534769,-0.55220270225605,-10.0378572284002));
#32094=CARTESIAN_POINT('Ctrl Pts',(95.4273602683316,-0.56567746326182,-10.0368499613925));
#32095=CARTESIAN_POINT('Ctrl Pts',(95.4374233055472,-0.583502166092287,
-10.035482718913));
#32096=CARTESIAN_POINT('Ctrl Pts',(95.4399911069541,-0.587981461865471,
-10.035136140243));
#32097=CARTESIAN_POINT('Ctrl Pts',(95.4440694523484,-0.594988572672264,
-10.0345890214545));
#32098=CARTESIAN_POINT('Ctrl Pts',(95.4455602050996,-0.597527920064433,
-10.0343897177194));
#32099=CARTESIAN_POINT('Ctrl Pts',(95.4486397775407,-0.602728889068124,
-10.0339793373284));
#32100=CARTESIAN_POINT('Ctrl Pts',(95.4502295895196,-0.605389841116122,
-10.0337681917898));
#32101=CARTESIAN_POINT('Ctrl Pts',(95.4540610766905,-0.611745682069473,
-10.0332610625066));
#32102=CARTESIAN_POINT('Ctrl Pts',(95.4563126085743,-0.615434546903135,
-10.032964457346));
#32103=CARTESIAN_POINT('Ctrl Pts',(95.4641120340017,-0.628056224711486,
-10.0319419969388));
#32104=CARTESIAN_POINT('Ctrl Pts',(95.4697590395076,-0.636926773730438,
-10.0312102471663));
#32105=CARTESIAN_POINT('Ctrl Pts',(95.4839014940081,-0.658499140600936,
-10.029400354284));
#32106=CARTESIAN_POINT('Ctrl Pts',(95.4925266734307,-0.671113271764405,
-10.0283157031952));
#32107=CARTESIAN_POINT('Ctrl Pts',(95.5292590425077,-0.722651923900813,
-10.0237843863106));
#32108=CARTESIAN_POINT('Ctrl Pts',(95.5594867214393,-0.760005873761361,
-10.0202613152457));
#32109=CARTESIAN_POINT('Ctrl Pts',(95.6514427378895,-0.860420361980952,
-10.0102684222191));
#32110=CARTESIAN_POINT('Ctrl Pts',(95.7181000901939,-0.918554465293736,
-10.0038521042937));
#32111=CARTESIAN_POINT('Ctrl Pts',(95.8018228052623,-0.976447435199542,
-9.99680235943189));
#32112=CARTESIAN_POINT('Ctrl Pts',(95.8131462367423,-0.983990823712108,
-9.99586726028539));
#32113=CARTESIAN_POINT('Ctrl Pts',(95.8304001477105,-0.995058167986903,
-9.9944692739616));
#32114=CARTESIAN_POINT('Ctrl Pts',(95.8362347074016,-0.998728795613086,
-9.99400105322965));
#32115=CARTESIAN_POINT('Ctrl Pts',(95.8464380625732,-1.00502356268872,-9.99318994388906));
#32116=CARTESIAN_POINT('Ctrl Pts',(95.850792235726,-1.00767092954312,-9.99284621911854));
#32117=CARTESIAN_POINT('Ctrl Pts',(95.8599331017923,-1.01314769925201,-9.99212957445861));
#32118=CARTESIAN_POINT('Ctrl Pts',(95.864722935638,-1.01597163769923,-9.99175685755465));
#32119=CARTESIAN_POINT('Ctrl Pts',(95.8761752479715,-1.02261472716414,-9.9908722483766));
#32120=CARTESIAN_POINT('Ctrl Pts',(95.8828554903665,-1.02640287736543,-9.99036146787082));
#32121=CARTESIAN_POINT('Ctrl Pts',(95.9057764301352,-1.03910595056267,-9.98862612915265));
#32122=CARTESIAN_POINT('Ctrl Pts',(95.9221907267037,-1.04770319137999,-9.98741267845175));
#32123=CARTESIAN_POINT('Ctrl Pts',(96.0027687103406,-1.08751326578403,-9.98158374131929));
#32124=CARTESIAN_POINT('Ctrl Pts',(96.0694775105861,-1.11324006429486,-9.97715581258178));
#32125=CARTESIAN_POINT('Ctrl Pts',(96.2113855190697,-1.15362494479511,-9.96802786074716));
#32126=CARTESIAN_POINT('Ctrl Pts',(96.2865000091455,-1.16731586352173,-9.96334830735557));
#32127=CARTESIAN_POINT('Ctrl Pts',(96.3718587889917,-1.17444936888773,-9.95770514904642));
#32128=CARTESIAN_POINT('Ctrl Pts',(96.3813291240349,-1.17512560262499,-9.95707448747302));
#32129=CARTESIAN_POINT('Ctrl Pts',(96.3946503808759,-1.17591505991703,-9.95617966354205));
#32130=CARTESIAN_POINT('Ctrl Pts',(96.3984955613975,-1.17612401664654,-9.95592047000262));
#32131=CARTESIAN_POINT('Ctrl Pts',(96.4054558151129,-1.17646802715395,-9.95544955249841));
#32132=CARTESIAN_POINT('Ctrl Pts',(96.4085705675512,-1.17660957680288,-9.95523818191956));
#32133=CARTESIAN_POINT('Ctrl Pts',(96.414953207416,-1.17687424195171,-9.954803688138));
#32134=CARTESIAN_POINT('Ctrl Pts',(96.4182210942268,-1.1769961175118,-9.95458050267244));
#32135=CARTESIAN_POINT('Ctrl Pts',(96.4266433346419,-1.17727510402364,-9.95400349326213));
#32136=CARTESIAN_POINT('Ctrl Pts',(96.4317982212409,-1.17741197266356,-9.95364859493921));
#32137=CARTESIAN_POINT('Ctrl Pts',(96.4536926575093,-1.17784943243337,-9.95213431927845));
#32138=CARTESIAN_POINT('Ctrl Pts',(96.470435786317,-1.17782689578065,-9.95095918858546));
#32139=CARTESIAN_POINT('Ctrl Pts',(96.516446127152,-1.17678392128936,-9.94769264404571));
#32140=CARTESIAN_POINT('Ctrl Pts',(96.5456838042588,-1.17502882621059,-9.94557558481078));
#32141=CARTESIAN_POINT('Ctrl Pts',(96.6690472386191,-1.16299515942741,-9.93653961912611));
#32142=CARTESIAN_POINT('Ctrl Pts',(96.7618363369293,-1.14247424365495,-9.92952377618136));
#32143=CARTESIAN_POINT('Ctrl Pts',(96.8786796636577,-1.1013878588755,-9.92077063703396));
#32144=CARTESIAN_POINT('Ctrl Pts',(96.9058218443952,-1.0906957066487,-9.91873992702453));
#32145=CARTESIAN_POINT('Ctrl Pts',(96.9411448422072,-1.07524205382913,-9.91609879669278));
#32146=CARTESIAN_POINT('Ctrl Pts',(96.9497033041997,-1.07137516706136,-9.91545896774468));
#32147=CARTESIAN_POINT('Ctrl Pts',(96.9635704411533,-1.06490889063338,-9.9144221716096));
#32148=CARTESIAN_POINT('Ctrl Pts',(96.9689072742165,-1.06237124231196,-9.91402313230847));
#32149=CARTESIAN_POINT('Ctrl Pts',(96.9790714965607,-1.05744404901172,-9.91326300862201));
#32150=CARTESIAN_POINT('Ctrl Pts',(96.9839020198036,-1.0550613522902,-9.91290170191342));
#32151=CARTESIAN_POINT('Ctrl Pts',(96.9950258677392,-1.04947921939243,-9.91206944042876));
#32152=CARTESIAN_POINT('Ctrl Pts',(97.0013071531924,-1.04625614577938,-9.91159931353711));
#32153=CARTESIAN_POINT('Ctrl Pts',(97.0144949258753,-1.03933869178777,-9.91061166562369));
#32154=CARTESIAN_POINT('Ctrl Pts',(97.0213943273127,-1.03563149317603,-9.91009460965194));
#32155=CARTESIAN_POINT('Ctrl Pts',(97.0397990658844,-1.02550434216245,-9.90871391134123));
#32156=CARTESIAN_POINT('Ctrl Pts',(97.0512347126509,-1.01895959120846,-9.90785454178366));
#32157=CARTESIAN_POINT('Ctrl Pts',(97.0866156254206,-0.997914792268039,
-9.90518802772534));
#32158=CARTESIAN_POINT('Ctrl Pts',(97.1101561097657,-0.982751706818436,
-9.90340288499774));
#32159=CARTESIAN_POINT('Ctrl Pts',(97.2248076452797,-0.902979497191556,
-9.89459247192391));
#32160=CARTESIAN_POINT('Ctrl Pts',(97.3069268645222,-0.826492477722364,
-9.88795467212626));
#32161=CARTESIAN_POINT('Ctrl Pts',(97.3862070410129,-0.728244019838939,
-9.87973277799941));
#32162=CARTESIAN_POINT('Ctrl Pts',(97.3951614703776,-0.716715023836339,
-9.87877121204384));
#32163=CARTESIAN_POINT('Ctrl Pts',(97.4069342223431,-0.700961465935517,
-9.8774570661882));
#32164=CARTESIAN_POINT('Ctrl Pts',(97.4099432926679,-0.696880212795816,
-9.87711659122189));
#32165=CARTESIAN_POINT('Ctrl Pts',(97.4146481318012,-0.690411923224071,
-9.87657672374598));
#32166=CARTESIAN_POINT('Ctrl Pts',(97.4163615572294,-0.688037716119957,
-9.8763785097204));
#32167=CARTESIAN_POINT('Ctrl Pts',(97.4198774149365,-0.683127488093659,
-9.87596840541136));
#32168=CARTESIAN_POINT('Ctrl Pts',(97.4216786600278,-0.680590701696456,
-9.87575643427933));
#32169=CARTESIAN_POINT('Ctrl Pts',(97.4259958715206,-0.674459227935635,
-9.8752439086207));
#32170=CARTESIAN_POINT('Ctrl Pts',(97.4285018271635,-0.670857580754674,
-9.87494269864116));
#32171=CARTESIAN_POINT('Ctrl Pts',(97.4371788796961,-0.658236769065402,
-9.87388691498471));
#32172=CARTESIAN_POINT('Ctrl Pts',(97.4432442978418,-0.649146108972023,
-9.87312593198335));
#32173=CARTESIAN_POINT('Ctrl Pts',(97.457924697957,-0.626466194525916,-9.871228631374));
#32174=CARTESIAN_POINT('Ctrl Pts',(97.4663891999685,-0.612782556946642,
-9.87008501300763));
#32175=CARTESIAN_POINT('Ctrl Pts',(97.5013283491712,-0.553624750344249,
-9.86515846798755));
#32176=CARTESIAN_POINT('Ctrl Pts',(97.5250188312985,-0.506578954432693,
-9.8612870786669));
#32177=CARTESIAN_POINT('Ctrl Pts',(97.5640175224767,-0.414213121392992,
-9.85393150416985));
#32178=CARTESIAN_POINT('Ctrl Pts',(97.5798717704727,-0.369229324892786,
-9.85045156034064));
#32179=CARTESIAN_POINT('Ctrl Pts',(97.6032868372855,-0.287236289973137,
-9.84434327526376));
#32180=CARTESIAN_POINT('Ctrl Pts',(97.611878053243,-0.250589743660362,-9.84169282201664));
#32181=CARTESIAN_POINT('Ctrl Pts',(97.6208371737923,-0.202007991339479,
-9.83828343368103));
#32182=CARTESIAN_POINT('Ctrl Pts',(97.6227994493443,-0.190393062337546,
-9.83747592967094));
#32183=CARTESIAN_POINT('Ctrl Pts',(97.6256590064557,-0.171770275114602,
-9.83619297917899));
#32184=CARTESIAN_POINT('Ctrl Pts',(97.6266680158628,-0.164780647625684,
-9.83571408758776));
#32185=CARTESIAN_POINT('Ctrl Pts',(97.6283480070159,-0.152353561576563,
-9.83486719100818));
#32186=CARTESIAN_POINT('Ctrl Pts',(97.6290440236013,-0.146919758176085,
-9.83449841766919));
#32187=CARTESIAN_POINT('Ctrl Pts',(97.6303123227838,-0.136438350955213,
-9.83378996016001));
#32188=CARTESIAN_POINT('Ctrl Pts',(97.6308899097117,-0.131391524674615,
-9.83345011919794));
#32189=CARTESIAN_POINT('Ctrl Pts',(97.6320625746442,-0.120523033875581,
-9.83272094112819));
#32190=CARTESIAN_POINT('Ctrl Pts',(97.6326469538532,-0.11470033288722,-9.83233194156775));
#32191=CARTESIAN_POINT('Ctrl Pts',(97.6339571437997,-0.100587900798589,
-9.83139296842295));
#32192=CARTESIAN_POINT('Ctrl Pts',(97.6346385516883,-0.0922942865073925,
-9.83084435762351));
#32193=CARTESIAN_POINT('Ctrl Pts',(97.6372463631197,-0.0558210827748878,
-9.82844486236497));
#32194=CARTESIAN_POINT('Ctrl Pts',(97.6382466819176,-0.0275837207897224,
-9.82662194597954));
#32195=CARTESIAN_POINT('Ctrl Pts',(97.638230762545,0.00066374236820414,
-9.82482230235678));
#32196=CARTESIAN_POINT('Origin',(96.460480949577,-8.32667268468867E-16,
1.18130019239114E-14));
#32197=CARTESIAN_POINT('',(97.9254959686812,0.00102976170736319,-0.160655045842894));
#32198=CARTESIAN_POINT('',(97.9240238517789,0.00148269405508262,-0.0893449541570721));
#32199=CARTESIAN_POINT('',(97.923980949577,-1.01189432752408E-15,1.19922289829666E-14));
#32200=CARTESIAN_POINT('',(95.825530156632,1.3210310846968,-3.74994559417826E-5));
#32201=CARTESIAN_POINT('Ctrl Pts',(97.9254959686812,0.00102976170736319,
-0.160655045842894));
#32202=CARTESIAN_POINT('Ctrl Pts',(97.9259403980951,0.0599082620416902,
-0.157443865218363));
#32203=CARTESIAN_POINT('Ctrl Pts',(97.8960926319347,0.60114388017442,-0.127899405977983));
#32204=CARTESIAN_POINT('Ctrl Pts',(97.2508483847669,1.50956313647968,-0.0743602238489917));
#32205=CARTESIAN_POINT('Ctrl Pts',(96.2230516351132,1.50901544022077,-0.0240322223445412));
#32206=CARTESIAN_POINT('Ctrl Pts',(95.825530156632,1.3210310846968,-3.74994559417826E-5));
#32207=CARTESIAN_POINT('',(97.0944880441522,1.31904027763685,1.17291095544168E-14));
#32208=CARTESIAN_POINT('Origin',(96.460480949577,-8.32667268468867E-16,
1.18130019239114E-14));
#32209=CARTESIAN_POINT('Ctrl Pts',(97.0944880441522,1.31904027763685,1.12063136548102E-14));
#32210=CARTESIAN_POINT('Ctrl Pts',(97.53097659376,1.10923861968598,-0.0263332786158426));
#32211=CARTESIAN_POINT('Ctrl Pts',(97.8934559885557,0.609749393684391,-0.0561149300015368));
#32212=CARTESIAN_POINT('Ctrl Pts',(97.9256366870345,0.0646804841820412,
-0.0858965813872315));
#32213=CARTESIAN_POINT('Ctrl Pts',(97.9251323125163,0.00148381702055458,
-0.0893449541570721));
#32214=CARTESIAN_POINT('Origin',(96.460480949577,-8.32667268468867E-16,
1.18130019239114E-14));
#32215=CARTESIAN_POINT('',(97.9237766744537,0.000379231245023859,-0.660655020925316));
#32216=CARTESIAN_POINT('',(97.9239809152273,0.0003170831650837,-0.589344954125679));
#32217=CARTESIAN_POINT('',(97.923980949577,-1.01189432752408E-15,1.19922289829666E-14));
#32218=CARTESIAN_POINT('Ctrl Pts',(97.9217394295534,0.000383291797303924,
-0.660654772361549));
#32219=CARTESIAN_POINT('Ctrl Pts',(97.9222492769024,0.219624290680771,-0.648776687925926));
#32220=CARTESIAN_POINT('Ctrl Pts',(97.7733939631201,0.924254639301895,-0.610565324874444));
#32221=CARTESIAN_POINT('Ctrl Pts',(96.6848024105838,1.71234718119464,-0.546020683207117));
#32222=CARTESIAN_POINT('Ctrl Pts',(95.1488986503746,1.12351576042364,-0.467020847359552));
#32223=CARTESIAN_POINT('Ctrl Pts',(94.8028899975499,-0.484641598927434,
-0.38802101151199));
#32224=CARTESIAN_POINT('Ctrl Pts',(95.9606267756977,-1.65300325887114,-0.309021175664427));
#32225=CARTESIAN_POINT('Ctrl Pts',(97.506407164997,-1.33544801236195,-0.233232520441395));
#32226=CARTESIAN_POINT('Ctrl Pts',(97.9222958558073,-0.42292473151319,-0.183777143834217));
#32227=CARTESIAN_POINT('Ctrl Pts',(97.9254959686812,0.00102976170736319,
-0.160655045842894));
#32228=CARTESIAN_POINT('Ctrl Pts',(97.9239801985517,0.00148264983063222,
-0.0893449541570721));
#32229=CARTESIAN_POINT('Ctrl Pts',(97.9240347313566,-0.052345784526501,
-0.0922844814261104));
#32230=CARTESIAN_POINT('Ctrl Pts',(97.9211153199247,-0.106304899557918,
-0.0952240086951486));
#32231=CARTESIAN_POINT('Ctrl Pts',(97.9152052727089,-0.160029352584068,
-0.0981635359641869));
#32232=CARTESIAN_POINT('Ctrl Pts',(97.9093025720355,-0.213687022899094,
-0.101099409224866));
#32233=CARTESIAN_POINT('Ctrl Pts',(97.9004166445377,-0.267110062615521,
-0.104035282485545));
#32234=CARTESIAN_POINT('Ctrl Pts',(97.8885827988832,-0.319933364950077,
-0.106971155746224));
#32235=CARTESIAN_POINT('Ctrl Pts',(97.8767585287381,-0.372713924625424,
-0.109904653407031));
#32236=CARTESIAN_POINT('Ctrl Pts',(97.8619911791886,-0.424895168884155,
-0.112838151067839));
#32237=CARTESIAN_POINT('Ctrl Pts',(97.8443675010344,-0.476120008711344,
-0.115771648728646));
#32238=CARTESIAN_POINT('Ctrl Pts',(97.8267504432777,-0.527325605744948,
-0.118704044410605));
#32239=CARTESIAN_POINT('Ctrl Pts',(97.8062793621778,-0.57757498729588,-0.121636440092565));
#32240=CARTESIAN_POINT('Ctrl Pts',(97.7830907012564,-0.626526691181278,
-0.124568835774524));
#32241=CARTESIAN_POINT('Ctrl Pts',(97.7598840200597,-0.675516436210291,
-0.127503510267565));
#32242=CARTESIAN_POINT('Ctrl Pts',(97.7339557736685,-0.723205985975424,
-0.130438184760606));
#32243=CARTESIAN_POINT('Ctrl Pts',(97.7054896108962,-0.769276077387165,
-0.133372859253647));
#32244=CARTESIAN_POINT('Ctrl Pts',(97.677013067021,-0.815362969741224,-0.13630860397024));
#32245=CARTESIAN_POINT('Ctrl Pts',(97.6459970808003,-0.859828773056688,
-0.139244348686834));
#32246=CARTESIAN_POINT('Ctrl Pts',(97.6126681478676,-0.902384014760494,
-0.142180093403427));
#32247=CARTESIAN_POINT('Ctrl Pts',(97.5792764156735,-0.945019440181892,
-0.145121369728251));
#32248=CARTESIAN_POINT('Ctrl Pts',(97.5435634017889,-0.985736700446781,
-0.148062646053075));
#32249=CARTESIAN_POINT('Ctrl Pts',(97.5057943185634,-1.02428131419951,-0.151003922377899));
#32250=CARTESIAN_POINT('Ctrl Pts',(97.4758500575231,-1.0548404349761,-0.15333583881697));
#32251=CARTESIAN_POINT('Ctrl Pts',(97.444614229094,-1.08403456024074,-0.155667755256041));
#32252=CARTESIAN_POINT('Ctrl Pts',(97.4122330415994,-1.11175546112038,-0.157999671695112));
#32253=CARTESIAN_POINT('Ctrl Pts',(97.3703895406663,-1.14757686334716,-0.161013012317983));
#32254=CARTESIAN_POINT('Ctrl Pts',(97.3264338721171,-1.18110717537137,-0.164026352940854));
#32255=CARTESIAN_POINT('Ctrl Pts',(97.2806465605239,-1.21208936164794,-0.167039693563725));
#32256=CARTESIAN_POINT('Ctrl Pts',(97.2349409306402,-1.24301627763567,-0.170047658574781));
#32257=CARTESIAN_POINT('Ctrl Pts',(97.1874105755345,-1.27140379677066,-0.173055623585837));
#32258=CARTESIAN_POINT('Ctrl Pts',(97.1383689528339,-1.29703512097412,-0.176063588596893));
#32259=CARTESIAN_POINT('Ctrl Pts',(97.0893760987136,-1.32264095655748,-0.179068562389984));
#32260=CARTESIAN_POINT('Ctrl Pts',(97.0388754189467,-1.34549578440673,-0.182073536183075));
#32261=CARTESIAN_POINT('Ctrl Pts',(96.9872076383996,-1.36542712924639,-0.185078509976165));
#32262=CARTESIAN_POINT('Ctrl Pts',(96.9355709566339,-1.38534647743104,-0.188081675078766));
#32263=CARTESIAN_POINT('Ctrl Pts',(96.882769057068,-1.40234564142863,-0.191084840181366));
#32264=CARTESIAN_POINT('Ctrl Pts',(96.829163356026,-1.41629994463567,-0.194088005283967));
#32265=CARTESIAN_POINT('Ctrl Pts',(96.7755688796258,-1.43025132591364,-0.197090541545751));
#32266=CARTESIAN_POINT('Ctrl Pts',(96.7211714455109,-1.44115897994903,-0.200093077807535));
#32267=CARTESIAN_POINT('Ctrl Pts',(96.6663461461169,-1.44894850524564,-0.203095614069319));
#32268=CARTESIAN_POINT('Ctrl Pts',(96.6114718367766,-1.45674499382784,-0.206100834386511));
#32269=CARTESIAN_POINT('Ctrl Pts',(96.5561694206087,-1.46141771019846,-0.209106054703702));
#32270=CARTESIAN_POINT('Ctrl Pts',(96.5008211789853,-1.46294392096597,-0.212111275020894));
#32271=CARTESIAN_POINT('Ctrl Pts',(96.445448437896,-1.46447080729872,-0.215117825575331));
#32272=CARTESIAN_POINT('Ctrl Pts',(96.3900303584181,-1.46284842623924,-0.218124376129769));
#32273=CARTESIAN_POINT('Ctrl Pts',(96.3349480076539,-1.45810621372112,-0.221130926684206));
#32274=CARTESIAN_POINT('Ctrl Pts',(96.2797635962515,-1.45335521448221,-0.224143047997052));
#32275=CARTESIAN_POINT('Ctrl Pts',(96.2249166790471,-1.4454729104902,-0.227155169309899));
#32276=CARTESIAN_POINT('Ctrl Pts',(96.1707808295434,-1.4345403760273,-0.230167290622745));
#32277=CARTESIAN_POINT('Ctrl Pts',(96.1298497792372,-1.42627450189439,-0.232444696262722));
#32278=CARTESIAN_POINT('Ctrl Pts',(96.0893250666734,-1.41626602279057,-0.234722101902699));
#32279=CARTESIAN_POINT('Ctrl Pts',(96.049361832311,-1.40456873146829,-0.236999507542675));
#32280=CARTESIAN_POINT('Ctrl Pts',(95.9964555305478,-1.38908298727408,-0.240014506502302));
#32281=CARTESIAN_POINT('Ctrl Pts',(95.9443183765915,-1.37057251816803,-0.243029505461928));
#32282=CARTESIAN_POINT('Ctrl Pts',(95.8933191205839,-1.34913294738997,-0.246044504421554));
#32283=CARTESIAN_POINT('Ctrl Pts',(95.8424077195759,-1.32773030996411,-0.249054309526341));
#32284=CARTESIAN_POINT('Ctrl Pts',(95.7926308073448,-1.3034087877203,-0.252064114631127));
#32285=CARTESIAN_POINT('Ctrl Pts',(95.744341288851,-1.27631353371154,-0.255073919735913));
#32286=CARTESIAN_POINT('Ctrl Pts',(95.6960979979698,-1.24924421802115,-0.258080843550752));
#32287=CARTESIAN_POINT('Ctrl Pts',(95.6493397364313,-1.21940668764572,-0.26108776736559));
#32288=CARTESIAN_POINT('Ctrl Pts',(95.6043970392579,-1.18699308696079,-0.264094691180428));
#32289=CARTESIAN_POINT('Ctrl Pts',(95.5594797858355,-1.15459783683422,-0.267099912662611));
#32290=CARTESIAN_POINT('Ctrl Pts',(95.5163764850673,-1.11962971469893,-0.270105134144794));
#32291=CARTESIAN_POINT('Ctrl Pts',(95.4753888178461,-1.0823242314583,-0.273110355626977));
#32292=CARTESIAN_POINT('Ctrl Pts',(95.4344083235427,-1.04502527674649,-0.276115051189821));
#32293=CARTESIAN_POINT('Ctrl Pts',(95.3955431160815,-1.00539012750951,-0.279119746752666));
#32294=CARTESIAN_POINT('Ctrl Pts',(95.3590601363147,-0.963693126525499,
-0.28212444231551));
#32295=CARTESIAN_POINT('Ctrl Pts',(95.3225428291779,-0.921956892222702,
-0.285131965040406));
#32296=CARTESIAN_POINT('Ctrl Pts',(95.2884125745901,-0.878155327439156,
-0.288139487765303));
#32297=CARTESIAN_POINT('Ctrl Pts',(95.2568968923074,-0.832596941554766,
-0.291147010490199));
#32298=CARTESIAN_POINT('Ctrl Pts',(95.2253664007609,-0.787017147720452,
-0.294155946454275));
#32299=CARTESIAN_POINT('Ctrl Pts',(95.1964532052038,-0.739679336939152,
-0.297164882418351));
#32300=CARTESIAN_POINT('Ctrl Pts',(95.1703404015189,-0.690919399247418,
-0.300173818382427));
#32301=CARTESIAN_POINT('Ctrl Pts',(95.1441783218411,-0.642067449438771,
-0.30318843233915));
#32302=CARTESIAN_POINT('Ctrl Pts',(95.1208274126701,-0.591788490069951,
-0.306203046295873));
#32303=CARTESIAN_POINT('Ctrl Pts',(95.1004233833001,-0.540440252398773,
-0.309217660252597));
#32304=CARTESIAN_POINT('Ctrl Pts',(95.085123064707,-0.50193587753671,-0.311478221298477));
#32305=CARTESIAN_POINT('Ctrl Pts',(95.0714787848521,-0.462830705618857,
-0.313738782344358));
#32306=CARTESIAN_POINT('Ctrl Pts',(95.0595291290122,-0.423280340266479,
-0.315999343390238));
#32307=CARTESIAN_POINT('Ctrl Pts',(95.0436353007261,-0.370675752821941,
-0.319006038275412));
#32308=CARTESIAN_POINT('Ctrl Pts',(95.0306743464371,-0.317061713014208,
-0.322012733160585));
#32309=CARTESIAN_POINT('Ctrl Pts',(95.0207691273365,-0.262796725438043,
-0.325019428045759));
#32310=CARTESIAN_POINT('Ctrl Pts',(95.0108817741184,-0.208629614736458,
-0.328020699804321));
#32311=CARTESIAN_POINT('Ctrl Pts',(95.0040393134213,-0.153814402670927,
-0.331021971562884));
#32312=CARTESIAN_POINT('Ctrl Pts',(95.0003145610086,-0.0987236936862529,
-0.334023243321446));
#32313=CARTESIAN_POINT('Ctrl Pts',(94.9965935503585,-0.0436883269982326,
-0.337021500102074));
#32314=CARTESIAN_POINT('Ctrl Pts',(94.9959840799632,0.0116214628037488,
-0.340019756882702));
#32315=CARTESIAN_POINT('Ctrl Pts',(94.9985074346293,0.0668258302716808,
-0.343018013663329));
#32316=CARTESIAN_POINT('Ctrl Pts',(95.001029257557,0.121996687328589,-0.346014450428228));
#32317=CARTESIAN_POINT('Ctrl Pts',(95.0066801125293,0.177061721004989,-0.349010887193128));
#32318=CARTESIAN_POINT('Ctrl Pts',(95.0154292000922,0.231641298802641,-0.352007323958027));
#32319=CARTESIAN_POINT('Ctrl Pts',(95.0241764546891,0.286209441977913,-0.355003132958398));
#32320=CARTESIAN_POINT('Ctrl Pts',(95.0360205692775,0.340291808672809,-0.357998941958769));
#32321=CARTESIAN_POINT('Ctrl Pts',(95.0508792097159,0.393516435464501,-0.36099475095914));
#32322=CARTESIAN_POINT('Ctrl Pts',(95.0657514420968,0.446789749487463,-0.363993300376015));
#32323=CARTESIAN_POINT('Ctrl Pts',(95.0836435670714,0.499203244850938,-0.366991849792889));
#32324=CARTESIAN_POINT('Ctrl Pts',(95.1044230501465,0.550399149156465,-0.369990399209764));
#32325=CARTESIAN_POINT('Ctrl Pts',(95.125211897677,0.601618125343098,-0.372990299949104));
#32326=CARTESIAN_POINT('Ctrl Pts',(95.14889047002,0.651617937283341,-0.375990200688444));
#32327=CARTESIAN_POINT('Ctrl Pts',(95.175278973966,0.700062948516415,-0.378990101427784));
#32328=CARTESIAN_POINT('Ctrl Pts',(95.2017175231805,0.748599834741826,-0.381995691418719));
#32329=CARTESIAN_POINT('Ctrl Pts',(95.2308759905254,0.795575578942978,-0.385001281409655));
#32330=CARTESIAN_POINT('Ctrl Pts',(95.2625303434212,0.840682220111097,-0.38800687140059));
#32331=CARTESIAN_POINT('Ctrl Pts',(95.2870776015305,0.875661433454824,-0.39033764067966));
#32332=CARTESIAN_POINT('Ctrl Pts',(95.3131248754419,0.909517177915923,-0.392668409958731));
#32333=CARTESIAN_POINT('Ctrl Pts',(95.3405517846923,0.942120435847087,-0.394999179237801));
#32334=CARTESIAN_POINT('Ctrl Pts',(95.3759806229821,0.98423584675321,-0.398009961354197));
#32335=CARTESIAN_POINT('Ctrl Pts',(95.413862643576,1.02443824365443,-0.401020743470594));
#32336=CARTESIAN_POINT('Ctrl Pts',(95.4539634038702,1.06242867063366,-0.40403152558699));
#32337=CARTESIAN_POINT('Ctrl Pts',(95.4939929335618,1.10035161557538,-0.407036959679479));
#32338=CARTESIAN_POINT('Ctrl Pts',(95.5362330015292,1.13607002794812,-0.410042393771969));
#32339=CARTESIAN_POINT('Ctrl Pts',(95.5804100992899,1.16931926712725,-0.413047827864458));
#32340=CARTESIAN_POINT('Ctrl Pts',(95.6245435093959,1.20253562543929,-0.416050289820401));
#32341=CARTESIAN_POINT('Ctrl Pts',(95.6706097348918,1.23328733190982,-0.419052751776343));
#32342=CARTESIAN_POINT('Ctrl Pts',(95.7183011377446,1.26134903056547,-0.422055213732285));
#32343=CARTESIAN_POINT('Ctrl Pts',(95.7659641912214,1.28939404840236,-0.425055890923721));
#32344=CARTESIAN_POINT('Ctrl Pts',(95.815250053192,1.31475196071634,-0.428056568115158));
#32345=CARTESIAN_POINT('Ctrl Pts',(95.8658228891346,1.33724120529953,-0.431057245306594));
#32346=CARTESIAN_POINT('Ctrl Pts',(95.9163856120044,1.3597259526983,-0.434057322451254));
#32347=CARTESIAN_POINT('Ctrl Pts',(95.9682343157003,1.37934295726238,-0.437057399595914));
#32348=CARTESIAN_POINT('Ctrl Pts',(96.0210115009846,1.39595804154492,-0.440057476740574));
#32349=CARTESIAN_POINT('Ctrl Pts',(96.0738370533894,1.41258835255428,-0.443060303275749));
#32350=CARTESIAN_POINT('Ctrl Pts',(96.1275922828073,1.42621108810601,-0.446063129810924));
#32351=CARTESIAN_POINT('Ctrl Pts',(96.1819042023455,1.43674188562243,-0.449065956346099));
#32352=CARTESIAN_POINT('Ctrl Pts',(96.236240774168,1.44727746308802,-0.45207014586999));
#32353=CARTESIAN_POINT('Ctrl Pts',(96.2911340158551,1.45471823372441,-0.455074335393881));
#32354=CARTESIAN_POINT('Ctrl Pts',(96.3462036908734,1.45903151375945,-0.458078524917772));
#32355=CARTESIAN_POINT('Ctrl Pts',(96.4013770235376,1.46335291268123,-0.461088369227421));
#32356=CARTESIAN_POINT('Ctrl Pts',(96.4567269239329,1.46453504965939,-0.46409821353707));
#32357=CARTESIAN_POINT('Ctrl Pts',(96.511872186207,1.46259741241315,-0.467108057846719));
#32358=CARTESIAN_POINT('Ctrl Pts',(96.5539567156322,1.46111868970258,-0.469405043592934));
#32359=CARTESIAN_POINT('Ctrl Pts',(96.5959220275134,1.45782406683853,-0.471702029339148));
#32360=CARTESIAN_POINT('Ctrl Pts',(96.6376020196412,1.45274236413044,-0.473999015085362));
#32361=CARTESIAN_POINT('Ctrl Pts',(96.692231930419,1.44608178308497,-0.477009671277152));
#32362=CARTESIAN_POINT('Ctrl Pts',(96.7465999137415,1.43632147318516,-0.480020327468943));
#32363=CARTESIAN_POINT('Ctrl Pts',(96.8003275092147,1.42349449099827,-0.483030983660733));
#32364=CARTESIAN_POINT('Ctrl Pts',(96.8539599582826,1.41069022416342,-0.486036308269905));
#32365=CARTESIAN_POINT('Ctrl Pts',(96.9069537607428,1.39483018417317,-0.489041632879076));
#32366=CARTESIAN_POINT('Ctrl Pts',(96.9589378579191,1.37599889553953,-0.492046957488248));
#32367=CARTESIAN_POINT('Ctrl Pts',(97.0108707209289,1.35718616653143,-0.495049320128088));
#32368=CARTESIAN_POINT('Ctrl Pts',(97.0617953560977,1.33540816888856,-0.498051682767928));
#32369=CARTESIAN_POINT('Ctrl Pts',(97.1113549683908,1.31079947422679,-0.501054045407768));
#32370=CARTESIAN_POINT('Ctrl Pts',(97.1608852907622,1.28620532339832,-0.504054633639725));
#32371=CARTESIAN_POINT('Ctrl Pts',(97.2090517174039,1.25878402582337,-0.507055221871683));
#32372=CARTESIAN_POINT('Ctrl Pts',(97.255518735269,1.22871769309386,-0.510055810103641));
#32373=CARTESIAN_POINT('Ctrl Pts',(97.3019766243376,1.19865726712249,-0.513055808847379));
#32374=CARTESIAN_POINT('Ctrl Pts',(97.3467353247295,1.16595312463451,-0.516055807591117));
#32375=CARTESIAN_POINT('Ctrl Pts',(97.3894871816032,1.13083140691108,-0.519055806334855));
#32376=CARTESIAN_POINT('Ctrl Pts',(97.4322784630212,1.09567730094023,-0.522058571591961));
#32377=CARTESIAN_POINT('Ctrl Pts',(97.4730587948287,1.05810150152605,-0.525061336849067));
#32378=CARTESIAN_POINT('Ctrl Pts',(97.5115537886237,1.01837033392487,-0.528064102106173));
#32379=CARTESIAN_POINT('Ctrl Pts',(97.5500663765137,0.97862100723683,-0.531068239773867));
#32380=CARTESIAN_POINT('Ctrl Pts',(97.5862911984259,0.936714748696337,-0.534072377441562));
#32381=CARTESIAN_POINT('Ctrl Pts',(97.6199931960324,0.892952182549568,-0.537076515109257));
#32382=CARTESIAN_POINT('Ctrl Pts',(97.6537588140523,0.849107004310048,-0.540086323790365));
#32383=CARTESIAN_POINT('Ctrl Pts',(97.6849917955423,0.803398955181929,-0.543096132471473));
#32384=CARTESIAN_POINT('Ctrl Pts',(97.7135002540531,0.756157968026738,-0.546105941152582));
#32385=CARTESIAN_POINT('Ctrl Pts',(97.7352631248655,0.720095004463755,-0.54840357774603));
#32386=CARTESIAN_POINT('Ctrl Pts',(97.7554391613811,0.683139338022428,-0.550701214339477));
#32387=CARTESIAN_POINT('Ctrl Pts',(97.7739617263499,0.645445969115977,-0.552998850932925));
#32388=CARTESIAN_POINT('Ctrl Pts',(97.7999214270754,0.592618049343745,-0.556219029047693));
#32389=CARTESIAN_POINT('Ctrl Pts',(97.8227287513135,0.538143597802004,-0.55943920716246));
#32390=CARTESIAN_POINT('Ctrl Pts',(97.8421887872528,0.482406158029926,-0.562659385277227));
#32391=CARTESIAN_POINT('Ctrl Pts',(97.8616014987721,0.426804264873654,-0.565871732313862));
#32392=CARTESIAN_POINT('Ctrl Pts',(97.8776829711369,0.369945875263667,-0.569084079350498));
#32393=CARTESIAN_POINT('Ctrl Pts',(97.8902854901268,0.312235849676686,-0.572296426387133));
#32394=CARTESIAN_POINT('Ctrl Pts',(97.9028432269035,0.254730892827498,-0.575497358562217));
#32395=CARTESIAN_POINT('Ctrl Pts',(97.9119465324078,0.196380723927314,-0.578698290737302));
#32396=CARTESIAN_POINT('Ctrl Pts',(97.917497523185,0.137604339435666,-0.581899222912386));
#32397=CARTESIAN_POINT('Ctrl Pts',(97.9218016011884,0.0920308276505253,
-0.584381133316817));
#32398=CARTESIAN_POINT('Ctrl Pts',(97.9239709738696,0.046201501282702,-0.586863043721248));
#32399=CARTESIAN_POINT('Ctrl Pts',(97.9239809152272,0.000317083165083229,
-0.589344954125678));
#32400=CARTESIAN_POINT('Origin',(96.460480949577,-8.32667268468867E-16,
1.18130019239114E-14));
#32401=CARTESIAN_POINT('',(97.923980378536,-0.00129284060398358,-1.16065504579921));
#32402=CARTESIAN_POINT('',(97.9239803891082,-0.00128081692310598,-1.08934495412119));
#32403=CARTESIAN_POINT('',(97.923980949577,-1.01189432752408E-15,1.19922289829666E-14));
#32404=CARTESIAN_POINT('Ctrl Pts',(97.923980378536,-0.00129284060398456,
-1.16065504579921));
#32405=CARTESIAN_POINT('Ctrl Pts',(97.9240284830895,0.0531616577923571,
-1.15769184059285));
#32406=CARTESIAN_POINT('Ctrl Pts',(97.9210330828335,0.10770563227362,-1.1547286353865));
#32407=CARTESIAN_POINT('Ctrl Pts',(97.9149908304708,0.161966837291652,-1.15176543018014));
#32408=CARTESIAN_POINT('Ctrl Pts',(97.9089535018915,0.216183825285511,-1.14880463966613));
#32409=CARTESIAN_POINT('Ctrl Pts',(97.8998742957547,0.270117961430168,-1.14584384915211));
#32410=CARTESIAN_POINT('Ctrl Pts',(97.8878018665388,0.323399520722398,-1.1428830586381));
#32411=CARTESIAN_POINT('Ctrl Pts',(97.875734196129,0.376660077065522,-1.13992343523206));
#32412=CARTESIAN_POINT('Ctrl Pts',(97.8606757609156,0.429268036549174,-1.13696381182601));
#32413=CARTESIAN_POINT('Ctrl Pts',(97.842726312339,0.480863813488882,-1.13400418841997));
#32414=CARTESIAN_POINT('Ctrl Pts',(97.8247633560666,0.532498418365578,-1.131042337776));
#32415=CARTESIAN_POINT('Ctrl Pts',(97.80390521258,0.58311880194702,-1.12808048713203));
#32416=CARTESIAN_POINT('Ctrl Pts',(97.7803010259489,0.632382175591351,-1.12511863648806));
#32417=CARTESIAN_POINT('Ctrl Pts',(97.756689115767,0.681661668756108,-1.12215581669382));
#32418=CARTESIAN_POINT('Ctrl Pts',(97.7303296319005,0.729582788236327,-1.11919299689958));
#32419=CARTESIAN_POINT('Ctrl Pts',(97.7014176884102,0.775827468071288,-1.11623017710534));
#32420=CARTESIAN_POINT('Ctrl Pts',(97.6724504556885,0.822160583082206,-1.11326169141633));
#32421=CARTESIAN_POINT('Ctrl Pts',(97.6409213252783,0.866810407157974,-1.11029320572732));
#32422=CARTESIAN_POINT('Ctrl Pts',(97.6070680237593,0.909489049586677,-1.1073247200383));
#32423=CARTESIAN_POINT('Ctrl Pts',(97.5754965996013,0.949290943704698,-1.10455632473889));
#32424=CARTESIAN_POINT('Ctrl Pts',(97.541904427265,0.987378510028894,-1.10178792943947));
#32425=CARTESIAN_POINT('Ctrl Pts',(97.5065125074113,1.02354786405657,-1.09901953414006));
#32426=CARTESIAN_POINT('Ctrl Pts',(97.4680301976465,1.0628754928328,-1.09600940510767));
#32427=CARTESIAN_POINT('Ctrl Pts',(97.4272460484989,1.10011250778398,-1.09299927607529));
#32428=CARTESIAN_POINT('Ctrl Pts',(97.384416116279,1.13497843932444,-1.08998914704291));
#32429=CARTESIAN_POINT('Ctrl Pts',(97.3416623051393,1.16978240409934,-1.08698436787361));
#32430=CARTESIAN_POINT('Ctrl Pts',(97.2968703327355,1.2022233176518,-1.08397958870431));
#32431=CARTESIAN_POINT('Ctrl Pts',(97.2503326451425,1.23205785132527,-1.08097480953501));
#32432=CARTESIAN_POINT('Ctrl Pts',(97.2038409990339,1.2618628685727,-1.07797300310674));
#32433=CARTESIAN_POINT('Ctrl Pts',(97.1556075014537,1.28906633038001,-1.07497119667846));
#32434=CARTESIAN_POINT('Ctrl Pts',(97.1059556912606,1.31346663750871,-1.07196939025018));
#32435=CARTESIAN_POINT('Ctrl Pts',(97.0563333922172,1.33785244202183,-1.0689693679816));
#32436=CARTESIAN_POINT('Ctrl Pts',(97.0052949244536,1.35943816169359,-1.06596934571303));
#32437=CARTESIAN_POINT('Ctrl Pts',(96.9531886625336,1.37806798075895,-1.06296932344445));
#32438=CARTESIAN_POINT('Ctrl Pts',(96.9010927911103,1.39669408485678,-1.05996989940956));
#32439=CARTESIAN_POINT('Ctrl Pts',(96.8479300454059,1.41236528124363,-1.05697047537467));
#32440=CARTESIAN_POINT('Ctrl Pts',(96.7940668498442,1.42497463035062,-1.05397105133977));
#32441=CARTESIAN_POINT('Ctrl Pts',(96.7401541352334,1.43759557184408,-1.05096886978883));
#32442=CARTESIAN_POINT('Ctrl Pts',(96.6855401995404,1.44714892160775,-1.04796668823788));
#32443=CARTESIAN_POINT('Ctrl Pts',(96.6306031734235,1.45357857680743,-1.04496450668694));
#32444=CARTESIAN_POINT('Ctrl Pts',(96.575641141385,1.46001115862082,-1.04196095862015));
#32445=CARTESIAN_POINT('Ctrl Pts',(96.5203562538571,1.46331717997922,-1.03895741055337));
#32446=CARTESIAN_POINT('Ctrl Pts',(96.4651299873959,1.46349261578163,-1.03595386248658));
#32447=CARTESIAN_POINT('Ctrl Pts',(96.4097994910381,1.46366838268837,-1.03294464574935));
#32448=CARTESIAN_POINT('Ctrl Pts',(96.3545283654123,1.46070178940425,-1.02993542901212));
#32449=CARTESIAN_POINT('Ctrl Pts',(96.2996951330034,1.45464090798684,-1.0269262122749));
#32450=CARTESIAN_POINT('Ctrl Pts',(96.2577455140603,1.45000409095543,-1.02462404094743));
#32451=CARTESIAN_POINT('Ctrl Pts',(96.2160521425861,1.44355731388188,-1.02232186961996));
#32452=CARTESIAN_POINT('Ctrl Pts',(96.1747796245323,1.43534212049522,-1.02001969829249));
#32453=CARTESIAN_POINT('Ctrl Pts',(96.1208150390998,1.42460060225827,-1.01700956643865));
#32454=CARTESIAN_POINT('Ctrl Pts',(96.0673436858459,1.41078892254573,-1.01399943458481));
#32455=CARTESIAN_POINT('Ctrl Pts',(96.014740374309,1.39396828857753,-1.01098930273097));
#32456=CARTESIAN_POINT('Ctrl Pts',(95.9622305532285,1.37717754947145,-1.00798452070383));
#32457=CARTESIAN_POINT('Ctrl Pts',(95.9105862112277,1.35738862827198,-1.0049797386767));
#32458=CARTESIAN_POINT('Ctrl Pts',(95.8601709344612,1.33471350324768,-1.00197495664956));
#32459=CARTESIAN_POINT('Ctrl Pts',(95.8098055350403,1.31206081140475,-0.998973147343418));
#32460=CARTESIAN_POINT('Ctrl Pts',(95.7606672713862,1.28652778772483,-0.995971338037275));
#32461=CARTESIAN_POINT('Ctrl Pts',(95.7131017690514,1.2582752522866,-0.992969528731132));
#32462=CARTESIAN_POINT('Ctrl Pts',(95.6655645375839,1.23003950892752,-0.989969503569977));
#32463=CARTESIAN_POINT('Ctrl Pts',(95.6195986677897,1.19908772670014,-0.986969478408821));
#32464=CARTESIAN_POINT('Ctrl Pts',(95.575525010414,1.16562654213948,-0.983969453247666));
#32465=CARTESIAN_POINT('Ctrl Pts',(95.5314601416081,1.13217202995358,-0.980970026310765));
#32466=CARTESIAN_POINT('Ctrl Pts',(95.4892871562698,1.09620942835326,-0.977970599373865));
#32467=CARTESIAN_POINT('Ctrl Pts',(95.4492958323556,1.0579871968554,-0.974971172436964));
#32468=CARTESIAN_POINT('Ctrl Pts',(95.4092677426307,1.01972982595246,-0.971968987992874));
#32469=CARTESIAN_POINT('Ctrl Pts',(95.3714257040584,0.979209040496911,-0.968966803548784));
#32470=CARTESIAN_POINT('Ctrl Pts',(95.336023313683,0.936710881264692,-0.965964619104694));
#32471=CARTESIAN_POINT('Ctrl Pts',(95.300604809071,0.894193377988669,-0.962961068145243));
#32472=CARTESIAN_POINT('Ctrl Pts',(95.2676284812852,0.849697131787614,-0.959957517185793));
#32473=CARTESIAN_POINT('Ctrl Pts',(95.2373061390484,0.803539440779607,-0.956953966226342));
#32474=CARTESIAN_POINT('Ctrl Pts',(95.2069265691368,0.757294635876738,-0.95394474663363));
#32475=CARTESIAN_POINT('Ctrl Pts',(95.179211255907,0.709382580456583,-0.950935527040919));
#32476=CARTESIAN_POINT('Ctrl Pts',(95.1543267612167,0.660146564202886,-0.947926307448207));
#32477=CARTESIAN_POINT('Ctrl Pts',(95.1352893343227,0.622479451743986,-0.945624159113781));
#32478=CARTESIAN_POINT('Ctrl Pts',(95.1179077774405,0.584038014560071,-0.943322010779356));
#32479=CARTESIAN_POINT('Ctrl Pts',(95.1022372350482,0.544982808850793,-0.94101986244493));
#32480=CARTESIAN_POINT('Ctrl Pts',(95.0817475827641,0.49391708535329,-0.938009742074009));
#32481=CARTESIAN_POINT('Ctrl Pts',(95.0640987500391,0.441586937083567,-0.934999621703088));
#32482=CARTESIAN_POINT('Ctrl Pts',(95.0494442690851,0.388339717652553,-0.931989501332166));
#32483=CARTESIAN_POINT('Ctrl Pts',(95.0348158332484,0.335187133444637,-0.928984730788258));
#32484=CARTESIAN_POINT('Ctrl Pts',(95.0231713270365,0.281121217675837,-0.925979960244349));
#32485=CARTESIAN_POINT('Ctrl Pts',(95.014615628215,0.226507665395155,-0.92297518970044));
#32486=CARTESIAN_POINT('Ctrl Pts',(95.0060683938113,0.171948143993042,-0.919973391869084));
#32487=CARTESIAN_POINT('Ctrl Pts',(95.0006039946378,0.116842578536681,-0.916971594037727));
#32488=CARTESIAN_POINT('Ctrl Pts',(94.9982765885658,0.0615683087298558,
-0.91396979620637));
#32489=CARTESIAN_POINT('Ctrl Pts',(94.995950565786,0.00632689114651344,
-0.910969782491449));
#32490=CARTESIAN_POINT('Ctrl Pts',(94.9967578627805,-0.049082505448643,
-0.907969768776527));
#32491=CARTESIAN_POINT('Ctrl Pts',(95.0007007280563,-0.104278256874737,
-0.904969755061606));
#32492=CARTESIAN_POINT('Ctrl Pts',(95.0046428071603,-0.159463002767406,
-0.901970339522275));
#32493=CARTESIAN_POINT('Ctrl Pts',(95.0117191753086,-0.214433661608961,
-0.898970923982944));
#32494=CARTESIAN_POINT('Ctrl Pts',(95.0218800750811,-0.268811781549082,
-0.895971508443614));
#32495=CARTESIAN_POINT('Ctrl Pts',(95.0320503168185,-0.323239896912986,
-0.89296933523169));
#32496=CARTESIAN_POINT('Ctrl Pts',(95.0453106587844,-0.377073864721718,
-0.889967162019767));
#32497=CARTESIAN_POINT('Ctrl Pts',(95.0615600991256,-0.429945001334288,
-0.886964988807844));
#32498=CARTESIAN_POINT('Ctrl Pts',(95.0778169362157,-0.482840204900062,
-0.883961449006003));
#32499=CARTESIAN_POINT('Ctrl Pts',(95.0970654001508,-0.534771207526567,
-0.880957909204163));
#32500=CARTESIAN_POINT('Ctrl Pts',(95.1191554772583,-0.585387245598138,
-0.877954369402322));
#32501=CARTESIAN_POINT('Ctrl Pts',(95.141287247273,-0.636098816599104,-0.874945160706456));
#32502=CARTESIAN_POINT('Ctrl Pts',(95.1662711054648,-0.685489992710375,
-0.871935952010591));
#32503=CARTESIAN_POINT('Ctrl Pts',(95.1939105468442,-0.73323370416353,-0.868926743314725));
#32504=CARTESIAN_POINT('Ctrl Pts',(95.2150565037084,-0.769760725425008,
-0.866624504408938));
#32505=CARTESIAN_POINT('Ctrl Pts',(95.237755862403,-0.805323924891907,-0.864322265503151));
#32506=CARTESIAN_POINT('Ctrl Pts',(95.2619042701106,-0.839789374450085,
-0.862020026597364));
#32507=CARTESIAN_POINT('Ctrl Pts',(95.2934778596986,-0.884852302511112,
-0.859009892462434));
#32508=CARTESIAN_POINT('Ctrl Pts',(95.3276626704499,-0.928226826378056,
-0.855999758327504));
#32509=CARTESIAN_POINT('Ctrl Pts',(95.364251671266,-0.96959456443078,-0.852989624192575));
#32510=CARTESIAN_POINT('Ctrl Pts',(95.4007756417765,-1.0108887788402,-0.849984840024524));
#32511=CARTESIAN_POINT('Ctrl Pts',(95.4396949754759,-1.05018289318898,-0.846980055856473));
#32512=CARTESIAN_POINT('Ctrl Pts',(95.4807606953364,-1.08718925373214,-0.843975271688422));
#32513=CARTESIAN_POINT('Ctrl Pts',(95.5217857864876,-1.12415900172672,-0.840973460328415));
#32514=CARTESIAN_POINT('Ctrl Pts',(95.5649526667679,-1.15884512781821,-0.837971648968408));
#32515=CARTESIAN_POINT('Ctrl Pts',(95.6099748933604,-1.19099609501409,-0.834969837608402));
#32516=CARTESIAN_POINT('Ctrl Pts',(95.6549703593724,-1.22312795212576,-0.831969810482988));
#32517=CARTESIAN_POINT('Ctrl Pts',(95.7018185569693,-1.25272733074513,-0.828969783357574));
#32518=CARTESIAN_POINT('Ctrl Pts',(95.7502010919244,-1.2795838283649,-0.82596975623216));
#32519=CARTESIAN_POINT('Ctrl Pts',(95.79857397761,-1.3064349698043,-0.822970327423273));
#32520=CARTESIAN_POINT('Ctrl Pts',(95.8484801314558,-1.33054406046041,-0.819970898614386));
#32521=CARTESIAN_POINT('Ctrl Pts',(95.8995754002831,-1.35174598751809,-0.816971469805499));
#32522=CARTESIAN_POINT('Ctrl Pts',(95.9507176405937,-1.37296740534246,-0.813969283645031));
#32523=CARTESIAN_POINT('Ctrl Pts',(96.003050691011,-1.39127611735242,-0.810967097484562));
#32524=CARTESIAN_POINT('Ctrl Pts',(96.0562105796949,-1.40655526661251,-0.807964911324094));
#32525=CARTESIAN_POINT('Ctrl Pts',(96.1093946638648,-1.42184137010918,-0.804961358731997));
#32526=CARTESIAN_POINT('Ctrl Pts',(96.1634058205693,-1.43409504507892,-0.801957806139899));
#32527=CARTESIAN_POINT('Ctrl Pts',(96.217868306426,-1.44325027468672,-0.798954253547802));
#32528=CARTESIAN_POINT('Ctrl Pts',(96.2724335770256,-1.45242278257159,-0.795945032478112));
#32529=CARTESIAN_POINT('Ctrl Pts',(96.3274513521043,-1.45848510569075,-0.792935811408423));
#32530=CARTESIAN_POINT('Ctrl Pts',(96.3825403296723,-1.46142311113821,-0.789926590338733));
#32531=CARTESIAN_POINT('Ctrl Pts',(96.4246848451709,-1.46367076251207,-0.787624457142423));
#32532=CARTESIAN_POINT('Ctrl Pts',(96.4668709014751,-1.46409093676975,-0.785322323946113));
#32533=CARTESIAN_POINT('Ctrl Pts',(96.5089293361716,-1.46269785117651,-0.783020190749803));
#32534=CARTESIAN_POINT('Ctrl Pts',(96.5639227450316,-1.46087632533612,-0.780010041821803));
#32535=CARTESIAN_POINT('Ctrl Pts',(96.618928819811,-1.45594525965707,-0.776999892893803));
#32536=CARTESIAN_POINT('Ctrl Pts',(96.6735677828057,-1.44790408919395,-0.773989743965802));
#32537=CARTESIAN_POINT('Ctrl Pts',(96.7281096409166,-1.43987720957533,-0.770984944703056));
#32538=CARTESIAN_POINT('Ctrl Pts',(96.7822851637495,-1.42875127042837,-0.76798014544031));
#32539=CARTESIAN_POINT('Ctrl Pts',(96.8357173904326,-1.41457762722801,-0.764975346177563));
#32540=CARTESIAN_POINT('Ctrl Pts',(96.8890967568334,-1.40041800595463,-0.76197351955038));
#32541=CARTESIAN_POINT('Ctrl Pts',(96.9417337758131,-1.38321678810163,-0.758971692923197));
#32542=CARTESIAN_POINT('Ctrl Pts',(96.9932612645381,-1.36307644172656,-0.755969866296014));
#32543=CARTESIAN_POINT('Ctrl Pts',(97.0447581286649,-1.34294806546747,-0.752969823759938));
#32544=CARTESIAN_POINT('Ctrl Pts',(97.095146278689,-1.31988421488643,-0.749969781223863));
#32545=CARTESIAN_POINT('Ctrl Pts',(97.1440755252397,-1.29403659381197,-0.746969738687787));
#32546=CARTESIAN_POINT('Ctrl Pts',(97.1929950154074,-1.26819412669574,-0.743970294353529));
#32547=CARTESIAN_POINT('Ctrl Pts',(97.2404557131263,-1.23956923798579,-0.740970850019272));
#32548=CARTESIAN_POINT('Ctrl Pts',(97.2861312860237,-1.20835995130818,-0.737971405685014));
#32549=CARTESIAN_POINT('Ctrl Pts',(97.3318488486723,-1.17712197379864,-0.734969203948634));
#32550=CARTESIAN_POINT('Ctrl Pts',(97.3757775708721,-1.14329515026359,-0.731967002212255));
#32551=CARTESIAN_POINT('Ctrl Pts',(97.41762070718,-1.1071204696941,-0.728964800475876));
#32552=CARTESIAN_POINT('Ctrl Pts',(97.4594828888301,-1.07092932383948,-0.7259612322559));
#32553=CARTESIAN_POINT('Ctrl Pts',(97.499257212345,-1.03238855880676,-0.722957664035924));
#32554=CARTESIAN_POINT('Ctrl Pts',(97.5366830803905,-0.991776801317935,
-0.719954095815949));
#32555=CARTESIAN_POINT('Ctrl Pts',(97.5741795789177,-0.951088400904303,
-0.716944859231256));
#32556=CARTESIAN_POINT('Ctrl Pts',(97.6093184322226,-0.908321609442644,
-0.713935622646564));
#32557=CARTESIAN_POINT('Ctrl Pts',(97.64187946,-0.863788058247059,-0.710926386061871));
#32558=CARTESIAN_POINT('Ctrl Pts',(97.6667880446296,-0.82972071441527,-0.708624375675328));
#32559=CARTESIAN_POINT('Ctrl Pts',(97.6901889246574,-0.794620167352733,
-0.706322365288784));
#32560=CARTESIAN_POINT('Ctrl Pts',(97.7120015906264,-0.758635838216996,
-0.70402035490224));
#32561=CARTESIAN_POINT('Ctrl Pts',(97.741399837912,-0.710137584594984,-0.700917796476155));
#32562=CARTESIAN_POINT('Ctrl Pts',(97.7680288183907,-0.659840015559768,
-0.69781523805007));
#32563=CARTESIAN_POINT('Ctrl Pts',(97.7916721500935,-0.60808078218895,-0.694712679623984));
#32564=CARTESIAN_POINT('Ctrl Pts',(97.8152569502764,-0.556449684168549,
-0.691617801903065));
#32565=CARTESIAN_POINT('Ctrl Pts',(97.8358705995206,-0.503364553578691,
-0.688522924182145));
#32566=CARTESIAN_POINT('Ctrl Pts',(97.8533420610875,-0.449188350296177,
-0.685428046461226));
#32567=CARTESIAN_POINT('Ctrl Pts',(97.870787851703,-0.395091748521366,-0.68233771606769));
#32568=CARTESIAN_POINT('Ctrl Pts',(97.8851004704575,-0.339907713157234,
-0.679247385674154));
#32569=CARTESIAN_POINT('Ctrl Pts',(97.8961568904179,-0.284019088954735,
-0.676157055280619));
#32570=CARTESIAN_POINT('Ctrl Pts',(97.9071974005993,-0.228210886413188,
-0.6730711717581));
#32571=CARTESIAN_POINT('Ctrl Pts',(97.9149909322888,-0.171700582918234,
-0.669985288235581));
#32572=CARTESIAN_POINT('Ctrl Pts',(97.9194648072646,-0.114884085090813,
-0.666899404713062));
#32573=CARTESIAN_POINT('Ctrl Pts',(97.9224824714857,-0.0765609058358133,
-0.664817951756339));
#32574=CARTESIAN_POINT('Ctrl Pts',(97.9239908603876,-0.0380987204141508,
-0.662736498799616));
#32575=CARTESIAN_POINT('Ctrl Pts',(97.923980900548,0.000378824190018902,
-0.660655045842893));
#32576=CARTESIAN_POINT('Ctrl Pts',(97.9239809152274,0.000317082584714552,
-0.589344954157071));
#32577=CARTESIAN_POINT('Ctrl Pts',(97.9239933057583,-0.0568716200036579,
-0.592438318784791));
#32578=CARTESIAN_POINT('Ctrl Pts',(97.9206492531944,-0.114020603425716,
-0.595531683412511));
#32579=CARTESIAN_POINT('Ctrl Pts',(97.9139886755651,-0.170726507880078,
-0.598625048040231));
#32580=CARTESIAN_POINT('Ctrl Pts',(97.9073139831515,-0.227552580832559,
-0.601724967981458));
#32581=CARTESIAN_POINT('Ctrl Pts',(97.8973087906183,-0.283933222963652,
-0.604824887922686));
#32582=CARTESIAN_POINT('Ctrl Pts',(97.8840645854727,-0.339472946801535,
-0.607924807863914));
#32583=CARTESIAN_POINT('Ctrl Pts',(97.8708054908208,-0.395075109951672,
-0.611028212821915));
#32584=CARTESIAN_POINT('Ctrl Pts',(97.854300269648,-0.449834012993639,-0.614131617779916));
#32585=CARTESIAN_POINT('Ctrl Pts',(97.8346900561714,-0.503370222950273,
-0.617235022737918));
#32586=CARTESIAN_POINT('Ctrl Pts',(97.8150310332347,-0.557039683547313,
-0.620346152013692));
#32587=CARTESIAN_POINT('Ctrl Pts',(97.7922517696555,-0.609479930850509,
-0.623457281289467));
#32588=CARTESIAN_POINT('Ctrl Pts',(97.7665410147506,-0.660332761688246,
-0.626568410565242));
#32589=CARTESIAN_POINT('Ctrl Pts',(97.7515821912859,-0.689919544417623,
-0.62837850263699));
#32590=CARTESIAN_POINT('Ctrl Pts',(97.7356318962316,-0.718969462504072,
-0.630188594708739));
#32591=CARTESIAN_POINT('Ctrl Pts',(97.7187340105644,-0.747416540167404,
-0.631998686780487));
#32592=CARTESIAN_POINT('Ctrl Pts',(97.6906322104425,-0.794725067771984,
-0.635008935908942));
#32593=CARTESIAN_POINT('Ctrl Pts',(97.659799592515,-0.840545848997746,-0.638019185037397));
#32594=CARTESIAN_POINT('Ctrl Pts',(97.6264187277055,-0.884545842527611,
-0.641029434165853));
#32595=CARTESIAN_POINT('Ctrl Pts',(97.5930971746869,-0.928467655985254,
-0.644034334623197));
#32596=CARTESIAN_POINT('Ctrl Pts',(97.557236676801,-0.970574684766163,-0.647039235080541));
#32597=CARTESIAN_POINT('Ctrl Pts',(97.5190639381818,-1.0105613817263,-0.650044135537886));
#32598=CARTESIAN_POINT('Ctrl Pts',(97.4809289557043,-1.050508528383,-0.653046063888656));
#32599=CARTESIAN_POINT('Ctrl Pts',(97.4404866258037,-1.08833911758349,-0.656047992239426));
#32600=CARTESIAN_POINT('Ctrl Pts',(97.3980037229298,-1.12378080578237,-0.659049920590196));
#32601=CARTESIAN_POINT('Ctrl Pts',(97.3555460634466,-1.15920143448855,-0.66205006519162));
#32602=CARTESIAN_POINT('Ctrl Pts',(97.3110506389538,-1.19223563811482,-0.665050209793043));
#32603=CARTESIAN_POINT('Ctrl Pts',(97.2648191723575,-1.22264969364665,-0.668050354394467));
#32604=CARTESIAN_POINT('Ctrl Pts',(97.2185969215074,-1.25305768646333,-0.671049900949303));
#32605=CARTESIAN_POINT('Ctrl Pts',(97.1706397567342,-1.28084627838922,-0.67404944750414));
#32606=CARTESIAN_POINT('Ctrl Pts',(97.1212784867775,-1.30582497480703,-0.677048994058976));
#32607=CARTESIAN_POINT('Ctrl Pts',(97.0718718499882,-1.33082662858267,-0.680051297429556));
#32608=CARTESIAN_POINT('Ctrl Pts',(97.0210590019866,-1.35301298838269,-0.683053600800137));
#32609=CARTESIAN_POINT('Ctrl Pts',(96.9691941368395,-1.37224019147716,-0.686055904170717));
#32610=CARTESIAN_POINT('Ctrl Pts',(96.9173056685843,-1.39147614465225,-0.689059573855287));
#32611=CARTESIAN_POINT('Ctrl Pts',(96.8643647344388,-1.40775010116467,-0.692063243539857));
#32612=CARTESIAN_POINT('Ctrl Pts',(96.8107410842013,-1.42096801093233,-0.695066913224427));
#32613=CARTESIAN_POINT('Ctrl Pts',(96.7570162660442,-1.43421085798841,-0.698076249718543));
#32614=CARTESIAN_POINT('Ctrl Pts',(96.7026066790907,-1.4443860432448,-0.701085586212659));
#32615=CARTESIAN_POINT('Ctrl Pts',(96.6478915120193,-1.45145083660628,-0.704094922706775));
#32616=CARTESIAN_POINT('Ctrl Pts',(96.6060515445464,-1.45685319102222,-0.706396122680534));
#32617=CARTESIAN_POINT('Ctrl Pts',(96.5640331021084,-1.46043782114926,-0.708697322654292));
#32618=CARTESIAN_POINT('Ctrl Pts',(96.5220057229805,-1.46220619348218,-0.71099852262805));
#32619=CARTESIAN_POINT('Ctrl Pts',(96.4670300437293,-1.46451938721895,-0.71400870394974));
#32620=CARTESIAN_POINT('Ctrl Pts',(96.4118082692967,-1.46373268471372,-0.717018885271431));
#32621=CARTESIAN_POINT('Ctrl Pts',(96.3567190720768,-1.45981701688178,-0.720029066593121));
#32622=CARTESIAN_POINT('Ctrl Pts',(96.3017277439178,-1.45590830545424,-0.723033900158189));
#32623=CARTESIAN_POINT('Ctrl Pts',(96.2468690480662,-1.44888169729207,-0.726038733723258));
#32624=CARTESIAN_POINT('Ctrl Pts',(96.1925227449652,-1.4387601087677,-0.729043567288326));
#32625=CARTESIAN_POINT('Ctrl Pts',(96.1382301851588,-1.42864852952606,-0.732045429360466));
#32626=CARTESIAN_POINT('Ctrl Pts',(96.084449530955,-1.4154481291282,-0.735047291432605));
#32627=CARTESIAN_POINT('Ctrl Pts',(96.0315546285661,-1.39923352630791,-0.738049153504745));
#32628=CARTESIAN_POINT('Ctrl Pts',(95.9786911441165,-1.3830285544612,-0.741049232563472));
#32629=CARTESIAN_POINT('Ctrl Pts',(95.9267128725939,-1.36381308324272,-0.744049311622199));
#32630=CARTESIAN_POINT('Ctrl Pts',(95.8759804102237,-1.3417121038046,-0.747049390680926));
#32631=CARTESIAN_POINT('Ctrl Pts',(95.8252580465204,-1.31961552372768,-0.750048872552027));
#32632=CARTESIAN_POINT('Ctrl Pts',(95.7757814833515,-1.29463478692838,-0.753048354423129));
#32633=CARTESIAN_POINT('Ctrl Pts',(95.7278910040907,-1.2669428644467,-0.75604783629423));
#32634=CARTESIAN_POINT('Ctrl Pts',(95.6799564790391,-1.23922547317367,-0.759050076846242));
#32635=CARTESIAN_POINT('Ctrl Pts',(95.6336114104374,-1.2087921793971,-0.762052317398254));
#32636=CARTESIAN_POINT('Ctrl Pts',(95.5891698035265,-1.17586101932509,-0.765054557950266));
#32637=CARTESIAN_POINT('Ctrl Pts',(95.5447079574132,-1.14291486203625,-0.768058165756041));
#32638=CARTESIAN_POINT('Ctrl Pts',(95.5021517074917,-1.10746890938361,-0.771061773561816));
#32639=CARTESIAN_POINT('Ctrl Pts',(95.4617818382794,-1.06978144267575,-0.774065381367591));
#32640=CARTESIAN_POINT('Ctrl Pts',(95.4213357732141,-1.03202284299844,-0.777074658313824));
#32641=CARTESIAN_POINT('Ctrl Pts',(95.3830846983588,-0.992014660367753,
-0.780083935260056));
#32642=CARTESIAN_POINT('Ctrl Pts',(95.3472715729962,-0.950051121725918,
-0.783093212206289));
#32643=CARTESIAN_POINT('Ctrl Pts',(95.3198790715849,-0.91795433375132,-0.785394927629397));
#32644=CARTESIAN_POINT('Ctrl Pts',(95.2939120705789,-0.884714360878225,
-0.787696643052505));
#32645=CARTESIAN_POINT('Ctrl Pts',(95.2694620343073,-0.850474099235069,
-0.789998358475612));
#32646=CARTESIAN_POINT('Ctrl Pts',(95.2374875008111,-0.805696399085065,
-0.793008426684806));
#32647=CARTESIAN_POINT('Ctrl Pts',(95.2079744710546,-0.759018892219084,
-0.796018494894));
#32648=CARTESIAN_POINT('Ctrl Pts',(95.1811542053125,-0.710742802573144,
-0.799028563103194));
#32649=CARTESIAN_POINT('Ctrl Pts',(95.154381620755,-0.66255253836869,-0.802033280000075));
#32650=CARTESIAN_POINT('Ctrl Pts',(95.1302925543921,-0.612769789221488,
-0.805037996896956));
#32651=CARTESIAN_POINT('Ctrl Pts',(95.1090753245261,-0.561725098763481,
-0.808042713793837));
#32652=CARTESIAN_POINT('Ctrl Pts',(95.0878790920242,-0.510730924039845,
-0.811044457110523));
#32653=CARTESIAN_POINT('Ctrl Pts',(95.069549267728,-0.458477767230515,-0.814046200427208));
#32654=CARTESIAN_POINT('Ctrl Pts',(95.0542276384143,-0.405319472569289,
-0.817047943743894));
#32655=CARTESIAN_POINT('Ctrl Pts',(95.0389151195809,-0.352192786661084,
-0.820047902177077));
#32656=CARTESIAN_POINT('Ctrl Pts',(95.0266073963545,-0.298162536132881,
-0.823047860610261));
#32657=CARTESIAN_POINT('Ctrl Pts',(95.0173968287886,-0.243598994924626,
-0.826047819043444));
#32658=CARTESIAN_POINT('Ctrl Pts',(95.00818809981,-0.189046345535501,-0.829047178633446));
#32659=CARTESIAN_POINT('Ctrl Pts',(95.0020753865468,-0.133961137359882,
-0.832046538223447));
#32660=CARTESIAN_POINT('Ctrl Pts',(94.999099766334,-0.078722850959899,-0.835045897813449));
#32661=CARTESIAN_POINT('Ctrl Pts',(94.9961214108576,-0.0234337881634231,
-0.838048014488828));
#32662=CARTESIAN_POINT('Ctrl Pts',(94.9962859381515,0.032008105474783,-0.841050131164208));
#32663=CARTESIAN_POINT('Ctrl Pts',(94.99958232411,0.0872207321028154,-0.844052247839588));
#32664=CARTESIAN_POINT('Ctrl Pts',(95.0028802101587,0.142458484404836,-0.847055730691683));
#32665=CARTESIAN_POINT('Ctrl Pts',(95.0093127344966,0.197466236235169,-0.850059213543777));
#32666=CARTESIAN_POINT('Ctrl Pts',(95.0188170147424,0.251867721229272,-0.853062696395872));
#32667=CARTESIAN_POINT('Ctrl Pts',(95.0283392338549,0.306371886380417,-0.856071848175772));
#32668=CARTESIAN_POINT('Ctrl Pts',(95.0409446702839,0.360266983256315,-0.859080999955672));
#32669=CARTESIAN_POINT('Ctrl Pts',(95.0565196682152,0.413188783048457,-0.862090151735572));
#32670=CARTESIAN_POINT('Ctrl Pts',(95.0684380599395,0.453685914634258,-0.864392832598106));
#32671=CARTESIAN_POINT('Ctrl Pts',(95.0820942802859,0.493613346500161,-0.866695513460641));
#32672=CARTESIAN_POINT('Ctrl Pts',(95.0974185321669,0.532816193676603,-0.868998194323175));
#32673=CARTESIAN_POINT('Ctrl Pts',(95.1174509546978,0.584063589318232,-0.87200834296538));
#32674=CARTESIAN_POINT('Ctrl Pts',(95.1404196226556,0.634287332484554,-0.875018491607585));
#32675=CARTESIAN_POINT('Ctrl Pts',(95.1661985880499,0.683129137601182,-0.878028640249789));
#32676=CARTESIAN_POINT('Ctrl Pts',(95.1919317396107,0.731884142092216,-0.881033439319335));
#32677=CARTESIAN_POINT('Ctrl Pts',(95.220465032665,0.779261619118995,-0.88403823838888));
#32678=CARTESIAN_POINT('Ctrl Pts',(95.2516245008862,0.824923230645582,-0.887043037458425));
#32679=CARTESIAN_POINT('Ctrl Pts',(95.28275314376,0.870539670186896,-0.89004486394915));
#32680=CARTESIAN_POINT('Ctrl Pts',(95.3165025190425,0.914443172754508,-0.893046690439876));
#32681=CARTESIAN_POINT('Ctrl Pts',(95.3526537221496,0.956321642634158,-0.896048516930601));
#32682=CARTESIAN_POINT('Ctrl Pts',(95.3887834400069,0.998175223455973,-0.899048559386872));
#32683=CARTESIAN_POINT('Ctrl Pts',(95.4273118119942,1.03800575806257,-0.902048601843144));
#32684=CARTESIAN_POINT('Ctrl Pts',(95.4679791679586,1.07553357152821,-0.905048644299415));
#32685=CARTESIAN_POINT('Ctrl Pts',(95.5086384157101,1.11305390273951,-0.908048088610508));
#32686=CARTESIAN_POINT('Ctrl Pts',(95.5514354125987,1.14827206664514,-0.911047532921601));
#32687=CARTESIAN_POINT('Ctrl Pts',(95.5960747582377,1.18094630969162,-0.914046977232694));
#32688=CARTESIAN_POINT('Ctrl Pts',(95.6407551423232,1.21365059126475,-0.917049179033462));
#32689=CARTESIAN_POINT('Ctrl Pts',(95.6872808319539,1.24380596694346,-0.920051380834231));
#32690=CARTESIAN_POINT('Ctrl Pts',(95.7353257677288,1.27121289021105,-0.923053582634999));
#32691=CARTESIAN_POINT('Ctrl Pts',(95.7833925724393,1.29863228847165,-0.92605715096809));
#32692=CARTESIAN_POINT('Ctrl Pts',(95.8329795281481,1.32330050484317,-0.929060719301182));
#32693=CARTESIAN_POINT('Ctrl Pts',(95.8837371250765,1.34506461216572,-0.932064287634273));
#32694=CARTESIAN_POINT('Ctrl Pts',(95.9345905135792,1.36686979349945,-0.935073524410251));
#32695=CARTESIAN_POINT('Ctrl Pts',(95.9866184590551,1.38575973648157,-0.938082761186229));
#32696=CARTESIAN_POINT('Ctrl Pts',(96.0394537917025,1.40163061550898,-0.941091997962207));
#32697=CARTESIAN_POINT('Ctrl Pts',(96.0798718485249,1.41377154579581,-0.943394008698384));
#32698=CARTESIAN_POINT('Ctrl Pts',(96.1207620034452,1.42414674519917,-0.945696019434562));
#32699=CARTESIAN_POINT('Ctrl Pts',(96.1619565525049,1.43273006332412,-0.947998030170739));
#32700=CARTESIAN_POINT('Ctrl Pts',(96.2158229736495,1.44395369944809,-0.951008163370999));
#32701=CARTESIAN_POINT('Ctrl Pts',(96.2704364123061,1.45215886524671,-0.95401829657126));
#32702=CARTESIAN_POINT('Ctrl Pts',(96.3254279810839,1.45725527815177,-0.95702842977152));
#32703=CARTESIAN_POINT('Ctrl Pts',(96.3803218186441,1.46234263369313,-0.960033213352021));
#32704=CARTESIAN_POINT('Ctrl Pts',(96.4355919311008,1.46433215217651,-0.963037996932523));
#32705=CARTESIAN_POINT('Ctrl Pts',(96.4908599002698,1.46318466686704,-0.966042780513024));
#32706=CARTESIAN_POINT('Ctrl Pts',(96.5460731935169,1.46203831675066,-0.969044591498098));
#32707=CARTESIAN_POINT('Ctrl Pts',(96.6012838222717,1.45776112143561,-0.972046402483172));
#32708=CARTESIAN_POINT('Ctrl Pts',(96.6561107926275,1.45036588987332,-0.975048213468245));
#32709=CARTESIAN_POINT('Ctrl Pts',(96.7109051784694,1.4429750534112,-0.978048240430755));
#32710=CARTESIAN_POINT('Ctrl Pts',(96.7653158355214,1.43246992411588,-0.981048267393265));
#32711=CARTESIAN_POINT('Ctrl Pts',(96.8189666488126,1.41891516781079,-0.984048294355775));
#32712=CARTESIAN_POINT('Ctrl Pts',(96.87260676593,1.40536311386977,-0.987047723213468));
#32713=CARTESIAN_POINT('Ctrl Pts',(96.9254868283957,1.38876276965795,-0.99004715207116));
#32714=CARTESIAN_POINT('Ctrl Pts',(96.9772429584354,1.36922944614868,-0.993046580928853));
#32715=CARTESIAN_POINT('Ctrl Pts',(97.0290466731114,1.34967816368277,-0.996048767464354));
#32716=CARTESIAN_POINT('Ctrl Pts',(97.0797238957159,1.32718870137387,-0.999050953999855));
#32717=CARTESIAN_POINT('Ctrl Pts',(97.1289293459707,1.30192510973508,-1.00205314053536));
#32718=CARTESIAN_POINT('Ctrl Pts',(97.1781571948424,1.27665001795743,-1.00505669368422));
#32719=CARTESIAN_POINT('Ctrl Pts',(97.2259114796891,1.24859854749759,-1.00806024683309));
#32720=CARTESIAN_POINT('Ctrl Pts',(97.2718731520585,1.21797986180077,-1.01106379998196));
#32721=CARTESIAN_POINT('Ctrl Pts',(97.3179215703662,1.1873033878103,-1.01407302189835));
#32722=CARTESIAN_POINT('Ctrl Pts',(97.3621701943197,1.15405033751025,-1.01708224381475));
#32723=CARTESIAN_POINT('Ctrl Pts',(97.4043314500332,1.11847149395439,-1.02009146573115));
#32724=CARTESIAN_POINT('Ctrl Pts',(97.4365859127766,1.09125274858017,-1.0223935991602));
#32725=CARTESIAN_POINT('Ctrl Pts',(97.4676193537472,1.06267367304437,-1.02469573258925));
#32726=CARTESIAN_POINT('Ctrl Pts',(97.4973182204881,1.03286045700743,-1.0269978660183));
#32727=CARTESIAN_POINT('Ctrl Pts',(97.5355982365663,0.994433051706249,-1.02996517468524));
#32728=CARTESIAN_POINT('Ctrl Pts',(97.5718303382193,0.953782712209917,-1.03293248335217));
#32729=CARTESIAN_POINT('Ctrl Pts',(97.6057410346534,0.911159474258424,-1.0358997920191));
#32730=CARTESIAN_POINT('Ctrl Pts',(97.6396034125982,0.868596969075096,-1.03886287264335));
#32731=CARTESIAN_POINT('Ctrl Pts',(97.6711505948298,0.824067549603088,-1.0418259532676));
#32732=CARTESIAN_POINT('Ctrl Pts',(97.7001459760191,0.777857874046635,-1.04478903389186));
#32733=CARTESIAN_POINT('Ctrl Pts',(97.7291122718648,0.731694551537961,-1.04774914224209));
#32734=CARTESIAN_POINT('Ctrl Pts',(97.7555315468684,0.683854768797007,-1.05070925059233));
#32735=CARTESIAN_POINT('Ctrl Pts',(97.779209119628,0.634656019835896,-1.05366935894257));
#32736=CARTESIAN_POINT('Ctrl Pts',(97.8029895413964,0.585243564739738,-1.05664232520746));
#32737=CARTESIAN_POINT('Ctrl Pts',(97.8240040853246,0.534460775308565,-1.05961529147234));
#32738=CARTESIAN_POINT('Ctrl Pts',(97.8421020126223,0.482654626155905,-1.06258825773722));
#32739=CARTESIAN_POINT('Ctrl Pts',(97.8601149766387,0.431091688302801,-1.0655472669912));
#32740=CARTESIAN_POINT('Ctrl Pts',(97.8752384986032,0.378515507001031,-1.06850627624518));
#32741=CARTESIAN_POINT('Ctrl Pts',(97.8873731861014,0.32528571340656,-1.07146528549916));
#32742=CARTESIAN_POINT('Ctrl Pts',(97.8995937286703,0.271679309562145,-1.07444523026949));
#32743=CARTESIAN_POINT('Ctrl Pts',(97.9087828366365,0.217410549822793,-1.07742517503983));
#32744=CARTESIAN_POINT('Ctrl Pts',(97.9148914798562,0.162856560853815,-1.08040511981017));
#32745=CARTESIAN_POINT('Ctrl Pts',(97.9210001230758,0.108302571884838,-1.08338506458051));
#32746=CARTESIAN_POINT('Ctrl Pts',(97.9240283002846,0.0534639155643919,
-1.08636500935085));
#32747=CARTESIAN_POINT('Ctrl Pts',(97.9239803891082,-0.00128081692310628,
-1.08934495412119));
#32748=CARTESIAN_POINT('Origin',(96.460480949577,-8.32667268468867E-16,
1.18130019239114E-14));
#32749=CARTESIAN_POINT('',(97.9239806916945,0.000868804938495186,-1.66065504587772));
#32750=CARTESIAN_POINT('',(97.9239806575939,0.000924464373925031,-1.58934495419106));
#32751=CARTESIAN_POINT('',(97.923980949577,-1.01189432752408E-15,1.19922289829666E-14));
#32752=CARTESIAN_POINT('Ctrl Pts',(97.9239806916941,0.00086880557632569,
-1.66065504584289));
#32753=CARTESIAN_POINT('Ctrl Pts',(97.9239493983902,0.0535822589773747,
-1.65777615891959));
#32754=CARTESIAN_POINT('Ctrl Pts',(97.9210702361685,0.106209644580605,-1.65489727199629));
#32755=CARTESIAN_POINT('Ctrl Pts',(97.9153700635578,0.158524181184318,-1.65201838507299));
#32756=CARTESIAN_POINT('Ctrl Pts',(97.9094100334058,0.213223615190671,-1.64900825642623));
#32757=CARTESIAN_POINT('Ctrl Pts',(97.9003483914511,0.267701392550938,-1.64599812777947));
#32758=CARTESIAN_POINT('Ctrl Pts',(97.8882131864674,0.32157877688655,-1.64298799913271));
#32759=CARTESIAN_POINT('Ctrl Pts',(97.876099549162,0.375360405930611,-1.63998322033264));
#32760=CARTESIAN_POINT('Ctrl Pts',(97.8609233044749,0.428543248510851,-1.63697844153257));
#32761=CARTESIAN_POINT('Ctrl Pts',(97.8427640618136,0.48075528871314,-1.63397366273249));
#32762=CARTESIAN_POINT('Ctrl Pts',(97.824622784714,0.532915673752846,-1.63097185666317));
#32763=CARTESIAN_POINT('Ctrl Pts',(97.8035045284219,0.584106662660049,-1.62797005059385));
#32764=CARTESIAN_POINT('Ctrl Pts',(97.7795391329655,0.633969840635917,-1.62496824452453));
#32765=CARTESIAN_POINT('Ctrl Pts',(97.7555879815453,0.683803382008644,-1.62196822260413));
#32766=CARTESIAN_POINT('Ctrl Pts',(97.728793273371,0.732310201644931,-1.61896820068373));
#32767=CARTESIAN_POINT('Ctrl Pts',(97.6993326639567,0.779152539480246,-1.61596817876332));
#32768=CARTESIAN_POINT('Ctrl Pts',(97.6698779291648,0.825985536672102,-1.61296875506531));
#32769=CARTESIAN_POINT('Ctrl Pts',(97.6377586298672,0.8711542644181,-1.60996933136729));
#32770=CARTESIAN_POINT('Ctrl Pts',(97.6031968122026,0.914348241811566,-1.60696990766928));
#32771=CARTESIAN_POINT('Ctrl Pts',(97.5686032199489,0.95758192981558,-1.60396772643529));
#32772=CARTESIAN_POINT('Ctrl Pts',(97.5315629536859,0.998836827095143,-1.60096554520131));
#32773=CARTESIAN_POINT('Ctrl Pts',(97.4923386735164,1.03783519286378,-1.59796336396732));
#32774=CARTESIAN_POINT('Ctrl Pts',(97.4530965393233,1.07685130982479,-1.59495981620693));
#32775=CARTESIAN_POINT('Ctrl Pts',(97.4116688052513,1.11360849666281,-1.59195626844654));
#32776=CARTESIAN_POINT('Ctrl Pts',(97.3683529384007,1.14786789392742,-1.58895272068615));
#32777=CARTESIAN_POINT('Ctrl Pts',(97.3249553201348,1.18219195004367,-1.58594350423441));
#32778=CARTESIAN_POINT('Ctrl Pts',(97.2796628835873,1.21400849500905,-1.58293428778266));
#32779=CARTESIAN_POINT('Ctrl Pts',(97.2328029612089,1.24312145840578,-1.57992507133092));
#32780=CARTESIAN_POINT('Ctrl Pts',(97.1969531982159,1.2653940697295,-1.57762289729576));
#32781=CARTESIAN_POINT('Ctrl Pts',(97.1601866391868,1.28608518851574,-1.57532072326059));
#32782=CARTESIAN_POINT('Ctrl Pts',(97.1226583816472,1.30512577878795,-1.57301854922542));
#32783=CARTESIAN_POINT('Ctrl Pts',(97.0735895963715,1.3300216491759,-1.57000842057024));
#32784=CARTESIAN_POINT('Ctrl Pts',(97.023011745983,1.35219872387494,-1.56699829191506));
#32785=CARTESIAN_POINT('Ctrl Pts',(96.9712573581323,1.37147355441633,-1.56398816325988));
#32786=CARTESIAN_POINT('Ctrl Pts',(96.9195949524165,1.39071412815095,-1.56098338445177));
#32787=CARTESIAN_POINT('Ctrl Pts',(96.8667606498236,1.40706251119664,-1.55797860564366));
#32788=CARTESIAN_POINT('Ctrl Pts',(96.8131095219622,1.42038211053843,-1.55497382683554));
#32789=CARTESIAN_POINT('Ctrl Pts',(96.7595114730062,1.43368853234262,-1.55197202075842));
#32790=CARTESIAN_POINT('Ctrl Pts',(96.7050987096523,1.44397197970206,-1.5489702146813));
#32791=CARTESIAN_POINT('Ctrl Pts',(96.650242358023,1.4511453606943,-1.54596840860417));
#32792=CARTESIAN_POINT('Ctrl Pts',(96.5954186107365,1.45831447812607,-1.54296838667622));
#32793=CARTESIAN_POINT('Ctrl Pts',(96.5401523203595,1.46237712468802,-1.53996836474827));
#32794=CARTESIAN_POINT('Ctrl Pts',(96.484823440313,1.46329754087976,-1.53696834282032));
#32795=CARTESIAN_POINT('Ctrl Pts',(96.4295055931821,1.46421777353491,-1.53396891911501));
#32796=CARTESIAN_POINT('Ctrl Pts',(96.374125708915,1.46199701140134,-1.5309694954097));
#32797=CARTESIAN_POINT('Ctrl Pts',(96.3190651487667,1.45665157854621,-1.52797007170439));
#32798=CARTESIAN_POINT('Ctrl Pts',(96.2639539684111,1.45130123134007,-1.52496789046357));
#32799=CARTESIAN_POINT('Ctrl Pts',(96.2091632254679,1.44282052530776,-1.52196570922275));
#32800=CARTESIAN_POINT('Ctrl Pts',(96.1550690517712,1.43127768887756,-1.51896352798193));
#32801=CARTESIAN_POINT('Ctrl Pts',(96.1009502556092,1.4197295984048,-1.51595998021495));
#32802=CARTESIAN_POINT('Ctrl Pts',(96.0475291710268,1.40511673864792,-1.51295643244796));
#32803=CARTESIAN_POINT('Ctrl Pts',(95.9951683840998,1.38755773444171,-1.50995288468098));
#32804=CARTESIAN_POINT('Ctrl Pts',(95.9427087750004,1.36996559057045,-1.50694366822311));
#32805=CARTESIAN_POINT('Ctrl Pts',(95.8913139527062,1.34941639113035,-1.50393445176525));
#32806=CARTESIAN_POINT('Ctrl Pts',(95.8413269846373,1.32607715375067,-1.50092523530739));
#32807=CARTESIAN_POINT('Ctrl Pts',(95.80308490446,1.3082216801816,-1.49862306133088));
#32808=CARTESIAN_POINT('Ctrl Pts',(95.7656664330478,1.28873424402576,-1.49632088735437));
#32809=CARTESIAN_POINT('Ctrl Pts',(95.7292141345577,1.26770702264027,-1.49401871337787));
#32810=CARTESIAN_POINT('Ctrl Pts',(95.6815521802114,1.24021359953075,-1.49100858464771));
#32811=CARTESIAN_POINT('Ctrl Pts',(95.6353427432839,1.20997075436495,-1.48799845591755));
#32812=CARTESIAN_POINT('Ctrl Pts',(95.5909211586164,1.177156752495,-1.4849883271874));
#32813=CARTESIAN_POINT('Ctrl Pts',(95.5465785236169,1.14440107034893,-1.48198354830384));
#32814=CARTESIAN_POINT('Ctrl Pts',(95.5040178564245,1.10908361128876,-1.47897876942029));
#32815=CARTESIAN_POINT('Ctrl Pts',(95.4635475671057,1.07142712347335,-1.47597399053673));
#32816=CARTESIAN_POINT('Ctrl Pts',(95.4231173164316,1.0338078905123,-1.47297218438394));
#32817=CARTESIAN_POINT('Ctrl Pts',(95.3847737315916,0.993854570862867,-1.46997037823114));
#32818=CARTESIAN_POINT('Ctrl Pts',(95.3487925362772,0.95183040597314,-1.46696857207835));
#32819=CARTESIAN_POINT('Ctrl Pts',(95.312832726693,0.909831218504103,-1.46396855007464));
#32820=CARTESIAN_POINT('Ctrl Pts',(95.2792328663936,0.865764025730836,-1.46096852807092));
#32821=CARTESIAN_POINT('Ctrl Pts',(95.2482305099858,0.819927510034295,-1.4579685060672));
#32822=CARTESIAN_POINT('Ctrl Pts',(95.217234335637,0.774100134418602,-1.45496908228618));
#32823=CARTESIAN_POINT('Ctrl Pts',(95.188834932249,0.726504573758012,-1.45196965850515));
#32824=CARTESIAN_POINT('Ctrl Pts',(95.1632270022737,0.677469147788982,-1.44897023472413));
#32825=CARTESIAN_POINT('Ctrl Pts',(95.1375955295234,0.628388640862618,-1.44596805340826));
#32826=CARTESIAN_POINT('Ctrl Pts',(95.1147609024247,0.577866093083683,-1.44296587209239));
#32827=CARTESIAN_POINT('Ctrl Pts',(95.0948714947951,0.526253804746486,-1.43996369077653));
#32828=CARTESIAN_POINT('Ctrl Pts',(95.0749730339511,0.474618023647986,-1.43696014293476));
#32829=CARTESIAN_POINT('Ctrl Pts',(95.0580226268801,0.421892016848949,-1.43395659509298));
#32830=CARTESIAN_POINT('Ctrl Pts',(95.0441190377038,0.368444276105352,-1.43095304725121));
#32831=CARTESIAN_POINT('Ctrl Pts',(95.0301892078499,0.314895661773628,-1.42794383071992));
#32832=CARTESIAN_POINT('Ctrl Pts',(95.0193177870982,0.260623111488979,-1.42493461418863));
#32833=CARTESIAN_POINT('Ctrl Pts',(95.0115523443857,0.206005211240961,-1.42192539765733));
#32834=CARTESIAN_POINT('Ctrl Pts',(95.0056114640013,0.164220289990292,-1.41962322428166));
#32835=CARTESIAN_POINT('Ctrl Pts',(95.0014874118531,0.122233465416819,-1.41732105090598));
#32836=CARTESIAN_POINT('Ctrl Pts',(94.9991808834234,0.0802145040471148,
-1.41501887753031));
#32837=CARTESIAN_POINT('Ctrl Pts',(94.996165060584,0.0252740395133446,-1.41200874899372));
#32838=CARTESIAN_POINT('Ctrl Pts',(94.9962456021385,-0.029952176063699,
-1.40899862045712));
#32839=CARTESIAN_POINT('Ctrl Pts',(94.999456431718,-0.0850858872831129,
-1.40598849192053));
#32840=CARTESIAN_POINT('Ctrl Pts',(95.0026615547491,-0.140121610370722,
-1.40298371323007));
#32841=CARTESIAN_POINT('Ctrl Pts',(95.0089858947382,-0.195064632407521,
-1.39997893453962));
#32842=CARTESIAN_POINT('Ctrl Pts',(95.0184114081778,-0.249534942981575,
-1.39697415584916));
#32843=CARTESIAN_POINT('Ctrl Pts',(95.0278275966346,-0.303951364214357,
-1.39397234988903));
#32844=CARTESIAN_POINT('Ctrl Pts',(95.0403387911852,-0.357895482590965,
-1.3909705439289));
#32845=CARTESIAN_POINT('Ctrl Pts',(95.0558751743951,-0.410992538041389,
-1.38796873796877));
#32846=CARTESIAN_POINT('Ctrl Pts',(95.0714023234266,-0.464058034815733,
-1.38496871615696));
#32847=CARTESIAN_POINT('Ctrl Pts',(95.0899509492582,-0.516276960700702,
-1.38196869434514));
#32848=CARTESIAN_POINT('Ctrl Pts',(95.1114006962819,-0.567287158473805,
-1.37896867253333));
#32849=CARTESIAN_POINT('Ctrl Pts',(95.1328461661028,-0.61828718452033,-1.3759692489431));
#32850=CARTESIAN_POINT('Ctrl Pts',(95.1571914036437,-0.668078474571037,
-1.37296982535288));
#32851=CARTESIAN_POINT('Ctrl Pts',(95.1842678169643,-0.716318567501113,
-1.36997040176265));
#32852=CARTESIAN_POINT('Ctrl Pts',(95.2113691231477,-0.764603010249576,
-1.36696822063438));
#32853=CARTESIAN_POINT('Ctrl Pts',(95.2412063625633,-0.811332945188495,
-1.36396603950611));
#32854=CARTESIAN_POINT('Ctrl Pts',(95.2735655451241,-0.856191609788615,
-1.36096385837785));
#32855=CARTESIAN_POINT('Ctrl Pts',(95.3059394568793,-0.901070693074843,
-1.35796031072218));
#32856=CARTESIAN_POINT('Ctrl Pts',(95.3408372667544,-0.944076397294422,
-1.35495676306652));
#32857=CARTESIAN_POINT('Ctrl Pts',(95.3780043173352,-0.984924662423716,
-1.35195321541085));
#32858=CARTESIAN_POINT('Ctrl Pts',(95.4152415145129,-1.02585002182717,-1.34894399906092));
#32859=CARTESIAN_POINT('Ctrl Pts',(95.4547561300347,-1.06460943735449,-1.34593478271099));
#32860=CARTESIAN_POINT('Ctrl Pts',(95.4962570794472,-1.1009562108785,-1.34292556636105));
#32861=CARTESIAN_POINT('Ctrl Pts',(95.5280070211773,-1.12876299500753,-1.34062339146828));
#32862=CARTESIAN_POINT('Ctrl Pts',(95.5609187717421,-1.15515845393747,-1.33832121657551));
#32863=CARTESIAN_POINT('Ctrl Pts',(95.5948505268175,-1.18004924524072,-1.33601904168274));
#32864=CARTESIAN_POINT('Ctrl Pts',(95.6392168123026,-1.21259433318144,-1.33300891302001));
#32865=CARTESIAN_POINT('Ctrl Pts',(95.6855142634369,-1.2427022656769,-1.32999878435727));
#32866=CARTESIAN_POINT('Ctrl Pts',(95.7334446168608,-1.27013795349584,-1.32698865569453));
#32867=CARTESIAN_POINT('Ctrl Pts',(95.7812897845072,-1.2975248803474,-1.32398387688074));
#32868=CARTESIAN_POINT('Ctrl Pts',(95.8307616405166,-1.3222487273719,-1.32097909806695));
#32869=CARTESIAN_POINT('Ctrl Pts',(95.8815320570206,-1.34411697028485,-1.31797431925316));
#32870=CARTESIAN_POINT('Ctrl Pts',(95.9322522445866,-1.36596357818489,-1.3149725131715));
#32871=CARTESIAN_POINT('Ctrl Pts',(95.9842679650452,-1.38495997056511,-1.31197070708984));
#32872=CARTESIAN_POINT('Ctrl Pts',(96.0372271987598,-1.40095985396412,-1.30896890100819));
#32873=CARTESIAN_POINT('Ctrl Pts',(96.0901549556799,-1.41695022768923,-1.30596887907684));
#32874=CARTESIAN_POINT('Ctrl Pts',(96.1440246098036,-1.42994747006617,-1.3029688571455));
#32875=CARTESIAN_POINT('Ctrl Pts',(96.198467082858,-1.43985450086005,-1.29996883521415));
#32876=CARTESIAN_POINT('Ctrl Pts',(96.2528986997311,-1.44975955612791,-1.29696941150659));
#32877=CARTESIAN_POINT('Ctrl Pts',(96.3079023893993,-1.45657552907886,-1.29396998779902));
#32878=CARTESIAN_POINT('Ctrl Pts',(96.3630992134576,-1.4602565005746,-1.29097056409146));
#32879=CARTESIAN_POINT('Ctrl Pts',(96.4183467829659,-1.46394085618814,-1.28796838285013));
#32880=CARTESIAN_POINT('Ctrl Pts',(96.4737873135262,-1.46448441691325,-1.28496620160881));
#32881=CARTESIAN_POINT('Ctrl Pts',(96.5290385846283,-1.461893327393,-1.28196402036748));
#32882=CARTESIAN_POINT('Ctrl Pts',(96.5843150048629,-1.45930105846724,-1.27896047260096));
#32883=CARTESIAN_POINT('Ctrl Pts',(96.6394014677138,-1.45357134975605,-1.27595692483444));
#32884=CARTESIAN_POINT('Ctrl Pts',(96.6939209214289,-1.44476227440427,-1.27295337706792));
#32885=CARTESIAN_POINT('Ctrl Pts',(96.7485432714083,-1.43593657341001,-1.26994416061208));
#32886=CARTESIAN_POINT('Ctrl Pts',(96.8025959574962,-1.42402000981103,-1.26693494415624));
#32887=CARTESIAN_POINT('Ctrl Pts',(96.8557133159405,-1.40912157977184,-1.26392572770041));
#32888=CARTESIAN_POINT('Ctrl Pts',(96.8963502727589,-1.39772367001324,-1.26162355374533));
#32889=CARTESIAN_POINT('Ctrl Pts',(96.9364400149676,-1.38458157295015,-1.25932137979025));
#32890=CARTESIAN_POINT('Ctrl Pts',(96.9758268846356,-1.36976305148684,-1.25701920583518));
#32891=CARTESIAN_POINT('Ctrl Pts',(97.0273258444945,-1.35038759848846,-1.2540090766957));
#32892=CARTESIAN_POINT('Ctrl Pts',(97.0778388018055,-1.32806308923919,-1.25099894755622));
#32893=CARTESIAN_POINT('Ctrl Pts',(97.1270058930076,-1.30291087561076,-1.24798881841674));
#32894=CARTESIAN_POINT('Ctrl Pts',(97.1760856004827,-1.27780336452865,-1.24498403912199));
#32895=CARTESIAN_POINT('Ctrl Pts',(97.2238237223901,-1.24987836102905,-1.24197925982723));
#32896=CARTESIAN_POINT('Ctrl Pts',(97.2698797266185,-1.21930548662905,-1.23897448053247));
#32897=CARTESIAN_POINT('Ctrl Pts',(97.3158901660822,-1.18876285900914,-1.23597267396764));
#32898=CARTESIAN_POINT('Ctrl Pts',(97.3602213466864,-1.15557784048893,-1.23297086740281));
#32899=CARTESIAN_POINT('Ctrl Pts',(97.4025584015194,-1.11996532291928,-1.22996906083797));
#32900=CARTESIAN_POINT('Ctrl Pts',(97.4448702929678,-1.08437397194896,-1.22696903842212));
#32901=CARTESIAN_POINT('Ctrl Pts',(97.485190004498,-1.04635832094007,-1.22396901600626));
#32902=CARTESIAN_POINT('Ctrl Pts',(97.523234565834,-1.00617443871958,-1.22096899359041));
#32903=CARTESIAN_POINT('Ctrl Pts',(97.5612715408454,-0.965998569417716,
-1.21796956939787));
#32904=CARTESIAN_POINT('Ctrl Pts',(97.5970339037676,-0.923655710838852,
-1.21497014520534));
#32905=CARTESIAN_POINT('Ctrl Pts',(97.6302761455861,-0.879438144154546,
-1.2119707210128));
#32906=CARTESIAN_POINT('Ctrl Pts',(97.6635489487699,-0.835179925903617,
-1.20896853928968));
#32907=CARTESIAN_POINT('Ctrl Pts',(97.6942966839872,-0.789043979217203,
-1.20596635756657));
#32908=CARTESIAN_POINT('Ctrl Pts',(97.7223156537142,-0.741353781561064,
-1.20296417584345));
#32909=CARTESIAN_POINT('Ctrl Pts',(97.7503473770328,-0.69364187642226,-1.19996062759616));
#32910=CARTESIAN_POINT('Ctrl Pts',(97.775647617204,-0.644374780652279,-1.19695707934888));
#32911=CARTESIAN_POINT('Ctrl Pts',(97.7980589924109,-0.593900016272528,
-1.19395353110159));
#32912=CARTESIAN_POINT('Ctrl Pts',(97.8205126652406,-0.543329989441457,
-1.19094431417269));
#32913=CARTESIAN_POINT('Ctrl Pts',(97.8400663943914,-0.491548236086386,
-1.18793509724379));
#32914=CARTESIAN_POINT('Ctrl Pts',(97.8566116698041,-0.438920564610642,
-1.1849258803149));
#32915=CARTESIAN_POINT('Ctrl Pts',(97.869269460652,-0.398658311989629,-1.1826237102058));
#32916=CARTESIAN_POINT('Ctrl Pts',(97.880167457635,-0.357901350998972,-1.18032154009671));
#32917=CARTESIAN_POINT('Ctrl Pts',(97.8892773632463,-0.316817073854785,
-1.17801936998761));
#32918=CARTESIAN_POINT('Ctrl Pts',(97.9055044705775,-0.243635308500493,
-1.17391860725207));
#32919=CARTESIAN_POINT('Ctrl Pts',(97.9161139965923,-0.169166208287235,
-1.16981784451653));
#32920=CARTESIAN_POINT('Ctrl Pts',(97.9209501091143,-0.0941386426520588,
-1.16571708178099));
#32921=CARTESIAN_POINT('Ctrl Pts',(97.9229400296052,-0.0632669684386882,
-1.16402973646829));
#32922=CARTESIAN_POINT('Ctrl Pts',(97.9239529862227,-0.0323010019033244,
-1.16234239115559));
#32923=CARTESIAN_POINT('Ctrl Pts',(97.9239803785352,-0.00129284140671581,
-1.16065504584289));
#32924=CARTESIAN_POINT('Ctrl Pts',(97.9239803891076,-0.00128081758231612,
-1.08934495415707));
#32925=CARTESIAN_POINT('Ctrl Pts',(97.923913186341,-0.0780686541499415,
-1.09352478117624));
#32926=CARTESIAN_POINT('Ctrl Pts',(97.9177989441704,-0.154598277700433,
-1.09770460819541));
#32927=CARTESIAN_POINT('Ctrl Pts',(97.9057798266317,-0.230094341487387,
-1.10188443521458));
#32928=CARTESIAN_POINT('Ctrl Pts',(97.9018372523638,-0.254858958145268,
-1.10325552409834));
#32929=CARTESIAN_POINT('Ctrl Pts',(97.8972596717829,-0.279512589571985,
-1.1046266129821));
#32930=CARTESIAN_POINT('Ctrl Pts',(97.8920531495257,-0.304028430140903,
-1.10599770186586));
#32931=CARTESIAN_POINT('Ctrl Pts',(97.8806225864053,-0.357851279488796,
-1.1090078336305));
#32932=CARTESIAN_POINT('Ctrl Pts',(97.8661284184552,-0.411141685375522,
-1.11201796539513));
#32933=CARTESIAN_POINT('Ctrl Pts',(97.8486366398626,-0.463525651423493,
-1.11502809715977));
#32934=CARTESIAN_POINT('Ctrl Pts',(97.8311759487617,-0.515816517384617,
-1.11803287912846));
#32935=CARTESIAN_POINT('Ctrl Pts',(97.8107283854768,-0.567203643637056,
-1.12103766109716));
#32936=CARTESIAN_POINT('Ctrl Pts',(97.7874105676034,-0.617324905381474,
-1.12404244306586));
#32937=CARTESIAN_POINT('Ctrl Pts',(97.7641158186009,-0.667396580971582,
-1.12704425233241));
#32938=CARTESIAN_POINT('Ctrl Pts',(97.7379566618143,-0.716204396420274,
-1.13004606159897));
#32939=CARTESIAN_POINT('Ctrl Pts',(97.7090983230289,-0.763404810512815,
-1.13304787086552));
#32940=CARTESIAN_POINT('Ctrl Pts',(97.6802571362052,-0.81057717102601,-1.13604789600589));
#32941=CARTESIAN_POINT('Ctrl Pts',(97.6487202220611,-0.856143574095053,
-1.13904792114627));
#32942=CARTESIAN_POINT('Ctrl Pts',(97.6146983023442,-0.899785837058556,
-1.14204794628664));
#32943=CARTESIAN_POINT('Ctrl Pts',(97.5806831666032,-0.943419397748199,
-1.14504737322154));
#32944=CARTESIAN_POINT('Ctrl Pts',(97.5441843338644,-0.98512916401779,-1.14804680015645));
#32945=CARTESIAN_POINT('Ctrl Pts',(97.5054539481688,-1.02462855816834,-1.15104622709135));
#32946=CARTESIAN_POINT('Ctrl Pts',(97.4666879555246,-1.06416426625868,-1.15404841156246));
#32947=CARTESIAN_POINT('Ctrl Pts',(97.4256866816569,-1.10148516443139,-1.15705059603356));
#32948=CARTESIAN_POINT('Ctrl Pts',(97.3827393862181,-1.13634133342247,-1.16005278050466));
#32949=CARTESIAN_POINT('Ctrl Pts',(97.3397725420696,-1.17121336821187,-1.16305633150727));
#32950=CARTESIAN_POINT('Ctrl Pts',(97.2948583396211,-1.20361812786644,-1.16605988250989));
#32951=CARTESIAN_POINT('Ctrl Pts',(97.2483167590414,-1.23334787765881,-1.1690634335125));
#32952=CARTESIAN_POINT('Ctrl Pts',(97.2016873396489,-1.26313373697509,-1.17207265317422));
#32953=CARTESIAN_POINT('Ctrl Pts',(97.1534248681767,-1.29023424186537,-1.17508187283594));
#32954=CARTESIAN_POINT('Ctrl Pts',(97.1038747357487,-1.31448723307444,-1.17809109249765));
#32955=CARTESIAN_POINT('Ctrl Pts',(97.0659673141667,-1.33304153994176,-1.18039324090291));
#32956=CARTESIAN_POINT('Ctrl Pts',(97.0273068012296,-1.34993021255995,-1.18269538930817));
#32957=CARTESIAN_POINT('Ctrl Pts',(96.9880544450365,-1.36510016368348,-1.18499753771342));
#32958=CARTESIAN_POINT('Ctrl Pts',(96.9367307977058,-1.38493533530114,-1.18800766664105));
#32959=CARTESIAN_POINT('Ctrl Pts',(96.8841791451047,-1.40191373683725,-1.19101779556867));
#32960=CARTESIAN_POINT('Ctrl Pts',(96.8307487774288,-1.41588628980505,-1.1940279244963));
#32961=CARTESIAN_POINT('Ctrl Pts',(96.7774133701589,-1.42983400971704,-1.19703270359989));
#32962=CARTESIAN_POINT('Ctrl Pts',(96.7232028538547,-1.4407863501921,-1.20003748270348));
#32963=CARTESIAN_POINT('Ctrl Pts',(96.6684842364518,-1.44864311776547,-1.20304226180707));
#32964=CARTESIAN_POINT('Ctrl Pts',(96.6138197538003,-1.45649211240562,-1.20604406819356));
#32965=CARTESIAN_POINT('Ctrl Pts',(96.5586486860187,-1.46125152620207,-1.20904587458005));
#32966=CARTESIAN_POINT('Ctrl Pts',(96.5033490361798,-1.46287203033998,-1.21204768096654));
#32967=CARTESIAN_POINT('Ctrl Pts',(96.4480822539129,-1.46449157132466,-1.21504770321718));
#32968=CARTESIAN_POINT('Ctrl Pts',(96.3926875679001,-1.46297588500113,-1.21804772546782));
#32969=CARTESIAN_POINT('Ctrl Pts',(96.3375466016096,-1.45832760245764,-1.22104774771846));
#32970=CARTESIAN_POINT('Ctrl Pts',(96.2824166305276,-1.45368024679009,-1.22404717175923));
#32971=CARTESIAN_POINT('Ctrl Pts',(96.2275408046486,-1.44590157975849,-1.22704659580001));
#32972=CARTESIAN_POINT('Ctrl Pts',(96.1732969104484,-1.43504619356653,-1.23004601984078));
#32973=CARTESIAN_POINT('Ctrl Pts',(96.1190031465407,-1.42418082735853,-1.23304820143431));
#32974=CARTESIAN_POINT('Ctrl Pts',(96.0653429939818,-1.41023319464078,-1.23605038302783));
#32975=CARTESIAN_POINT('Ctrl Pts',(96.0126838166709,-1.39330900297137,-1.23905256462135));
#32976=CARTESIAN_POINT('Ctrl Pts',(95.9600006698984,-1.37637710773,-1.24205611275116));
#32977=CARTESIAN_POINT('Ctrl Pts',(95.9083199002972,-1.35646614288436,-1.24505966088096));
#32978=CARTESIAN_POINT('Ctrl Pts',(95.8579903266545,-1.33373059471938,-1.24806320901076));
#32979=CARTESIAN_POINT('Ctrl Pts',(95.8075657642202,-1.3109521369469,-1.25107242584362));
#32980=CARTESIAN_POINT('Ctrl Pts',(95.7584979614032,-1.2853386914663,-1.25408164267648));
#32981=CARTESIAN_POINT('Ctrl Pts',(95.7111114507522,-1.25709092918178,-1.25709085950934));
#32982=CARTESIAN_POINT('Ctrl Pts',(95.6748588729945,-1.23548026014044,-1.25939303085989));
#32983=CARTESIAN_POINT('Ctrl Pts',(95.6395898415557,-1.21232872962806,-1.26169520221044));
#32984=CARTESIAN_POINT('Ctrl Pts',(95.605436927778,-1.18774238401507,-1.26399737356099));
#32985=CARTESIAN_POINT('Ctrl Pts',(95.5607814193552,-1.15559532415497,-1.26700750127086));
#32986=CARTESIAN_POINT('Ctrl Pts',(95.5178475527745,-1.12085885059954,-1.27001762898074));
#32987=CARTESIAN_POINT('Ctrl Pts',(95.476951036042,-1.0837440468957,-1.27302775669062));
#32988=CARTESIAN_POINT('Ctrl Pts',(95.4361272043169,-1.04669520699502,-1.27603253452789));
#32989=CARTESIAN_POINT('Ctrl Pts',(95.3973339245293,-1.00727677746951,-1.27903731236516));
#32990=CARTESIAN_POINT('Ctrl Pts',(95.3608556431135,-0.965741391566654,
-1.28204209020243));
#32991=CARTESIAN_POINT('Ctrl Pts',(95.3244134511082,-0.924247098268254,
-1.28504389529383));
#32992=CARTESIAN_POINT('Ctrl Pts',(95.2902820672444,-0.880640392334413,
-1.28804570038522));
#32993=CARTESIAN_POINT('Ctrl Pts',(95.2587093451839,-0.835210908019247,
-1.29104750547661));
#32994=CARTESIAN_POINT('Ctrl Pts',(95.2271553887851,-0.789808425314378,
-1.29404752640575));
#32995=CARTESIAN_POINT('Ctrl Pts',(95.1981573807067,-0.742585744386444,
-1.29704754733489));
#32996=CARTESIAN_POINT('Ctrl Pts',(95.1719216349935,-0.693863922394019,
-1.30004756826402));
#32997=CARTESIAN_POINT('Ctrl Pts',(95.1456911209483,-0.645151816016436,
-1.30304699095921));
#32998=CARTESIAN_POINT('Ctrl Pts',(95.1222220256048,-0.594941626990456,
-1.3060464136544));
#32999=CARTESIAN_POINT('Ctrl Pts',(95.1016750476782,-0.543579590276448,
-1.30904583634959));
#33000=CARTESIAN_POINT('Ctrl Pts',(95.0811091798411,-0.492170333757866,
-1.31204801657082));
#33001=CARTESIAN_POINT('Ctrl Pts',(95.0634709931864,-0.439607605289542,
-1.31505019679204));
#33002=CARTESIAN_POINT('Ctrl Pts',(95.0488726811017,-0.386256839903434,
-1.31805237701327));
#33003=CARTESIAN_POINT('Ctrl Pts',(95.0342677242209,-0.332881790548091,
-1.32105592375382));
#33004=CARTESIAN_POINT('Ctrl Pts',(95.0227055106196,-0.278718506621066,
-1.32405947049438));
#33005=CARTESIAN_POINT('Ctrl Pts',(95.0142472472189,-0.224143543657761,
-1.32706301723493));
#33006=CARTESIAN_POINT('Ctrl Pts',(95.0057730202597,-0.169465579573552,
-1.33007223266795));
#33007=CARTESIAN_POINT('Ctrl Pts',(95.0004144973922,-0.11437491124949,-1.33308144810096));
#33008=CARTESIAN_POINT('Ctrl Pts',(94.9981809347718,-0.0592529889609269,
-1.33609066353397));
#33009=CARTESIAN_POINT('Ctrl Pts',(94.9964721612787,-0.0170822976898624,
-1.33839284549217));
#33010=CARTESIAN_POINT('Ctrl Pts',(94.9965913237324,0.0251065685188833,
-1.34069502745036));
#33011=CARTESIAN_POINT('Ctrl Pts',(94.998522041667,0.0671446318229337,-1.34299720940855));
#33012=CARTESIAN_POINT('Ctrl Pts',(95.0010464773481,0.12210987820601,-1.34600733852977));
#33013=CARTESIAN_POINT('Ctrl Pts',(95.0066803182552,0.177048047429061,-1.34901746765098));
#33014=CARTESIAN_POINT('Ctrl Pts',(95.0154192774912,0.231579389990714,-1.35202759677219));
#33015=CARTESIAN_POINT('Ctrl Pts',(95.0241427051611,0.286013815159483,-1.35503237605507));
#33016=CARTESIAN_POINT('Ctrl Pts',(95.0359602164494,0.340042331308619,-1.35803715533795));
#33017=CARTESIAN_POINT('Ctrl Pts',(95.0508156442684,0.393288668803274,-1.36104193462083));
#33018=CARTESIAN_POINT('Ctrl Pts',(95.0656563751288,0.446482327962045,-1.3640437411777));
#33019=CARTESIAN_POINT('Ctrl Pts',(95.0835289275258,0.498894835207535,-1.36704554773457));
#33020=CARTESIAN_POINT('Ctrl Pts',(95.1043261508944,0.550160351179653,-1.37004735429144));
#33021=CARTESIAN_POINT('Ctrl Pts',(95.1251110132854,0.60139539712783,-1.37304737670324));
#33022=CARTESIAN_POINT('Ctrl Pts',(95.1488169030918,0.651484314618733,-1.37604739911504));
#33023=CARTESIAN_POINT('Ctrl Pts',(95.1752876551499,0.700078885526163,-1.37904742152684));
#33024=CARTESIAN_POINT('Ctrl Pts',(95.2017531288081,0.748663766433972,-1.38204684571922));
#33025=CARTESIAN_POINT('Ctrl Pts',(95.230982117318,0.795754429021658,-1.3850462699116));
#33026=CARTESIAN_POINT('Ctrl Pts',(95.2627724444077,0.841027102206065,-1.38804569410398));
#33027=CARTESIAN_POINT('Ctrl Pts',(95.2945919981039,0.886341397063631,-1.39104787583296));
#33028=CARTESIAN_POINT('Ctrl Pts',(95.328977290781,0.929833930189806,-1.39405005756194));
#33029=CARTESIAN_POINT('Ctrl Pts',(95.3656835624845,0.971211064195376,-1.39705223929092));
#33030=CARTESIAN_POINT('Ctrl Pts',(95.4024065420808,1.01260703216817,-1.40005578754742));
#33031=CARTESIAN_POINT('Ctrl Pts',(95.4414522337086,1.05188530638393,-1.40305933580393));
#33032=CARTESIAN_POINT('Ctrl Pts',(95.4825387048994,1.0887888758042,-1.40606288406043));
#33033=CARTESIAN_POINT('Ctrl Pts',(95.5237027198233,1.12576209444113,-1.4090721010039));
#33034=CARTESIAN_POINT('Ctrl Pts',(95.5669147952189,1.16035132425278,-1.41208131794738));
#33035=CARTESIAN_POINT('Ctrl Pts',(95.6118605134582,1.19234038990616,-1.41509053489085));
#33036=CARTESIAN_POINT('Ctrl Pts',(95.6462457676871,1.2168132918449,-1.4173927050126));
#33037=CARTESIAN_POINT('Ctrl Pts',(95.6816450099557,1.23976519443698,-1.41969487513436));
#33038=CARTESIAN_POINT('Ctrl Pts',(95.717907768993,1.26111748916484,-1.42199704525611));
#33039=CARTESIAN_POINT('Ctrl Pts',(95.765321975675,1.28903599680838,-1.42500717390786));
#33040=CARTESIAN_POINT('Ctrl Pts',(95.8144124710483,1.31433550009617,-1.42801730255961));
#33041=CARTESIAN_POINT('Ctrl Pts',(95.8648588624843,1.33681209575889,-1.43102743121136));
#33042=CARTESIAN_POINT('Ctrl Pts',(95.9152155965013,1.35924874419255,-1.43403221001829));
#33043=CARTESIAN_POINT('Ctrl Pts',(95.966922965802,1.37887222827389,-1.43703698882523));
#33044=CARTESIAN_POINT('Ctrl Pts',(96.0196351450947,1.39552399716749,-1.44004176763216));
#33045=CARTESIAN_POINT('Ctrl Pts',(96.0722951744402,1.41215929190123,-1.44304357370949));
#33046=CARTESIAN_POINT('Ctrl Pts',(96.1259575434175,1.42582853718202,-1.44604537978682));
#33047=CARTESIAN_POINT('Ctrl Pts',(96.1802573051872,1.43642158126537,-1.44904718586414));
#33048=CARTESIAN_POINT('Ctrl Pts',(96.2345247934531,1.44700832928704,-1.45204720779368));
#33049=CARTESIAN_POINT('Ctrl Pts',(96.2894284063168,1.45452239913185,-1.45504722972322));
#33050=CARTESIAN_POINT('Ctrl Pts',(96.3445911738028,1.45890431827142,-1.45804725165275));
#33051=CARTESIAN_POINT('Ctrl Pts',(96.3997429415224,1.46328536363165,-1.46104667536103));
#33052=CARTESIAN_POINT('Ctrl Pts',(96.4551532350738,1.46453545685652,-1.4640460990693));
#33053=CARTESIAN_POINT('Ctrl Pts',(96.5104404192415,1.46264701872695,-1.46704552277757));
#33054=CARTESIAN_POINT('Ctrl Pts',(96.5657784320038,1.4607568444508,-1.47004770402349));
#33055=CARTESIAN_POINT('Ctrl Pts',(96.6209925803185,1.45572239217891,-1.4730498852694));
#33056=CARTESIAN_POINT('Ctrl Pts',(96.6757031991877,1.44758821260485,-1.47605206651532));
#33057=CARTESIAN_POINT('Ctrl Pts',(96.7304387211361,1.43945033052985,-1.47905561428859));
#33058=CARTESIAN_POINT('Ctrl Pts',(96.7846697387265,1.42821001593459,-1.48205916206186));
#33059=CARTESIAN_POINT('Ctrl Pts',(96.8380269515981,1.41396296498808,-1.48506270983512));
#33060=CARTESIAN_POINT('Ctrl Pts',(96.8914848672617,1.39968902512196,-1.48807192630116));
#33061=CARTESIAN_POINT('Ctrl Pts',(96.9440651808393,1.38239717817992,-1.49108114276719));
#33062=CARTESIAN_POINT('Ctrl Pts',(96.9954150432075,1.36223263999644,-1.49409035923323));
#33063=CARTESIAN_POINT('Ctrl Pts',(97.0346997929637,1.34680594165778,-1.49639253319004));
#33064=CARTESIAN_POINT('Ctrl Pts',(97.0732647016424,1.32969892729858,-1.49869470714686));
#33065=CARTESIAN_POINT('Ctrl Pts',(97.1109617148245,1.31099466972333,-1.50099688110367));
#33066=CARTESIAN_POINT('Ctrl Pts',(97.160251150663,1.28653855965416,-1.50400700965113));
#33067=CARTESIAN_POINT('Ctrl Pts',(97.2082630176524,1.25924749917942,-1.50701713819859));
#33068=CARTESIAN_POINT('Ctrl Pts',(97.2546514800504,1.22927841375647,-1.51002726674605));
#33069=CARTESIAN_POINT('Ctrl Pts',(97.300957497026,1.19936259187746,-1.51303204544342));
#33070=CARTESIAN_POINT('Ctrl Pts',(97.3456453951994,1.16677847478941,-1.51603682414079));
#33071=CARTESIAN_POINT('Ctrl Pts',(97.3883934264001,1.13172906888357,-1.51904160283817));
#33072=CARTESIAN_POINT('Ctrl Pts',(97.4310991654771,1.09671433858191,-1.52204340880279));
#33073=CARTESIAN_POINT('Ctrl Pts',(97.4718684329952,1.05923948419602,-1.52504521476742));
#33074=CARTESIAN_POINT('Ctrl Pts',(97.5104095683821,1.01954997200432,-1.52804702073204));
#33075=CARTESIAN_POINT('Ctrl Pts',(97.548927796494,0.97988404963583,-1.53104704254594));
#33076=CARTESIAN_POINT('Ctrl Pts',(97.5852201501666,0.938006456577654,-1.53404706435984));
#33077=CARTESIAN_POINT('Ctrl Pts',(97.6190308446368,0.89420041973649,-1.53704708617374));
#33078=CARTESIAN_POINT('Ctrl Pts',(97.6528347970331,0.850403118105972,-1.54004650976364));
#33079=CARTESIAN_POINT('Ctrl Pts',(97.6841577504972,0.804678554218957,-1.54304593335354));
#33080=CARTESIAN_POINT('Ctrl Pts',(97.7127848332375,0.757342216549942,-1.54604535694344));
#33081=CARTESIAN_POINT('Ctrl Pts',(97.7414382344224,0.709962359993977,-1.54904753806766));
#33082=CARTESIAN_POINT('Ctrl Pts',(97.7673905393589,0.660968222103689,-1.55204971919189));
#33083=CARTESIAN_POINT('Ctrl Pts',(97.7904716129776,0.610702124826206,-1.55505190031612));
#33084=CARTESIAN_POINT('Ctrl Pts',(97.8135631925819,0.560413147551788,-1.55805544796568));
#33085=CARTESIAN_POINT('Ctrl Pts',(97.8337807424909,0.508851549286685,-1.56105899561523));
#33086=CARTESIAN_POINT('Ctrl Pts',(97.8510026265431,0.456378917005767,-1.56406254326478));
#33087=CARTESIAN_POINT('Ctrl Pts',(97.8682570140046,0.403807251457771,-1.5670717596053));
#33088=CARTESIAN_POINT('Ctrl Pts',(97.8825043049642,0.350321628651735,-1.57008097594582));
#33089=CARTESIAN_POINT('Ctrl Pts',(97.8936733262038,0.29629691456199,-1.57309019228634));
#33090=CARTESIAN_POINT('Ctrl Pts',(97.9022180891303,0.254965775138703,-1.57539236717464));
#33091=CARTESIAN_POINT('Ctrl Pts',(97.9089622223474,0.213319403591485,-1.57769454206294));
#33092=CARTESIAN_POINT('Ctrl Pts',(97.9138944051945,0.171527190352026,-1.57999671695124));
#33093=CARTESIAN_POINT('Ctrl Pts',(97.9205702975477,0.114959880210447,-1.58311279601985));
#33094=CARTESIAN_POINT('Ctrl Pts',(97.923944606945,0.0579954345134518,-1.58622887508846));
#33095=CARTESIAN_POINT('Ctrl Pts',(97.9239806575935,0.000924464996447671,
-1.58934495415707));
#33096=CARTESIAN_POINT('Origin',(96.460480949577,-8.32667268468867E-16,
1.18130019239114E-14));
#33097=CARTESIAN_POINT('',(97.9239808736879,0.000471303870065604,-2.16065504579701));
#33098=CARTESIAN_POINT('',(97.9239808936025,0.000404768228816884,-2.08934495411702));
#33099=CARTESIAN_POINT('',(97.923980949577,-1.01189432752408E-15,1.19922289829666E-14));
#33100=CARTESIAN_POINT('Ctrl Pts',(97.9239808736879,0.000471303870068238,
-2.16065504579701));
#33101=CARTESIAN_POINT('Ctrl Pts',(97.9239615958962,0.0603329949048461,
-2.15741638815146));
#33102=CARTESIAN_POINT('Ctrl Pts',(97.92026528758,0.120088518536624,-2.1541777305059));
#33103=CARTESIAN_POINT('Ctrl Pts',(97.912956108285,0.179299089055256,-2.15093907286035));
#33104=CARTESIAN_POINT('Ctrl Pts',(97.905627399874,0.238667862028564,-2.14769176196953));
#33105=CARTESIAN_POINT('Ctrl Pts',(97.8946666302688,0.297488396255375,-2.1444444510787));
#33106=CARTESIAN_POINT('Ctrl Pts',(97.8801887931385,0.355333489738872,-2.14119714018788));
#33107=CARTESIAN_POINT('Ctrl Pts',(97.8656522053234,0.413413317100202,-2.13793665179431));
#33108=CARTESIAN_POINT('Ctrl Pts',(97.8475701160377,0.470509414487508,-2.13467616340075));
#33109=CARTESIAN_POINT('Ctrl Pts',(97.8261072647801,0.526210050478789,-2.13141567500718));
#33110=CARTESIAN_POINT('Ctrl Pts',(97.8142621712294,0.556950572147068,-2.12961625005758));
#33111=CARTESIAN_POINT('Ctrl Pts',(97.801388201685,0.587266460099237,-2.12781682510797));
#33112=CARTESIAN_POINT('Ctrl Pts',(97.7875190028352,0.617091772109138,-2.12601740015837));
#33113=CARTESIAN_POINT('Ctrl Pts',(97.7643182169546,0.666984392818874,-2.1230072714973));
#33114=CARTESIAN_POINT('Ctrl Pts',(97.7382510539732,0.715671604914073,-2.11999714283623));
#33115=CARTESIAN_POINT('Ctrl Pts',(97.7094656361879,0.76280371171842,-2.11698701417517));
#33116=CARTESIAN_POINT('Ctrl Pts',(97.6807313782009,0.809852051488635,-2.11398223536089));
#33117=CARTESIAN_POINT('Ctrl Pts',(97.6492887258075,0.855350323806215,-2.11097745654661));
#33118=CARTESIAN_POINT('Ctrl Pts',(97.61533247712,0.898971745569159,-2.10797267773233));
#33119=CARTESIAN_POINT('Ctrl Pts',(97.5814098225148,0.942550011162192,-2.10497087164888));
#33120=CARTESIAN_POINT('Ctrl Pts',(97.5449788206278,0.984254689807881,-2.10196906556542));
#33121=CARTESIAN_POINT('Ctrl Pts',(97.5062774773565,1.02378800172905,-2.09896725948197));
#33122=CARTESIAN_POINT('Ctrl Pts',(97.4675991365583,1.0632978166895,-2.09596723754753));
#33123=CARTESIAN_POINT('Ctrl Pts',(97.4266534976736,1.10063844628959,-2.0929672156131));
#33124=CARTESIAN_POINT('Ctrl Pts',(97.3837172231288,1.13554701936915,-2.08996719367866));
#33125=CARTESIAN_POINT('Ctrl Pts',(97.3407895103367,1.17044863146824,-2.08696776996673));
#33126=CARTESIAN_POINT('Ctrl Pts',(97.2958723597416,1.20291881719933,-2.0839683462548));
#33127=CARTESIAN_POINT('Ctrl Pts',(97.2492757204877,1.2327347887457,-2.08096892254287));
#33128=CARTESIAN_POINT('Ctrl Pts',(97.202636242373,1.26257817175942,-2.07796674129527));
#33129=CARTESIAN_POINT('Ctrl Pts',(97.1543146365936,1.28976218020006,-2.07496456004767));
#33130=CARTESIAN_POINT('Ctrl Pts',(97.1046488094327,1.31410806950148,-2.07196237880007));
#33131=CARTESIAN_POINT('Ctrl Pts',(97.0549603754898,1.3384650405113,-2.0689588310262));
#33132=CARTESIAN_POINT('Ctrl Pts',(97.0039269879474,1.359981111644,-2.06595528325234));
#33133=CARTESIAN_POINT('Ctrl Pts',(96.9519070394269,1.37852553411781,-2.06295173547847));
#33134=CARTESIAN_POINT('Ctrl Pts',(96.8997889120081,1.39710495606818,-2.05994251901365));
#33135=CARTESIAN_POINT('Ctrl Pts',(96.8466810120016,1.41270137636166,-2.05693330254884));
#33136=CARTESIAN_POINT('Ctrl Pts',(96.7929562839649,1.42523415691025,-2.05392408608402));
#33137=CARTESIAN_POINT('Ctrl Pts',(96.7518546651787,1.43482224766962,-2.05162191215962));
#33138=CARTESIAN_POINT('Ctrl Pts',(96.710392342561,1.44261826540517,-2.04931973823521));
#33139=CARTESIAN_POINT('Ctrl Pts',(96.6687383655387,1.44860660591374,-2.04701756431081));
#33140=CARTESIAN_POINT('Ctrl Pts',(96.6142751346129,1.45643645543345,-2.04400743564988));
#33141=CARTESIAN_POINT('Ctrl Pts',(96.559255288647,1.46120700645385,-2.04099730698895));
#33142=CARTESIAN_POINT('Ctrl Pts',(96.5040526414606,1.46285124249406,-2.03798717832802));
#33143=CARTESIAN_POINT('Ctrl Pts',(96.4489481049327,1.46449255626352,-2.03498239951388));
#33144=CARTESIAN_POINT('Ctrl Pts',(96.3936619355416,1.463018566056,-2.03197762069975));
#33145=CARTESIAN_POINT('Ctrl Pts',(96.3385742598537,1.45841386752894,-2.02897284188562));
#33146=CARTESIAN_POINT('Ctrl Pts',(96.2835410842944,1.45381372458819,-2.02597103580231));
#33147=CARTESIAN_POINT('Ctrl Pts',(96.228706537119,1.4460890527391,-2.02296922971901));
#33148=CARTESIAN_POINT('Ctrl Pts',(96.1744500623932,1.43527648262515,-2.0199674236357));
#33149=CARTESIAN_POINT('Ctrl Pts',(96.1202258354654,1.42447033905438,-2.01696740170142));
#33150=CARTESIAN_POINT('Ctrl Pts',(96.066579516882,1.41058003795132,-2.01396737976714));
#33151=CARTESIAN_POINT('Ctrl Pts',(96.0138824355779,1.39369365977383,-2.01096735783286));
#33152=CARTESIAN_POINT('Ctrl Pts',(95.9611958623903,1.37681064884223,-2.00796793412108));
#33153=CARTESIAN_POINT('Ctrl Pts',(95.9094586532168,1.35693290838663,-2.00496851040931));
#33154=CARTESIAN_POINT('Ctrl Pts',(95.8590267538452,1.33419829876846,-2.00196908669753));
#33155=CARTESIAN_POINT('Ctrl Pts',(95.8085484896468,1.31144278796962,-1.99896690545009));
#33156=CARTESIAN_POINT('Ctrl Pts',(95.759378415272,1.28582537815373,-1.99596472420265));
#33157=CARTESIAN_POINT('Ctrl Pts',(95.7118508647721,1.25753140959782,-1.9929625429552));
#33158=CARTESIAN_POINT('Ctrl Pts',(95.6643016807864,1.22922456225549,-1.9899589951815));
#33159=CARTESIAN_POINT('Ctrl Pts',(95.6183969495375,1.19823902353665,-1.9869554474078));
#33160=CARTESIAN_POINT('Ctrl Pts',(95.5744420009703,1.16480351628584,-1.98395189963409));
#33161=CARTESIAN_POINT('Ctrl Pts',(95.5304040948349,1.13130490514201,-1.98094268316944));
#33162=CARTESIAN_POINT('Ctrl Pts',(95.4883237250118,1.09534743242324,-1.97793346670479));
#33163=CARTESIAN_POINT('Ctrl Pts',(95.4484722035119,1.05719938889871,-1.97492425024013));
#33164=CARTESIAN_POINT('Ctrl Pts',(95.417984156284,1.02801457213745,-1.9726220763145));
#33165=CARTESIAN_POINT('Ctrl Pts',(95.3887999312872,0.997548474542972,-1.97031990238887));
#33166=CARTESIAN_POINT('Ctrl Pts',(95.3610249654051,0.96593415348494,-1.96801772846325));
#33167=CARTESIAN_POINT('Ctrl Pts',(95.3247087601124,0.924597930837241,-1.96500759980071));
#33168=CARTESIAN_POINT('Ctrl Pts',(95.2906506673778,0.881123939421362,-1.96199747113817));
#33169=CARTESIAN_POINT('Ctrl Pts',(95.2591110657112,0.83578864082984,-1.95898734247562));
#33170=CARTESIAN_POINT('Ctrl Pts',(95.2276275188036,0.790533915837978,-1.95598256365988));
#33171=CARTESIAN_POINT('Ctrl Pts',(95.1986538793383,0.743424878570124,-1.95297778484413));
#33172=CARTESIAN_POINT('Ctrl Pts',(95.1724107485305,0.694771478384037,-1.94997300602838));
#33173=CARTESIAN_POINT('Ctrl Pts',(95.1461935809528,0.646166212676844,-1.94697119994346));
#33174=CARTESIAN_POINT('Ctrl Pts',(95.1227018201985,0.596020073256171,-1.94396939385854));
#33175=CARTESIAN_POINT('Ctrl Pts',(95.1021121138656,0.544670869579148,-1.94096758777362));
#33176=CARTESIAN_POINT('Ctrl Pts',(95.0815346452002,0.49335218573886,-1.93796756583772));
#33177=CARTESIAN_POINT('Ctrl Pts',(95.0638560083256,0.440832344121254,-1.93496754390182));
#33178=CARTESIAN_POINT('Ctrl Pts',(95.0492053261603,0.387470469519647,-1.93196752196592));
#33179=CARTESIAN_POINT('Ctrl Pts',(95.0345575654296,0.334119235598484,-1.92896809825254));
#33180=CARTESIAN_POINT('Ctrl Pts',(95.0229367000457,0.279926811133344,-1.92596867453915));
#33181=CARTESIAN_POINT('Ctrl Pts',(95.0144217556271,0.225266636661854,-1.92296925082577));
#33182=CARTESIAN_POINT('Ctrl Pts',(95.0058989829504,0.170556210077254,-1.91996706957673));
#33183=CARTESIAN_POINT('Ctrl Pts',(95.0004879175099,0.115377697289208,-1.9169648883277));
#33184=CARTESIAN_POINT('Ctrl Pts',(94.9982160106488,0.0601123812637398,
-1.91396270707866));
#33185=CARTESIAN_POINT('Ctrl Pts',(94.995943069666,0.00482190969338436,
-1.91095915930338));
#33186=CARTESIAN_POINT('Ctrl Pts',(94.9968121273256,-0.0505549149049093,
-1.90795561152809));
#33187=CARTESIAN_POINT('Ctrl Pts',(95.0007984531729,-0.105637397220232,
-1.9049520637528));
#33188=CARTESIAN_POINT('Ctrl Pts',(95.0047923025393,-0.160823838450338,
-1.9019428472866));
#33189=CARTESIAN_POINT('Ctrl Pts',(95.0119151048094,-0.215714302647041,
-1.8989336308204));
#33190=CARTESIAN_POINT('Ctrl Pts',(95.0220904030614,-0.269934965675806,
-1.89592441435419));
#33191=CARTESIAN_POINT('Ctrl Pts',(95.0298749232028,-0.311415994828604,
-1.89362224044135));
#33192=CARTESIAN_POINT('Ctrl Pts',(95.0394449538539,-0.352505124594627,
-1.89132006652851));
#33193=CARTESIAN_POINT('Ctrl Pts',(95.0507466661871,-0.393041346724551,
-1.88901789261568));
#33194=CARTESIAN_POINT('Ctrl Pts',(95.0655238331106,-0.446043095769737,
-1.88600776395604));
#33195=CARTESIAN_POINT('Ctrl Pts',(95.0833252627432,-0.49832168324049,-1.8829976352964));
#33196=CARTESIAN_POINT('Ctrl Pts',(95.1040616808569,-0.549507977598812,
-1.87998750663677));
#33197=CARTESIAN_POINT('Ctrl Pts',(95.1247612445128,-0.600603299489543,
-1.87698272782391));
#33198=CARTESIAN_POINT('Ctrl Pts',(95.1483852481736,-0.65060969529963,-1.87397794901105));
#33199=CARTESIAN_POINT('Ctrl Pts',(95.1747946365492,-0.699173050462454,
-1.87097317019819));
#33200=CARTESIAN_POINT('Ctrl Pts',(95.2011778972104,-0.747688360231163,
-1.86797136411614));
#33201=CARTESIAN_POINT('Ctrl Pts',(95.2303408326612,-0.794762995788238,
-1.8649695580341));
#33202=CARTESIAN_POINT('Ctrl Pts',(95.2620970379445,-0.840064432255227,
-1.86196775195205));
#33203=CARTESIAN_POINT('Ctrl Pts',(95.2938343686567,-0.885338943427676,
-1.85896773001902));
#33204=CARTESIAN_POINT('Ctrl Pts',(95.3281616116412,-0.928841912857284,
-1.85596770808598));
#33205=CARTESIAN_POINT('Ctrl Pts',(95.3648485424746,-0.970268972247914,
-1.85296768615294));
#33206=CARTESIAN_POINT('Ctrl Pts',(95.4015281577124,-1.0116877708327,-1.84996826244239));
#33207=CARTESIAN_POINT('Ctrl Pts',(95.4405661764015,-1.0510310863171,-1.84696883873185));
#33208=CARTESIAN_POINT('Ctrl Pts',(95.4816930113293,-1.08802868617554,-1.8439694150213));
#33209=CARTESIAN_POINT('Ctrl Pts',(95.5228576564256,-1.12506029996881,-1.84096723377505));
#33210=CARTESIAN_POINT('Ctrl Pts',(95.5661145609304,-1.15974153567516,-1.8379650525288));
#33211=CARTESIAN_POINT('Ctrl Pts',(95.611159389405,-1.19184107054045,-1.83496287128255));
#33212=CARTESIAN_POINT('Ctrl Pts',(95.6562247212858,-1.22395521640164,-1.83195932351002));
#33213=CARTESIAN_POINT('Ctrl Pts',(95.7030791518731,-1.25348503679986,-1.82895577573749));
#33214=CARTESIAN_POINT('Ctrl Pts',(95.7513903259753,-1.28024323373342,-1.82595222796496));
#33215=CARTESIAN_POINT('Ctrl Pts',(95.7997926792891,-1.30705193226092,-1.82294301150144));
#33216=CARTESIAN_POINT('Ctrl Pts',(95.8496567914534,-1.33107832783827,-1.81993379503791));
#33217=CARTESIAN_POINT('Ctrl Pts',(95.9006277989334,-1.35218219915604,-1.81692457857439));
#33218=CARTESIAN_POINT('Ctrl Pts',(95.9396227088394,-1.36832752571304,-1.81462240463897));
#33219=CARTESIAN_POINT('Ctrl Pts',(95.9792649884082,-1.38276330684499,-1.81232023070354));
#33220=CARTESIAN_POINT('Ctrl Pts',(96.0193903770325,-1.39544665136734,-1.81001805676812));
#33221=CARTESIAN_POINT('Ctrl Pts',(96.071854954282,-1.41203032398187,-1.80700792810848));
#33222=CARTESIAN_POINT('Ctrl Pts',(96.1253663095231,-1.42568596254127,-1.80399779944884));
#33223=CARTESIAN_POINT('Ctrl Pts',(96.1795665060706,-1.43628664459066,-1.8009876707892));
#33224=CARTESIAN_POINT('Ctrl Pts',(96.2336703735963,-1.44686848624097,-1.79798289197639));
#33225=CARTESIAN_POINT('Ctrl Pts',(96.2884601387621,-1.45440604574688,-1.79497811316358));
#33226=CARTESIAN_POINT('Ctrl Pts',(96.3435632418238,-1.45882229884717,-1.79197333435077));
#33227=CARTESIAN_POINT('Ctrl Pts',(96.3986118294937,-1.46323418279665,-1.78897152826881));
#33228=CARTESIAN_POINT('Ctrl Pts',(96.4539726171324,-1.46453083556758,-1.78596972218684));
#33229=CARTESIAN_POINT('Ctrl Pts',(96.509265255268,-1.46268668603985,-1.78296791610488));
#33230=CARTESIAN_POINT('Ctrl Pts',(96.5645250297528,-1.46084363259812,-1.77996789417195));
#33231=CARTESIAN_POINT('Ctrl Pts',(96.6197162082497,-1.45586349447287,-1.77696787223902));
#33232=CARTESIAN_POINT('Ctrl Pts',(96.6744580803983,-1.44777278517228,-1.77396785030609));
#33233=CARTESIAN_POINT('Ctrl Pts',(96.7291890366864,-1.43968368920807,-1.77096842659568));
#33234=CARTESIAN_POINT('Ctrl Pts',(96.7834703424089,-1.42848533106372,-1.76796900288527));
#33235=CARTESIAN_POINT('Ctrl Pts',(96.8369283691581,-1.41425584329382,-1.76496957917486));
#33236=CARTESIAN_POINT('Ctrl Pts',(96.8904355428201,-1.40001327357093,-1.7619673979288));
#33237=CARTESIAN_POINT('Ctrl Pts',(96.9431174139069,-1.38273414292471,-1.75896521668273));
#33238=CARTESIAN_POINT('Ctrl Pts',(96.9946139556971,-1.36254694663086,-1.75596303543666));
#33239=CARTESIAN_POINT('Ctrl Pts',(97.04613393757,-1.34235056157342,-1.75295948766434));
#33240=CARTESIAN_POINT('Ctrl Pts',(97.0964670338264,-1.31924369291165,-1.74995593989202));
#33241=CARTESIAN_POINT('Ctrl Pts',(97.1452747797773,-1.29340235816995,-1.74695239211969));
#33242=CARTESIAN_POINT('Ctrl Pts',(97.1941746421349,-1.26751225225774,-1.74394317565641));
#33243=CARTESIAN_POINT('Ctrl Pts',(97.2415429501902,-1.23887764455822,-1.74093395919313));
#33244=CARTESIAN_POINT('Ctrl Pts',(97.2870683687802,-1.20771912645907,-1.73792474272985));
#33245=CARTESIAN_POINT('Ctrl Pts',(97.3218971800013,-1.1838815829852,-1.73562256879342));
#33246=CARTESIAN_POINT('Ctrl Pts',(97.3556479211617,-1.15856776108528,-1.73332039485699));
#33247=CARTESIAN_POINT('Ctrl Pts',(97.3881949183888,-1.13189179786385,-1.73101822092056));
#33248=CARTESIAN_POINT('Ctrl Pts',(97.4301821350619,-1.09747850191746,-1.72804830405806));
#33249=CARTESIAN_POINT('Ctrl Pts',(97.4703512820927,-1.06064408240767,-1.72507838719557));
#33250=CARTESIAN_POINT('Ctrl Pts',(97.5084048713763,-1.02161034847966,-1.72210847033308));
#33251=CARTESIAN_POINT('Ctrl Pts',(97.5464054283538,-0.982631012808632,
-1.71914269241105));
#33252=CARTESIAN_POINT('Ctrl Pts',(97.582295884973,-0.941458811592886,-1.71617691448902));
#33253=CARTESIAN_POINT('Ctrl Pts',(97.6158117674441,-0.898355693078501,
-1.71321113656699));
#33254=CARTESIAN_POINT('Ctrl Pts',(97.6492950240057,-0.855294533132349,
-1.7102482456703));
#33255=CARTESIAN_POINT('Ctrl Pts',(97.680407949961,-0.810306603147918,-1.7072853547736));
#33256=CARTESIAN_POINT('Ctrl Pts',(97.7089246749727,-0.763688755004287,
-1.70432246387691));
#33257=CARTESIAN_POINT('Ctrl Pts',(97.7374256171912,-0.71709670785511,-1.7013612128142));
#33258=CARTESIAN_POINT('Ctrl Pts',(97.763332922242,-0.668876992338361,-1.69839996175149));
#33259=CARTESIAN_POINT('Ctrl Pts',(97.7864640610347,-0.619355340760716,
-1.69543871068878));
#33260=CARTESIAN_POINT('Ctrl Pts',(97.8096066161747,-0.569809247828204,
-1.69247599810397));
#33261=CARTESIAN_POINT('Ctrl Pts',(97.8299700258084,-0.518960422619599,
-1.68951328551917));
#33262=CARTESIAN_POINT('Ctrl Pts',(97.8474186374867,-0.467157467943752,
-1.68655057293436));
#33263=CARTESIAN_POINT('Ctrl Pts',(97.8648705622482,-0.41534467709887,-1.68358729779975));
#33264=CARTESIAN_POINT('Ctrl Pts',(97.8794064323308,-0.362577917863619,
-1.68062402266515));
#33265=CARTESIAN_POINT('Ctrl Pts',(97.8909405843745,-0.30922076776162,-1.67766074753054));
#33266=CARTESIAN_POINT('Ctrl Pts',(97.9024939141118,-0.255774901378304,
-1.67469254539458));
#33267=CARTESIAN_POINT('Ctrl Pts',(97.9110354636563,-0.20173722036308,-1.67172434325863));
#33268=CARTESIAN_POINT('Ctrl Pts',(97.9165310580184,-0.147479936628166,
-1.66875614112267));
#33269=CARTESIAN_POINT('Ctrl Pts',(97.9215307549522,-0.0981185832863154,
-1.66605577604102));
#33270=CARTESIAN_POINT('Ctrl Pts',(97.9240100444567,-0.0485758494338648,
-1.66335541095937));
#33271=CARTESIAN_POINT('Ctrl Pts',(97.9239806916945,0.000868804938497931,
-1.66065504587772));
#33272=CARTESIAN_POINT('Ctrl Pts',(97.9239806575939,0.000924464373924056,
-1.58934495419106));
#33273=CARTESIAN_POINT('Ctrl Pts',(97.9240149768248,-0.0534055734513773,
-1.59231137819076));
#33274=CARTESIAN_POINT('Ctrl Pts',(97.921019683887,-0.107852860549419,-1.59527780219046));
#33275=CARTESIAN_POINT('Ctrl Pts',(97.9149819784938,-0.162046310911714,
-1.59824422619017));
#33276=CARTESIAN_POINT('Ctrl Pts',(97.9089514956399,-0.216174932948707,
-1.60120710163744));
#33277=CARTESIAN_POINT('Ctrl Pts',(97.8998858605244,-0.270049782617476,
-1.60416997708471));
#33278=CARTESIAN_POINT('Ctrl Pts',(97.8878242733974,-0.323300612349155,
-1.60713285253198));
#33279=CARTESIAN_POINT('Ctrl Pts',(97.8757720383231,-0.376510153603537,
-1.61009343068893));
#33280=CARTESIAN_POINT('Ctrl Pts',(97.8607285693229,-0.42909610405418,-1.61305400884588));
#33281=CARTESIAN_POINT('Ctrl Pts',(97.8427844382153,-0.480696697823331,
-1.61601458700284));
#33282=CARTESIAN_POINT('Ctrl Pts',(97.8248466701853,-0.532278993767196,
-1.61897411532416));
#33283=CARTESIAN_POINT('Ctrl Pts',(97.804010457373,-0.582876112447669,-1.62193364364548));
#33284=CARTESIAN_POINT('Ctrl Pts',(97.7804159654134,-0.632142233970416,
-1.6248931719668));
#33285=CARTESIAN_POINT('Ctrl Pts',(97.7568030420099,-0.681446840990178,
-1.62785501219974));
#33286=CARTESIAN_POINT('Ctrl Pts',(97.7304277661814,-0.729417880164871,
-1.63081685243267));
#33287=CARTESIAN_POINT('Ctrl Pts',(97.7014774289467,-0.775731904843368,
-1.6337786926656));
#33288=CARTESIAN_POINT('Ctrl Pts',(97.6725165864269,-0.822062735614098,
-1.63674160766931));
#33289=CARTESIAN_POINT('Ctrl Pts',(97.640979133725,-0.866734907890897,-1.63970452267302));
#33290=CARTESIAN_POINT('Ctrl Pts',(97.6070951758126,-0.909454818115819,
-1.64266743767673));
#33291=CARTESIAN_POINT('Ctrl Pts',(97.5731476039496,-0.952254930962463,
-1.64563591527525));
#33292=CARTESIAN_POINT('Ctrl Pts',(97.5368450900147,-0.993095053534944,
-1.64860439287378));
#33293=CARTESIAN_POINT('Ctrl Pts',(97.4984565286632,-1.03171650525743,-1.6515728704723));
#33294=CARTESIAN_POINT('Ctrl Pts',(97.4664553344499,-1.06391183985348,-1.6540474312478));
#33295=CARTESIAN_POINT('Ctrl Pts',(97.4330053213571,-1.09456596514532,-1.6565219920233));
#33296=CARTESIAN_POINT('Ctrl Pts',(97.3982789955736,-1.12355110027316,-1.65899655279881));
#33297=CARTESIAN_POINT('Ctrl Pts',(97.3560368694842,-1.1588094728525,-1.66200668145296));
#33298=CARTESIAN_POINT('Ctrl Pts',(97.3117148111456,-1.19175635038155,-1.66501681010711));
#33299=CARTESIAN_POINT('Ctrl Pts',(97.2655957836383,-1.2221384348651,-1.66802693876127));
#33300=CARTESIAN_POINT('Ctrl Pts',(97.2195587226361,-1.25246652182484,-1.67103171756874));
#33301=CARTESIAN_POINT('Ctrl Pts',(97.1717314678766,-1.2802385736523,-1.67403649637622));
#33302=CARTESIAN_POINT('Ctrl Pts',(97.1224294527346,-1.30524190446346,-1.6770412751837));
#33303=CARTESIAN_POINT('Ctrl Pts',(97.0731762137674,-1.33022049862179,-1.68004308126043));
#33304=CARTESIAN_POINT('Ctrl Pts',(97.0224515733797,-1.35243556027356,-1.68304488733716));
#33305=CARTESIAN_POINT('Ctrl Pts',(96.970597703677,-1.37171904819699,-1.6860466934139));
#33306=CARTESIAN_POINT('Ctrl Pts',(96.9187746537621,-1.39099107481565,-1.6890467153417));
#33307=CARTESIAN_POINT('Ctrl Pts',(96.8658241988373,-1.40733479755615,-1.6920467372695));
#33308=CARTESIAN_POINT('Ctrl Pts',(96.8121086166901,-1.42063022413315,-1.69504675919731));
#33309=CARTESIAN_POINT('Ctrl Pts',(96.7584037457529,-1.43392299952217,-1.6980461829027));
#33310=CARTESIAN_POINT('Ctrl Pts',(96.7039345629515,-1.44416855909227,-1.7010456066081));
#33311=CARTESIAN_POINT('Ctrl Pts',(96.6490763892943,-1.45129735413451,-1.7040450303135));
#33312=CARTESIAN_POINT('Ctrl Pts',(96.5941677814879,-1.4584327030718,-1.70704721155478));
#33313=CARTESIAN_POINT('Ctrl Pts',(96.5388699931839,-1.46244549455437,-1.71004939279606));
#33314=CARTESIAN_POINT('Ctrl Pts',(96.4835648799873,-1.46331793611533,-1.71305157403735));
#33315=CARTESIAN_POINT('Ctrl Pts',(96.4282345931287,-1.46419077479235,-1.716055121805));
#33316=CARTESIAN_POINT('Ctrl Pts',(96.3728975033235,-1.46192043578891,-1.71905866957266));
#33317=CARTESIAN_POINT('Ctrl Pts',(96.3179335580145,-1.45654127684688,-1.72206221734031));
#33318=CARTESIAN_POINT('Ctrl Pts',(96.2628658775037,-1.45115196564713,-1.72507143379917));
#33319=CARTESIAN_POINT('Ctrl Pts',(96.2081732714503,-1.44264219490996,-1.72808065025804));
#33320=CARTESIAN_POINT('Ctrl Pts',(96.1542275091506,-1.43109785836854,-1.7310898667169));
#33321=CARTESIAN_POINT('Ctrl Pts',(96.1129567890792,-1.42226596756747,-1.73339204069339));
#33322=CARTESIAN_POINT('Ctrl Pts',(96.0721230332597,-1.41165905690264,-1.73569421466988));
#33323=CARTESIAN_POINT('Ctrl Pts',(96.031885835997,-1.39933501300273,-1.73799638864636));
#33324=CARTESIAN_POINT('Ctrl Pts',(95.9792750683316,-1.38322113195669,-1.74100651729453));
#33325=CARTESIAN_POINT('Ctrl Pts',(95.9274637731497,-1.36410225986706,-1.7440166459427));
#33326=CARTESIAN_POINT('Ctrl Pts',(95.8768187042549,-1.34207698489527,-1.74702677459087));
#33327=CARTESIAN_POINT('Ctrl Pts',(95.826263645925,-1.3200908550463,-1.75003155339184));
#33328=CARTESIAN_POINT('Ctrl Pts',(95.7768711809521,-1.29520878219504,-1.75303633219281));
#33329=CARTESIAN_POINT('Ctrl Pts',(95.7289917910453,-1.26757873954662,-1.75604111099377));
#33330=CARTESIAN_POINT('Ctrl Pts',(95.6811597698665,-1.23997603225015,-1.75904291706368));
#33331=CARTESIAN_POINT('Ctrl Pts',(95.6348383135608,-1.2096310033596,-1.76204472313358));
#33332=CARTESIAN_POINT('Ctrl Pts',(95.5903551226692,-1.176738414155,-1.76504652920349));
#33333=CARTESIAN_POINT('Ctrl Pts',(95.5458983707444,-1.1438653749435,-1.76804655112416));
#33334=CARTESIAN_POINT('Ctrl Pts',(95.5032781424389,-1.10844808995638,-1.77104657304482));
#33335=CARTESIAN_POINT('Ctrl Pts',(95.4627928816826,-1.07072441327407,-1.77404659496549));
#33336=CARTESIAN_POINT('Ctrl Pts',(95.4223156939345,-1.03300825892333,-1.77704601866346));
#33337=CARTESIAN_POINT('Ctrl Pts',(95.3839730144261,-0.992986986058309,
-1.78004544236143));
#33338=CARTESIAN_POINT('Ctrl Pts',(95.348028165999,-0.950936934980199,-1.7830448660594));
#33339=CARTESIAN_POINT('Ctrl Pts',(95.312050271492,-0.908848224972956,-1.78604704729286));
#33340=CARTESIAN_POINT('Ctrl Pts',(95.2784749561784,-0.864727412690527,
-1.78904922852632));
#33341=CARTESIAN_POINT('Ctrl Pts',(95.2475257661328,-0.818884590742626,
-1.79205140975978));
#33342=CARTESIAN_POINT('Ctrl Pts',(95.216562488704,-0.773020902161633,-1.79505495751938));
#33343=CARTESIAN_POINT('Ctrl Pts',(95.1882279900561,-0.72543409598279,-1.79805850527897));
#33344=CARTESIAN_POINT('Ctrl Pts',(95.162701096448,-0.676461161348169,-1.80106205303857));
#33345=CARTESIAN_POINT('Ctrl Pts',(95.1371260251242,-0.627395798541108,
-1.80407126948909));
#33346=CARTESIAN_POINT('Ctrl Pts',(95.1143693618401,-0.576939563841812,
-1.80708048593961));
#33347=CARTESIAN_POINT('Ctrl Pts',(95.0945623015679,-0.525450756038149,
-1.81008970239013));
#33348=CARTESIAN_POINT('Ctrl Pts',(95.0794090878959,-0.486059705794032,
-1.81239187642473));
#33349=CARTESIAN_POINT('Ctrl Pts',(95.0659812567716,-0.446064760948663,
-1.81469405045933));
#33350=CARTESIAN_POINT('Ctrl Pts',(95.054317528291,-0.405631215067501,-1.81699622449392));
#33351=CARTESIAN_POINT('Ctrl Pts',(95.0390670203038,-0.352763719443278,
-1.82000635316426));
#33352=CARTESIAN_POINT('Ctrl Pts',(95.0267701018704,-0.298923888233537,
-1.8230164818346));
#33353=CARTESIAN_POINT('Ctrl Pts',(95.0175445955868,-0.24447275581039,-1.82602661050493));
#33354=CARTESIAN_POINT('Ctrl Pts',(95.0083354856268,-0.1901183983884,-1.82903138932867));
#33355=CARTESIAN_POINT('Ctrl Pts',(95.002187042368,-0.135155412313231,-1.83203616815241));
#33356=CARTESIAN_POINT('Ctrl Pts',(94.9991668360948,-0.0799581874332898,
-1.83504094697615));
#33357=CARTESIAN_POINT('Ctrl Pts',(94.9961496178151,-0.0248155710604053,
-1.83804275306917));
#33358=CARTESIAN_POINT('Ctrl Pts',(94.9962545344399,0.0305603003156849,
-1.8410445591622));
#33359=CARTESIAN_POINT('Ctrl Pts',(94.9994975224402,0.0857885518684098,
-1.84404636525523));
#33360=CARTESIAN_POINT('Ctrl Pts',(95.0027385829432,0.140983978041141,-1.84704638719933));
#33361=CARTESIAN_POINT('Ctrl Pts',(95.0091139870974,0.19603143213972,-1.85004640914343));
#33362=CARTESIAN_POINT('Ctrl Pts',(95.0185875942964,0.250550996800594,-1.85304643108753));
#33363=CARTESIAN_POINT('Ctrl Pts',(95.0280593124013,0.305059689932115,-1.8560458548092));
#33364=CARTESIAN_POINT('Ctrl Pts',(95.0406279162633,0.359040182648933,-1.85904527853087));
#33365=CARTESIAN_POINT('Ctrl Pts',(95.056205842006,0.41212094372446,-1.86204470225253));
#33366=CARTESIAN_POINT('Ctrl Pts',(95.0717980893953,0.4652505048723,-1.86504688350992));
#33367=CARTESIAN_POINT('Ctrl Pts',(95.090405037007,0.517478173961618,-1.8680490647673));
#33368=CARTESIAN_POINT('Ctrl Pts',(95.1118891186283,0.568447291750489,-1.87105124602469));
#33369=CARTESIAN_POINT('Ctrl Pts',(95.133382979327,0.619439609550978,-1.87405479380837));
#33370=CARTESIAN_POINT('Ctrl Pts',(95.1577563518279,0.669171759032316,-1.87705834159206));
#33371=CARTESIAN_POINT('Ctrl Pts',(95.184824708617,0.71730983884226,-1.88006188937574));
#33372=CARTESIAN_POINT('Ctrl Pts',(95.2119441523736,0.765538771175316,-1.88307110585032));
#33373=CARTESIAN_POINT('Ctrl Pts',(95.2417684558908,0.812167177828806,-1.88608032232489));
#33374=CARTESIAN_POINT('Ctrl Pts',(95.274069218705,0.85688940642843,-1.88908953879947));
#33375=CARTESIAN_POINT('Ctrl Pts',(95.2987806251552,0.891103742933179,-1.89139171264681));
#33376=CARTESIAN_POINT('Ctrl Pts',(95.3249405515936,0.924202990934809,-1.89369388649415));
#33377=CARTESIAN_POINT('Ctrl Pts',(95.3524317167492,0.956064405586572,-1.89599606034149));
#33378=CARTESIAN_POINT('Ctrl Pts',(95.3883768493095,0.997723708374811,-1.89900618900105));
#33379=CARTESIAN_POINT('Ctrl Pts',(95.4267501688151,1.03744058079069,-1.90201631766061));
#33380=CARTESIAN_POINT('Ctrl Pts',(95.4673136770704,1.07491907547582,-1.90502644632017));
#33381=CARTESIAN_POINT('Ctrl Pts',(95.5078050925418,1.11233096031552,-1.90803122513294));
#33382=CARTESIAN_POINT('Ctrl Pts',(95.5504785871506,1.14751200675065,-1.9110360039457));
#33383=CARTESIAN_POINT('Ctrl Pts',(95.5950575194639,1.18020105770639,-1.91404078275847));
#33384=CARTESIAN_POINT('Ctrl Pts',(95.6395923483092,1.21285776826188,-1.91704258884041));
#33385=CARTESIAN_POINT('Ctrl Pts',(95.6860284567455,1.24302705644994,-1.92004439492235));
#33386=CARTESIAN_POINT('Ctrl Pts',(95.7340555594834,1.2704874665369,-1.92304620100429));
#33387=CARTESIAN_POINT('Ctrl Pts',(95.7820541169036,1.29793155529517,-1.92604622293721));
#33388=CARTESIAN_POINT('Ctrl Pts',(95.8316413367919,1.32266969555349,-1.92904624487013));
#33389=CARTESIAN_POINT('Ctrl Pts',(95.8824792810488,1.34452457068608,-1.93204626680305));
#33390=CARTESIAN_POINT('Ctrl Pts',(95.9333070879124,1.36637508782451,-1.93504569051347));
#33391=CARTESIAN_POINT('Ctrl Pts',(95.9853846389323,1.38534327318461,-1.93804511422389));
#33392=CARTESIAN_POINT('Ctrl Pts',(96.0383529221512,1.40129946066557,-1.94104453793431));
#33393=CARTESIAN_POINT('Ctrl Pts',(96.0913699020352,1.41727031754997,-1.94404671918042));
#33394=CARTESIAN_POINT('Ctrl Pts',(96.1452787434154,1.43022349160589,-1.94704890042653));
#33395=CARTESIAN_POINT('Ctrl Pts',(96.1997055689419,1.44007932102875,-1.95005108167264));
#33396=CARTESIAN_POINT('Ctrl Pts',(96.2541571683514,1.44993963660641,-1.95305462944502));
#33397=CARTESIAN_POINT('Ctrl Pts',(96.3091266968271,1.45669973255316,-1.9560581772174));
#33398=CARTESIAN_POINT('Ctrl Pts',(96.3642336778932,1.46033171323964,-1.95906172498978));
#33399=CARTESIAN_POINT('Ctrl Pts',(96.4194446641128,1.46397054867848,-1.96207094145314));
#33400=CARTESIAN_POINT('Ctrl Pts',(96.4747930917616,1.46446947034545,-1.96508015791651));
#33401=CARTESIAN_POINT('Ctrl Pts',(96.5298981716358,1.46185276251805,-1.96808937437987));
#33402=CARTESIAN_POINT('Ctrl Pts',(96.5720558163894,1.45985087377633,-1.97039154831627));
#33403=CARTESIAN_POINT('Ctrl Pts',(96.6140710101391,1.45602653043774,-1.97269372225266));
#33404=CARTESIAN_POINT('Ctrl Pts',(96.6557768687262,1.4504108914248,-1.97499589618905));
#33405=CARTESIAN_POINT('Ctrl Pts',(96.710307935311,1.44306835502092,-1.97800602484887));
#33406=CARTESIAN_POINT('Ctrl Pts',(96.7645389159977,1.43263081037028,-1.98101615350868));
#33407=CARTESIAN_POINT('Ctrl Pts',(96.8180919056289,1.41913588289201,-1.9840262821685));
#33408=CARTESIAN_POINT('Ctrl Pts',(96.8715497165069,1.40566493970255,-1.98703106098147));
#33409=CARTESIAN_POINT('Ctrl Pts',(96.9243314196578,1.38914752516233,-1.99003583979444));
#33410=CARTESIAN_POINT('Ctrl Pts',(96.9760671332099,1.36967263871585,-1.99304061860741));
#33411=CARTESIAN_POINT('Ctrl Pts',(97.0277516628442,1.35021701944321,-1.99604242468953));
#33412=CARTESIAN_POINT('Ctrl Pts',(97.0783917610071,1.32780990952682,-1.99904423077165));
#33413=CARTESIAN_POINT('Ctrl Pts',(97.1276324138976,1.30259017870354,-2.00204603685377));
#33414=CARTESIAN_POINT('Ctrl Pts',(97.1768438001859,1.27738543744239,-2.00504605878684));
#33415=CARTESIAN_POINT('Ctrl Pts',(97.224656920717,1.24937162897035,-2.00804608071991));
#33416=CARTESIAN_POINT('Ctrl Pts',(97.2707386199934,1.21873490043214,-2.01104610265298));
#33417=CARTESIAN_POINT('Ctrl Pts',(97.3168111303002,1.18810428104301,-2.01404552636353));
#33418=CARTESIAN_POINT('Ctrl Pts',(97.3611524654717,1.15485207251944,-2.01704495007407));
#33419=CARTESIAN_POINT('Ctrl Pts',(97.4034578639348,1.11920810798898,-2.02004437378461));
#33420=CARTESIAN_POINT('Ctrl Pts',(97.4458021560839,1.08353137399608,-2.0230465550308));
#33421=CARTESIAN_POINT('Ctrl Pts',(97.48610636727,1.04545883194557,-2.02604873627698));
#33422=CARTESIAN_POINT('Ctrl Pts',(97.5240994934715,1.00526008728279,-2.02905091752317));
#33423=CARTESIAN_POINT('Ctrl Pts',(97.5621099133003,0.965043045044023,-2.0320544652956));
#33424=CARTESIAN_POINT('Ctrl Pts',(97.5978068101609,0.922698275436627,-2.03505801306803));
#33425=CARTESIAN_POINT('Ctrl Pts',(97.6309589298598,0.878529195686235,-2.03806156084045));
#33426=CARTESIAN_POINT('Ctrl Pts',(97.6641736186053,0.834276754231234,-2.04107077730382));
#33427=CARTESIAN_POINT('Ctrl Pts',(97.69483364252,0.78819356532067,-2.04407999376719));
#33428=CARTESIAN_POINT('Ctrl Pts',(97.7227512786132,0.740611818994866,-2.04708921023056));
#33429=CARTESIAN_POINT('Ctrl Pts',(97.7441094145043,0.704209832789047,-2.04939138416591));
#33430=CARTESIAN_POINT('Ctrl Pts',(97.7638633609549,0.66693137109563,-2.05169355810126));
#33431=CARTESIAN_POINT('Ctrl Pts',(97.781948029552,0.628933229001592,-2.05399573203661));
#33432=CARTESIAN_POINT('Ctrl Pts',(97.8074222819931,0.575408650500181,-2.0572385982068));
#33433=CARTESIAN_POINT('Ctrl Pts',(97.8296770995285,0.520258080670813,-2.06048146437699));
#33434=CARTESIAN_POINT('Ctrl Pts',(97.8485205066686,0.463873299456797,-2.06372433054717));
#33435=CARTESIAN_POINT('Ctrl Pts',(97.8673150132779,0.407634842403311,-2.06695878115451));
#33436=CARTESIAN_POINT('Ctrl Pts',(97.8827155902678,0.350168916233823,-2.07019323176185));
#33437=CARTESIAN_POINT('Ctrl Pts',(97.8945777827573,0.291887860422791,-2.07342768236918));
#33438=CARTESIAN_POINT('Ctrl Pts',(97.9063938671677,0.233833341783416,-2.07664956073873));
#33439=CARTESIAN_POINT('Ctrl Pts',(97.9146988686464,0.174970387112386,-2.07987143910827));
#33440=CARTESIAN_POINT('Ctrl Pts',(97.9193983752572,0.11572465185336,-2.08309331747781));
#33441=CARTESIAN_POINT('Ctrl Pts',(97.9224379693847,0.0774050996357042,
-2.08517719635755));
#33442=CARTESIAN_POINT('Ctrl Pts',(97.9239702396369,0.0389257709143198,
-2.08726107523728));
#33443=CARTESIAN_POINT('Ctrl Pts',(97.9239808936025,0.000404768228821613,
-2.08934495411702));
#33444=CARTESIAN_POINT('Origin',(96.460480949577,-8.32667268468867E-16,
1.18130019239114E-14));
#33445=CARTESIAN_POINT('',(97.9239803697841,-0.00130271001786886,-2.6606550458059));
#33446=CARTESIAN_POINT('',(97.9239803753015,-0.00129649685740057,-2.58934495412449));
#33447=CARTESIAN_POINT('',(97.923980949577,-1.01189432752408E-15,1.19922289829666E-14));
#33448=CARTESIAN_POINT('Ctrl Pts',(97.9239803697841,-0.00130271001787374,
-2.6606550458059));
#33449=CARTESIAN_POINT('Ctrl Pts',(97.924028892116,0.0532085807223716,-2.65769006743583));
#33450=CARTESIAN_POINT('Ctrl Pts',(97.9210275607864,0.107804431595655,-2.65472508906576));
#33451=CARTESIAN_POINT('Ctrl Pts',(97.9149746591878,0.162111994320599,-2.6517601106957));
#33452=CARTESIAN_POINT('Ctrl Pts',(97.9089263301197,0.216378531600288,-2.64879737215286));
#33453=CARTESIAN_POINT('Ctrl Pts',(97.8998310544556,0.270356673964938,-2.64583463361002));
#33454=CARTESIAN_POINT('Ctrl Pts',(97.887739109395,0.323676374227503,-2.64287189506718));
#33455=CARTESIAN_POINT('Ctrl Pts',(97.8756512268637,0.376978160676594,-2.63991015191527));
#33456=CARTESIAN_POINT('Ctrl Pts',(97.8605687908678,0.429621414540402,-2.63694840876335));
#33457=CARTESIAN_POINT('Ctrl Pts',(97.8425931245834,0.481246491622603,-2.63398666561144));
#33458=CARTESIAN_POINT('Ctrl Pts',(97.8246030797137,0.53291286317251,-2.63102255338592));
#33459=CARTESIAN_POINT('Ctrl Pts',(97.803715356552,0.583558915781514,-2.62805844116042));
#33460=CARTESIAN_POINT('Ctrl Pts',(97.7800805804418,0.632842053139188,-2.62509432893491));
#33461=CARTESIAN_POINT('Ctrl Pts',(97.7564368907842,0.682143776989095,-2.62212909883314));
#33462=CARTESIAN_POINT('Ctrl Pts',(97.7300443453952,0.7300810844637,-2.61916386873138));
#33463=CARTESIAN_POINT('Ctrl Pts',(97.701099412135,0.776336319104215,-2.61619863862962));
#33464=CARTESIAN_POINT('Ctrl Pts',(97.6721000727146,0.822678497103016,-2.61322783495191));
#33465=CARTESIAN_POINT('Ctrl Pts',(97.6405390775404,0.867331843094967,-2.61025703127421));
#33466=CARTESIAN_POINT('Ctrl Pts',(97.6066552965318,0.910009129834844,-2.6072862275965));
#33467=CARTESIAN_POINT('Ctrl Pts',(97.5790164534826,0.944820794733497,-2.60486295681224));
#33468=CARTESIAN_POINT('Ctrl Pts',(97.549832995274,0.978318193879708,-2.60243968602799));
#33469=CARTESIAN_POINT('Ctrl Pts',(97.5192522745611,1.01036405883789,-2.60001641524373));
#33470=CARTESIAN_POINT('Ctrl Pts',(97.4812656391025,1.05017066122483,-2.5970062865825));
#33471=CARTESIAN_POINT('Ctrl Pts',(97.4409511564579,1.08791564893057,-2.59399615792126));
#33472=CARTESIAN_POINT('Ctrl Pts',(97.3985613494285,1.12331536685584,-2.59098602926002));
#33473=CARTESIAN_POINT('Ctrl Pts',(97.3562468810303,1.15865216950778,-2.58798125044558));
#33474=CARTESIAN_POINT('Ctrl Pts',(97.3118648100527,1.1916516384344,-2.58497647163114));
#33475=CARTESIAN_POINT('Ctrl Pts',(97.2657045114627,1.22206680070452,-2.5819716928167));
#33476=CARTESIAN_POINT('Ctrl Pts',(97.2195898808406,1.25245187221056,-2.57896988673308));
#33477=CARTESIAN_POINT('Ctrl Pts',(97.1717009464437,1.28025741270252,-2.57596808064946));
#33478=CARTESIAN_POINT('Ctrl Pts',(97.122358696316,1.30527778590293,-2.57296627456584));
#33479=CARTESIAN_POINT('Ctrl Pts',(97.0730457731752,1.33028328803137,-2.56996625263124));
#33480=CARTESIAN_POINT('Ctrl Pts',(97.0222817164732,1.35250666558854,-2.56696623069665));
#33481=CARTESIAN_POINT('Ctrl Pts',(96.9704129215266,1.37178775106925,-2.56396620876205));
#33482=CARTESIAN_POINT('Ctrl Pts',(96.9185544695313,1.39106499178496,-2.56096678504996));
#33483=CARTESIAN_POINT('Ctrl Pts',(96.8655922115242,1.40740092169674,-2.55796736133787));
#33484=CARTESIAN_POINT('Ctrl Pts',(96.8118912035211,1.42068401955641,-2.55496793762578));
#33485=CARTESIAN_POINT('Ctrl Pts',(96.7581408252191,1.43397932930064,-2.55196575637802));
#33486=CARTESIAN_POINT('Ctrl Pts',(96.7036508537876,1.44421607261516,-2.54896357513026));
#33487=CARTESIAN_POINT('Ctrl Pts',(96.6487986873739,1.45133341435765,-2.54596139388251));
#33488=CARTESIAN_POINT('Ctrl Pts',(96.5939215534718,1.45845399575611,-2.54295784610849));
#33489=CARTESIAN_POINT('Ctrl Pts',(96.5386824236007,1.46245230695219,-2.53995429833447));
#33490=CARTESIAN_POINT('Ctrl Pts',(96.4834626938998,1.46331954453833,-2.53695075056046));
#33491=CARTESIAN_POINT('Ctrl Pts',(96.4281387462522,1.46418841888947,-2.53394153409549));
#33492=CARTESIAN_POINT('Ctrl Pts',(96.3728348008828,1.46191443648741,-2.53093231763053));
#33493=CARTESIAN_POINT('Ctrl Pts',(96.3179299526928,1.45654092400019,-2.52792310116557));
#33494=CARTESIAN_POINT('Ctrl Pts',(96.2759254936491,1.45242996672353,-2.52562092724244));
#33495=CARTESIAN_POINT('Ctrl Pts',(96.2341545894424,1.44650597742633,-2.52331875331931));
#33496=CARTESIAN_POINT('Ctrl Pts',(96.1927823540791,1.43880843477109,-2.52101657939618));
#33497=CARTESIAN_POINT('Ctrl Pts',(96.1386875047738,1.42874377652143,-2.51800645073495));
#33498=CARTESIAN_POINT('Ctrl Pts',(96.085047386684,1.41560302543568,-2.51499632207372));
#33499=CARTESIAN_POINT('Ctrl Pts',(96.0322375460565,1.39944268812308,-2.5119861934125));
#33500=CARTESIAN_POINT('Ctrl Pts',(95.9795215633959,1.38331107228337,-2.50898141459806));
#33501=CARTESIAN_POINT('Ctrl Pts',(95.927633430702,1.36417067366608,-2.50597663578363));
#33502=CARTESIAN_POINT('Ctrl Pts',(95.8769381077974,1.342128906554,-2.50297185696919));
#33503=CARTESIAN_POINT('Ctrl Pts',(95.826292939516,1.32010894611872,-2.49997005088558));
#33504=CARTESIAN_POINT('Ctrl Pts',(95.7768387252643,1.29519351290047,-2.49696824480197));
#33505=CARTESIAN_POINT('Ctrl Pts',(95.7289230775661,1.26753908417015,-2.49396643871835));
#33506=CARTESIAN_POINT('Ctrl Pts',(95.6810359089415,1.23990109208518,-2.49096641678377));
#33507=CARTESIAN_POINT('Ctrl Pts',(95.6346859508392,1.20952759464432,-2.48796639484918));
#33508=CARTESIAN_POINT('Ctrl Pts',(95.5901966168965,1.17662119235161,-2.48496637291459));
#33509=CARTESIAN_POINT('Ctrl Pts',(95.545716154396,1.14372135179439,-2.4819669492025));
#33510=CARTESIAN_POINT('Ctrl Pts',(95.5030960035813,1.10828992331889,-2.47896752549042));
#33511=CARTESIAN_POINT('Ctrl Pts',(95.4626290316732,1.07057171639067,-2.47596810177833));
#33512=CARTESIAN_POINT('Ctrl Pts',(95.4221248562456,1.03281883303431,-2.47296592053058));
#33513=CARTESIAN_POINT('Ctrl Pts',(95.3837782017353,0.992775331836872,-2.46996373928283));
#33514=CARTESIAN_POINT('Ctrl Pts',(95.3478462280774,0.950724053820785,-2.46696155803508));
#33515=CARTESIAN_POINT('Ctrl Pts',(95.3118978989827,0.908653634996414,-2.46395801026106));
#33516=CARTESIAN_POINT('Ctrl Pts',(95.2783667620356,0.864574038623944,-2.46095446248705));
#33517=CARTESIAN_POINT('Ctrl Pts',(95.24746858368,0.818799884087048,-2.45795091471304));
#33518=CARTESIAN_POINT('Ctrl Pts',(95.2165120902127,0.772939338536952,-2.45494169824808));
#33519=CARTESIAN_POINT('Ctrl Pts',(95.1881987530261,0.725378300840873,-2.45193248178312));
#33520=CARTESIAN_POINT('Ctrl Pts',(95.1626994208353,0.67645794670244,-2.44892326531817));
#33521=CARTESIAN_POINT('Ctrl Pts',(95.1431913866637,0.639031870871124,-2.44662109139498));
#33522=CARTESIAN_POINT('Ctrl Pts',(95.1253294290495,0.600810769922743,-2.4443189174718));
#33523=CARTESIAN_POINT('Ctrl Pts',(95.1091707011953,0.56195450226743,-2.44201674354862));
#33524=CARTESIAN_POINT('Ctrl Pts',(95.0880429100438,0.511149320364774,-2.43900661488736));
#33525=CARTESIAN_POINT('Ctrl Pts',(95.0697398927803,0.459044223043108,-2.4359964862261));
#33526=CARTESIAN_POINT('Ctrl Pts',(95.0544195205938,0.405984615380659,-2.43298635756484));
#33527=CARTESIAN_POINT('Ctrl Pts',(95.0391263770255,0.353019309591584,-2.42998157875037));
#33528=CARTESIAN_POINT('Ctrl Pts',(95.0268055039807,0.299103363331115,-2.4269767999359));
#33529=CARTESIAN_POINT('Ctrl Pts',(95.017566351721,0.244601131015325,-2.42397202112144));
#33530=CARTESIAN_POINT('Ctrl Pts',(95.0083363400718,0.190152819628835,-2.42097021503779));
#33531=CARTESIAN_POINT('Ctrl Pts',(95.0021820974107,0.135119889332189,-2.41796840895415));
#33532=CARTESIAN_POINT('Ctrl Pts',(94.9991625039305,0.0798789735359879,
-2.41496660287051));
#33533=CARTESIAN_POINT('Ctrl Pts',(94.9961447051714,0.0246708906487744,
-2.41196658093589));
#33534=CARTESIAN_POINT('Ctrl Pts',(94.9962578915633,-0.0307444064430082,
-2.40896655900127));
#33535=CARTESIAN_POINT('Ctrl Pts',(94.9995090916734,-0.0859853499940245,
-2.40596653706665));
#33536=CARTESIAN_POINT('Ctrl Pts',(95.0027596434745,-0.141215278166994,
-2.40296711335454));
#33537=CARTESIAN_POINT('Ctrl Pts',(95.009146935292,-0.196270394937041,-2.39996768964242));
#33538=CARTESIAN_POINT('Ctrl Pts',(95.0186259541096,-0.25077165319408,-2.39696826593031));
#33539=CARTESIAN_POINT('Ctrl Pts',(95.0281136875121,-0.305323017464164,
-2.39396608468253));
#33540=CARTESIAN_POINT('Ctrl Pts',(95.0406987359633,-0.359318984497081,
-2.39096390343475));
#33541=CARTESIAN_POINT('Ctrl Pts',(95.0562847236741,-0.412389632701869,
-2.38796172218697));
#33542=CARTESIAN_POINT('Ctrl Pts',(95.0718778057804,-0.465484437487563,
-2.38495817441293));
#33543=CARTESIAN_POINT('Ctrl Pts',(95.0904743724567,-0.517652585520922,
-2.38195462663889));
#33544=CARTESIAN_POINT('Ctrl Pts',(95.1119288154397,-0.568541459802043,
-2.37895107886486));
#33545=CARTESIAN_POINT('Ctrl Pts',(95.1334237500733,-0.619526378269138,
-2.37594186239987));
#33546=CARTESIAN_POINT('Ctrl Pts',(95.15778710286,-0.669226724449195,-2.37293264593488));
#33547=CARTESIAN_POINT('Ctrl Pts',(95.1848264810336,-0.717312990879972,
-2.3699234294699));
#33548=CARTESIAN_POINT('Ctrl Pts',(95.2055127134958,-0.754100955427203,
-2.36762125554695));
#33549=CARTESIAN_POINT('Ctrl Pts',(95.2277642106588,-0.789944685160006,
-2.365319081624));
#33550=CARTESIAN_POINT('Ctrl Pts',(95.2514783150874,-0.824708966725413,
-2.36301690770106));
#33551=CARTESIAN_POINT('Ctrl Pts',(95.2824848801017,-0.870163812375398,
-2.36000677903983));
#33552=CARTESIAN_POINT('Ctrl Pts',(95.3161236046273,-0.913963102553221,
-2.3569966503786));
#33553=CARTESIAN_POINT('Ctrl Pts',(95.3521914628132,-0.955785887910526,
-2.35398652171737));
#33554=CARTESIAN_POINT('Ctrl Pts',(95.3881952182524,-0.997534342393801,
-2.35098174290295));
#33555=CARTESIAN_POINT('Ctrl Pts',(95.4266191976168,-1.03731286654294,-2.34797696408852));
#33556=CARTESIAN_POINT('Ctrl Pts',(95.4672180474705,-1.07483071099548,-2.34497218527409));
#33557=CARTESIAN_POINT('Ctrl Pts',(95.5077767314886,-1.11231143775669,-2.34197037919048));
#33558=CARTESIAN_POINT('Ctrl Pts',(95.5505056376785,-1.14753555868996,-2.33896857310687));
#33559=CARTESIAN_POINT('Ctrl Pts',(95.5951214973287,-1.18024796903217,-2.33596676702326));
#33560=CARTESIAN_POINT('Ctrl Pts',(95.6397108391626,-1.21294093647456,-2.33296674508868));
#33561=CARTESIAN_POINT('Ctrl Pts',(95.6861844864651,-1.24312484061695,-2.32996672315409));
#33562=CARTESIAN_POINT('Ctrl Pts',(95.7342267063618,-1.27058530772705,-2.32696670121951));
#33563=CARTESIAN_POINT('Ctrl Pts',(95.7822593463493,-1.29804029905401,-2.32396727750743));
#33564=CARTESIAN_POINT('Ctrl Pts',(95.8318594795136,-1.3227726699341,-2.32096785379535));
#33565=CARTESIAN_POINT('Ctrl Pts',(95.8826850487632,-1.34461301012697,-2.31796843008327));
#33566=CARTESIAN_POINT('Ctrl Pts',(95.9335573447621,-1.36647342934929,-2.31496624883553));
#33567=CARTESIAN_POINT('Ctrl Pts',(95.9856568414113,-1.38543629699036,-2.31196406758778));
#33568=CARTESIAN_POINT('Ctrl Pts',(96.0386210600697,-1.40138020666232,-2.30896188634003));
#33569=CARTESIAN_POINT('Ctrl Pts',(96.0916093868648,-1.41733137364803,-2.30595833856603));
#33570=CARTESIAN_POINT('Ctrl Pts',(96.1454627058692,-1.43026071986212,-2.30295479079202));
#33571=CARTESIAN_POINT('Ctrl Pts',(96.1998061310722,-1.44009752759925,-2.29995124301801));
#33572=CARTESIAN_POINT('Ctrl Pts',(96.2542521203446,-1.44995290065552,-2.29694202655306));
#33573=CARTESIAN_POINT('Ctrl Pts',(96.3091895381736,-1.45670401105605,-2.29393281008811));
#33574=CARTESIAN_POINT('Ctrl Pts',(96.3642372905393,-1.46033195133676,-2.29092359362315));
#33575=CARTESIAN_POINT('Ctrl Pts',(96.4063510771359,-1.46310747433637,-2.28862141969993));
#33576=CARTESIAN_POINT('Ctrl Pts',(96.4485292961512,-1.46405611982684,-2.28631924577671));
#33577=CARTESIAN_POINT('Ctrl Pts',(96.4906026111435,-1.46318998612773,-2.28401707185349));
#33578=CARTESIAN_POINT('Ctrl Pts',(96.5456141331019,-1.46205750267555,-2.28100694319231));
#33579=CARTESIAN_POINT('Ctrl Pts',(96.6006772844208,-1.45781592578263,-2.27799681453112));
#33580=CARTESIAN_POINT('Ctrl Pts',(96.6554123288551,-1.45045992959914,-2.27498668586993));
#33581=CARTESIAN_POINT('Ctrl Pts',(96.7100500936928,-1.44311700709357,-2.27198190705554));
#33582=CARTESIAN_POINT('Ctrl Pts',(96.7643603897109,-1.43267071971393,-2.26897712824115));
#33583=CARTESIAN_POINT('Ctrl Pts',(96.8179656463394,-1.4191676932557,-2.26597234942676));
#33584=CARTESIAN_POINT('Ctrl Pts',(96.8715178694473,-1.40567802580508,-2.2629705433432));
#33585=CARTESIAN_POINT('Ctrl Pts',(96.9243659253177,-1.38913773831275,-2.25996873725964));
#33586=CARTESIAN_POINT('Ctrl Pts',(96.976141379934,-1.36964468770702,-2.25696693117608));
#33587=CARTESIAN_POINT('Ctrl Pts',(97.0278860613677,-1.35016322296197,-2.25396690924153));
#33588=CARTESIAN_POINT('Ctrl Pts',(97.0785589118724,-1.32773265933739,-2.25096688730699));
#33589=CARTESIAN_POINT('Ctrl Pts',(97.1278078724749,-1.30250029864706,-2.24796686537244));
#33590=CARTESIAN_POINT('Ctrl Pts',(97.1770470125367,-1.27727296944203,-2.24496744166041));
#33591=CARTESIAN_POINT('Ctrl Pts',(97.224862356819,-1.24924519339155,-2.24196801794838));
#33592=CARTESIAN_POINT('Ctrl Pts',(97.2709251210342,-1.21861088742511,-2.23896859423635));
#33593=CARTESIAN_POINT('Ctrl Pts',(97.3170302332895,-1.18794841765132,-2.23596641298864));
#33594=CARTESIAN_POINT('Ctrl Pts',(97.3613791057318,-1.15467492349606,-2.23296423174094));
#33595=CARTESIAN_POINT('Ctrl Pts',(97.4036720003372,-1.11902765460283,-2.22996205049323));
#33596=CARTESIAN_POINT('Ctrl Pts',(97.4459841457293,-1.08336415986417,-2.22695850271927));
#33597=CARTESIAN_POINT('Ctrl Pts',(97.4862380632468,-1.04532509986363,-2.22395495494531));
#33598=CARTESIAN_POINT('Ctrl Pts',(97.5241696886636,-1.00518581184794,-2.22095140717135));
#33599=CARTESIAN_POINT('Ctrl Pts',(97.5621729036397,-0.964970767681221,
-2.21794219070643));
#33600=CARTESIAN_POINT('Ctrl Pts',(97.5978447297311,-0.922647981943616,
-2.21493297424152));
#33601=CARTESIAN_POINT('Ctrl Pts',(97.6309611031513,-0.878526300169063,
-2.2119237577766));
#33602=CARTESIAN_POINT('Ctrl Pts',(97.656296486039,-0.844771405355317,-2.20962158385304));
#33603=CARTESIAN_POINT('Ctrl Pts',(97.6801370154664,-0.809964347957141,
-2.20731940992948));
#33604=CARTESIAN_POINT('Ctrl Pts',(97.7024002993347,-0.774253562276253,
-2.20501723600592));
#33605=CARTESIAN_POINT('Ctrl Pts',(97.7322757960106,-0.726332623693341,
-2.20192790786333));
#33606=CARTESIAN_POINT('Ctrl Pts',(97.7594296788854,-0.676590924984949,
-2.19883857972074));
#33607=CARTESIAN_POINT('Ctrl Pts',(97.7836425547771,-0.625360389314989,
-2.19574925157814));
#33608=CARTESIAN_POINT('Ctrl Pts',(97.8077982313761,-0.574250878112431,
-2.19266722151058));
#33609=CARTESIAN_POINT('Ctrl Pts',(97.8290265048961,-0.521659961848709,
-2.18958519144301));
#33610=CARTESIAN_POINT('Ctrl Pts',(97.847152932833,-0.467945574669573,-2.18650316137545));
#33611=CARTESIAN_POINT('Ctrl Pts',(97.8652540308782,-0.414306248038114,
-2.18342543814032));
#33612=CARTESIAN_POINT('Ctrl Pts',(97.8802617284973,-0.359547027438996,
-2.18034771490519));
#33613=CARTESIAN_POINT('Ctrl Pts',(97.8920493474776,-0.304046332213235,
-2.17726999167006));
#33614=CARTESIAN_POINT('Ctrl Pts',(97.9038220450869,-0.248615892606251,
-2.17419616437442));
#33615=CARTESIAN_POINT('Ctrl Pts',(97.9123826613459,-0.192446321192262,
-2.17112233707877));
#33616=CARTESIAN_POINT('Ctrl Pts',(97.9176547047841,-0.13592975073733,-2.16804850978313));
#33617=CARTESIAN_POINT('Ctrl Pts',(97.9218816461293,-0.0906167272115239,
-2.16558402180305));
#33618=CARTESIAN_POINT('Ctrl Pts',(97.9239955432845,-0.0450810319793854,
-2.16311953382297));
#33619=CARTESIAN_POINT('Ctrl Pts',(97.9239808736882,0.000471303021997256,
-2.16065504584289));
#33620=CARTESIAN_POINT('Ctrl Pts',(97.9239808936027,0.000404767488459722,
-2.08934495415707));
#33621=CARTESIAN_POINT('Ctrl Pts',(97.9239966450049,-0.0565468821818031,
-2.09242587966883));
#33622=CARTESIAN_POINT('Ctrl Pts',(97.9206836795153,-0.113466791214522,
-2.09550680518059));
#33623=CARTESIAN_POINT('Ctrl Pts',(97.9140791524384,-0.169954448715279,
-2.09858773069235));
#33624=CARTESIAN_POINT('Ctrl Pts',(97.9074619006337,-0.226550939151006,
-2.10167459212322));
#33625=CARTESIAN_POINT('Ctrl Pts',(97.8975404829998,-0.282713030988987,
-2.10476145355409));
#33626=CARTESIAN_POINT('Ctrl Pts',(97.8844036811519,-0.338047784350542,
-2.10784831498497));
#33627=CARTESIAN_POINT('Ctrl Pts',(97.8712537796522,-0.393437715982223,
-2.11093825454782));
#33628=CARTESIAN_POINT('Ctrl Pts',(97.8548822482323,-0.447998199943239,
-2.11402819411067));
#33629=CARTESIAN_POINT('Ctrl Pts',(97.8354276192171,-0.501352077532047,
-2.11711813367352));
#33630=CARTESIAN_POINT('Ctrl Pts',(97.8159252667035,-0.554836835729674,
-2.12021565306355));
#33631=CARTESIAN_POINT('Ctrl Pts',(97.7933248982422,-0.607108625827405,
-2.12331317245358));
#33632=CARTESIAN_POINT('Ctrl Pts',(97.7678128057932,-0.657811270595443,
-2.12641069184361));
#33633=CARTESIAN_POINT('Ctrl Pts',(97.7497344722237,-0.693740088539389,
-2.12860565052379));
#33634=CARTESIAN_POINT('Ctrl Pts',(97.7301950372407,-0.728881467022591,
-2.13080060920398));
#33635=CARTESIAN_POINT('Ctrl Pts',(97.7092738802521,-0.763117596636286,
-2.13299556788417));
#33636=CARTESIAN_POINT('Ctrl Pts',(97.6805829646373,-0.810068437178112,
-2.1360056965451));
#33637=CARTESIAN_POINT('Ctrl Pts',(97.6491802703056,-0.855497639194756,
-2.13901582520603));
#33638=CARTESIAN_POINT('Ctrl Pts',(97.6152524926459,-0.899074487080088,
-2.14202595386695));
#33639=CARTESIAN_POINT('Ctrl Pts',(97.5813850142069,-0.94257388662803,-2.14503073268108));
#33640=CARTESIAN_POINT('Ctrl Pts',(97.5450016802927,-0.984227052010367,
-2.14803551149521));
#33641=CARTESIAN_POINT('Ctrl Pts',(97.5063329733976,-1.02373130960729,-2.15104029030934));
#33642=CARTESIAN_POINT('Ctrl Pts',(97.4677025227817,-1.0631964842861,-2.15404209639265));
#33643=CARTESIAN_POINT('Ctrl Pts',(97.4267915457187,-1.100516587111,-2.15704390247595));
#33644=CARTESIAN_POINT('Ctrl Pts',(97.3838701777455,-1.1354226452306,-2.16004570855925));
#33645=CARTESIAN_POINT('Ctrl Pts',(97.340974320453,-1.17030795663712,-2.16304573049353));
#33646=CARTESIAN_POINT('Ctrl Pts',(97.2960708495153,-1.20278173467465,-2.16604575242781));
#33647=CARTESIAN_POINT('Ctrl Pts',(97.2494643640091,-1.23261406034128,-2.16904577436209));
#33648=CARTESIAN_POINT('Ctrl Pts',(97.2028671721178,-1.26244043726185,-2.17204519807386));
#33649=CARTESIAN_POINT('Ctrl Pts',(97.1545680846216,-1.28962612330639,-2.17504462178563));
#33650=CARTESIAN_POINT('Ctrl Pts',(97.1049002438924,-1.31398478800708,-2.1780440454974));
#33651=CARTESIAN_POINT('Ctrl Pts',(97.0551867407775,-1.33836584697191,-2.18104622674485));
#33652=CARTESIAN_POINT('Ctrl Pts',(97.0041024455503,-1.35991445901165,-2.18404840799229));
#33653=CARTESIAN_POINT('Ctrl Pts',(96.9520033009044,-1.37849121438824,-2.18705058923974));
#33654=CARTESIAN_POINT('Ctrl Pts',(96.8998804418844,-1.39707642549151,-2.19005413701344));
#33655=CARTESIAN_POINT('Ctrl Pts',(96.8467423201935,-1.41268693425617,-2.19305768478715));
#33656=CARTESIAN_POINT('Ctrl Pts',(96.7929598092032,-1.42523333454619,-2.19606123256085));
#33657=CARTESIAN_POINT('Ctrl Pts',(96.7390757927746,-1.4378034140553,-2.19907044902551));
#33658=CARTESIAN_POINT('Ctrl Pts',(96.6845454791106,-1.44729774186084,-2.20207966549016));
#33659=CARTESIAN_POINT('Ctrl Pts',(96.6297485368579,-1.45367834609177,-2.20508888195482));
#33660=CARTESIAN_POINT('Ctrl Pts',(96.5878266302286,-1.45855976983206,-2.20739105588046));
#33661=CARTESIAN_POINT('Ctrl Pts',(96.5457488678837,-1.46161983639159,-2.2096932298061));
#33662=CARTESIAN_POINT('Ctrl Pts',(96.5036849796955,-1.46286214722424,-2.21199540373174));
#33663=CARTESIAN_POINT('Ctrl Pts',(96.4486857834913,-1.46448648820115,-2.21500553239283));
#33664=CARTESIAN_POINT('Ctrl Pts',(96.3934792952583,-1.46300822420362,-2.21801566105392));
#33665=CARTESIAN_POINT('Ctrl Pts',(96.3384445078446,-1.45840301593534,-2.22102578971501));
#33666=CARTESIAN_POINT('Ctrl Pts',(96.2835075327554,-1.45380599241977,-2.22403056852931));
#33667=CARTESIAN_POINT('Ctrl Pts',(96.2287421749122,-1.44609309713392,-2.2270353473436));
#33668=CARTESIAN_POINT('Ctrl Pts',(96.1745278663474,-1.43529198569194,-2.23004012615789));
#33669=CARTESIAN_POINT('Ctrl Pts',(96.1203671938593,-1.42450156016029,-2.23304193224136));
#33670=CARTESIAN_POINT('Ctrl Pts',(96.0667570060808,-1.41062907351305,-2.23604373832482));
#33671=CARTESIAN_POINT('Ctrl Pts',(96.0140701760109,-1.3937538058223,-2.23904554440829));
#33672=CARTESIAN_POINT('Ctrl Pts',(95.9614146608074,-1.37688856809069,-2.24204556634273));
#33673=CARTESIAN_POINT('Ctrl Pts',(95.9096819174873,-1.35702424753404,-2.24504558827717));
#33674=CARTESIAN_POINT('Ctrl Pts',(95.8592309411424,-1.33429032723671,-2.24804561021161));
#33675=CARTESIAN_POINT('Ctrl Pts',(95.8087900250273,-1.31156094022055,-2.25104503392354));
#33676=CARTESIAN_POINT('Ctrl Pts',(95.7596308495122,-1.28596330670364,-2.25404445763547));
#33677=CARTESIAN_POINT('Ctrl Pts',(95.7120914990629,-1.25767463215221,-2.2570438813474));
#33678=CARTESIAN_POINT('Ctrl Pts',(95.6645084430664,-1.22935995026184,-2.26004606259499));
#33679=CARTESIAN_POINT('Ctrl Pts',(95.6185486421705,-1.1983495552044,-2.26304824384259));
#33680=CARTESIAN_POINT('Ctrl Pts',(95.5745233414731,-1.16486538563163,-2.26605042509019));
#33681=CARTESIAN_POINT('Ctrl Pts',(95.5304780014361,-1.13136597480818,-2.26905397286404));
#33682=CARTESIAN_POINT('Ctrl Pts',(95.488369319128,-1.09539088849361,-2.2720575206379));
#33683=CARTESIAN_POINT('Ctrl Pts',(95.4484748183483,-1.05720189195612,-2.27506106841175));
#33684=CARTESIAN_POINT('Ctrl Pts',(95.4085050234125,-1.01894082011465,-2.27807028487655));
#33685=CARTESIAN_POINT('Ctrl Pts',(95.3707581190338,-0.978457878288022,
-2.28107950134135));
#33686=CARTESIAN_POINT('Ctrl Pts',(95.3354733571345,-0.936050301504515,
-2.28408871780615));
#33687=CARTESIAN_POINT('Ctrl Pts',(95.3084790681816,-0.903606767245913,
-2.28639089173054));
#33688=CARTESIAN_POINT('Ctrl Pts',(95.2829250559329,-0.870037517218534,
-2.28869306565492));
#33689=CARTESIAN_POINT('Ctrl Pts',(95.2589010438097,-0.835486672578428,
-2.2909952395793));
#33690=CARTESIAN_POINT('Ctrl Pts',(95.2274892696218,-0.790310899095273,
-2.29400536824071));
#33691=CARTESIAN_POINT('Ctrl Pts',(95.1985627470502,-0.743266261780503,
-2.29701549690211));
#33692=CARTESIAN_POINT('Ctrl Pts',(95.172348941115,-0.694656878448467,-2.30002562556351));
#33693=CARTESIAN_POINT('Ctrl Pts',(95.1461817244992,-0.646133887687202,
-2.30303040437812));
#33694=CARTESIAN_POINT('Ctrl Pts',(95.1227179053385,-0.596052130884527,
-2.30603518319273));
#33695=CARTESIAN_POINT('Ctrl Pts',(95.1021416414848,-0.544744503498396,
-2.30903996200734));
#33696=CARTESIAN_POINT('Ctrl Pts',(95.0815857344353,-0.493487636509195,
-2.31204176809113));
#33697=CARTESIAN_POINT('Ctrl Pts',(95.0639119192025,-0.441007789184984,
-2.31504357417491));
#33698=CARTESIAN_POINT('Ctrl Pts',(95.0492575329352,-0.387660571017612,
-2.3180453802587));
#33699=CARTESIAN_POINT('Ctrl Pts',(95.0346118566272,-0.334345060223814,
-2.32104540219347));
#33700=CARTESIAN_POINT('Ctrl Pts',(95.0229821918346,-0.280163708634643,
-2.32404542412824));
#33701=CARTESIAN_POINT('Ctrl Pts',(95.0144562464984,-0.225487933350093,
-2.32704544606301));
#33702=CARTESIAN_POINT('Ctrl Pts',(95.0059320012873,-0.170823060745626,
-2.33004486977527));
#33703=CARTESIAN_POINT('Ctrl Pts',(95.0005103277463,-0.115664481760865,
-2.33304429348754));
#33704=CARTESIAN_POINT('Ctrl Pts',(94.9982275395534,-0.0603921756059455,
-2.3360437171998));
#33705=CARTESIAN_POINT('Ctrl Pts',(94.9959426526674,-0.00506905457112808,
-2.33904589844773));
#33706=CARTESIAN_POINT('Ctrl Pts',(94.9968024383236,0.050367473722371,-2.34204807969566));
#33707=CARTESIAN_POINT('Ctrl Pts',(95.000791080028,0.105535466720293,-2.34505026094359));
#33708=CARTESIAN_POINT('Ctrl Pts',(95.0047815372734,0.160728570963964,-2.34805380871778));
#33709=CARTESIAN_POINT('Ctrl Pts',(95.0119036215515,0.215652371608006,-2.35105735649198));
#33710=CARTESIAN_POINT('Ctrl Pts',(95.0220897353198,0.269931407486378,-2.35406090426617));
#33711=CARTESIAN_POINT('Ctrl Pts',(95.0322950736635,0.324312885910187,-2.3570701207313));
#33712=CARTESIAN_POINT('Ctrl Pts',(95.0455758665916,0.378046654705103,-2.36007933719644));
#33713=CARTESIAN_POINT('Ctrl Pts',(95.0618138980795,0.430769925894763,-2.36308855366158));
#33714=CARTESIAN_POINT('Ctrl Pts',(95.0742366576468,0.471105389098869,-2.36539072758334));
#33715=CARTESIAN_POINT('Ctrl Pts',(95.0883891959999,0.510849668479265,-2.3676929015051));
#33716=CARTESIAN_POINT('Ctrl Pts',(95.1041998323173,0.549848871022576,-2.36999507542686));
#33717=CARTESIAN_POINT('Ctrl Pts',(95.1248724883147,0.60084094257259,-2.37300520408805));
#33718=CARTESIAN_POINT('Ctrl Pts',(95.1484682997943,0.650772688870073,-2.37601533274923));
#33719=CARTESIAN_POINT('Ctrl Pts',(95.1748568458959,0.699287433059006,-2.37902546141042));
#33720=CARTESIAN_POINT('Ctrl Pts',(95.2011984921157,0.747715952877547,-2.38203024022481));
#33721=CARTESIAN_POINT('Ctrl Pts',(95.2303227726028,0.79473200821732,-2.3850350190392));
#33722=CARTESIAN_POINT('Ctrl Pts',(95.2620515015793,0.839999469149773,-2.3880397978536));
#33723=CARTESIAN_POINT('Ctrl Pts',(95.2937488402351,0.885222145429272,-2.39104160393717));
#33724=CARTESIAN_POINT('Ctrl Pts',(95.32804522149,0.928699223901158,-2.39404341002074));
#33725=CARTESIAN_POINT('Ctrl Pts',(95.3647178533028,0.970121377376899,-2.39704521610431));
#33726=CARTESIAN_POINT('Ctrl Pts',(95.4013686884245,1.0115189112428,-2.40004523803885));
#33727=CARTESIAN_POINT('Ctrl Pts',(95.4403926253668,1.05086354630681,-2.4030452599734));
#33728=CARTESIAN_POINT('Ctrl Pts',(95.4815265155872,1.08787888396257,-2.40604528190795));
#33729=CARTESIAN_POINT('Ctrl Pts',(95.5226522034612,1.12488684053629,-2.40904470561999));
#33730=CARTESIAN_POINT('Ctrl Pts',(95.5658866166968,1.15956606906539,-2.41204412933204));
#33731=CARTESIAN_POINT('Ctrl Pts',(95.61093135413,1.19167853671865,-2.41504355304408));
#33732=CARTESIAN_POINT('Ctrl Pts',(95.6560175036751,1.22382052713472,-2.41804573429179));
#33733=CARTESIAN_POINT('Ctrl Pts',(95.7029168715836,1.25339073494567,-2.42104791553949));
#33734=CARTESIAN_POINT('Ctrl Pts',(95.7513009286169,1.28019371497873,-2.4240500967872));
#33735=CARTESIAN_POINT('Ctrl Pts',(95.7997070089989,1.3070088951333,-2.42705364456116));
#33736=CARTESIAN_POINT('Ctrl Pts',(95.8495986490855,1.33105410693755,-2.43005719233513));
#33737=CARTESIAN_POINT('Ctrl Pts',(95.9006244550134,1.35218081464536,-2.4330607401091));
#33738=CARTESIAN_POINT('Ctrl Pts',(95.9517465635629,1.37334739545852,-2.43606995657401));
#33739=CARTESIAN_POINT('Ctrl Pts',(96.0040066141782,1.39158429428956,-2.43907917303893));
#33740=CARTESIAN_POINT('Ctrl Pts',(96.0570361693938,1.4067922943146,-2.44208838950384));
#33741=CARTESIAN_POINT('Ctrl Pts',(96.0976059524642,1.41842703760901,-2.44439056342737));
#33742=CARTESIAN_POINT('Ctrl Pts',(96.1386257475107,1.42829002409361,-2.4466927373509));
#33743=CARTESIAN_POINT('Ctrl Pts',(96.1799274988729,1.4363572018471,-2.44899491127443));
#33744=CARTESIAN_POINT('Ctrl Pts',(96.2339301892273,1.44690516380721,-2.45200503993565));
#33745=CARTESIAN_POINT('Ctrl Pts',(96.2886420293264,1.45442554682468,-2.45501516859687));
#33746=CARTESIAN_POINT('Ctrl Pts',(96.3436930312583,1.45883269504587,-2.45802529725809));
#33747=CARTESIAN_POINT('Ctrl Pts',(96.3986461920481,1.46323201052287,-2.46103007607252));
#33748=CARTESIAN_POINT('Ctrl Pts',(96.4539367962634,1.46452902986565,-2.46403485488695));
#33749=CARTESIAN_POINT('Ctrl Pts',(96.5091859660334,1.46268932838521,-2.46703963370137));
#33750=CARTESIAN_POINT('Ctrl Pts',(96.5643804759032,1.4608514469846,-2.47004143978498));
#33751=CARTESIAN_POINT('Ctrl Pts',(96.6195331073032,1.45588300966985,-2.47304324586858));
#33752=CARTESIAN_POINT('Ctrl Pts',(96.6742630576916,1.44780159560973,-2.47604505195219));
#33753=CARTESIAN_POINT('Ctrl Pts',(96.7289604788675,1.43972498480692,-2.47904507388677));
#33754=CARTESIAN_POINT('Ctrl Pts',(96.7832351955663,1.42853914151569,-2.48204509582136));
#33755=CARTESIAN_POINT('Ctrl Pts',(96.8367119331856,1.41431343660905,-2.48504511775594));
#33756=CARTESIAN_POINT('Ctrl Pts',(96.8901780072203,1.40009056839394,-2.48804454146802));
#33757=CARTESIAN_POINT('Ctrl Pts',(96.9428459081041,1.38282917807458,-2.4910439651801));
#33758=CARTESIAN_POINT('Ctrl Pts',(96.9943532317103,1.36264912445198,-2.49404338889218));
#33759=CARTESIAN_POINT('Ctrl Pts',(97.0459079088402,1.34245051819298,-2.49704557013992));
#33760=CARTESIAN_POINT('Ctrl Pts',(97.0962993842198,1.31932808083586,-2.50004775138766));
#33761=CARTESIAN_POINT('Ctrl Pts',(97.1451844601707,1.29345017398454,-2.50304993263541));
#33762=CARTESIAN_POINT('Ctrl Pts',(97.194091787523,1.26756048808447,-2.50605348040941));
#33763=CARTESIAN_POINT('Ctrl Pts',(97.2414908958246,1.23891310611822,-2.50905702818341));
#33764=CARTESIAN_POINT('Ctrl Pts',(97.2870653821634,1.2077211705546,-2.51206057595742));
#33765=CARTESIAN_POINT('Ctrl Pts',(97.3327258826753,1.17647036546201,-2.51506979242237));
#33766=CARTESIAN_POINT('Ctrl Pts',(97.3765544627584,1.14266573652958,-2.51807900888731));
#33767=CARTESIAN_POINT('Ctrl Pts',(97.4182667128676,1.10656164836748,-2.52108822535226));
#33768=CARTESIAN_POINT('Ctrl Pts',(97.450178293706,1.07894054125959,-2.5233903992755));
#33769=CARTESIAN_POINT('Ctrl Pts',(97.4808518653103,1.04997445604528,-2.52569257319875));
#33770=CARTESIAN_POINT('Ctrl Pts',(97.5101754585963,1.0197910019875,-2.52799474712199));
#33771=CARTESIAN_POINT('Ctrl Pts',(97.5479955087937,0.980861947950277,-2.53096397168089));
#33772=CARTESIAN_POINT('Ctrl Pts',(97.583736810613,0.939733435353951,-2.53393319623979));
#33773=CARTESIAN_POINT('Ctrl Pts',(97.6171288425952,0.896659300724986,-2.5369024207987));
#33774=CARTESIAN_POINT('Ctrl Pts',(97.650473055172,0.853646850856692,-2.53986739324882));
#33775=CARTESIAN_POINT('Ctrl Pts',(97.6814743257114,0.808694718016118,-2.54283236569893));
#33776=CARTESIAN_POINT('Ctrl Pts',(97.7098994920492,0.762092878674607,-2.54579733814905));
#33777=CARTESIAN_POINT('Ctrl Pts',(97.7382959113231,0.7155381689097,-2.54875931205023));
#33778=CARTESIAN_POINT('Ctrl Pts',(97.7641211034871,0.667337517991422,-2.5517212859514));
#33779=CARTESIAN_POINT('Ctrl Pts',(97.7871842221689,0.617811198096895,-2.55468325985257));
#33780=CARTESIAN_POINT('Ctrl Pts',(97.8102422235838,0.568295867149768,-2.55764457654813));
#33781=CARTESIAN_POINT('Ctrl Pts',(97.8305391172134,0.517455933024783,-2.56060589324369));
#33782=CARTESIAN_POINT('Ctrl Pts',(97.8479302400693,0.465635819404298,-2.56356720993925));
#33783=CARTESIAN_POINT('Ctrl Pts',(97.8653178582868,0.413826148511774,-2.56652792987378));
#33784=CARTESIAN_POINT('Ctrl Pts',(97.8798007010528,0.361037207951688,-2.5694886498083));
#33785=CARTESIAN_POINT('Ctrl Pts',(97.8912835084281,0.307630114886793,-2.57244936974282));
#33786=CARTESIAN_POINT('Ctrl Pts',(97.9027779699189,0.254168817966135,-2.57541309456728));
#33787=CARTESIAN_POINT('Ctrl Pts',(97.9112662065411,0.20008864975942,-2.57837681939174));
#33788=CARTESIAN_POINT('Ctrl Pts',(97.916704153813,0.145760863898986,-2.5813405442162));
#33789=CARTESIAN_POINT('Ctrl Pts',(97.9215997454083,0.0968514797968769,
-2.58400868085229));
#33790=CARTESIAN_POINT('Ctrl Pts',(97.9240238177501,0.0477418006625273,
-2.58667681748839));
#33791=CARTESIAN_POINT('Ctrl Pts',(97.9239803753015,-0.00129649685740054,
-2.58934495412449));
#33792=CARTESIAN_POINT('Origin',(96.460480949577,-8.32667268468867E-16,
1.18130019239114E-14));
#33793=CARTESIAN_POINT('',(97.9239807388018,0.000785454741002297,-3.16065504587761));
#33794=CARTESIAN_POINT('',(97.9239807053004,0.000845575209100124,-3.08934495419159));
#33795=CARTESIAN_POINT('',(97.923980949577,-1.01189432752408E-15,1.19922289829666E-14));
#33796=CARTESIAN_POINT('Ctrl Pts',(97.9239807388014,0.000785455376517466,
-3.16065504584289));
#33797=CARTESIAN_POINT('Ctrl Pts',(97.9239557214913,0.0473989602722419,
-3.15810845262082));
#33798=CARTESIAN_POINT('Ctrl Pts',(97.9217038592401,0.0939508689700229,
-3.15556185939875));
#33799=CARTESIAN_POINT('Ctrl Pts',(97.9172417156336,0.140286565566206,-3.15301526617668));
#33800=CARTESIAN_POINT('Ctrl Pts',(97.9119673646911,0.195056368279042,-3.15000513751544));
#33801=CARTESIAN_POINT('Ctrl Pts',(97.9035888686244,0.249643385155502,-3.1469950088542));
#33802=CARTESIAN_POINT('Ctrl Pts',(97.8921295296342,0.303668558168621,-3.14398488019296));
#33803=CARTESIAN_POINT('Ctrl Pts',(97.8806905571183,0.357597713226631,-3.14098010137851));
#33804=CARTESIAN_POINT('Ctrl Pts',(97.866181716592,0.4109664936164,-3.13797532256407));
#33805=CARTESIAN_POINT('Ctrl Pts',(97.8486779510305,0.463401915356002,-3.13497054374962));
#33806=CARTESIAN_POINT('Ctrl Pts',(97.8311915025451,0.515785460932966,-3.131968737666));
#33807=CARTESIAN_POINT('Ctrl Pts',(97.8107161649499,0.567236978598564,-3.12896693158238));
#33808=CARTESIAN_POINT('Ctrl Pts',(97.7873772782786,0.617396455187672,-3.12596512549876));
#33809=CARTESIAN_POINT('Ctrl Pts',(97.7640522632734,0.667526119064526,-3.12296510356416));
#33810=CARTESIAN_POINT('Ctrl Pts',(97.7378672949656,0.716364786098106,-3.11996508162956));
#33811=CARTESIAN_POINT('Ctrl Pts',(97.7089957838616,0.76357249725958,-3.11696505969495));
#33812=CARTESIAN_POINT('Ctrl Pts',(97.6801300299115,0.810770794918064,-3.11396563598286));
#33813=CARTESIAN_POINT('Ctrl Pts',(97.6485790724551,0.856338332297967,-3.11096621227077));
#33814=CARTESIAN_POINT('Ctrl Pts',(97.6145610508622,0.899961871313187,-3.10796678855868));
#33815=CARTESIAN_POINT('Ctrl Pts',(97.5805117546256,0.943625515854127,-3.10496460731091));
#33816=CARTESIAN_POINT('Ctrl Pts',(97.5439911883238,0.985341174032972,-3.10196242606315));
#33817=CARTESIAN_POINT('Ctrl Pts',(97.5052585122345,1.02482783654984,-3.09896024481539));
#33818=CARTESIAN_POINT('Ctrl Pts',(97.4665082058909,1.06433247251896,-3.09595669704137));
#33819=CARTESIAN_POINT('Ctrl Pts',(97.4255441738651,1.10160573426969,-3.09295314926735));
#33820=CARTESIAN_POINT('Ctrl Pts',(97.3826608677621,1.13640505476529,-3.08994960149332));
#33821=CARTESIAN_POINT('Ctrl Pts',(97.3396966266358,1.17127005312182,-3.08694038502836));
#33822=CARTESIAN_POINT('Ctrl Pts',(97.2948063046736,1.20365147315747,-3.08393116856339));
#33823=CARTESIAN_POINT('Ctrl Pts',(97.2483147524996,1.23334915939184,-3.08092195209842));
#33824=CARTESIAN_POINT('Ctrl Pts',(97.2127468097126,1.25606910646815,-3.07861977817532));
#33825=CARTESIAN_POINT('Ctrl Pts',(97.176242331798,1.27721916981499,-3.07631760425222));
#33826=CARTESIAN_POINT('Ctrl Pts',(97.1389555392849,1.2967283759989,-3.07401543032911));
#33827=CARTESIAN_POINT('Ctrl Pts',(97.0902024708467,1.32223697033355,-3.07100530166787));
#33828=CARTESIAN_POINT('Ctrl Pts',(97.0399063977555,1.34504588612147,-3.06799517300663));
#33829=CARTESIAN_POINT('Ctrl Pts',(96.9883975235416,1.36496752376511,-3.06498504434539));
#33830=CARTESIAN_POINT('Ctrl Pts',(96.9369801951108,1.38485375504535,-3.06198026553094));
#33831=CARTESIAN_POINT('Ctrl Pts',(96.8843548317162,1.40186270272879,-3.0589754867165));
#33832=CARTESIAN_POINT('Ctrl Pts',(96.8308747660283,1.41585333659058,-3.05597070790205));
#33833=CARTESIAN_POINT('Ctrl Pts',(96.7774476100051,1.42983012903804,-3.05296890181843));
#33834=CARTESIAN_POINT('Ctrl Pts',(96.7231679351649,1.4407943900243,-3.04996709573481));
#33835=CARTESIAN_POINT('Ctrl Pts',(96.6684057475248,1.4486543854206,-3.04696528965118));
#33836=CARTESIAN_POINT('Ctrl Pts',(96.6136761082576,1.45650970916167,-3.04396526771658));
#33837=CARTESIAN_POINT('Ctrl Pts',(96.5584650463337,1.46126434943487,-3.04096524578198));
#33838=CARTESIAN_POINT('Ctrl Pts',(96.503152037409,1.46287778992752,-3.03796522384738));
#33839=CARTESIAN_POINT('Ctrl Pts',(96.4478500582326,1.46449090869039,-3.03496580013529));
#33840=CARTESIAN_POINT('Ctrl Pts',(96.3924467000232,1.46296405623548,-3.03196637642319));
#33841=CARTESIAN_POINT('Ctrl Pts',(96.3373234986036,1.45830877809527,-3.0289669527111));
#33842=CARTESIAN_POINT('Ctrl Pts',(96.2821496193843,1.45364922010109,-3.02596477146334));
#33843=CARTESIAN_POINT('Ctrl Pts',(96.2272569389069,1.44585553481691,-3.02296259021558));
#33844=CARTESIAN_POINT('Ctrl Pts',(96.1730224141812,1.43499123357187,-3.01996040896782));
#33845=CARTESIAN_POINT('Ctrl Pts',(96.1187632031039,1.42412198713808,-3.01695686119379));
#33846=CARTESIAN_POINT('Ctrl Pts',(96.0651632569648,1.41017947175422,-3.01395331341977));
#33847=CARTESIAN_POINT('Ctrl Pts',(96.0125866193864,1.39327776088728,-3.01094976564575));
#33848=CARTESIAN_POINT('Ctrl Pts',(95.9599107522528,1.37634415088552,-3.00794054918078));
#33849=CARTESIAN_POINT('Ctrl Pts',(95.9082625457957,1.35644037890225,-3.00493133271581));
#33850=CARTESIAN_POINT('Ctrl Pts',(95.8579871327224,1.33372915190904,-3.00192211625084));
#33851=CARTESIAN_POINT('Ctrl Pts',(95.8195243812728,1.31635413247992,-2.99961994232775));
#33852=CARTESIAN_POINT('Ctrl Pts',(95.7818647305796,1.2973369613695,-2.99731776840465));
#33853=CARTESIAN_POINT('Ctrl Pts',(95.7451518882949,1.27676802281594,-2.99501559448156));
#33854=CARTESIAN_POINT('Ctrl Pts',(95.6971492688196,1.24987381171829,-2.99200546582032));
#33855=CARTESIAN_POINT('Ctrl Pts',(95.6505646110984,1.22021219893694,-2.98899533715909));
#33856=CARTESIAN_POINT('Ctrl Pts',(95.6057354567556,1.18795723513156,-2.98598520849785));
#33857=CARTESIAN_POINT('Ctrl Pts',(95.5609859764515,1.15575959748532,-2.98298042968341));
#33858=CARTESIAN_POINT('Ctrl Pts',(95.517986233034,1.12097806158295,-2.97997565086897));
#33859=CARTESIAN_POINT('Ctrl Pts',(95.4770474026959,1.08383149468393,-2.97697087205453));
#33860=CARTESIAN_POINT('Ctrl Pts',(95.4361490745479,1.04672167815864,-2.97396906597091));
#33861=CARTESIAN_POINT('Ctrl Pts',(95.3973080096399,1.007251818816,-2.97096725988729));
#33862=CARTESIAN_POINT('Ctrl Pts',(95.3608032076086,0.965681683485441,-2.96796545380367));
#33863=CARTESIAN_POINT('Ctrl Pts',(95.3243201025174,0.924136255718989,-2.96496543186907));
#33864=CARTESIAN_POINT('Ctrl Pts',(95.2901708558294,0.880493422246292,-2.96196540993448));
#33865=CARTESIAN_POINT('Ctrl Pts',(95.2585967450554,0.835048866187807,-2.95896538799988));
#33866=CARTESIAN_POINT('Ctrl Pts',(95.22702893035,0.78961337204849,-2.95596596428779));
#33867=CARTESIAN_POINT('Ctrl Pts',(95.1980355329397,0.742377302293595,-2.9529665405757));
#33868=CARTESIAN_POINT('Ctrl Pts',(95.171815352806,0.693666511876485,-2.94996711686361));
#33869=CARTESIAN_POINT('Ctrl Pts',(95.1455710670144,0.644910938942837,-2.94696493561586));
#33870=CARTESIAN_POINT('Ctrl Pts',(95.1221053430655,0.594678402675534,-2.9439627543681));
#33871=CARTESIAN_POINT('Ctrl Pts',(95.1015709563422,0.543319317056278,-2.94096057312034));
#33872=CARTESIAN_POINT('Ctrl Pts',(95.0810272228218,0.491936853921341,-2.93795702534632));
#33873=CARTESIAN_POINT('Ctrl Pts',(95.0634176545321,0.4394273208251,-2.93495347757231));
#33874=CARTESIAN_POINT('Ctrl Pts',(95.0488456238805,0.386157943393404,-2.93194992979829));
#33875=CARTESIAN_POINT('Ctrl Pts',(95.0342460909735,0.332788028976673,-2.92894071333332));
#33876=CARTESIAN_POINT('Ctrl Pts',(95.0226956584212,0.278655923186859,-2.92593149686836));
#33877=CARTESIAN_POINT('Ctrl Pts',(95.0142466339124,0.224139586405414,-2.9229222804034));
#33878=CARTESIAN_POINT('Ctrl Pts',(95.0077827838947,0.182432354511517,-2.92062010648026));
#33879=CARTESIAN_POINT('Ctrl Pts',(95.003133091206,0.140500475882642,-2.91831793255712));
#33880=CARTESIAN_POINT('Ctrl Pts',(95.0003003779112,0.0985136951381245,
-2.91601575863398));
#33881=CARTESIAN_POINT('Ctrl Pts',(94.9965965606662,0.0436153180685221,
-2.91300562997275));
#33882=CARTESIAN_POINT('Ctrl Pts',(94.9959852855462,-0.0116075752867995,
-2.90999550131151));
#33883=CARTESIAN_POINT('Ctrl Pts',(94.998505211858,-0.0667771841359344,
-2.90698537265027));
#33884=CARTESIAN_POINT('Ctrl Pts',(95.0010206595508,-0.121848741045036,
-2.90398059383583));
#33885=CARTESIAN_POINT('Ctrl Pts',(95.0066562409394,-0.176866678084867,
-2.90097581502138));
#33886=CARTESIAN_POINT('Ctrl Pts',(95.015398674254,-0.231450788607809,-2.89797103620694));
#33887=CARTESIAN_POINT('Ctrl Pts',(95.0241324583791,-0.285980897196529,
-2.89496923012332));
#33888=CARTESIAN_POINT('Ctrl Pts',(95.0359669224377,-0.340077510585632,
-2.8919674240397));
#33889=CARTESIAN_POINT('Ctrl Pts',(95.0508369490254,-0.393365023494636,
-2.88896561795608));
#33890=CARTESIAN_POINT('Ctrl Pts',(95.0656981374862,-0.446620864516341,
-2.88596559602148));
#33891=CARTESIAN_POINT('Ctrl Pts',(95.0835911707428,-0.499068050558755,
-2.88296557408688));
#33892=CARTESIAN_POINT('Ctrl Pts',(95.1044002393092,-0.550342945116653,
-2.87996555215228));
#33893=CARTESIAN_POINT('Ctrl Pts',(95.1252051584216,-0.601607615150639,
-2.87696612844019));
#33894=CARTESIAN_POINT('Ctrl Pts',(95.1489247595747,-0.651699968862824,
-2.8739667047281));
#33895=CARTESIAN_POINT('Ctrl Pts',(95.1753947540048,-0.700275460051026,
-2.87096728101601));
#33896=CARTESIAN_POINT('Ctrl Pts',(95.2018890837609,-0.74889560936772,-2.86796509976825));
#33897=CARTESIAN_POINT('Ctrl Pts',(95.2311386053416,-0.795995645329472,
-2.86496291852049));
#33898=CARTESIAN_POINT('Ctrl Pts',(95.2629333134761,-0.841256149617383,
-2.86196073727273));
#33899=CARTESIAN_POINT('Ctrl Pts',(95.2947424938559,-0.886537255482135,
-2.85895718949871));
#33900=CARTESIAN_POINT('Ctrl Pts',(95.3290988420247,-0.929976745601661,
-2.85595364172469));
#33901=CARTESIAN_POINT('Ctrl Pts',(95.3657512789154,-0.971287392162184,
-2.85295009395067));
#33902=CARTESIAN_POINT('Ctrl Pts',(95.4024728911124,-1.01267600561579,-2.84994087748571));
#33903=CARTESIAN_POINT('Ctrl Pts',(95.4414988755614,-1.05192737383626,-2.84693166102074));
#33904=CARTESIAN_POINT('Ctrl Pts',(95.4825412609867,-1.08879117165776,-2.84392244455577));
#33905=CARTESIAN_POINT('Ctrl Pts',(95.5139403678866,-1.11699348778878,-2.84162027063266));
#33906=CARTESIAN_POINT('Ctrl Pts',(95.5465188709158,-1.1437991444267,-2.83931809670954));
#33907=CARTESIAN_POINT('Ctrl Pts',(95.5801361463526,-1.16911303022238,-2.83701592278643));
#33908=CARTESIAN_POINT('Ctrl Pts',(95.6240912634221,-1.20221133456672,-2.83400579412519));
#33909=CARTESIAN_POINT('Ctrl Pts',(95.6700079244915,-1.23289686607654,-2.83099566546395));
#33910=CARTESIAN_POINT('Ctrl Pts',(95.7175908345235,-1.26093081767231,-2.82798553680271));
#33911=CARTESIAN_POINT('Ctrl Pts',(95.7650891763169,-1.28891494503698,-2.82498075798827));
#33912=CARTESIAN_POINT('Ctrl Pts',(95.8142474388297,-1.31425657877337,-2.82197597917382));
#33913=CARTESIAN_POINT('Ctrl Pts',(95.8647399316551,-1.33675909930151,-2.81897120035938));
#33914=CARTESIAN_POINT('Ctrl Pts',(95.9151824705241,-1.35923935731366,-2.81596939427576));
#33915=CARTESIAN_POINT('Ctrl Pts',(95.9669561448404,-1.37888585235778,-2.81296758819214));
#33916=CARTESIAN_POINT('Ctrl Pts',(96.0197107951788,-1.39554789276175,-2.80996578210852));
#33917=CARTESIAN_POINT('Ctrl Pts',(96.0724340903412,-1.41220002994005,-2.80696576017392));
#33918=CARTESIAN_POINT('Ctrl Pts',(96.12613670329,-1.42587106959966,-2.80396573823932));
#33919=CARTESIAN_POINT('Ctrl Pts',(96.1804508008166,-1.43645931574313,-2.80096571630472));
#33920=CARTESIAN_POINT('Ctrl Pts',(96.2347540677838,-1.44704545052631,-2.79796629259263));
#33921=CARTESIAN_POINT('Ctrl Pts',(96.2896680591062,-1.45454991162158,-2.79496686888053));
#33922=CARTESIAN_POINT('Ctrl Pts',(96.3448144413312,-1.45892203659765,-2.79196744516844));
#33923=CARTESIAN_POINT('Ctrl Pts',(96.4000115226672,-1.46329818110938,-2.78896526392068));
#33924=CARTESIAN_POINT('Ctrl Pts',(96.4554408941549,-1.46453619434792,-2.78596308267292));
#33925=CARTESIAN_POINT('Ctrl Pts',(96.5107202883001,-1.46263743246393,-2.78296090142516));
#33926=CARTESIAN_POINT('Ctrl Pts',(96.5660248443985,-1.46073780630567,-2.77995735365114));
#33927=CARTESIAN_POINT('Ctrl Pts',(96.6211787602276,-1.45569860695866,-2.77695380587712));
#33928=CARTESIAN_POINT('Ctrl Pts',(96.6758042861467,-1.44757317974896,-2.7739502581031));
#33929=CARTESIAN_POINT('Ctrl Pts',(96.7305329085528,-1.43943241716285,-2.77094104163813));
#33930=CARTESIAN_POINT('Ctrl Pts',(96.7847306305091,-1.42819389839289,-2.76793182517316));
#33931=CARTESIAN_POINT('Ctrl Pts',(96.8380304515775,-1.41396203044465,-2.7649226087082));
#33932=CARTESIAN_POINT('Ctrl Pts',(96.8788069990937,-1.40307406819633,-2.76262043478509));
#33933=CARTESIAN_POINT('Ctrl Pts',(96.9190582241114,-1.39043520068447,-2.76031826086198));
#33934=CARTESIAN_POINT('Ctrl Pts',(96.9586276320664,-1.37611123559282,-2.75801608693887));
#33935=CARTESIAN_POINT('Ctrl Pts',(97.0103652561433,-1.3573824256484,-2.75500595827763));
#33936=CARTESIAN_POINT('Ctrl Pts',(97.0611538979779,-1.33569244020793,-2.75199582961639));
#33937=CARTESIAN_POINT('Ctrl Pts',(97.1106322021646,-1.31115811356172,-2.74898570095516));
#33938=CARTESIAN_POINT('Ctrl Pts',(97.1600225694634,-1.286667391327,-2.74598092214071));
#33939=CARTESIAN_POINT('Ctrl Pts',(97.208106751396,-1.25934259267139,-2.74297614332627));
#33940=CARTESIAN_POINT('Ctrl Pts',(97.254542117813,-1.22934905990921,-2.73997136451183));
#33941=CARTESIAN_POINT('Ctrl Pts',(97.300931544128,-1.19938520077857,-2.73696955842821));
#33942=CARTESIAN_POINT('Ctrl Pts',(97.3456749448753,-1.16675812292461,-2.7339677523446));
#33943=CARTESIAN_POINT('Ctrl Pts',(97.3884547859886,-1.13167875695163,-2.73096594626098));
#33944=CARTESIAN_POINT('Ctrl Pts',(97.4312092005388,-1.09662024069868,-2.72796592432638));
#33945=CARTESIAN_POINT('Ctrl Pts',(97.472001961081,-1.05911265946188,-2.72496590239178));
#33946=CARTESIAN_POINT('Ctrl Pts',(97.5105469118594,-1.01940851715887,-2.72196588045719));
#33947=CARTESIAN_POINT('Ctrl Pts',(97.5490841765415,-0.979712292101846,
-2.7189664567451));
#33948=CARTESIAN_POINT('Ctrl Pts',(97.5853741539633,-0.937820754555385,
-2.71596703303301));
#33949=CARTESIAN_POINT('Ctrl Pts',(97.6191676930618,-0.894023087214543,
-2.71296760932092));
#33950=CARTESIAN_POINT('Ctrl Pts',(97.6529923004249,-0.85018515426221,-2.70996542807316));
#33951=CARTESIAN_POINT('Ctrl Pts',(97.6843155608173,-0.804438009447671,
-2.70696324682541));
#33952=CARTESIAN_POINT('Ctrl Pts',(97.7129297405936,-0.757102553080593,
-2.70396106557765));
#33953=CARTESIAN_POINT('Ctrl Pts',(97.7415569449093,-0.709745550664548,
-2.70095751780363));
#33954=CARTESIAN_POINT('Ctrl Pts',(97.7674723629326,-0.660799263062575,
-2.69795397002962));
#33955=CARTESIAN_POINT('Ctrl Pts',(97.7905142718888,-0.610609213441926,
-2.6949504222556));
#33956=CARTESIAN_POINT('Ctrl Pts',(97.8135996685704,-0.560324438549256,
-2.69194120579064));
#33957=CARTESIAN_POINT('Ctrl Pts',(97.8338005291566,-0.508791705253196,
-2.68893198932567));
#33958=CARTESIAN_POINT('Ctrl Pts',(97.8510037697259,-0.45637543387556,-2.68592277286071));
#33959=CARTESIAN_POINT('Ctrl Pts',(97.8641649538059,-0.416274838083115,
-2.68362059893757));
#33960=CARTESIAN_POINT('Ctrl Pts',(97.8755726734547,-0.375657526258517,
-2.68131842501444));
#33961=CARTESIAN_POINT('Ctrl Pts',(97.885196536363,-0.334690523871024,-2.67901625109131));
#33962=CARTESIAN_POINT('Ctrl Pts',(97.901927104205,-0.263471594501355,-2.6750140455973));
#33963=CARTESIAN_POINT('Ctrl Pts',(97.9133233497531,-0.190955566274591,
-2.67101184010329));
#33964=CARTESIAN_POINT('Ctrl Pts',(97.9192301652513,-0.117826040286424,
-2.66700963460928));
#33965=CARTESIAN_POINT('Ctrl Pts',(97.9223563901513,-0.079121708801346,
-2.66489143835382));
#33966=CARTESIAN_POINT('Ctrl Pts',(97.9239457051545,-0.0402458655927077,
-2.66277324209836));
#33967=CARTESIAN_POINT('Ctrl Pts',(97.9239803697835,-0.00130271069809296,
-2.6606550458429));
#33968=CARTESIAN_POINT('Ctrl Pts',(97.923980375301,-0.00129649745620706,
-2.58934495415707));
#33969=CARTESIAN_POINT('Ctrl Pts',(97.9239140881349,-0.0761221201656831,
-2.59341615963053));
#33970=CARTESIAN_POINT('Ctrl Pts',(97.918105600398,-0.1506992465285,-2.59748736510399));
#33971=CARTESIAN_POINT('Ctrl Pts',(97.9066901297894,-0.22430170991184,-2.60155857057746));
#33972=CARTESIAN_POINT('Ctrl Pts',(97.9016093545666,-0.257060549658327,
-2.60337057470815));
#33973=CARTESIAN_POINT('Ctrl Pts',(97.8954184794346,-0.289626688431987,
-2.60518257883885));
#33974=CARTESIAN_POINT('Ctrl Pts',(97.8881323183465,-0.321937601485883,
-2.60699458296955));
#33975=CARTESIAN_POINT('Ctrl Pts',(97.8760284373731,-0.375612978824297,
-2.61000471163078));
#33976=CARTESIAN_POINT('Ctrl Pts',(97.860867868147,-0.42871758077675,-2.61301484029201));
#33977=CARTESIAN_POINT('Ctrl Pts',(97.842721283876,-0.480878267586448,-2.61602496895323));
#33978=CARTESIAN_POINT('Ctrl Pts',(97.8246069511984,-0.532946250158388,
-2.61902974776767));
#33979=CARTESIAN_POINT('Ctrl Pts',(97.8035173073587,-0.584073152043793,
-2.6220345265821));
#33980=CARTESIAN_POINT('Ctrl Pts',(97.7795734963088,-0.633898338187242,
-2.62503930539654));
#33981=CARTESIAN_POINT('Ctrl Pts',(97.7556533736932,-0.683674230563705,
-2.62804111148015));
#33982=CARTESIAN_POINT('Ctrl Pts',(97.7288849051549,-0.732150484666301,
-2.63104291756376));
#33983=CARTESIAN_POINT('Ctrl Pts',(97.6994376062592,-0.778985656390934,
-2.63404472364737));
#33984=CARTESIAN_POINT('Ctrl Pts',(97.6700078096165,-0.825792991232241,
-2.63704474558196));
#33985=CARTESIAN_POINT('Ctrl Pts',(97.6379026189751,-0.870960730789967,
-2.64004476751655));
#33986=CARTESIAN_POINT('Ctrl Pts',(97.6033367246649,-0.914173357382652,
-2.64304478945114));
#33987=CARTESIAN_POINT('Ctrl Pts',(97.5687777230029,-0.957377367116386,
-2.64604421316322));
#33988=CARTESIAN_POINT('Ctrl Pts',(97.5317593218419,-0.998626625955224,
-2.6490436368753));
#33989=CARTESIAN_POINT('Ctrl Pts',(97.4925372346774,-1.03763773754852,-2.65204306058738));
#33990=CARTESIAN_POINT('Ctrl Pts',(97.4532790884846,-1.07668471420857,-2.65504524183513));
#33991=CARTESIAN_POINT('Ctrl Pts',(97.411813583908,-1.11348905947499,-2.65804742308288));
#33992=CARTESIAN_POINT('Ctrl Pts',(97.3684330879568,-1.14780449746962,-2.66104960433063));
#33993=CARTESIAN_POINT('Ctrl Pts',(97.3250328461669,-1.18213555508986,-2.66405315210464));
#33994=CARTESIAN_POINT('Ctrl Pts',(97.2797163082787,-1.21397514295071,-2.66705669987865));
#33995=CARTESIAN_POINT('Ctrl Pts',(97.2328060309846,-1.24311955122135,-2.67006024765266));
#33996=CARTESIAN_POINT('Ctrl Pts',(97.1858072184368,-1.27231896465781,-2.67306946411761));
#33997=CARTESIAN_POINT('Ctrl Pts',(97.1372091225313,-1.29881278363015,-2.67607868058257));
#33998=CARTESIAN_POINT('Ctrl Pts',(97.0873591380174,-1.32244318851801,-2.67908789704753));
#33999=CARTESIAN_POINT('Ctrl Pts',(97.0492218568493,-1.34052141670828,-2.68139007097072));
#34000=CARTESIAN_POINT('Ctrl Pts',(97.0103523913196,-1.35692467056133,-2.68369224489392));
#34001=CARTESIAN_POINT('Ctrl Pts',(96.9709126475336,-1.37160188528639,-2.68599441881711));
#34002=CARTESIAN_POINT('Ctrl Pts',(96.9193445614017,-1.39079257468909,-2.68900454747835));
#34003=CARTESIAN_POINT('Ctrl Pts',(96.8665843525549,-1.40711133598553,-2.69201467613959));
#34004=CARTESIAN_POINT('Ctrl Pts',(96.812983151145,-1.42041347779078,-2.69502480480083));
#34005=CARTESIAN_POINT('Ctrl Pts',(96.7594772141733,-1.4336919779419,-2.69802958361527));
#34006=CARTESIAN_POINT('Ctrl Pts',(96.7051337592647,-1.44396437212756,-2.70103436242972));
#34007=CARTESIAN_POINT('Ctrl Pts',(96.6503210205638,-1.45113507208934,-2.70403914124416));
#34008=CARTESIAN_POINT('Ctrl Pts',(96.5955625099868,-1.4582986778315,-2.70704094732778));
#34009=CARTESIAN_POINT('Ctrl Pts',(96.5403361564106,-1.46236659995512,-2.7100427534114));
#34010=CARTESIAN_POINT('Ctrl Pts',(96.4850205511011,-1.46329424859016,-2.71304455949502));
#34011=CARTESIAN_POINT('Ctrl Pts',(96.4297378230929,-1.46422134586933,-2.71604458142962));
#34012=CARTESIAN_POINT('Ctrl Pts',(96.3743664754827,-1.46201186024532,-2.71904460336422));
#34013=CARTESIAN_POINT('Ctrl Pts',(96.3192880687736,-1.45667320302477,-2.72204462529882));
#34014=CARTESIAN_POINT('Ctrl Pts',(96.2642206450318,-1.45133561036474,-2.72504404901091));
#34015=CARTESIAN_POINT('Ctrl Pts',(96.209446571541,-1.44287013621926,-2.728043472723));
#34016=CARTESIAN_POINT('Ctrl Pts',(96.155342921222,-1.43133610086925,-2.73104289643509));
#34017=CARTESIAN_POINT('Ctrl Pts',(96.1011895304327,-1.41979146164432,-2.73404507768285));
#34018=CARTESIAN_POINT('Ctrl Pts',(96.0477083118358,-1.40517273537667,-2.73704725893061));
#34019=CARTESIAN_POINT('Ctrl Pts',(95.9952652762933,-1.38759022313189,-2.74004944017837));
#34020=CARTESIAN_POINT('Ctrl Pts',(95.9427983698451,-1.36999970771783,-2.74305298795239));
#34021=CARTESIAN_POINT('Ctrl Pts',(95.8913710797078,-1.34944291345235,-2.74605653572641));
#34022=CARTESIAN_POINT('Ctrl Pts',(95.8413302620576,-1.32607868399435,-2.74906008350042));
#34023=CARTESIAN_POINT('Ctrl Pts',(95.7911950007855,-1.30267035848528,-2.75206929996539));
#34024=CARTESIAN_POINT('Ctrl Pts',(95.7424519055442,-1.27644426392872,-2.75507851643036));
#34025=CARTESIAN_POINT('Ctrl Pts',(95.6954229696403,-1.24760512075542,-2.75808773289532));
#34026=CARTESIAN_POINT('Ctrl Pts',(95.659443906276,-1.22554199430654,-2.76038990681844));
#34027=CARTESIAN_POINT('Ctrl Pts',(95.6244676163366,-1.20195044434708,-2.76269208074156));
#34028=CARTESIAN_POINT('Ctrl Pts',(95.5906253328191,-1.1769381699965,-2.76499425466467));
#34029=CARTESIAN_POINT('Ctrl Pts',(95.5463760141404,-1.1442342273667,-2.76800438332591));
#34030=CARTESIAN_POINT('Ctrl Pts',(95.5038806413711,-1.10896263963651,-2.77101451198715));
#34031=CARTESIAN_POINT('Ctrl Pts',(95.4634522535768,-1.07133842895327,-2.77402464064839));
#34032=CARTESIAN_POINT('Ctrl Pts',(95.423095718419,-1.03378108709376,-2.77702941946283));
#34033=CARTESIAN_POINT('Ctrl Pts',(95.3847992613976,-0.99387977692337,-2.78003419827728));
#34034=CARTESIAN_POINT('Ctrl Pts',(95.3488441419424,-0.951890675399192,
-2.78303897709173));
#34035=CARTESIAN_POINT('Ctrl Pts',(95.3129245941211,-0.909943115134485,
-2.78604078317535));
#34036=CARTESIAN_POINT('Ctrl Pts',(95.2793421370661,-0.865912254390238,
-2.78904258925897));
#34037=CARTESIAN_POINT('Ctrl Pts',(95.2483409767751,-0.82009080981064,-2.79204439534259));
#34038=CARTESIAN_POINT('Ctrl Pts',(95.2173582422879,-0.774296599597015,
-2.79504441727719));
#34039=CARTESIAN_POINT('Ctrl Pts',(95.188954058994,-0.726714351496427,-2.79804443921179));
#34040=CARTESIAN_POINT('Ctrl Pts',(95.1633307028859,-0.677667682208029,
-2.80104446114639));
#34041=CARTESIAN_POINT('Ctrl Pts',(95.1377124562299,-0.628630793121955,
-2.80404388485849));
#34042=CARTESIAN_POINT('Ctrl Pts',(95.114874179924,-0.578130530601198,-2.80704330857058));
#34043=CARTESIAN_POINT('Ctrl Pts',(95.0949722228001,-0.526515115733661,
-2.81004273228267));
#34044=CARTESIAN_POINT('Ctrl Pts',(95.0750519687092,-0.474852247968114,
-2.81304491353043));
#34045=CARTESIAN_POINT('Ctrl Pts',(95.0580736174965,-0.422072673411288,
-2.8160470947782));
#34046=CARTESIAN_POINT('Ctrl Pts',(95.0441447759492,-0.368543204079821,
-2.81904927602596));
#34047=CARTESIAN_POINT('Ctrl Pts',(95.0302095943025,-0.314989369322186,
-2.82205282379998));
#34048=CARTESIAN_POINT('Ctrl Pts',(95.0193267932962,-0.260685478084066,
-2.825056371574));
#34049=CARTESIAN_POINT('Ctrl Pts',(95.0115528579442,-0.206008823299595,
-2.82805991934802));
#34050=CARTESIAN_POINT('Ctrl Pts',(95.0037642505975,-0.151228975530921,
-2.83106913581299));
#34051=CARTESIAN_POINT('Ctrl Pts',(94.9990962747166,-0.0960754863342362,
-2.83407835227796));
#34052=CARTESIAN_POINT('Ctrl Pts',(94.9975534073099,-0.0409298922093092,
-2.83708756874293));
#34053=CARTESIAN_POINT('Ctrl Pts',(94.9963730505121,0.00125874734068382,
-2.83938974266603));
#34054=CARTESIAN_POINT('Ctrl Pts',(94.9970207010016,0.0434426617659435,
-2.84169191658913));
#34055=CARTESIAN_POINT('Ctrl Pts',(94.9994778630617,0.0854530935235066,
-2.84399409051224));
#34056=CARTESIAN_POINT('Ctrl Pts',(95.002690641153,0.140382394665889,-2.84700421917347));
#34057=CARTESIAN_POINT('Ctrl Pts',(95.0090122402784,0.195245670108552,-2.85001434783471));
#34058=CARTESIAN_POINT('Ctrl Pts',(95.018433616919,0.249663253952133,-2.85302447649594));
#34059=CARTESIAN_POINT('Ctrl Pts',(95.0278382491187,0.303984122416013,-2.85602925531038));
#34060=CARTESIAN_POINT('Ctrl Pts',(95.0403316364684,0.357860355081541,-2.85903403412482));
#34061=CARTESIAN_POINT('Ctrl Pts',(95.0558529029206,0.410916415522879,-2.86203881293927));
#34062=CARTESIAN_POINT('Ctrl Pts',(95.071358813651,0.463919985782394,-2.86504061902288));
#34063=CARTESIAN_POINT('Ctrl Pts',(95.089886521821,0.516104486830948,-2.8680424251065));
#34064=CARTESIAN_POINT('Ctrl Pts',(95.1113243025617,0.567105450347909,-2.87104423119012));
#34065=CARTESIAN_POINT('Ctrl Pts',(95.1327493415746,0.618076101007678,-2.87404425312471));
#34066=CARTESIAN_POINT('Ctrl Pts',(95.157080820689,0.667864122528863,-2.87704427505931));
#34067=CARTESIAN_POINT('Ctrl Pts',(95.1841582250178,0.716123280430041,-2.88004429699391));
#34068=CARTESIAN_POINT('Ctrl Pts',(95.2112302299486,0.764372815163445,-2.883043720706));
#34069=CARTESIAN_POINT('Ctrl Pts',(95.2410468144008,0.811093631411541,-2.88604314441809));
#34070=CARTESIAN_POINT('Ctrl Pts',(95.2734017622296,0.855964516184354,-2.88904256813017));
#34071=CARTESIAN_POINT('Ctrl Pts',(95.3057864557467,0.90087665323662,-2.89204474937793));
#34072=CARTESIAN_POINT('Ctrl Pts',(95.3407138654392,0.943935031660171,-2.89504693062569));
#34073=CARTESIAN_POINT('Ctrl Pts',(95.3779355722973,0.984849103228719,-2.89804911187344));
#34074=CARTESIAN_POINT('Ctrl Pts',(95.4151742216501,1.02578179797441,-2.90105265964746));
#34075=CARTESIAN_POINT('Ctrl Pts',(95.4547088722911,1.0645678697017,-2.90405620742148));
#34076=CARTESIAN_POINT('Ctrl Pts',(95.4962543944235,1.10095385931328,-2.90705975519549));
#34077=CARTESIAN_POINT('Ctrl Pts',(95.5378783267371,1.13740852135674,-2.91006897166046));
#34078=CARTESIAN_POINT('Ctrl Pts',(95.581520294585,1.1714537267717,-2.91307818812542));
#34079=CARTESIAN_POINT('Ctrl Pts',(95.6268631971002,1.20287725589749,-2.91608740459038));
#34080=CARTESIAN_POINT('Ctrl Pts',(95.6615523758234,1.22691754351679,-2.91838957851352));
#34081=CARTESIAN_POINT('Ctrl Pts',(95.6972364131332,1.24942424404626,-2.92069175243666));
#34082=CARTESIAN_POINT('Ctrl Pts',(95.7337638640587,1.27032063968737,-2.9229939263598));
#34083=CARTESIAN_POINT('Ctrl Pts',(95.7815240814113,1.29764300608362,-2.92600405502104));
#34084=CARTESIAN_POINT('Ctrl Pts',(95.8309276480725,1.32232557501321,-2.92901418368228));
#34085=CARTESIAN_POINT('Ctrl Pts',(95.8816516422904,1.34416847270948,-2.93202431234352));
#34086=CARTESIAN_POINT('Ctrl Pts',(95.9322854856781,1.3659725494219,-2.93502909115797));
#34087=CARTESIAN_POINT('Ctrl Pts',(95.984234618307,1.38494676331392,-2.93803386997242));
#34088=CARTESIAN_POINT('Ctrl Pts',(96.0371512558801,1.40093690808491,-2.94103864878686));
#34089=CARTESIAN_POINT('Ctrl Pts',(96.0900155412073,1.41691123325679,-2.94404045487048));
#34090=CARTESIAN_POINT('Ctrl Pts',(96.1438449322852,1.42990718554609,-2.94704226095411));
#34091=CARTESIAN_POINT('Ctrl Pts',(96.1982731310567,1.43981919347772,-2.95004406703773));
#34092=CARTESIAN_POINT('Ctrl Pts',(96.2526689799646,1.44972531012299,-2.95304408897233));
#34093=CARTESIAN_POINT('Ctrl Pts',(96.3076624126027,1.45655102104374,-2.95604411090693));
#34094=CARTESIAN_POINT('Ctrl Pts',(96.3628757435706,1.46024158061618,-2.95904413284153));
#34095=CARTESIAN_POINT('Ctrl Pts',(96.4180780646666,1.46393140426874,-2.96204355655362));
#34096=CARTESIAN_POINT('Ctrl Pts',(96.4734996703651,1.46448728292817,-2.96504298026572));
#34097=CARTESIAN_POINT('Ctrl Pts',(96.5287588604504,1.46190641864887,-2.96804240397781));
#34098=CARTESIAN_POINT('Ctrl Pts',(96.5840688533572,1.45932318163867,-2.97104458522557));
#34099=CARTESIAN_POINT('Ctrl Pts',(96.6392156036589,1.453597464962,-2.97404676647333));
#34100=CARTESIAN_POINT('Ctrl Pts',(96.6938200342248,1.44477857181498,-2.97704894772109));
#34101=CARTESIAN_POINT('Ctrl Pts',(96.7484493195153,1.43595566450357,-2.98005249549511));
#34102=CARTESIAN_POINT('Ctrl Pts',(96.8025352763465,1.42403688793077,-2.98305604326913));
#34103=CARTESIAN_POINT('Ctrl Pts',(96.8557098321016,1.40912255691915,-2.98605959104315));
#34104=CARTESIAN_POINT('Ctrl Pts',(96.9089847458818,1.39418007761772,-2.98906880750812));
#34105=CARTESIAN_POINT('Ctrl Pts',(96.961344321584,1.37623092160183,-2.99207802397309));
#34106=CARTESIAN_POINT('Ctrl Pts',(97.0124375568619,1.35542471339227,-2.99508724043806));
#34107=CARTESIAN_POINT('Ctrl Pts',(97.0515259758152,1.33950711140641,-2.99738941436116));
#34108=CARTESIAN_POINT('Ctrl Pts',(97.0898735611337,1.32191834261412,-2.99969158828426));
#34109=CARTESIAN_POINT('Ctrl Pts',(97.1273333106589,1.30274332795046,-3.00199376220736));
#34110=CARTESIAN_POINT('Ctrl Pts',(97.1763125231142,1.27767169429172,-3.0050038908686));
#34111=CARTESIAN_POINT('Ctrl Pts',(97.2239787537575,1.24978133638679,-3.00801401952983));
#34112=CARTESIAN_POINT('Ctrl Pts',(97.2699881597525,1.21923349965211,-3.01102414819107));
#34113=CARTESIAN_POINT('Ctrl Pts',(97.315915794069,1.18873995503075,-3.01402892700551));
#34114=CARTESIAN_POINT('Ctrl Pts',(97.3601920109915,1.15559859433552,-3.01703370581995));
#34115=CARTESIAN_POINT('Ctrl Pts',(97.4024976306186,1.12001643855764,-3.0200384846344));
#34116=CARTESIAN_POINT('Ctrl Pts',(97.4447613958441,1.08446948542787,-3.02304029071802));
#34117=CARTESIAN_POINT('Ctrl Pts',(97.4850580236171,1.04648685900687,-3.02604209680163));
#34118=CARTESIAN_POINT('Ctrl Pts',(97.5230989511658,1.00631765993617,-3.02904390288525));
#34119=CARTESIAN_POINT('Ctrl Pts',(97.5611172687651,0.966172335771173,-3.03204392481985));
#34120=CARTESIAN_POINT('Ctrl Pts',(97.5968821810716,0.923843397553973,-3.03504394675445));
#34121=CARTESIAN_POINT('Ctrl Pts',(97.630141471332,0.879617254178147,-3.03804396868905));
#34122=CARTESIAN_POINT('Ctrl Pts',(97.6633941294888,0.835399929762643,-3.04104339240114));
#34123=CARTESIAN_POINT('Ctrl Pts',(97.6941418406163,0.78928657334929,-3.04404281611323));
#34124=CARTESIAN_POINT('Ctrl Pts',(97.7221737018601,0.741595340355052,-3.04704223982532));
#34125=CARTESIAN_POINT('Ctrl Pts',(97.7502313343402,0.693860262179654,-3.05004442107307));
#34126=CARTESIAN_POINT('Ctrl Pts',(97.7755678604076,0.644544865525786,-3.05304660232083));
#34127=CARTESIAN_POINT('Ctrl Pts',(97.79801744656,0.593993576765358,-3.05604878356859));
#34128=CARTESIAN_POINT('Ctrl Pts',(97.8204772512656,0.543419278180456,-3.05905233134261));
#34129=CARTESIAN_POINT('Ctrl Pts',(97.8400473096086,0.491608460991503,-3.06205587911662));
#34130=CARTESIAN_POINT('Ctrl Pts',(97.8566105245198,0.438924207546307,-3.06505942689064));
#34131=CARTESIAN_POINT('Ctrl Pts',(97.8732049997116,0.386140521439122,-3.0680686433556));
#34132=CARTESIAN_POINT('Ctrl Pts',(97.886781165104,0.332480619252992,-3.07107785982057));
#34133=CARTESIAN_POINT('Ctrl Pts',(97.8972725489559,0.278320229150155,-3.07408707628553));
#34134=CARTESIAN_POINT('Ctrl Pts',(97.9052988875735,0.236885311053383,-3.07638925020866));
#34135=CARTESIAN_POINT('Ctrl Pts',(97.9115207904248,0.195157742081021,-3.07869142413179));
#34136=CARTESIAN_POINT('Ctrl Pts',(97.9159290596762,0.153307040962702,-3.08099359805492));
#34137=CARTESIAN_POINT('Ctrl Pts',(97.9212595324585,0.102701233895996,-3.08377738342231));
#34138=CARTESIAN_POINT('Ctrl Pts',(97.9239512576967,0.0518126899422455,
-3.08656116878969));
#34139=CARTESIAN_POINT('Ctrl Pts',(97.9239807053001,0.000845575841043114,
-3.08934495415707));
#34140=CARTESIAN_POINT('Origin',(96.460480949577,-8.32667268468867E-16,
1.18130019239114E-14));
#34141=CARTESIAN_POINT('',(97.9239808415864,0.000562217564739472,-3.66065504578966));
#34142=CARTESIAN_POINT('',(97.9239808649782,0.000497614912990139,-3.58934495410898));
#34143=CARTESIAN_POINT('',(97.923980949577,-1.01189432752408E-15,1.19922289829666E-14));
#34144=CARTESIAN_POINT('Ctrl Pts',(97.9239808415864,0.000562217564739831,
-3.66065504578966));
#34145=CARTESIAN_POINT('Ctrl Pts',(97.9239576848819,0.0608410786727076,
-3.657393306043));
#34146=CARTESIAN_POINT('Ctrl Pts',(97.9202061513422,0.121005515574799,-3.65413156629635));
#34147=CARTESIAN_POINT('Ctrl Pts',(97.9127935705301,0.180610910579241,-3.65086982654969));
#34148=CARTESIAN_POINT('Ctrl Pts',(97.9053586167204,0.240396209371518,-3.64759824206775));
#34149=CARTESIAN_POINT('Ctrl Pts',(97.8942406267972,0.299618735368977,-3.64432665758581));
#34150=CARTESIAN_POINT('Ctrl Pts',(97.8795576996842,0.357845535538924,-3.64105507310387));
#34151=CARTESIAN_POINT('Ctrl Pts',(97.8648121525538,0.416320662436631,-3.63776953590829));
#34152=CARTESIAN_POINT('Ctrl Pts',(97.8464713619942,0.473791213877508,-3.63448399871271));
#34153=CARTESIAN_POINT('Ctrl Pts',(97.824703128336,0.529839689889331,-3.63119846151713));
#34154=CARTESIAN_POINT('Ctrl Pts',(97.8154624057349,0.553632544522167,-3.62980373476544));
#34155=CARTESIAN_POINT('Ctrl Pts',(97.8056046193567,0.57716942246352,-3.62840900801375));
#34156=CARTESIAN_POINT('Ctrl Pts',(97.7951450939575,0.600419746265101,-3.62701428126206));
#34157=CARTESIAN_POINT('Ctrl Pts',(97.7725711258674,0.650599084958767,-3.62400415260082));
#34158=CARTESIAN_POINT('Ctrl Pts',(97.7471159056111,0.699609016294283,-3.62099402393958));
#34159=CARTESIAN_POINT('Ctrl Pts',(97.7189231632658,0.747098015528166,-3.61798389527834));
#34160=CARTESIAN_POINT('Ctrl Pts',(97.6907805273674,0.794502613429475,-3.61497911646389));
#34161=CARTESIAN_POINT('Ctrl Pts',(97.6599102921119,0.840391193152365,-3.61197433764944));
#34162=CARTESIAN_POINT('Ctrl Pts',(97.6265031467642,0.884434557028855,-3.608969558835));
#34163=CARTESIAN_POINT('Ctrl Pts',(97.593129052252,0.928434347293605,-3.60596775275137));
#34164=CARTESIAN_POINT('Ctrl Pts',(97.5572233371307,0.970592119309586,-3.60296594666775));
#34165=CARTESIAN_POINT('Ctrl Pts',(97.5190202583804,1.01060713520049,-3.59996414058413));
#34166=CARTESIAN_POINT('Ctrl Pts',(97.4808398859554,1.05059836782577,-3.59696411864953));
#34167=CARTESIAN_POINT('Ctrl Pts',(97.4403652202861,1.08844898739605,-3.59396409671493));
#34168=CARTESIAN_POINT('Ctrl Pts',(97.3978696091432,1.12389267766842,-3.59096407478032));
#34169=CARTESIAN_POINT('Ctrl Pts',(97.3553824718821,1.15932930025471,-3.58796465106823));
#34170=CARTESIAN_POINT('Ctrl Pts',(97.3108755948043,1.19235960864079,-3.58496522735613));
#34171=CARTESIAN_POINT('Ctrl Pts',(97.2646561119048,1.22275694980441,-3.58196580364404));
#34172=CARTESIAN_POINT('Ctrl Pts',(97.2183941368853,1.25318223692048,-3.57896362239628));
#34173=CARTESIAN_POINT('Ctrl Pts',(97.1704168526017,1.28096942988906,-3.57596144114851));
#34174=CARTESIAN_POINT('Ctrl Pts',(97.1210598997175,1.30593556526777,-3.57295925990075));
#34175=CARTESIAN_POINT('Ctrl Pts',(97.071680480644,1.33091306467712,-3.56995571212673));
#34176=CARTESIAN_POINT('Ctrl Pts',(97.0209206259756,1.35306673514927,-3.5669521643527));
#34177=CARTESIAN_POINT('Ctrl Pts',(96.9691370623423,1.37226134863099,-3.56394861657868));
#34178=CARTESIAN_POINT('Ctrl Pts',(96.9172557659474,1.39149218871532,-3.56093940011371));
#34179=CARTESIAN_POINT('Ctrl Pts',(96.8643474070127,1.4077526599334,-3.55793018364874));
#34180=CARTESIAN_POINT('Ctrl Pts',(96.8107838906918,1.42095745870392,-3.55492096718377));
#34181=CARTESIAN_POINT('Ctrl Pts',(96.7698056055007,1.4310596709386,-3.55261879326068));
#34182=CARTESIAN_POINT('Ctrl Pts',(96.7284441957512,1.43937446924753,-3.55031661933758));
#34183=CARTESIAN_POINT('Ctrl Pts',(96.6868685021343,1.44588413299514,-3.54801444541448));
#34184=CARTESIAN_POINT('Ctrl Pts',(96.6325076279573,1.45439562086541,-3.54500431675325));
#34185=CARTESIAN_POINT('Ctrl Pts',(96.577551859042,1.45985502291365,-3.54199418809201));
#34186=CARTESIAN_POINT('Ctrl Pts',(96.5223741403715,1.46219064520782,-3.53898405943078));
#34187=CARTESIAN_POINT('Ctrl Pts',(96.4672944880545,1.46452211644307,-3.53597928061634));
#34188=CARTESIAN_POINT('Ctrl Pts',(96.4119941921812,1.46374080342767,-3.53297450180189));
#34189=CARTESIAN_POINT('Ctrl Pts',(96.3568531565239,1.45982654123939,-3.52996972298745));
#34190=CARTESIAN_POINT('Ctrl Pts',(96.3017666737861,1.45591615156505,-3.52696791690384));
#34191=CARTESIAN_POINT('Ctrl Pts',(96.2468396633429,1.44887898995706,-3.52396611082022));
#34192=CARTESIAN_POINT('Ctrl Pts',(96.1924519983541,1.43874693094593,-3.5209643047366));
#34193=CARTESIAN_POINT('Ctrl Pts',(96.1380966591373,1.42862089401041,-3.51796428280201));
#34194=CARTESIAN_POINT('Ctrl Pts',(96.0842805481421,1.41540370216654,-3.51496426086741));
#34195=CARTESIAN_POINT('Ctrl Pts',(96.0313760685382,1.3991787773793,-3.51196423893282));
#34196=CARTESIAN_POINT('Ctrl Pts',(95.9784821384072,1.38295708794013,-3.50896481522073));
#34197=CARTESIAN_POINT('Ctrl Pts',(95.9264999832728,1.3637290114147,-3.50596539150864));
#34198=CARTESIAN_POINT('Ctrl Pts',(95.8757872479501,1.34162793846799,-3.50296596779655));
#34199=CARTESIAN_POINT('Ctrl Pts',(95.8250278896126,1.31950654678581,-3.49996378654879));
#34200=CARTESIAN_POINT('Ctrl Pts',(95.7755407678742,1.29450709314496,-3.49696160530104));
#34201=CARTESIAN_POINT('Ctrl Pts',(95.7276625122829,1.26681071512748,-3.49395942405328));
#34202=CARTESIAN_POINT('Ctrl Pts',(95.6797624635725,1.23910173033355,-3.49095587627927));
#34203=CARTESIAN_POINT('Ctrl Pts',(95.6334731830045,1.20869366453128,-3.48795232850525));
#34204=CARTESIAN_POINT('Ctrl Pts',(95.5891028417432,1.17581139779641,-3.48494878073123));
#34205=CARTESIAN_POINT('Ctrl Pts',(95.54464875893,1.14286707131694,-3.48193956426627));
#34206=CARTESIAN_POINT('Ctrl Pts',(95.5021212570437,1.10743955443111,-3.4789303478013));
#34207=CARTESIAN_POINT('Ctrl Pts',(95.4617949876454,1.06979371817218,-3.47592113133634));
#34208=CARTESIAN_POINT('Ctrl Pts',(95.4309437388545,1.04099311058575,-3.4736189574132));
#34209=CARTESIAN_POINT('Ctrl Pts',(95.4013801595763,1.01089498991828,-3.47131678349007));
#34210=CARTESIAN_POINT('Ctrl Pts',(95.3732113452109,0.979631082306743,-3.46901460956693));
#34211=CARTESIAN_POINT('Ctrl Pts',(95.3363801767998,0.938753030732131,-3.46600448090569));
#34212=CARTESIAN_POINT('Ctrl Pts',(95.3017801642556,0.89570909109196,-3.46299435224445));
#34213=CARTESIAN_POINT('Ctrl Pts',(95.2696751288506,0.850772441563674,-3.45998422358322));
#34214=CARTESIAN_POINT('Ctrl Pts',(95.2376271531398,0.805915657123372,-3.45697944476877));
#34215=CARTESIAN_POINT('Ctrl Pts',(95.20806565924,0.759173264671544,-3.45397466595433));
#34216=CARTESIAN_POINT('Ctrl Pts',(95.1812151137463,0.710852425807484,-3.45096988713989));
#34217=CARTESIAN_POINT('Ctrl Pts',(95.1543911324189,0.662579392407994,-3.44796808105627));
#34218=CARTESIAN_POINT('Ctrl Pts',(95.1302730417724,0.612731465437158,-3.44496627497265));
#34219=CARTESIAN_POINT('Ctrl Pts',(95.1090417072327,0.561644215007995,-3.44196446888903));
#34220=CARTESIAN_POINT('Ctrl Pts',(95.0878229917177,0.510587328721379,-3.43896444695443));
#34221=CARTESIAN_POINT('Ctrl Pts',(95.0694878338139,0.458293065675287,-3.43596442501983));
#34222=CARTESIAN_POINT('Ctrl Pts',(95.0541698450105,0.405118904980973,-3.43296440308523));
#34223=CARTESIAN_POINT('Ctrl Pts',(95.0388549107067,0.351955347535718,-3.42996497937314));
#34224=CARTESIAN_POINT('Ctrl Pts',(95.0265560967773,0.297912748086633,-3.42696555566105));
#34225=CARTESIAN_POINT('Ctrl Pts',(95.0173571006733,0.24336352792737,-3.42396613194896));
#34226=CARTESIAN_POINT('Ctrl Pts',(95.0081496474247,0.188764157661057,-3.4209639507012));
#34227=CARTESIAN_POINT('Ctrl Pts',(95.0020477936072,0.133657758030095,-3.41796176945344));
#34228=CARTESIAN_POINT('Ctrl Pts',(94.9990837646842,0.0784252382043858,
-3.41495958820568));
#34229=CARTESIAN_POINT('Ctrl Pts',(94.9961183866011,0.0231675777617289,
-3.41195604043166));
#34230=CARTESIAN_POINT('Ctrl Pts',(94.9962936788924,-0.0322157882785609,
-3.40895249265764));
#34231=CARTESIAN_POINT('Ctrl Pts',(94.9995896819569,-0.0873438846820572,
-3.40594894488362));
#34232=CARTESIAN_POINT('Ctrl Pts',(95.0028919056725,-0.142576026089837,
-3.40293972841866));
#34233=CARTESIAN_POINT('Ctrl Pts',(95.0093265444389,-0.19755140961134,-3.39993051195369));
#34234=CARTESIAN_POINT('Ctrl Pts',(95.018821830172,-0.251895282679696,-3.39692129548872));
#34235=CARTESIAN_POINT('Ctrl Pts',(95.0260861129053,-0.2934705727646,-3.39461912156561));
#34236=CARTESIAN_POINT('Ctrl Pts',(95.0351406753307,-0.334676361031573,
-3.39231694764249));
#34237=CARTESIAN_POINT('Ctrl Pts',(95.0459337097695,-0.375350977556801,
-3.39001477371937));
#34238=CARTESIAN_POINT('Ctrl Pts',(95.0600457722768,-0.428533679244961,
-3.38700464505813));
#34239=CARTESIAN_POINT('Ctrl Pts',(95.0771909191365,-0.481031160584242,
-3.38399451639689));
#34240=CARTESIAN_POINT('Ctrl Pts',(95.0972845071804,-0.532473200675086,
-3.38098438773565));
#34241=CARTESIAN_POINT('Ctrl Pts',(95.1173423832566,-0.583823813765898,
-3.37797960892121));
#34242=CARTESIAN_POINT('Ctrl Pts',(95.1403381106903,-0.634122220236709,
-3.37497483010676));
#34243=CARTESIAN_POINT('Ctrl Pts',(95.1661370810418,-0.683012591381184,
-3.37197005129231));
#34244=CARTESIAN_POINT('Ctrl Pts',(95.1919105275863,-0.731854593603253,
-3.36896824520869));
#34245=CARTESIAN_POINT('Ctrl Pts',(95.2204814779276,-0.779290855221575,
-3.36596643912507));
#34246=CARTESIAN_POINT('Ctrl Pts',(95.2516677072236,-0.824986542381811,
-3.36296463304145));
#34247=CARTESIAN_POINT('Ctrl Pts',(95.2828354007185,-0.870655069921066,
-3.35996461110685));
#34248=CARTESIAN_POINT('Ctrl Pts',(95.31661499511,-0.914584638159802,-3.35696458917225));
#34249=CARTESIAN_POINT('Ctrl Pts',(95.3527800968148,-0.956468018696854,
-3.35396456723765));
#34250=CARTESIAN_POINT('Ctrl Pts',(95.3889379869797,-0.998343047434655,
-3.35096514352556));
#34251=CARTESIAN_POINT('Ctrl Pts',(95.4274800948128,-1.03817229928642,-3.34796571981346));
#34252=CARTESIAN_POINT('Ctrl Pts',(95.4681402394164,-1.07568218585139,-3.34496629610137));
#34253=CARTESIAN_POINT('Ctrl Pts',(95.5088377651339,-1.11322655732413,-3.34196411485361));
#34254=CARTESIAN_POINT('Ctrl Pts',(95.5516568289275,-1.14844694454707,-3.33896193360585));
#34255=CARTESIAN_POINT('Ctrl Pts',(95.5962960169831,-1.18110823055201,-3.33595975235809));
#34256=CARTESIAN_POINT('Ctrl Pts',(95.6409555238062,-1.21378438324931,-3.33295620458407));
#34257=CARTESIAN_POINT('Ctrl Pts',(95.6874363624139,-1.24389882502842,-3.32995265681005));
#34258=CARTESIAN_POINT('Ctrl Pts',(95.7354085499465,-1.27126010922002,-3.32694910903603));
#34259=CARTESIAN_POINT('Ctrl Pts',(95.7834712769097,-1.2986730332308,-3.32393989257106));
#34260=CARTESIAN_POINT('Ctrl Pts',(95.8330305015201,-1.32332218383296,-3.32093067610609));
#34261=CARTESIAN_POINT('Ctrl Pts',(95.8837331446179,-1.34506290539695,-3.31792145964112));
#34262=CARTESIAN_POINT('Ctrl Pts',(95.9225227445457,-1.36169544839836,-3.31561928571802));
#34263=CARTESIAN_POINT('Ctrl Pts',(95.9619810785525,-1.37662668963317,-3.31331711179491));
#34264=CARTESIAN_POINT('Ctrl Pts',(96.0019444362136,-1.38981168361493,-3.3110149378718));
#34265=CARTESIAN_POINT('Ctrl Pts',(96.0541971557357,-1.40705127089561,-3.30800480921057));
#34266=CARTESIAN_POINT('Ctrl Pts',(96.1075332501576,-1.42137616669331,-3.30499468054933));
#34267=CARTESIAN_POINT('Ctrl Pts',(96.1615964008176,-1.43265497469311,-3.30198455188809));
#34268=CARTESIAN_POINT('Ctrl Pts',(96.2155634660256,-1.44391373707307,-3.29897977307365));
#34269=CARTESIAN_POINT('Ctrl Pts',(96.2702545103201,-1.45213704830828,-3.29597499425921));
#34270=CARTESIAN_POINT('Ctrl Pts',(96.3252979680604,-1.45724322318146,-3.29297021544476));
#34271=CARTESIAN_POINT('Ctrl Pts',(96.3802869694184,-1.46234434634055,-3.28996840936115));
#34272=CARTESIAN_POINT('Ctrl Pts',(96.4356271702808,-1.46433439363331,-3.28696660327753));
#34273=CARTESIAN_POINT('Ctrl Pts',(96.4909385713449,-1.46318303136561,-3.28396479719391));
#34274=CARTESIAN_POINT('Ctrl Pts',(96.5462170976066,-1.46203235341987,-3.28096477525931));
#34275=CARTESIAN_POINT('Ctrl Pts',(96.6014663310501,-1.45774397764402,-3.27796475332471));
#34276=CARTESIAN_POINT('Ctrl Pts',(96.6563052590559,-1.45033964636464,-3.27496473139011));
#34277=CARTESIAN_POINT('Ctrl Pts',(96.711133251848,-1.44293679155368,-3.27196530767802));
#34278=CARTESIAN_POINT('Ctrl Pts',(96.7655505786146,-1.43241928581969,-3.26896588396593));
#34279=CARTESIAN_POINT('Ctrl Pts',(96.8191826615094,-1.41886057519997,-3.26596646025384));
#34280=CARTESIAN_POINT('Ctrl Pts',(96.8728640513364,-1.40528939930967,-3.26296427900608));
#34281=CARTESIAN_POINT('Ctrl Pts',(96.9257582418854,-1.38867156231267,-3.25996209775832));
#34282=CARTESIAN_POINT('Ctrl Pts',(96.977503625043,-1.36913103940199,-3.25695991651056));
#34283=CARTESIAN_POINT('Ctrl Pts',(97.0292725615504,-1.34958162207904,-3.25395636873654));
#34284=CARTESIAN_POINT('Ctrl Pts',(97.0798911647579,-1.32710708157964,-3.25095282096253));
#34285=CARTESIAN_POINT('Ctrl Pts',(97.1290187915884,-1.30187918172107,-3.24794927318851));
#34286=CARTESIAN_POINT('Ctrl Pts',(97.1782391385467,-1.2766036684472,-3.24494005672354));
#34287=CARTESIAN_POINT('Ctrl Pts',(97.2259624313338,-1.24856468317768,-3.24193084025858));
#34288=CARTESIAN_POINT('Ctrl Pts',(97.2718745959,-1.21797889994313,-3.23892162379361));
#34289=CARTESIAN_POINT('Ctrl Pts',(97.3069992834222,-1.19457952226435,-3.23661944987049));
#34290=CARTESIAN_POINT('Ctrl Pts',(97.3410644786033,-1.16969047719024,-3.23431727594736));
#34291=CARTESIAN_POINT('Ctrl Pts',(97.3739430876555,-1.1434243185699,-3.23201510202424));
#34292=CARTESIAN_POINT('Ctrl Pts',(97.4164069259365,-1.10950068420493,-3.22904176635146));
#34293=CARTESIAN_POINT('Ctrl Pts',(97.4570782501623,-1.07312835567167,-3.22606843067869));
#34294=CARTESIAN_POINT('Ctrl Pts',(97.4956562800578,-1.03452611623096,-3.22309509500591));
#34295=CARTESIAN_POINT('Ctrl Pts',(97.5341692430004,-0.995988984575801,
-3.22012677425725));
#34296=CARTESIAN_POINT('Ctrl Pts',(97.5705955300688,-0.955229777234613,
-3.21715845350858));
#34297=CARTESIAN_POINT('Ctrl Pts',(97.604667165064,-0.912507618757003,-3.21419013275992));
#34298=CARTESIAN_POINT('Ctrl Pts',(97.6387056440851,-0.869827034297733,
-3.21122470055962));
#34299=CARTESIAN_POINT('Ctrl Pts',(97.6703936701961,-0.825187701695912,
-3.20825926835933));
#34300=CARTESIAN_POINT('Ctrl Pts',(97.699501443502,-0.778884115664169,-3.20529383615903));
#34301=CARTESIAN_POINT('Ctrl Pts',(97.7285930751017,-0.732606207270699,
-3.20233004843818));
#34302=CARTESIAN_POINT('Ctrl Pts',(97.755107000612,-0.684666332170437,-3.19936626071733));
#34303=CARTESIAN_POINT('Ctrl Pts',(97.7788564003111,-0.635388401610821,
-3.19640247299648));
#34304=CARTESIAN_POINT('Ctrl Pts',(97.8027273163715,-0.58585833521259,-3.19342352073657));
#34305=CARTESIAN_POINT('Ctrl Pts',(97.8238050598094,-0.534976961069053,
-3.19044456847667));
#34306=CARTESIAN_POINT('Ctrl Pts',(97.8419475559497,-0.483096538465318,
-3.18746561621676));
#34307=CARTESIAN_POINT('Ctrl Pts',(97.8600104555927,-0.431443730622092,
-3.18449973350162));
#34308=CARTESIAN_POINT('Ctrl Pts',(97.8751636881653,-0.378801157440791,
-3.18153385078646));
#34309=CARTESIAN_POINT('Ctrl Pts',(97.8873170410266,-0.325531900336655,
-3.17856796807132));
#34310=CARTESIAN_POINT('Ctrl Pts',(97.8995507268635,-0.271910536453492,
-3.17558248103903));
#34311=CARTESIAN_POINT('Ctrl Pts',(97.9087446207047,-0.217654719128803,
-3.17259699400675));
#34312=CARTESIAN_POINT('Ctrl Pts',(97.9148594487037,-0.163142365061595,
-3.16961150697446));
#34313=CARTESIAN_POINT('Ctrl Pts',(97.9209742767027,-0.108630010994388,
-3.16662601994218));
#34314=CARTESIAN_POINT('Ctrl Pts',(97.9240100677082,-0.0538616766468094,
-3.16364053290989));
#34315=CARTESIAN_POINT('Ctrl Pts',(97.9239807388017,0.000785454740996269,
-3.16065504587761));
#34316=CARTESIAN_POINT('Ctrl Pts',(97.9239807053004,0.000845575209102073,
-3.08934495419159));
#34317=CARTESIAN_POINT('Ctrl Pts',(97.9240121116984,-0.0535118081674962,
-3.0923139135121));
#34318=CARTESIAN_POINT('Ctrl Pts',(97.9210108565796,-0.107988214502587,
-3.09528287283261));
#34319=CARTESIAN_POINT('Ctrl Pts',(97.9149634846939,-0.162212222227354,
-3.09825183215312));
#34320=CARTESIAN_POINT('Ctrl Pts',(97.9089235593934,-0.216369459840959,
-3.10121713557006));
#34321=CARTESIAN_POINT('Ctrl Pts',(97.8998449981556,-0.270274378405412,
-3.10418243898699));
#34322=CARTESIAN_POINT('Ctrl Pts',(97.887766341459,-0.323556270407781,-3.10714774240393));
#34323=CARTESIAN_POINT('Ctrl Pts',(97.8756974888544,-0.376794914176668,
-3.11011063892183));
#34324=CARTESIAN_POINT('Ctrl Pts',(97.8606334808327,-0.429411004759582,
-3.11307353543973));
#34325=CARTESIAN_POINT('Ctrl Pts',(97.8426642475837,-0.481042181841941,
-3.11603643195763));
#34326=CARTESIAN_POINT('Ctrl Pts',(97.8247020604722,-0.532653113187079,
-3.11899816665765));
#34327=CARTESIAN_POINT('Ctrl Pts',(97.8038370841483,-0.583279384134176,
-3.12195990135768));
#34328=CARTESIAN_POINT('Ctrl Pts',(97.780208886654,-0.63257443996624,-3.1249216360577));
#34329=CARTESIAN_POINT('Ctrl Pts',(97.7565628657859,-0.681906680361391,
-3.12788560487247));
#34330=CARTESIAN_POINT('Ctrl Pts',(97.7301496885838,-0.729905205756458,
-3.13084957368724));
#34331=CARTESIAN_POINT('Ctrl Pts',(97.7011561263692,-0.776245679982617,
-3.133813542502));
#34332=CARTESIAN_POINT('Ctrl Pts',(97.6721530801836,-0.822601312460516,
-3.13677848084904));
#34333=CARTESIAN_POINT('Ctrl Pts',(97.6405682784201,-0.867297366750257,
-3.13974341919608));
#34334=CARTESIAN_POINT('Ctrl Pts',(97.6066314129966,-0.910039210805195,
-3.14270835754312));
#34335=CARTESIAN_POINT('Ctrl Pts',(97.5726295608355,-0.952862902519668,
-3.14567897354095));
#34336=CARTESIAN_POINT('Ctrl Pts',(97.5362670075506,-0.99372449954857,-3.14864958953877));
#34337=CARTESIAN_POINT('Ctrl Pts',(97.497812431789,-1.03236410534844,-3.1516202055366));
#34338=CARTESIAN_POINT('Ctrl Pts',(97.4616819967994,-1.06866838741961,-3.15441128165856));
#34339=CARTESIAN_POINT('Ctrl Pts',(97.4237054074271,-1.10301125847572,-3.15720235778053));
#34340=CARTESIAN_POINT('Ctrl Pts',(97.3841308561572,-1.13521059723489,-3.15999343390249));
#34341=CARTESIAN_POINT('Ctrl Pts',(97.3414503681205,-1.16993704260454,-3.16300356256373));
#34342=CARTESIAN_POINT('Ctrl Pts',(97.2967190667783,-1.20232611928244,-3.16601369122497));
#34343=CARTESIAN_POINT('Ctrl Pts',(97.2502230660361,-1.23212809378356,-3.16902381988621));
#34344=CARTESIAN_POINT('Ctrl Pts',(97.2038097017883,-1.2618771017787,-3.17202859870065));
#34345=CARTESIAN_POINT('Ctrl Pts',(97.1556383033114,-1.28904784969789,-3.1750333775151));
#34346=CARTESIAN_POINT('Ctrl Pts',(97.1060269435155,-1.31343161973127,-3.17803815632954));
#34347=CARTESIAN_POINT('Ctrl Pts',(97.0564646659408,-1.33779126606395,-3.18103996241316));
#34348=CARTESIAN_POINT('Ctrl Pts',(97.00546572075,-1.35936916469082,-3.18404176849678));
#34349=CARTESIAN_POINT('Ctrl Pts',(96.9533743582289,-1.37800157391331,-3.1870435745804));
#34350=CARTESIAN_POINT('Ctrl Pts',(96.9013139566528,-1.39662290880462,-3.190043596515));
#34351=CARTESIAN_POINT('Ctrl Pts',(96.8481629209475,-1.41230204673818,-3.1930436184496));
#34352=CARTESIAN_POINT('Ctrl Pts',(96.7942850036013,-1.42492354304256,-3.1960436403842));
#34353=CARTESIAN_POINT('Ctrl Pts',(96.7404178298375,-1.43754252254429,-3.19904306409629));
#34354=CARTESIAN_POINT('Ctrl Pts',(96.6858245761938,-1.44710495089075,-3.20204248780838));
#34355=CARTESIAN_POINT('Ctrl Pts',(96.6308814054568,-1.4535459864194,-3.20504191152047));
#34356=CARTESIAN_POINT('Ctrl Pts',(96.5758877224324,-1.4599929435473,-3.20804409276823));
#34357=CARTESIAN_POINT('Ctrl Pts',(96.520544005255,-1.4633127130099,-3.21104627401599));
#34358=CARTESIAN_POINT('Ctrl Pts',(96.4652323024529,-1.46349228718359,-3.21404845526375));
#34359=CARTESIAN_POINT('Ctrl Pts',(96.4098954229915,-1.46367194309546,-3.21705200303776));
#34360=CARTESIAN_POINT('Ctrl Pts',(96.3545911152333,-1.46070858272002,-3.22005555081178));
#34361=CARTESIAN_POINT('Ctrl Pts',(96.2996988664161,-1.45464132064727,-3.2230590985858));
#34362=CARTESIAN_POINT('Ctrl Pts',(96.2447030177171,-1.44856260763843,-3.22606831505077));
#34363=CARTESIAN_POINT('Ctrl Pts',(96.1901213035764,-1.43936837842356,-3.22907753151573));
#34364=CARTESIAN_POINT('Ctrl Pts',(96.1363243881436,-1.42714917709386,-3.2320867479807));
#34365=CARTESIAN_POINT('Ctrl Pts',(96.095167543066,-1.41780098729428,-3.23438892190381));
#34366=CARTESIAN_POINT('Ctrl Pts',(96.0544698633411,-1.40668339077257,-3.23669109582693));
#34367=CARTESIAN_POINT('Ctrl Pts',(96.0143902056032,-1.39385626882433,-3.23899326975004));
#34368=CARTESIAN_POINT('Ctrl Pts',(95.9619854218993,-1.37708460486363,-3.24200339841128));
#34369=CARTESIAN_POINT('Ctrl Pts',(95.9104176910409,-1.35731820048868,-3.24501352707252));
#34370=CARTESIAN_POINT('Ctrl Pts',(95.8600525030574,-1.33466023039948,-3.24802365573375));
#34371=CARTESIAN_POINT('Ctrl Pts',(95.8097768282042,-1.31204252990746,-3.25102843454819));
#34372=CARTESIAN_POINT('Ctrl Pts',(95.7606999325518,-1.28654367725042,-3.25403321336264));
#34373=CARTESIAN_POINT('Ctrl Pts',(95.7131704166725,-1.2583160244589,-3.25703799217708));
#34374=CARTESIAN_POINT('Ctrl Pts',(95.6656879233748,-1.23011629825322,-3.2600397982607));
#34375=CARTESIAN_POINT('Ctrl Pts',(95.6197502291,-1.19919338822771,-3.26304160434432));
#34376=CARTESIAN_POINT('Ctrl Pts',(95.5756825689323,-1.16574614544013,-3.26604341042795));
#34377=CARTESIAN_POINT('Ctrl Pts',(95.5316411007539,-1.13231878230631,-3.26904343236254));
#34378=CARTESIAN_POINT('Ctrl Pts',(95.4894678835039,-1.09637037886921,-3.27204345429714));
#34379=CARTESIAN_POINT('Ctrl Pts',(95.4494583581334,-1.05814250911235,-3.27504347623174));
#34380=CARTESIAN_POINT('Ctrl Pts',(95.409456810904,-1.0199222622238,-3.27804289994383));
#34381=CARTESIAN_POINT('Ctrl Pts',(95.3716184803319,-0.979423816342476,
-3.28104232365592));
#34382=CARTESIAN_POINT('Ctrl Pts',(95.3362032069245,-0.936926788696039,
-3.28404174736801));
#34383=CARTESIAN_POINT('Ctrl Pts',(95.3007553743028,-0.894390691187924,
-3.28704392861577));
#34384=CARTESIAN_POINT('Ctrl Pts',(95.2677353882254,-0.849852747592058,
-3.29004610986353));
#34385=CARTESIAN_POINT('Ctrl Pts',(95.2373628927433,-0.803625826518439,
-3.29304829111129));
#34386=CARTESIAN_POINT('Ctrl Pts',(95.2069765723756,-0.757377863976506,
-3.29605183888531));
#34387=CARTESIAN_POINT('Ctrl Pts',(95.1792404097869,-0.70943984935139,-3.29905538665933));
#34388=CARTESIAN_POINT('Ctrl Pts',(95.1543289957927,-0.660150985476428,
-3.30205893443335));
#34389=CARTESIAN_POINT('Ctrl Pts',(95.129370565697,-0.610769097165899,-3.30506815089832));
#34390=CARTESIAN_POINT('Ctrl Pts',(95.1072477457684,-0.560031751868807,
-3.30807736736329));
#34391=CARTESIAN_POINT('Ctrl Pts',(95.0880872323301,-0.508298863722103,
-3.31108658382825));
#34392=CARTESIAN_POINT('Ctrl Pts',(95.0734286542899,-0.468721084108807,
-3.31338875775137));
#34393=CARTESIAN_POINT('Ctrl Pts',(95.0605028881457,-0.428561070948869,
-3.3156909316745));
#34394=CARTESIAN_POINT('Ctrl Pts',(95.0493465803421,-0.387984589853703,
-3.31799310559762));
#34395=CARTESIAN_POINT('Ctrl Pts',(95.0347595321891,-0.334930201785944,
-3.32100323425886));
#34396=CARTESIAN_POINT('Ctrl Pts',(95.023138022119,-0.280940553597613,-3.32401336292009));
#34397=CARTESIAN_POINT('Ctrl Pts',(95.0145953408613,-0.226378127275874,
-3.32702349158133));
#34398=CARTESIAN_POINT('Ctrl Pts',(95.0060678423553,-0.171912673759762,
-3.33002827039578));
#34399=CARTESIAN_POINT('Ctrl Pts',(95.0006083945771,-0.116876979854245,
-3.33303304921022));
#34400=CARTESIAN_POINT('Ctrl Pts',(94.9982798725851,-0.0616462524720104,
-3.33603782802466));
#34401=CARTESIAN_POINT('Ctrl Pts',(94.9959536542799,-0.00647016674420076,
-3.33903963410828));
#34402=CARTESIAN_POINT('Ctrl Pts',(94.9967522478346,0.0489000451757762,
-3.34204144019191));
#34403=CARTESIAN_POINT('Ctrl Pts',(95.0006868173097,0.104083338714638,-3.34504324627553));
#34404=CARTESIAN_POINT('Ctrl Pts',(95.0046190482399,0.15923383359278,-3.34804326821013));
#34405=CARTESIAN_POINT('Ctrl Pts',(95.011683523246,0.214197104563301,-3.35104329014472));
#34406=CARTESIAN_POINT('Ctrl Pts',(95.0218393453912,0.268593716802291,-3.35404331207932));
#34407=CARTESIAN_POINT('Ctrl Pts',(95.031993142404,0.3229794820279,-3.35704273579141));
#34408=CARTESIAN_POINT('Ctrl Pts',(95.0452369654758,0.376798294070868,-3.36004215950349));
#34409=CARTESIAN_POINT('Ctrl Pts',(95.0614786034864,0.429679747757636,-3.36304158321558));
#34410=CARTESIAN_POINT('Ctrl Pts',(95.0777351733308,0.482609818281835,-3.36604376446333));
#34411=CARTESIAN_POINT('Ctrl Pts',(95.0969949089703,0.534600302828475,-3.36904594571109));
#34412=CARTESIAN_POINT('Ctrl Pts',(95.119115787171,0.585296293413356,-3.37204812695885));
#34413=CARTESIAN_POINT('Ctrl Pts',(95.1412467343044,0.636015359687777,-3.37505167473287));
#34414=CARTESIAN_POINT('Ctrl Pts',(95.1662411813487,0.6854382853224,-3.37805522250689));
#34415=CARTESIAN_POINT('Ctrl Pts',(95.1939104325383,0.733233506714116,-3.38105877028091));
#34416=CARTESIAN_POINT('Ctrl Pts',(95.2216319047829,0.781118933542593,-3.38406798674587));
#34417=CARTESIAN_POINT('Ctrl Pts',(95.2520379749969,0.827370076917965,-3.38707720321084));
#34418=CARTESIAN_POINT('Ctrl Pts',(95.2848964317778,0.871684169588323,-3.3900864196758));
#34419=CARTESIAN_POINT('Ctrl Pts',(95.3100344978611,0.905586266616025,-3.39238859359893));
#34420=CARTESIAN_POINT('Ctrl Pts',(95.3366070018268,0.938355217170115,-3.39469076752205));
#34421=CARTESIAN_POINT('Ctrl Pts',(95.3644951339879,0.969869755187488,-3.39699294144517));
#34422=CARTESIAN_POINT('Ctrl Pts',(95.4009593059964,1.01107550996512,-3.40000307010641));
#34423=CARTESIAN_POINT('Ctrl Pts',(95.4398271418934,1.05030856924532,-3.40301319876765));
#34424=CARTESIAN_POINT('Ctrl Pts',(95.4808569548691,1.08727599025845,-3.40602332742889));
#34425=CARTESIAN_POINT('Ctrl Pts',(95.5218138463062,1.12417770974817,-3.40902810624333));
#34426=CARTESIAN_POINT('Ctrl Pts',(95.5649247002899,1.15882143129332,-3.41203288505777));
#34427=CARTESIAN_POINT('Ctrl Pts',(95.6099096256182,1.1909494837561,-3.41503766387222));
#34428=CARTESIAN_POINT('Ctrl Pts',(95.6548500458156,1.2230457508337,-3.41803946995583));
#34429=CARTESIAN_POINT('Ctrl Pts',(95.7016604368568,1.25263097367015,-3.42104127603945));
#34430=CARTESIAN_POINT('Ctrl Pts',(95.7500277636557,1.2794876008052,-3.42404308212307));
#34431=CARTESIAN_POINT('Ctrl Pts',(95.7983663429219,1.30632826547513,-3.42704310405767));
#34432=CARTESIAN_POINT('Ctrl Pts',(95.8482595629937,1.33044329302549,-3.43004312599227));
#34433=CARTESIAN_POINT('Ctrl Pts',(95.8993672910688,1.35165961404323,-3.43304314792687));
#34434=CARTESIAN_POINT('Ctrl Pts',(95.9504648279539,1.3728717043983,-3.43604257163895));
#34435=CARTESIAN_POINT('Ctrl Pts',(96.0027759043986,1.39118603377389,-3.43904199535104));
#34436=CARTESIAN_POINT('Ctrl Pts',(96.0559399123072,1.40647744353213,-3.44204141906313));
#34437=CARTESIAN_POINT('Ctrl Pts',(96.1091527968208,1.42178291152683,-3.44504360031089));
#34438=CARTESIAN_POINT('Ctrl Pts',(96.1632196707923,1.43405976125441,-3.44804578155864));
#34439=CARTESIAN_POINT('Ctrl Pts',(96.217765688296,1.4432330206662,-3.4510479628064));
#34440=CARTESIAN_POINT('Ctrl Pts',(96.272336533936,1.45241045554205,-3.45405151058041));
#34441=CARTESIAN_POINT('Ctrl Pts',(96.3273864320175,1.45848142601984,-3.45705505835442));
#34442=CARTESIAN_POINT('Ctrl Pts',(96.382534586474,1.46142280483062,-3.46005860612844));
#34443=CARTESIAN_POINT('Ctrl Pts',(96.437786823791,1.46436973499891,-3.4630678225934));
#34444=CARTESIAN_POINT('Ctrl Pts',(96.4931371585245,1.4641752760542,-3.46607703905837));
#34445=CARTESIAN_POINT('Ctrl Pts',(96.5482051355539,1.46086848045767,-3.46908625552334));
#34446=CARTESIAN_POINT('Ctrl Pts',(96.5903343948453,1.45833864630313,-3.47138842944647));
#34447=CARTESIAN_POINT('Ctrl Pts',(96.6322983846968,1.45398828503215,-3.47369060336961));
#34448=CARTESIAN_POINT('Ctrl Pts',(96.6739306243701,1.44785064365449,-3.47599277729274));
#34449=CARTESIAN_POINT('Ctrl Pts',(96.7283654334054,1.43982558089201,-3.47900290595397));
#34450=CARTESIAN_POINT('Ctrl Pts',(96.7824614093834,1.42870951185747,-3.48201303461521));
#34451=CARTESIAN_POINT('Ctrl Pts',(96.8358411481265,1.41454479297931,-3.48502316327644));
#34452=CARTESIAN_POINT('Ctrl Pts',(96.8891260160331,1.40040524879775,-3.48802794209089));
#34453=CARTESIAN_POINT('Ctrl Pts',(96.9416966665717,1.38322794180103,-3.49103272090533));
#34454=CARTESIAN_POINT('Ctrl Pts',(96.9931843617755,1.36310649790546,-3.49403749971977));
#34455=CARTESIAN_POINT('Ctrl Pts',(97.044621118435,1.34300496084503,-3.49703930580339));
#34456=CARTESIAN_POINT('Ctrl Pts',(97.0949765526913,1.31996524816049,-3.50004111188701));
#34457=CARTESIAN_POINT('Ctrl Pts',(97.1438974181991,1.29413066589739,-3.50304291797063));
#34458=CARTESIAN_POINT('Ctrl Pts',(97.1927892071738,1.26831143863836,-3.50604293990523));
#34459=CARTESIAN_POINT('Ctrl Pts',(97.2402476513393,1.23970088044227,-3.50904296183983));
#34460=CARTESIAN_POINT('Ctrl Pts',(97.2859419531762,1.20848929723727,-3.51204298377443));
#34461=CARTESIAN_POINT('Ctrl Pts',(97.3316271432932,1.17728393781056,-3.51504240748653));
#34462=CARTESIAN_POINT('Ctrl Pts',(97.3755484538541,1.14347888111908,-3.51804183119863));
#34463=CARTESIAN_POINT('Ctrl Pts',(97.4174040262834,1.10730775995957,-3.52104125491073));
#34464=CARTESIAN_POINT('Ctrl Pts',(97.4592980788492,1.07110338469324,-3.52404343615849));
#34465=CARTESIAN_POINT('Ctrl Pts',(97.4991221985946,1.03252894514053,-3.52704561740625));
#34466=CARTESIAN_POINT('Ctrl Pts',(97.5366087800687,0.991857420419461,-3.53004779865401));
#34467=CARTESIAN_POINT('Ctrl Pts',(97.5741124246027,0.951167382923171,-3.53305134642803));
#34468=CARTESIAN_POINT('Ctrl Pts',(97.6092760739727,0.908378766162039,-3.53605489420205));
#34469=CARTESIAN_POINT('Ctrl Pts',(97.6418722929925,0.863797860441228,-3.53905844197608));
#34470=CARTESIAN_POINT('Ctrl Pts',(97.6745300318901,0.81913281576358,-3.54206765844104));
#34471=CARTESIAN_POINT('Ctrl Pts',(97.7046103729047,0.772669169180129,-3.54507687490601));
#34472=CARTESIAN_POINT('Ctrl Pts',(97.7319297690702,0.72474143624424,-3.54808609137097));
#34473=CARTESIAN_POINT('Ctrl Pts',(97.7528302267739,0.688074756314997,-3.55038826529408));
#34474=CARTESIAN_POINT('Ctrl Pts',(97.7721156414486,0.650551765119928,-3.55269043921719));
#34475=CARTESIAN_POINT('Ctrl Pts',(97.7897228939381,0.612330060793356,-3.5549926131403));
#34476=CARTESIAN_POINT('Ctrl Pts',(97.8147040021358,0.558101240490146,-3.55825892944363));
#34477=CARTESIAN_POINT('Ctrl Pts',(97.8363970660602,0.502267217142413,-3.56152524574696));
#34478=CARTESIAN_POINT('Ctrl Pts',(97.8546129689978,0.445228213869789,-3.56479156205029));
#34479=CARTESIAN_POINT('Ctrl Pts',(97.8727780892455,0.388348225169438,-3.56804877244609));
#34480=CARTESIAN_POINT('Ctrl Pts',(97.8874852156449,0.330270297420546,-3.57130598284188));
#34481=CARTESIAN_POINT('Ctrl Pts',(97.898593061022,0.271414452296158,-3.57456319323767));
#34482=CARTESIAN_POINT('Ctrl Pts',(97.9096536738433,0.212808872808053,-3.57780655338919));
#34483=CARTESIAN_POINT('Ctrl Pts',(97.9171454033261,0.153432332319883,-3.5810499135407));
#34484=CARTESIAN_POINT('Ctrl Pts',(97.9209772034918,0.0937173532535882,
-3.58429327369221));
#34485=CARTESIAN_POINT('Ctrl Pts',(97.9229666042936,0.0627144245782946,
-3.58597716716447));
#34486=CARTESIAN_POINT('Ctrl Pts',(97.9239702826564,0.0316205307435951,
-3.58766106063673));
#34487=CARTESIAN_POINT('Ctrl Pts',(97.9239808649782,0.000497614912986743,
-3.58934495410898));
#34488=CARTESIAN_POINT('Origin',(96.460480949577,-8.32667268468867E-16,
1.18130019239114E-14));
#34489=CARTESIAN_POINT('',(97.9239803682192,-0.00130446693377829,-4.16065504588301));
#34490=CARTESIAN_POINT('',(97.9239803685999,-0.00130403978581263,-4.08934495418713));
#34491=CARTESIAN_POINT('',(97.923980949577,-1.01189432752408E-15,1.19922289829666E-14));
#34492=CARTESIAN_POINT('Ctrl Pts',(97.9239803682198,-0.00130446619604857,
-4.1606550458429));
#34493=CARTESIAN_POINT('Ctrl Pts',(97.9240290145792,0.0532725852280853,
-4.15768779896672));
#34494=CARTESIAN_POINT('Ctrl Pts',(97.921020447974,0.107929002943695,-4.15472055209055));
#34495=CARTESIAN_POINT('Ctrl Pts',(97.914954670438,0.162291236130919,-4.15175330521438));
#34496=CARTESIAN_POINT('Ctrl Pts',(97.9088930972105,0.216615789794604,-4.14878811499485));
#34497=CARTESIAN_POINT('Ctrl Pts',(97.8997785687796,0.270646025560744,-4.14582292477533));
#34498=CARTESIAN_POINT('Ctrl Pts',(97.8876630704609,0.324011487187377,-4.14285773455581));
#34499=CARTESIAN_POINT('Ctrl Pts',(97.8755509065509,0.377362261654151,-4.13989336041135));
#34500=CARTESIAN_POINT('Ctrl Pts',(97.8604395308884,0.430048096798754,-4.1369289862669));
#34501=CARTESIAN_POINT('Ctrl Pts',(97.8424319199135,0.481709212685351,-4.13396461212244));
#34502=CARTESIAN_POINT('Ctrl Pts',(97.824409016481,0.533414200323036,-4.13099772056654));
#34503=CARTESIAN_POINT('Ctrl Pts',(97.8034851423599,0.584092217259106,-4.12803082901064));
#34504=CARTESIAN_POINT('Ctrl Pts',(97.7798124814009,0.633400788707461,-4.12506393745474));
#34505=CARTESIAN_POINT('Ctrl Pts',(97.7561296712694,0.682730500203988,-4.12209577390436));
#34506=CARTESIAN_POINT('Ctrl Pts',(97.729695989229,0.73068912166178,-4.11912761035398));
#34507=CARTESIAN_POINT('Ctrl Pts',(97.7007093301368,0.776959338739193,-4.11615944680361));
#34508=CARTESIAN_POINT('Ctrl Pts',(97.6716690716219,0.823315114380496,-4.11318579480241));
#34509=CARTESIAN_POINT('Ctrl Pts',(97.6400667247767,0.867975809663054,-4.11021214280122));
#34510=CARTESIAN_POINT('Ctrl Pts',(97.6061423735087,0.910654792835792,-4.10723849080002));
#34511=CARTESIAN_POINT('Ctrl Pts',(97.582469385632,0.940436911387082,-4.10516342598249));
#34512=CARTESIAN_POINT('Ctrl Pts',(97.5576665713033,0.969254718261061,-4.10308836116496));
#34513=CARTESIAN_POINT('Ctrl Pts',(97.5318258778327,0.997021712251408,-4.10101329634742));
#34514=CARTESIAN_POINT('Ctrl Pts',(97.4943408742874,1.03730104412602,-4.09800316768619));
#34515=CARTESIAN_POINT('Ctrl Pts',(97.4545023806711,1.07554808367405,-4.09499303902495));
#34516=CARTESIAN_POINT('Ctrl Pts',(97.412559346666,1.11147603473777,-4.09198291036371));
#34517=CARTESIAN_POINT('Ctrl Pts',(97.3706908572507,1.14734013170904,-4.08897813154927));
#34518=CARTESIAN_POINT('Ctrl Pts',(97.32672564806,1.18089297889855,-4.08597335273482));
#34519=CARTESIAN_POINT('Ctrl Pts',(97.2809499775627,1.2118839977969,-4.08296857392038));
#34520=CARTESIAN_POINT('Ctrl Pts',(97.2352195945075,1.24284435621644,-4.07996676783676));
#34521=CARTESIAN_POINT('Ctrl Pts',(97.1876827334991,1.27124761245919,-4.07696496175315));
#34522=CARTESIAN_POINT('Ctrl Pts',(97.1386577814209,1.29688412541374,-4.07396315566953));
#34523=CARTESIAN_POINT('Ctrl Pts',(97.0896619677406,1.32250540108839,-4.07096313373493));
#34524=CARTESIAN_POINT('Ctrl Pts',(97.0391802831046,1.34536294862066,-4.06796311180034));
#34525=CARTESIAN_POINT('Ctrl Pts',(96.9875570892554,1.36529227383068,-4.06496308986574));
#34526=CARTESIAN_POINT('Ctrl Pts',(96.935944189383,1.3852176250128,-4.06196366615365));
#34527=CARTESIAN_POINT('Ctrl Pts',(96.8831907247496,1.40221572339025,-4.05896424244156));
#34528=CARTESIAN_POINT('Ctrl Pts',(96.8296603257169,1.4161704834634,-4.05596481872947));
#34529=CARTESIAN_POINT('Ctrl Pts',(96.7760807132356,1.43013807291725,-4.05296263748172));
#34530=CARTESIAN_POINT('Ctrl Pts',(96.721723251454,1.44105660070094,-4.04996045623396));
#34531=CARTESIAN_POINT('Ctrl Pts',(96.6669645468348,1.44886050883564,-4.0469582749862));
#34532=CARTESIAN_POINT('Ctrl Pts',(96.6121809172688,1.4566679691361,-4.04395472721218));
#34533=CARTESIAN_POINT('Ctrl Pts',(96.5569962079277,1.46135793888929,-4.04095117943817));
#34534=CARTESIAN_POINT('Ctrl Pts',(96.501791674746,1.46291683768627,-4.03794763166415));
#34535=CARTESIAN_POINT('Ctrl Pts',(96.4464829522984,1.46447867864238,-4.03493841519918));
#34536=CARTESIAN_POINT('Ctrl Pts',(96.3911548604652,1.46289765888106,-4.03192919873422));
#34537=CARTESIAN_POINT('Ctrl Pts',(96.3361870071489,1.45821235280589,-4.02891998226925));
#34538=CARTESIAN_POINT('Ctrl Pts',(96.2941343466014,1.45462790163937,-4.02661780834612));
#34539=CARTESIAN_POINT('Ctrl Pts',(96.2522925109856,1.44922763500382,-4.024315634423));
#34540=CARTESIAN_POINT('Ctrl Pts',(96.2108270958956,1.44204896010572,-4.02201346049987));
#34541=CARTESIAN_POINT('Ctrl Pts',(96.1566104126298,1.43266272962009,-4.01900333183863));
#34542=CARTESIAN_POINT('Ctrl Pts',(96.1028098911466,1.42019495131143,-4.01599320317738));
#34543=CARTESIAN_POINT('Ctrl Pts',(96.0498017560758,1.40469742294388,-4.01298307451614));
#34544=CARTESIAN_POINT('Ctrl Pts',(95.9968878313971,1.38922743805099,-4.0099782957017));
#34545=CARTESIAN_POINT('Ctrl Pts',(95.9447640011588,1.37073853610967,-4.00697351688726));
#34546=CARTESIAN_POINT('Ctrl Pts',(95.8937965421099,1.34933355117765,-4.00396873807281));
#34547=CARTESIAN_POINT('Ctrl Pts',(95.8428795069179,1.327949742932,-4.00096693198919));
#34548=CARTESIAN_POINT('Ctrl Pts',(95.7931170611558,1.30365577019171,-3.99796512590557));
#34549=CARTESIAN_POINT('Ctrl Pts',(95.74485875024,1.27660374345999,-3.99496331982195));
#34550=CARTESIAN_POINT('Ctrl Pts',(95.6966291220623,1.24956779533082,-3.99196329788735));
#34551=CARTESIAN_POINT('Ctrl Pts',(95.6499023165267,1.21977730007933,-3.98896327595275));
#34552=CARTESIAN_POINT('Ctrl Pts',(95.6050042598401,1.18743079095867,-3.98596325401815));
#34553=CARTESIAN_POINT('Ctrl Pts',(95.5601151560974,1.1550907319275,-3.98296383030606));
#34554=CARTESIAN_POINT('Ctrl Pts',(95.5170545052516,1.12019597977172,-3.97996440659397));
#34555=CARTESIAN_POINT('Ctrl Pts',(95.4761182182349,1.08298765604447,-3.97696498288188));
#34556=CARTESIAN_POINT('Ctrl Pts',(95.4351442962315,1.04574512465277,-3.97396280163413));
#34557=CARTESIAN_POINT('Ctrl Pts',(95.396299031632,1.00618512821078,-3.97096062038637));
#34558=CARTESIAN_POINT('Ctrl Pts',(95.3598431073006,0.964587264144195,-3.96795843913861));
#34559=CARTESIAN_POINT('Ctrl Pts',(95.3233705890418,0.922970465653291,-3.96495489136459));
#34560=CARTESIAN_POINT('Ctrl Pts',(95.2892899046026,0.879314367459632,-3.96195134359057));
#34561=CARTESIAN_POINT('Ctrl Pts',(95.2578207446867,0.833930861386753,-3.95894779581655));
#34562=CARTESIAN_POINT('Ctrl Pts',(95.2262921920276,0.788461701583897,-3.95593857935158));
#34563=CARTESIAN_POINT('Ctrl Pts',(95.1973852864467,0.741259072640951,-3.95292936288661));
#34564=CARTESIAN_POINT('Ctrl Pts',(95.1712751371105,0.69266198329532,-3.94992014642165));
#34565=CARTESIAN_POINT('Ctrl Pts',(95.1512998027901,0.655483218280164,-3.94761797249853));
#34566=CARTESIAN_POINT('Ctrl Pts',(95.1329604567089,0.617488870375159,-3.94531579857542));
#34567=CARTESIAN_POINT('Ctrl Pts',(95.1163162501074,0.578838069497707,-3.94301362465231));
#34568=CARTESIAN_POINT('Ctrl Pts',(95.0945536878475,0.528301538641816,-3.94000349599107));
#34569=CARTESIAN_POINT('Ctrl Pts',(95.0755993939873,0.47642980884546,-3.93699336732983));
#34570=CARTESIAN_POINT('Ctrl Pts',(95.0596155541659,0.423566280456311,-3.93398323866859));
#34571=CARTESIAN_POINT('Ctrl Pts',(95.0436601221316,0.370796705452491,-3.93097845985415));
#34572=CARTESIAN_POINT('Ctrl Pts',(95.030664818874,0.317039331382095,-3.9279736810397));
#34573=CARTESIAN_POINT('Ctrl Pts',(95.0207436502798,0.262657113005483,-3.92496890222526));
#34574=CARTESIAN_POINT('Ctrl Pts',(95.0108322970383,0.208328696824217,-3.92196709614164));
#34575=CARTESIAN_POINT('Ctrl Pts',(95.0039891480142,0.153377177908357,-3.91896529005802));
#34576=CARTESIAN_POINT('Ctrl Pts',(95.0002777968106,0.0981784225329755,
-3.9159634839744));
#34577=CARTESIAN_POINT('Ctrl Pts',(94.9965686514802,0.0430124750081214,
-3.9129634620398));
#34578=CARTESIAN_POINT('Ctrl Pts',(94.9959876498898,-0.0123998918430344,
-3.9099634401052));
#34579=CARTESIAN_POINT('Ctrl Pts',(94.9985465998968,-0.0676772282603138,
-3.9069634181706));
#34580=CARTESIAN_POINT('Ctrl Pts',(95.0011050396336,-0.122943542042634,
-3.9039639944585));
#34581=CARTESIAN_POINT('Ctrl Pts',(95.0068021631017,-0.178074351609378,
-3.9009645707464));
#34582=CARTESIAN_POINT('Ctrl Pts',(95.0155977090828,-0.232690075720748,
-3.89796514703431));
#34583=CARTESIAN_POINT('Ctrl Pts',(95.0244013412944,-0.287356011079845,
-3.89496296578655));
#34584=CARTESIAN_POINT('Ctrl Pts',(95.0363090029046,-0.341505392380792,
-3.89196078453879));
#34585=CARTESIAN_POINT('Ctrl Pts',(95.0512289596384,-0.394767119773147,
-3.88895860329103));
#34586=CARTESIAN_POINT('Ctrl Pts',(95.0661557076052,-0.448053090721488,
-3.88595505551701));
#34587=CARTESIAN_POINT('Ctrl Pts',(95.0840973125663,-0.50045010182673,-3.88295150774299));
#34588=CARTESIAN_POINT('Ctrl Pts',(95.1049125948635,-0.551603739743897,
-3.87994795996897));
#34589=CARTESIAN_POINT('Ctrl Pts',(95.1257671625031,-0.602853921543803,
-3.87693874350401));
#34590=CARTESIAN_POINT('Ctrl Pts',(95.1495060148721,-0.652855564092704,
-3.87392952703904));
#34591=CARTESIAN_POINT('Ctrl Pts',(95.1759409019906,-0.701276775707584,
-3.87092031057407));
#34592=CARTESIAN_POINT('Ctrl Pts',(95.1961646740234,-0.73832098705067,-3.86861813665096));
#34593=CARTESIAN_POINT('Ctrl Pts',(95.2179654162278,-0.774440645503443,
-3.86631596272785));
#34594=CARTESIAN_POINT('Ctrl Pts',(95.2412421730209,-0.80949926234802,-3.86401378880474));
#34595=CARTESIAN_POINT('Ctrl Pts',(95.2716768991118,-0.855338956007903,
-3.8610036601435));
#34596=CARTESIAN_POINT('Ctrl Pts',(95.3047643170789,-0.899556196763965,
-3.85799353148226));
#34597=CARTESIAN_POINT('Ctrl Pts',(95.3403054374856,-0.941827517176502,
-3.85498340282102));
#34598=CARTESIAN_POINT('Ctrl Pts',(95.375783391307,-0.984023709541916,-3.85197862400658));
#34599=CARTESIAN_POINT('Ctrl Pts',(95.4137060561745,-1.02428044392341,-3.84897384519213));
#34600=CARTESIAN_POINT('Ctrl Pts',(95.453831740077,-1.06230392026625,-3.84596906637768));
#34601=CARTESIAN_POINT('Ctrl Pts',(95.4939177262631,-1.10028977867875,-3.84296726029406));
#34602=CARTESIAN_POINT('Ctrl Pts',(95.5362020324988,-1.13604639437285,-3.83996545421044));
#34603=CARTESIAN_POINT('Ctrl Pts',(95.5804046079581,-1.16931513413738,-3.83696364812682));
#34604=CARTESIAN_POINT('Ctrl Pts',(95.6245809112401,-1.20256410034297,-3.83396362619221));
#34605=CARTESIAN_POINT('Ctrl Pts',(95.6706728027993,-1.23332780453134,-3.83096360425761));
#34606=CARTESIAN_POINT('Ctrl Pts',(95.7183672599627,-1.26138793465255,-3.82796358232301));
#34607=CARTESIAN_POINT('Ctrl Pts',(95.7660522065629,-1.28944246941416,-3.82496415861092));
#34608=CARTESIAN_POINT('Ctrl Pts',(95.8153386292053,-1.31479423310827,-3.82196473489883));
#34609=CARTESIAN_POINT('Ctrl Pts',(95.8658866198142,-1.33726954388932,-3.81896531118674));
#34610=CARTESIAN_POINT('Ctrl Pts',(95.9164810819792,-1.35976551746334,-3.81596312993898));
#34611=CARTESIAN_POINT('Ctrl Pts',(95.9683389456966,-1.37937953976791,-3.81296094869122));
#34612=CARTESIAN_POINT('Ctrl Pts',(96.0210992816066,-1.39598567322575,-3.80995876744346));
#34613=CARTESIAN_POINT('Ctrl Pts',(96.0738836328503,-1.41259936542691,-3.80695521966944));
#34614=CARTESIAN_POINT('Ctrl Pts',(96.1275707623274,-1.42620230958819,-3.80395167189542));
#34615=CARTESIAN_POINT('Ctrl Pts',(96.1817866993122,-1.43671909741234,-3.8009481241214));
#34616=CARTESIAN_POINT('Ctrl Pts',(96.2361049597538,-1.44725573390359,-3.79793890765644));
#34617=CARTESIAN_POINT('Ctrl Pts',(96.2909534968245,-1.45469450736382,-3.79492969119147));
#34618=CARTESIAN_POINT('Ctrl Pts',(96.3459514832574,-1.459011737905,-3.79192047472651));
#34619=CARTESIAN_POINT('Ctrl Pts',(96.3880271968738,-1.46231459620305,-3.7896183008034));
#34620=CARTESIAN_POINT('Ctrl Pts',(96.4301902228732,-1.46379152747159,-3.78731612688029));
#34621=CARTESIAN_POINT('Ctrl Pts',(96.4722710865471,-1.46345250782874,-3.78501395295718));
#34622=CARTESIAN_POINT('Ctrl Pts',(96.5272924785292,-1.46300923430652,-3.78200382429594));
#34623=CARTESIAN_POINT('Ctrl Pts',(96.582404442967,-1.45945775804878,-3.7789936956347));
#34624=CARTESIAN_POINT('Ctrl Pts',(96.6372273401275,-1.45278799672471,-3.77598356697346));
#34625=CARTESIAN_POINT('Ctrl Pts',(96.6919528015522,-1.44613008944585,-3.77297878815902));
#34626=CARTESIAN_POINT('Ctrl Pts',(96.7463896952375,-1.43636495864272,-3.76997400934458));
#34627=CARTESIAN_POINT('Ctrl Pts',(96.8001598961644,-1.42353449668256,-3.76696923053014));
#34628=CARTESIAN_POINT('Ctrl Pts',(96.8538769003859,-1.41071672833884,-3.76396742444652));
#34629=CARTESIAN_POINT('Ctrl Pts',(96.9069280072805,-1.39483975832016,-3.7609656183629));
#34630=CARTESIAN_POINT('Ctrl Pts',(96.9589435859015,-1.375996820559,-3.75796381227928));
#34631=CARTESIAN_POINT('Ctrl Pts',(97.0109282486201,-1.35716508225845,-3.75496379034469));
#34632=CARTESIAN_POINT('Ctrl Pts',(97.0618781074284,-1.33537104981154,-3.75196376841009));
#34633=CARTESIAN_POINT('Ctrl Pts',(97.1114392857495,-1.3107576032843,-3.74896374647549));
#34634=CARTESIAN_POINT('Ctrl Pts',(97.1609905812721,-1.28614906482699,-3.74596432276339));
#34635=CARTESIAN_POINT('Ctrl Pts',(97.2091532735089,-1.25872246358273,-3.7429648990513));
#34636=CARTESIAN_POINT('Ctrl Pts',(97.2555961748016,-1.22866758263414,-3.7399654753392));
#34637=CARTESIAN_POINT('Ctrl Pts',(97.3020817736152,-1.19858507057575,-3.73696329409144));
#34638=CARTESIAN_POINT('Ctrl Pts',(97.3468439783274,-1.16586973885511,-3.73396111284368));
#34639=CARTESIAN_POINT('Ctrl Pts',(97.3895801024427,-1.13075506372698,-3.73095893159592));
#34640=CARTESIAN_POINT('Ctrl Pts',(97.432335679093,-1.09562440517823,-3.72795538382191));
#34641=CARTESIAN_POINT('Ctrl Pts',(97.4730629477146,-1.05809258465269,-3.72495183604789));
#34642=CARTESIAN_POINT('Ctrl Pts',(97.5114944156926,-1.01843160990011,-3.72194828827388));
#34643=CARTESIAN_POINT('Ctrl Pts',(97.5499984165987,-0.978695781732321,
-3.71893907180891));
#34644=CARTESIAN_POINT('Ctrl Pts',(97.5861976149122,-0.936823172417264,
-3.71592985534394));
#34645=CARTESIAN_POINT('Ctrl Pts',(97.6198640955659,-0.893119796442222,
-3.71292063887898));
#34646=CARTESIAN_POINT('Ctrl Pts',(97.6456203330272,-0.859684922715666,
-3.71061846495586));
#34647=CARTESIAN_POINT('Ctrl Pts',(97.6698950146036,-0.825179243157338,
-3.70831629103274));
#34648=CARTESIAN_POINT('Ctrl Pts',(97.692603895247,-0.789750148308665,-3.70601411710962));
#34649=CARTESIAN_POINT('Ctrl Pts',(97.7229545537649,-0.742398789329823,
-3.70293723737755));
#34650=CARTESIAN_POINT('Ctrl Pts',(97.7506298434866,-0.693205203985186,
-3.69986035764549));
#34651=CARTESIAN_POINT('Ctrl Pts',(97.775407355941,-0.642495755508686,-3.69678347791342));
#34652=CARTESIAN_POINT('Ctrl Pts',(97.8001289484294,-0.591900752364011,
-3.69371354234132));
#34653=CARTESIAN_POINT('Ctrl Pts',(97.8219655452006,-0.539797128016443,
-3.69064360676921));
#34654=CARTESIAN_POINT('Ctrl Pts',(97.8407392857753,-0.486537948525319,
-3.68757367119711));
#34655=CARTESIAN_POINT('Ctrl Pts',(97.8594879712184,-0.433349847876592,
-3.68450783271154));
#34656=CARTESIAN_POINT('Ctrl Pts',(97.8751817456071,-0.379009717014779,
-3.68144199422596));
#34657=CARTESIAN_POINT('Ctrl Pts',(97.8876902586357,-0.323891707420963,
-3.67837615574039));
#34658=CARTESIAN_POINT('Ctrl Pts',(97.9001850500302,-0.268834161382075,
-3.67531368042948));
#34659=CARTESIAN_POINT('Ctrl Pts',(97.9095014086337,-0.213000913674018,
-3.67225120511857));
#34660=CARTESIAN_POINT('Ctrl Pts',(97.9155589979105,-0.156780493869258,
-3.66918872980767));
#34661=CARTESIAN_POINT('Ctrl Pts',(97.9211855523835,-0.104560503363353,
-3.66634416848608));
#34662=CARTESIAN_POINT('Ctrl Pts',(97.9240010364998,-0.0520069428674101,
-3.66349960716449));
#34663=CARTESIAN_POINT('Ctrl Pts',(97.9239808415867,0.000562216580854143,
-3.6606550458429));
#34664=CARTESIAN_POINT('Ctrl Pts',(97.9239808649785,0.000497614024185356,
-3.58934495415707));
#34665=CARTESIAN_POINT('Ctrl Pts',(97.9240001510924,-0.056223508595772,
-3.59241382882926));
#34666=CARTESIAN_POINT('Ctrl Pts',(97.9207175741498,-0.112920864306401,
-3.59548270350144));
#34667=CARTESIAN_POINT('Ctrl Pts',(97.9141675493034,-0.169196689612829,
-3.59855157817363));
#34668=CARTESIAN_POINT('Ctrl Pts',(97.9076060721981,-0.225570909251625,
-3.60162581855787));
#34669=CARTESIAN_POINT('Ctrl Pts',(97.8977657979204,-0.281521635888496,
-3.60470005894212));
#34670=CARTESIAN_POINT('Ctrl Pts',(97.8847328229594,-0.336658359716137,
-3.60777429932636));
#34671=CARTESIAN_POINT('Ctrl Pts',(97.871688408699,-0.391843478134799,-3.61085123803208));
#34672=CARTESIAN_POINT('Ctrl Pts',(97.8554458536868,-0.446212697850251,
-3.61392817673781));
#34673=CARTESIAN_POINT('Ctrl Pts',(97.8361411092636,-0.499391004175057,
-3.61700511544353));
#34674=CARTESIAN_POINT('Ctrl Pts',(97.8167895597394,-0.552698243364627,
-3.6200895143064));
#34675=CARTESIAN_POINT('Ctrl Pts',(97.794361178821,-0.604808344405963,-3.62317391316927));
#34676=CARTESIAN_POINT('Ctrl Pts',(97.7690398263078,-0.65536700872792,-3.62625831203214));
#34677=CARTESIAN_POINT('Ctrl Pts',(97.7478753772047,-0.697625662850288,
-3.62883635768405));
#34678=CARTESIAN_POINT('Ctrl Pts',(97.7246907636451,-0.738800758044961,
-3.63141440333595));
#34679=CARTESIAN_POINT('Ctrl Pts',(97.6996164354008,-0.77870116076208,-3.63399244898786));
#34680=CARTESIAN_POINT('Ctrl Pts',(97.6703396248627,-0.825288910565818,
-3.6370025776491));
#34681=CARTESIAN_POINT('Ctrl Pts',(97.6383703097217,-0.870321171193224,
-3.64001270631033));
#34682=CARTESIAN_POINT('Ctrl Pts',(97.6038993135423,-0.913469591692513,
-3.64302283497157));
#34683=CARTESIAN_POINT('Ctrl Pts',(97.569489582036,-0.956541325290655,-3.64602761378601));
#34684=CARTESIAN_POINT('Ctrl Pts',(97.5325873199565,-0.997735453842115,
-3.64903239260045));
#34685=CARTESIAN_POINT('Ctrl Pts',(97.4934267832603,-1.03675221469564,-3.6520371714149));
#34686=CARTESIAN_POINT('Ctrl Pts',(97.4543049894273,-1.07573037492832,-3.65503897749851));
#34687=CARTESIAN_POINT('Ctrl Pts',(97.4129297190792,-1.11253506380539,-3.65804078358213));
#34688=CARTESIAN_POINT('Ctrl Pts',(97.3695744559394,-1.14690071352742,-3.66104258966574));
#34689=CARTESIAN_POINT('Ctrl Pts',(97.3262449613696,-1.18124593773276,-3.66404261160034));
#34690=CARTESIAN_POINT('Ctrl Pts',(97.2809382195961,-1.21315466871269,-3.66704263353494));
#34691=CARTESIAN_POINT('Ctrl Pts',(97.2339616859562,-1.24240082117255,-3.67004265546953));
#34692=CARTESIAN_POINT('Ctrl Pts',(97.1869945197212,-1.27164114177282,-3.67304207918162));
#34693=CARTESIAN_POINT('Ctrl Pts',(97.1383586709566,-1.29821965930521,-3.6760415028937));
#34694=CARTESIAN_POINT('Ctrl Pts',(97.0883895900285,-1.32195423114661,-3.67904092660579));
#34695=CARTESIAN_POINT('Ctrl Pts',(97.0383745697679,-1.34571062348912,-3.68204310785355));
#34696=CARTESIAN_POINT('Ctrl Pts',(96.98702434659,-1.36661761944437,-3.6850452891013));
#34697=CARTESIAN_POINT('Ctrl Pts',(96.9346965816245,-1.38454027905359,-3.68804747034906));
#34698=CARTESIAN_POINT('Ctrl Pts',(96.8823449982221,-1.40247109665959,-3.69105101812307));
#34699=CARTESIAN_POINT('Ctrl Pts',(96.8290154954596,-1.41741472729064,-3.69405456589709));
#34700=CARTESIAN_POINT('Ctrl Pts',(96.7750800375856,-1.42928641770085,-3.6970581136711));
#34701=CARTESIAN_POINT('Ctrl Pts',(96.7210427856119,-1.4411805139288,-3.70006733013607));
#34702=CARTESIAN_POINT('Ctrl Pts',(96.6663978165935,-1.44999100372014,-3.70307654660103));
#34703=CARTESIAN_POINT('Ctrl Pts',(96.6115252450547,-1.45568467423534,-3.706085763066));
#34704=CARTESIAN_POINT('Ctrl Pts',(96.5695454789716,-1.46004056552455,-3.70838793698914));
#34705=CARTESIAN_POINT('Ctrl Pts',(96.5274326852702,-1.46257329016688,-3.71069011091228));
#34706=CARTESIAN_POINT('Ctrl Pts',(96.4853565353895,-1.46328857551424,-3.71299228483542));
#34707=CARTESIAN_POINT('Ctrl Pts',(96.430341306767,-1.46422382237087,-3.71600241349666));
#34708=CARTESIAN_POINT('Ctrl Pts',(96.3751576682472,-1.46205411097958,-3.7190125421579));
#34709=CARTESIAN_POINT('Ctrl Pts',(96.3201848878356,-1.45675985154034,-3.72202267081915));
#34710=CARTESIAN_POINT('Ctrl Pts',(96.2653098095444,-1.45147500149189,-3.72502744963359));
#34711=CARTESIAN_POINT('Ctrl Pts',(96.2106453670913,-1.44307667398024,-3.72803222844804));
#34712=CARTESIAN_POINT('Ctrl Pts',(96.1565706162991,-1.43159727553768,-3.73103700726248));
#34713=CARTESIAN_POINT('Ctrl Pts',(96.102549363514,-1.42012923405805,-3.7340388133461));
#34714=CARTESIAN_POINT('Ctrl Pts',(96.0491171607622,-1.40558626913281,-3.73704061942973));
#34715=CARTESIAN_POINT('Ctrl Pts',(95.9966458586558,-1.38805232553751,-3.74004242551335));
#34716=CARTESIAN_POINT('Ctrl Pts',(95.9442057433148,-1.37052880339098,-3.74304244744795));
#34717=CARTESIAN_POINT('Ctrl Pts',(95.8927258965131,-1.35001799316413,-3.74604246938254));
#34718=CARTESIAN_POINT('Ctrl Pts',(95.842563663159,-1.32665386485917,-3.74904249131714));
#34719=CARTESIAN_POINT('Ctrl Pts',(95.7924114324574,-1.30329439550263,-3.75204191502923));
#34720=CARTESIAN_POINT('Ctrl Pts',(95.7435767718786,-1.2770829608713,-3.75504133874132));
#34721=CARTESIAN_POINT('Ctrl Pts',(95.6963955195345,-1.24820098766054,-3.75804076245341));
#34722=CARTESIAN_POINT('Ctrl Pts',(95.6491708908625,-1.21929246165864,-3.76104294370117));
#34723=CARTESIAN_POINT('Ctrl Pts',(95.6036031587181,-1.18770876827886,-3.76404512494893));
#34724=CARTESIAN_POINT('Ctrl Pts',(95.5600007635854,-1.15367572767935,-3.76704730619669));
#34725=CARTESIAN_POINT('Ctrl Pts',(95.5163785216103,-1.11962719599523,-3.77005085397072));
#34726=CARTESIAN_POINT('Ctrl Pts',(95.4747237978213,-1.08312744329179,-3.77305440174474));
#34727=CARTESIAN_POINT('Ctrl Pts',(95.4353108151481,-1.04444169079708,-3.77605794951876));
#34728=CARTESIAN_POINT('Ctrl Pts',(95.3958234471031,-1.00568292545508,-3.77906716598373));
#34729=CARTESIAN_POINT('Ctrl Pts',(95.35858662823,-0.964730310280806,-3.7820763824487));
#34730=CARTESIAN_POINT('Ctrl Pts',(95.3238358682598,-0.921884054053179,
-3.78508559891367));
#34731=CARTESIAN_POINT('Ctrl Pts',(95.2972501126844,-0.889104912061163,
-3.78738777283677));
#34732=CARTESIAN_POINT('Ctrl Pts',(95.2721186224739,-0.855218184759803,
-3.78968994675988));
#34733=CARTESIAN_POINT('Ctrl Pts',(95.2485293086253,-0.820369105948374,
-3.79199212068299));
#34734=CARTESIAN_POINT('Ctrl Pts',(95.2176859092619,-0.774803386566738,
-3.79500224934422));
#34735=CARTESIAN_POINT('Ctrl Pts',(95.1893509774879,-0.727400082365858,
-3.79801237800546));
#34736=CARTESIAN_POINT('Ctrl Pts',(95.1637481508373,-0.678466136717841,
-3.80102250666669));
#34737=CARTESIAN_POINT('Ctrl Pts',(95.1381908276239,-0.629619160479316,
-3.80402728548114));
#34738=CARTESIAN_POINT('Ctrl Pts',(95.1153562161736,-0.579247405560317,
-3.80703206429558));
#34739=CARTESIAN_POINT('Ctrl Pts',(95.0954242897573,-0.527686048216158,
-3.81003684311002));
#34740=CARTESIAN_POINT('Ctrl Pts',(95.07551208268,-0.476175702292761,-3.81303864919364));
#34741=CARTESIAN_POINT('Ctrl Pts',(95.0584970613695,-0.423478575525552,
-3.81604045527726));
#34742=CARTESIAN_POINT('Ctrl Pts',(95.0445120975315,-0.369951969905599,
-3.81904226136088));
#34743=CARTESIAN_POINT('Ctrl Pts',(95.030535445776,-0.316457178279727,-3.82204228329547));
#34744=CARTESIAN_POINT('Ctrl Pts',(95.0195854151447,-0.26213439491896,-3.82504230523007));
#34745=CARTESIAN_POINT('Ctrl Pts',(95.0117450540103,-0.207356106484561,
-3.82804232716467));
#34746=CARTESIAN_POINT('Ctrl Pts',(95.0039062562912,-0.152588741172005,
-3.83104175087676));
#34747=CARTESIAN_POINT('Ctrl Pts',(94.9991759713874,-0.0973665736664746,
-3.83404117458884));
#34748=CARTESIAN_POINT('Ctrl Pts',(94.9975857501847,-0.0420700082593357,
-3.83704059830093));
#34749=CARTESIAN_POINT('Ctrl Pts',(94.9959940670039,0.0132773943305955,
-3.84004277954869));
#34750=CARTESIAN_POINT('Ctrl Pts',(94.997548230257,0.0686988024404475,-3.84304496079645));
#34751=CARTESIAN_POINT('Ctrl Pts',(95.0022276401538,0.1238125016156,-3.84604714204421));
#34752=CARTESIAN_POINT('Ctrl Pts',(95.0069091800141,0.178951287323153,-3.84905068981822));
#34753=CARTESIAN_POINT('Ctrl Pts',(95.0147187276608,0.233781561140536,-3.85205423759224));
#34754=CARTESIAN_POINT('Ctrl Pts',(95.0255839875099,0.287928738146205,-3.85505778536626));
#34755=CARTESIAN_POINT('Ctrl Pts',(95.0364697537083,0.342178108835892,-3.85806700183122));
#34756=CARTESIAN_POINT('Ctrl Pts',(95.050422619417,0.395741294961268,-3.86107621829619));
#34757=CARTESIAN_POINT('Ctrl Pts',(95.0673198332966,0.4482570178862,-3.86408543476115));
#34758=CARTESIAN_POINT('Ctrl Pts',(95.080246894417,0.48843369818816,-3.86638760868429));
#34759=CARTESIAN_POINT('Ctrl Pts',(95.0948961929289,0.527997572373446,-3.86868978260742));
#34760=CARTESIAN_POINT('Ctrl Pts',(95.1111941258405,0.56679565743835,-3.87099195653056));
#34761=CARTESIAN_POINT('Ctrl Pts',(95.1325039297971,0.617524764688423,-3.87400208519179));
#34762=CARTESIAN_POINT('Ctrl Pts',(95.1567233773382,0.667157011953762,-3.87701221385303));
#34763=CARTESIAN_POINT('Ctrl Pts',(95.1837175897996,0.715337384127176,-3.88002234251427));
#34764=CARTESIAN_POINT('Ctrl Pts',(95.2106638259394,0.763432126203506,-3.88302712132871));
#34765=CARTESIAN_POINT('Ctrl Pts',(95.2403747842794,0.810079656987281,-3.88603190014316));
#34766=CARTESIAN_POINT('Ctrl Pts',(95.272668082374,0.854946105030524,-3.8890366789576));
#34767=CARTESIAN_POINT('Ctrl Pts',(95.3049294316002,0.899768165156598,-3.89203848504122));
#34768=CARTESIAN_POINT('Ctrl Pts',(95.3397677526525,0.942812206625506,-3.89504029112484));
#34769=CARTESIAN_POINT('Ctrl Pts',(95.376956396076,0.983771717402203,-3.89804209720846));
#34770=CARTESIAN_POINT('Ctrl Pts',(95.4141229361124,1.02470688354471,-3.90104211914306));
#34771=CARTESIAN_POINT('Ctrl Pts',(95.4536366754115,1.06355958447403,-3.90404214107766));
#34772=CARTESIAN_POINT('Ctrl Pts',(95.4952310236744,1.10005673969343,-3.90704216301226));
#34773=CARTESIAN_POINT('Ctrl Pts',(95.5368170777728,1.13654661715947,-3.91004158672435));
#34774=CARTESIAN_POINT('Ctrl Pts',(95.5804825201473,1.17068153361645,-3.91304101043644));
#34775=CARTESIAN_POINT('Ctrl Pts',(95.6259259912463,1.20222721293675,-3.91604043414853));
#34776=CARTESIAN_POINT('Ctrl Pts',(95.671411241035,1.23380189394011,-3.91904261539629));
#34777=CARTESIAN_POINT('Ctrl Pts',(95.7186773505804,1.26278228021673,-3.92204479664405));
#34778=CARTESIAN_POINT('Ctrl Pts',(95.7673933681092,1.28897705736568,-3.9250469778918));
#34779=CARTESIAN_POINT('Ctrl Pts',(95.8161315600878,1.31518375779572,-3.92805052566582));
#34780=CARTESIAN_POINT('Ctrl Pts',(95.8663204962306,1.33860209783507,-3.93105407343984));
#34781=CARTESIAN_POINT('Ctrl Pts',(95.9176069495612,1.35908795525045,-3.93405762121386));
#34782=CARTESIAN_POINT('Ctrl Pts',(95.9689901974413,1.37961247627406,-3.93706683767883));
#34783=CARTESIAN_POINT('Ctrl Pts',(96.0214745984137,1.3971932903609,-3.9400760541438));
#34784=CARTESIAN_POINT('Ctrl Pts',(96.0746905010476,1.41173580383282,-3.94308527060876));
#34785=CARTESIAN_POINT('Ctrl Pts',(96.1154028475223,1.42286142263805,-3.94538744453188));
#34786=CARTESIAN_POINT('Ctrl Pts',(96.1565429761317,1.43220978642091,-3.947689618455));
#34787=CARTESIAN_POINT('Ctrl Pts',(96.1979425431072,1.43975895035534,-3.94999179237811));
#34788=CARTESIAN_POINT('Ctrl Pts',(96.2520731289264,1.44962960109082,-3.95300192103935));
#34789=CARTESIAN_POINT('Ctrl Pts',(96.306874882821,1.45646402702742,-3.9560120497006));
#34790=CARTESIAN_POINT('Ctrl Pts',(96.3619767729118,1.46018121381543,-3.95902217836184));
#34791=CARTESIAN_POINT('Ctrl Pts',(96.4169807314178,1.46389179411512,-3.96202695717628));
#34792=CARTESIAN_POINT('Ctrl Pts',(96.4722832448745,1.46449609459621,-3.96503173599072));
#34793=CARTESIAN_POINT('Ctrl Pts',(96.5275050339065,1.46196443941698,-3.96803651480517));
#34794=CARTESIAN_POINT('Ctrl Pts',(96.582672190127,1.45943528889111,-3.97103832088879));
#34795=CARTESIAN_POINT('Ctrl Pts',(96.63775825516,1.45377635269252,-3.97404012697241));
#34796=CARTESIAN_POINT('Ctrl Pts',(96.6923826765546,1.44500997886685,-3.97704193305603));
#34797=CARTESIAN_POINT('Ctrl Pts',(96.746974631459,1.43624881541015,-3.98004195499063));
#34798=CARTESIAN_POINT('Ctrl Pts',(96.801104966165,1.42438395858349,-3.98304197692523));
#34799=CARTESIAN_POINT('Ctrl Pts',(96.8543993045145,1.40948947482533,-3.98604199885983));
#34800=CARTESIAN_POINT('Ctrl Pts',(96.9076830156505,1.3945979611173,-3.98904142257191));
#34801=CARTESIAN_POINT('Ctrl Pts',(96.9601305531537,1.37667816231497,-3.99204084628399));
#34802=CARTESIAN_POINT('Ctrl Pts',(97.0113810427862,1.35585446759676,-3.99504026999608));
#34803=CARTESIAN_POINT('Ctrl Pts',(97.0626786498209,1.3350116285073,-3.99804245124383));
#34804=CARTESIAN_POINT('Ctrl Pts',(97.112776519982,1.31125975898894,-4.00104463249159));
#34805=CARTESIAN_POINT('Ctrl Pts',(97.1613335915602,1.28477150662102,-4.00404681373935));
#34806=CARTESIAN_POINT('Ctrl Pts',(97.2099127652393,1.25827119738863,-4.00705036151336));
#34807=CARTESIAN_POINT('Ctrl Pts',(97.2569492929646,1.22903230170353,-4.01005390928738));
#34808=CARTESIAN_POINT('Ctrl Pts',(97.3021294666536,1.19727190884227,-4.01305745706139));
#34809=CARTESIAN_POINT('Ctrl Pts',(97.3473949103169,1.16545157358449,-4.01606667352636));
#34810=CARTESIAN_POINT('Ctrl Pts',(97.3907965859239,1.13110056306223,-4.01907588999133));
#34811=CARTESIAN_POINT('Ctrl Pts',(97.4320532926325,1.09447678468282,-4.0220851064563));
#34812=CARTESIAN_POINT('Ctrl Pts',(97.4636163640979,1.06645809326165,-4.02438728037942));
#34813=CARTESIAN_POINT('Ctrl Pts',(97.49392467513,1.03711003762231,-4.02668945430255));
#34814=CARTESIAN_POINT('Ctrl Pts',(97.5228678639721,1.0065616196349,-4.02899162822567));
#34815=CARTESIAN_POINT('Ctrl Pts',(97.5602276477705,0.967129810734345,-4.03196326761564));
#34816=CARTESIAN_POINT('Ctrl Pts',(97.5954772999918,0.925521827568755,-4.03493490700561));
#34817=CARTESIAN_POINT('Ctrl Pts',(97.6283492700598,0.881995371877195,-4.03790654639557));
#34818=CARTESIAN_POINT('Ctrl Pts',(97.6611738936125,0.838531608686043,-4.04087390564142));
#34819=CARTESIAN_POINT('Ctrl Pts',(97.6916272888325,0.793155270469379,-4.04384126488726));
#34820=CARTESIAN_POINT('Ctrl Pts',(97.7194797349499,0.746159707053038,-4.0468086241331));
#34821=CARTESIAN_POINT('Ctrl Pts',(97.7473037456196,0.699212122901529,-4.04977295390754));
#34822=CARTESIAN_POINT('Ctrl Pts',(97.7725317904146,0.650649051771042,-4.05273728368199));
#34823=CARTESIAN_POINT('Ctrl Pts',(97.794976850279,0.600793592683606,-4.05570161345643));
#34824=CARTESIAN_POINT('Ctrl Pts',(97.8174158723574,0.550951544858702,-4.0586651458176));
#34825=CARTESIAN_POINT('Ctrl Pts',(97.8370731533352,0.499818284313263,-4.06162867817877));
#34826=CARTESIAN_POINT('Ctrl Pts',(97.853808172062,0.447740439409174,-4.06459221053994));
#34827=CARTESIAN_POINT('Ctrl Pts',(97.8705396784872,0.39567352446584,-4.06755512092275));
#34828=CARTESIAN_POINT('Ctrl Pts',(97.8843499799722,0.34266293753326,-4.07051803130557));
#34829=CARTESIAN_POINT('Ctrl Pts',(97.895148151909,0.289071390062761,-4.07348094168838));
#34830=CARTESIAN_POINT('Ctrl Pts',(97.9059561540758,0.235431054960567,-4.07644654938798));
#34831=CARTESIAN_POINT('Ctrl Pts',(97.9137464504333,0.181209237719674,-4.07941215708758));
#34832=CARTESIAN_POINT('Ctrl Pts',(97.9184794312525,0.126778063685683,-4.08237776478718));
#34833=CARTESIAN_POINT('Ctrl Pts',(97.9221858749218,0.084152477798513,-4.08470016124381));
#34834=CARTESIAN_POINT('Ctrl Pts',(97.9240184185765,0.0413987541311476,
-4.08702255770044));
#34835=CARTESIAN_POINT('Ctrl Pts',(97.9239803686004,-0.0013040392330809,
-4.08934495415707));
#34836=CARTESIAN_POINT('Origin',(96.460480949577,-8.32667268468867E-16,
1.18130019239114E-14));
#34837=CARTESIAN_POINT('',(97.9239807839468,0.000696275558457232,-4.66065504587649));
#34838=CARTESIAN_POINT('',(97.9239807519797,0.000760504599680839,-4.58934495419114));
#34839=CARTESIAN_POINT('',(97.923980949577,-1.01189432752408E-15,1.19922289829666E-14));
#34840=CARTESIAN_POINT('Ctrl Pts',(97.9239807839465,0.000696276173079623,
-4.6606550458429));
#34841=CARTESIAN_POINT('Ctrl Pts',(97.9239615067044,0.0412150267063342,
-4.65844074632205));
#34842=CARTESIAN_POINT('Ctrl Pts',(97.9222596535451,0.0816919370260447,
-4.65622644680121));
#34843=CARTESIAN_POINT('Ctrl Pts',(97.9188847609986,0.122026934858089,-4.65401214728037));
#34844=CARTESIAN_POINT('Ctrl Pts',(97.9142969169933,0.176858511111745,-4.65100201861913));
#34845=CARTESIAN_POINT('Ctrl Pts',(97.9066028816966,0.231546201030747,-4.64799188995788));
#34846=CARTESIAN_POINT('Ctrl Pts',(97.8958212070784,0.285710684427393,-4.64498176129664));
#34847=CARTESIAN_POINT('Ctrl Pts',(97.8850586945338,0.339778902275131,-4.64197698248219));
#34848=CARTESIAN_POINT('Ctrl Pts',(97.8712195351239,0.393325245199246,-4.63897220366774));
#34849=CARTESIAN_POINT('Ctrl Pts',(97.8543739936292,0.445975819684259,-4.63596742485329));
#34850=CARTESIAN_POINT('Ctrl Pts',(97.8375451180069,0.49857430514863,-4.63296561876967));
#34851=CARTESIAN_POINT('Ctrl Pts',(97.8177159124216,0.550278277197155,-4.62996381268604));
#34852=CARTESIAN_POINT('Ctrl Pts',(97.7950071972413,0.600726180797032,-4.62696200660241));
#34853=CARTESIAN_POINT('Ctrl Pts',(97.7723119791794,0.651144100255606,-4.62396198466781));
#34854=CARTESIAN_POINT('Ctrl Pts',(97.746740860095,0.700306950373101,-4.6209619627332));
#34855=CARTESIAN_POINT('Ctrl Pts',(97.7184629782722,0.747872626507885,-4.61796194079859));
#34856=CARTESIAN_POINT('Ctrl Pts',(97.6901907352301,0.795428817759335,-4.61496251708649));
#34857=CARTESIAN_POINT('Ctrl Pts',(97.6592130710845,0.841388013829169,-4.61196309337439));
#34858=CARTESIAN_POINT('Ctrl Pts',(97.6257441842029,0.885434268610102,-4.60896366966229));
#34859=CARTESIAN_POINT('Ctrl Pts',(97.5922445275275,0.929521017542661,-4.60596148841453));
#34860=CARTESIAN_POINT('Ctrl Pts',(97.5562493925602,0.971690890188859,-4.60295930716676));
#34861=CARTESIAN_POINT('Ctrl Pts',(97.5180143990828,1.01165965283609,-4.59995712591899));
#34862=CARTESIAN_POINT('Ctrl Pts',(97.4797620018851,1.05164660837684,-4.59695357814496));
#34863=CARTESIAN_POINT('Ctrl Pts',(97.4392681006136,1.08943009579091,-4.59395003037094));
#34864=CARTESIAN_POINT('Ctrl Pts',(97.3968240851684,1.12476387852332,-4.59094648259691));
#34865=CARTESIAN_POINT('Ctrl Pts',(97.3542999637872,1.1601643478242,-4.58793726613193));
#34866=CARTESIAN_POINT('Ctrl Pts',(97.3098188012856,1.19310556140108,-4.58492804966696));
#34867=CARTESIAN_POINT('Ctrl Pts',(97.2637029154812,1.22338331012362,-4.58191883320198));
#34868=CARTESIAN_POINT('Ctrl Pts',(97.2284223728636,1.24654702877576,-4.57961665927892));
#34869=CARTESIAN_POINT('Ctrl Pts',(97.1921857029053,1.26815271871278,-4.57731448535586));
#34870=CARTESIAN_POINT('Ctrl Pts',(97.1551462249608,1.28812748017268,-4.5750123114328));
#34871=CARTESIAN_POINT('Ctrl Pts',(97.1067165242152,1.31424479536312,-4.57200218277157));
#34872=CARTESIAN_POINT('Ctrl Pts',(97.0567101214196,1.33768197282204,-4.56899205411033));
#34873=CARTESIAN_POINT('Ctrl Pts',(97.005454844163,1.35824729126172,-4.56598192544909));
#34874=CARTESIAN_POINT('Ctrl Pts',(96.9542906619762,1.37877605933586,-4.56297714663465));
#34875=CARTESIAN_POINT('Ctrl Pts',(96.9018824963136,1.39644290244907,-4.55997236782021));
#34876=CARTESIAN_POINT('Ctrl Pts',(96.8485818854573,1.41110237529701,-4.55696758900576));
#34877=CARTESIAN_POINT('Ctrl Pts',(96.7953340067249,1.42574734502525,-4.55396578292214));
#34878=CARTESIAN_POINT('Ctrl Pts',(96.7411959385386,1.4373906990429,-4.55096397683853));
#34879=CARTESIAN_POINT('Ctrl Pts',(96.6865365087437,1.44593607540922,-4.54796217075491));
#34880=CARTESIAN_POINT('Ctrl Pts',(96.6319095662466,1.45447637275829,-4.54496214882031));
#34881=CARTESIAN_POINT('Ctrl Pts',(96.5767623970712,1.45992226064101,-4.54196212688571));
#34882=CARTESIAN_POINT('Ctrl Pts',(96.5214739395565,1.46222847228925,-4.53896210495112));
#34883=CARTESIAN_POINT('Ctrl Pts',(96.4661965068944,1.46453422406495,-4.53596268123903));
#34884=CARTESIAN_POINT('Ctrl Pts',(96.4107783692063,1.46370152095767,-4.53296325752694));
#34885=CARTESIAN_POINT('Ctrl Pts',(96.3556011770071,1.45973712815208,-4.52996383381485));
#34886=CARTESIAN_POINT('Ctrl Pts',(96.3003732573715,1.45576909066151,-4.52696165256709));
#34887=CARTESIAN_POINT('Ctrl Pts',(96.2453872536722,1.44866364926291,-4.52395947131933));
#34888=CARTESIAN_POINT('Ctrl Pts',(96.1910208889382,1.43847958821824,-4.52095729007157));
#34889=CARTESIAN_POINT('Ctrl Pts',(96.1366297778418,1.42829089161505,-4.51795374229756));
#34890=CARTESIAN_POINT('Ctrl Pts',(96.0828593815767,1.41502090869013,-4.51495019452354));
#34891=CARTESIAN_POINT('Ctrl Pts',(96.0300751441821,1.39877914364003,-4.51194664674952));
#34892=CARTESIAN_POINT('Ctrl Pts',(95.9771912854226,1.38250672499177,-4.50893743028456));
#34893=CARTESIAN_POINT('Ctrl Pts',(95.9252977999323,1.36325150406209,-4.50592821381959));
#34894=CARTESIAN_POINT('Ctrl Pts',(95.8747418315436,1.34117185163032,-4.50291899735463));
#34895=CARTESIAN_POINT('Ctrl Pts',(95.8360644437792,1.3242800126244,-4.5006168234315));
#34896=CARTESIAN_POINT('Ctrl Pts',(95.7981695227691,1.30573609046451,-4.49831464950837));
#34897=CARTESIAN_POINT('Ctrl Pts',(95.7612018971196,1.28562866209272,-4.49601247558525));
#34898=CARTESIAN_POINT('Ctrl Pts',(95.7128661443829,1.25933788282638,-4.49300234692401));
#34899=CARTESIAN_POINT('Ctrl Pts',(95.665913575316,1.23026215642405,-4.48999221826277));
#34900=CARTESIAN_POINT('Ctrl Pts',(95.620683885365,1.19857129155546,-4.48698208960154));
#34901=CARTESIAN_POINT('Ctrl Pts',(95.5755345813174,1.16693675028326,-4.48397731078709));
#34902=CARTESIAN_POINT('Ctrl Pts',(95.5321025087596,1.13269659480699,-4.48097253197265));
#34903=CARTESIAN_POINT('Ctrl Pts',(95.4907015611857,1.09606577715547,-4.47796775315821));
#34904=CARTESIAN_POINT('Ctrl Pts',(95.4493415729904,1.05947119962927,-4.47496594707459));
#34905=CARTESIAN_POINT('Ctrl Pts',(95.4100091227119,1.02049099343673,-4.47196414099097));
#34906=CARTESIAN_POINT('Ctrl Pts',(95.3729864421558,0.979381410038385,-4.46896233490735));
#34907=CARTESIAN_POINT('Ctrl Pts',(95.3359857663454,0.938296260471181,-4.46596231297275));
#34908=CARTESIAN_POINT('Ctrl Pts',(95.3012924919278,0.89508463387512,-4.46296229103815));
#34909=CARTESIAN_POINT('Ctrl Pts',(95.2691515814606,0.85003916772303,-4.45996226910356));
#34910=CARTESIAN_POINT('Ctrl Pts',(95.2370170800852,0.805002683909167,-4.45696284539147));
#34911=CARTESIAN_POINT('Ctrl Pts',(95.2074342384654,0.758133516421519,-4.45396342167937));
#34912=CARTESIAN_POINT('Ctrl Pts',(95.1806059229202,0.709755004308049,-4.45096399796728));
#34913=CARTESIAN_POINT('Ctrl Pts',(95.1537529426247,0.661332015159822,-4.44796181671952));
#34914=CARTESIAN_POINT('Ctrl Pts',(95.1296598044568,0.611397371939726,-4.44495963547177));
#34915=CARTESIAN_POINT('Ctrl Pts',(95.1084836613955,0.560299547340288,-4.44195745422401));
#34916=CARTESIAN_POINT('Ctrl Pts',(95.0872978794238,0.509178464145387,-4.43895390644999));
#34917=CARTESIAN_POINT('Ctrl Pts',(95.0690319138202,0.456893643576649,-4.43595035867597));
#34918=CARTESIAN_POINT('Ctrl Pts',(95.0537937290614,0.40381098751529,-4.43294681090195));
#34919=CARTESIAN_POINT('Ctrl Pts',(95.0385267847933,0.350628146874057,-4.42993759443699));
#34920=CARTESIAN_POINT('Ctrl Pts',(95.0262991537784,0.296644979042319,-4.42692837797202));
#34921=CARTESIAN_POINT('Ctrl Pts',(95.017167874254,0.242238759494667,-4.42391916150706));
#34922=CARTESIAN_POINT('Ctrl Pts',(95.0101820711884,0.200615771797781,-4.42161698758393));
#34923=CARTESIAN_POINT('Ctrl Pts',(95.0050074689897,0.158745429316313,-4.4193148136608));
#34924=CARTESIAN_POINT('Ctrl Pts',(95.0016490158668,0.116797427999157,-4.41701263973768));
#34925=CARTESIAN_POINT('Ctrl Pts',(94.9972577855166,0.0619497556413082,
-4.41400251107644));
#34926=CARTESIAN_POINT('Ctrl Pts',(94.9959547894712,0.00673885265002533,
-4.4109923824152));
#34927=CARTESIAN_POINT('Ctrl Pts',(94.997783416658,-0.0484579941058989,
-4.40798225375396));
#34928=CARTESIAN_POINT('Ctrl Pts',(94.9996087938591,-0.103556740512358,
-4.40497747493951));
#34929=CARTESIAN_POINT('Ctrl Pts',(95.0045547316256,-0.158640956702821,
-4.40197269612507));
#34930=CARTESIAN_POINT('Ctrl Pts',(95.0126127120214,-0.213330299483491,
-4.39896791731062));
#34931=CARTESIAN_POINT('Ctrl Pts',(95.0206627203807,-0.267965536220054,
-4.395966111227));
#34932=CARTESIAN_POINT('Ctrl Pts',(95.0318185957106,-0.322206153522478,
-4.39296430514338));
#34933=CARTESIAN_POINT('Ctrl Pts',(95.0460199308673,-0.375675759865854,
-4.38996249905976));
#34934=CARTESIAN_POINT('Ctrl Pts',(95.0602128253395,-0.429113586093144,
-4.38696247712516));
#34935=CARTESIAN_POINT('Ctrl Pts',(95.0774474566162,-0.481780800255754,
-4.38396245519056));
#34936=CARTESIAN_POINT('Ctrl Pts',(95.0976125795179,-0.53331234365282,-4.38096243325596));
#34937=CARTESIAN_POINT('Ctrl Pts',(95.1177736813723,-0.584833611348646,
-4.37796300954387));
#34938=CARTESIAN_POINT('Ctrl Pts',(95.140863922,-0.635219166491393,-4.37496358583178));
#34939=CARTESIAN_POINT('Ctrl Pts',(95.1667233416066,-0.684122431892717,
-4.37196416211969));
#34940=CARTESIAN_POINT('Ctrl Pts',(95.1926065352042,-0.733070656763449,
-4.36896198087193));
#34941=CARTESIAN_POINT('Ctrl Pts',(95.2212637466744,-0.780533401427555,
-4.36595979962417));
#34942=CARTESIAN_POINT('Ctrl Pts',(95.2524889885297,-0.826188641924519,
-4.36295761837641));
#34943=CARTESIAN_POINT('Ctrl Pts',(95.2837284434219,-0.871864663673477,
-4.35995407060239));
#34944=CARTESIAN_POINT('Ctrl Pts',(95.3175379358857,-0.915731122166067,
-4.35695052282837));
#34945=CARTESIAN_POINT('Ctrl Pts',(95.3536700046144,-0.957497666895822,
-4.35394697505435));
#34946=CARTESIAN_POINT('Ctrl Pts',(95.389870266542,-0.999343038949732,-4.35093775858938));
#34947=CARTESIAN_POINT('Ctrl Pts',(95.4284014928612,-1.03908019999244,-4.34792854212442));
#34948=CARTESIAN_POINT('Ctrl Pts',(95.4689788706773,-1.07645523712673,-4.34491932565945));
#34949=CARTESIAN_POINT('Ctrl Pts',(95.5000222276987,-1.10504867228423,-4.34261715173634));
#34950=CARTESIAN_POINT('Ctrl Pts',(95.5322623840527,-1.13226033165432,-4.34031497781323));
#34951=CARTESIAN_POINT('Ctrl Pts',(95.5655599184972,-1.15799334977846,-4.33801280389012));
#34952=CARTESIAN_POINT('Ctrl Pts',(95.6090969691839,-1.1916396762432,-4.33500267522888));
#34953=CARTESIAN_POINT('Ctrl Pts',(95.6546256344026,-1.22289799115637,-4.33199254656764));
#34954=CARTESIAN_POINT('Ctrl Pts',(95.7018536337863,-1.25152580705963,-4.3289824179064));
#34955=CARTESIAN_POINT('Ctrl Pts',(95.7489976957078,-1.28010274326757,-4.32597763909196));
#34956=CARTESIAN_POINT('Ctrl Pts',(95.7978346502252,-1.30605818676549,-4.32297286027752));
#34957=CARTESIAN_POINT('Ctrl Pts',(95.8480412955106,-1.32919145352617,-4.31996808146307));
#34958=CARTESIAN_POINT('Ctrl Pts',(95.8981982696384,-1.35230183375197,-4.31696627537945));
#34959=CARTESIAN_POINT('Ctrl Pts',(95.9497217728902,-1.37259534829205,-4.31396446929583));
#34960=CARTESIAN_POINT('Ctrl Pts',(96.0022635610076,-1.38991693090367,-4.31096266321221));
#34961=CARTESIAN_POINT('Ctrl Pts',(96.0547741204656,-1.40722821828508,-4.30796264127761));
#34962=CARTESIAN_POINT('Ctrl Pts',(96.1083012646293,-1.42157090982359,-4.30496261934302));
#34963=CARTESIAN_POINT('Ctrl Pts',(96.1624784630826,-1.43283870970991,-4.30196259740842));
#34964=CARTESIAN_POINT('Ctrl Pts',(96.216644858275,-1.44410426272882,-4.29896317369633));
#34965=CARTESIAN_POINT('Ctrl Pts',(96.271460533566,-1.45229603431268,-4.29596374998423));
#34966=CARTESIAN_POINT('Ctrl Pts',(96.3265478198291,-1.45735862667908,-4.29296432627214));
#34967=CARTESIAN_POINT('Ctrl Pts',(96.3816857508732,-1.4624258733659,-4.28996214502438));
#34968=CARTESIAN_POINT('Ctrl Pts',(96.4370952647414,-1.4643581448739,-4.28695996377662));
#34969=CARTESIAN_POINT('Ctrl Pts',(96.4923941069457,-1.46315200863983,-4.28395778252887));
#34970=CARTESIAN_POINT('Ctrl Pts',(96.5477181199555,-1.46194532339932,-4.28095423475485));
#34971=CARTESIAN_POINT('Ctrl Pts',(96.6029308334775,-1.4575974242657,-4.27795068698083));
#34972=CARTESIAN_POINT('Ctrl Pts',(96.6576538592619,-1.45015692036635,-4.27494713920681));
#34973=CARTESIAN_POINT('Ctrl Pts',(96.7124801655479,-1.44270237376806,-4.27193792274184));
#34974=CARTESIAN_POINT('Ctrl Pts',(96.766814418167,-1.43214366353828,-4.26892870627687));
#34975=CARTESIAN_POINT('Ctrl Pts',(96.8202883375866,-1.41858059113104,-4.26591948981191));
#34976=CARTESIAN_POINT('Ctrl Pts',(96.8611980774767,-1.40820428488095,-4.26361731588879));
#34977=CARTESIAN_POINT('Ctrl Pts',(96.9016044694145,-1.39607063011443,-4.26131514196567));
#34978=CARTESIAN_POINT('Ctrl Pts',(96.9413502067518,-1.38224346896779,-4.25901296804255));
#34979=CARTESIAN_POINT('Ctrl Pts',(96.9933183842731,-1.36416423800567,-4.25600283938132));
#34980=CARTESIAN_POINT('Ctrl Pts',(97.0443747482134,-1.34311217613538,-4.25299271072008));
#34981=CARTESIAN_POINT('Ctrl Pts',(97.0941565079554,-1.31919958183506,-4.24998258205884));
#34982=CARTESIAN_POINT('Ctrl Pts',(97.1438497914834,-1.29532948695265,-4.2469778032444));
#34983=CARTESIAN_POINT('Ctrl Pts',(97.1922724941834,-1.26860917563466,-4.24397302442995));
#34984=CARTESIAN_POINT('Ctrl Pts',(97.2390799415717,-1.23919968514556,-4.24096824561551));
#34985=CARTESIAN_POINT('Ctrl Pts',(97.2858410807456,-1.20981929047493,-4.23796643953189));
#34986=CARTESIAN_POINT('Ctrl Pts',(97.3309896852464,-1.17775526653294,-4.23496463344827));
#34987=CARTESIAN_POINT('Ctrl Pts',(97.3742056036268,-1.14321454967189,-4.23196282736466));
#34988=CARTESIAN_POINT('Ctrl Pts',(97.4173958362581,-1.10869436238017,-4.22896280543006));
#34989=CARTESIAN_POINT('Ctrl Pts',(97.4586552478697,-1.07170072892314,-4.22596278349546));
#34990=CARTESIAN_POINT('Ctrl Pts',(97.4976945420802,-1.0324825487758,-4.22296276156086));
#34991=CARTESIAN_POINT('Ctrl Pts',(97.5367260516195,-0.993272188970639,
-4.21996333784877));
#34992=CARTESIAN_POINT('Ctrl Pts',(97.5735379505794,-0.951838537499286,
-4.21696391413667));
#34993=CARTESIAN_POINT('Ctrl Pts',(97.6078774848983,-0.908467633288419,
-4.21396449042458));
#34994=CARTESIAN_POINT('Ctrl Pts',(97.6422485894453,-0.865056855812966,
-4.21096230917682));
#34995=CARTESIAN_POINT('Ctrl Pts',(97.6741424596976,-0.819705682282122,
-4.20796012792906));
#34996=CARTESIAN_POINT('Ctrl Pts',(97.7033473584394,-0.77273238557824,-4.20495794668131));
#34997=CARTESIAN_POINT('Ctrl Pts',(97.7325655506029,-0.725737707672449,
-4.20195439890729));
#34998=CARTESIAN_POINT('Ctrl Pts',(97.7590920779884,-0.677119899143029,
-4.19895085113327));
#34999=CARTESIAN_POINT('Ctrl Pts',(97.7827609021939,-0.627222430169181,
-4.19594730335925));
#35000=CARTESIAN_POINT('Ctrl Pts',(97.8064743973219,-0.577230788120041,
-4.19293808689429));
#35001=CARTESIAN_POINT('Ctrl Pts',(97.8273192156744,-0.525955151437095,
-4.18992887042932));
#35002=CARTESIAN_POINT('Ctrl Pts',(97.8451777171641,-0.473758495262967,
-4.18691965396436));
#35003=CARTESIAN_POINT('Ctrl Pts',(97.8588402027029,-0.433825914101916,
-4.18461748004123));
#35004=CARTESIAN_POINT('Ctrl Pts',(97.8707558342186,-0.393354692066864,
-4.18231530611811));
#35005=CARTESIAN_POINT('Ctrl Pts',(97.8808921294835,-0.352511460801676,
-4.18001313219499));
#35006=CARTESIAN_POINT('Ctrl Pts',(97.8981315172016,-0.283046998585734,
-4.17609769092005));
#35007=CARTESIAN_POINT('Ctrl Pts',(97.9102820849996,-0.212273263424402,
-4.17218224964512));
#35008=CARTESIAN_POINT('Ctrl Pts',(97.917188724932,-0.140835745534943,-4.16826680837019));
#35009=CARTESIAN_POINT('Ctrl Pts',(97.9216643126592,-0.094543354233742,
-4.16572955420779));
#35010=CARTESIAN_POINT('Ctrl Pts',(97.9239387713273,-0.0479725928676012,
-4.1631923000454));
#35011=CARTESIAN_POINT('Ctrl Pts',(97.9239803682192,-0.00130446693377829,
-4.16065504588301));
#35012=CARTESIAN_POINT('Ctrl Pts',(97.9239803685999,-0.00130403978581689,
-4.08934495418713));
#35013=CARTESIAN_POINT('Ctrl Pts',(97.9239152216095,-0.0744172864775993,
-4.0933212267369));
#35014=CARTESIAN_POINT('Ctrl Pts',(97.9183674533638,-0.147291162013056,
-4.09729749928667));
#35015=CARTESIAN_POINT('Ctrl Pts',(97.9074660957169,-0.219240135127319,
-4.10127377183644));
#35016=CARTESIAN_POINT('Ctrl Pts',(97.9013270157352,-0.25975807012678,-4.10351300258204));
#35017=CARTESIAN_POINT('Ctrl Pts',(97.8934909747883,-0.299983198187053,
-4.10575223332764));
#35018=CARTESIAN_POINT('Ctrl Pts',(97.8839874350564,-0.339796315162533,
-4.10799146407324));
#35019=CARTESIAN_POINT('Ctrl Pts',(97.8712121204148,-0.393315857414546,
-4.11100159273448));
#35020=CARTESIAN_POINT('Ctrl Pts',(97.8553875073782,-0.446226378391438,
-4.11401172139571));
#35021=CARTESIAN_POINT('Ctrl Pts',(97.8365889378747,-0.498155652927126,
-4.11702185005695));
#35022=CARTESIAN_POINT('Ctrl Pts',(97.8178237787261,-0.54999263450987,-4.12002662887139));
#35023=CARTESIAN_POINT('Ctrl Pts',(97.7960953306467,-0.600851337971159,
-4.12303140768584));
#35024=CARTESIAN_POINT('Ctrl Pts',(97.7715292457042,-0.650372674104551,
-4.12603618650028));
#35025=CARTESIAN_POINT('Ctrl Pts',(97.7469874648329,-0.699845017080199,
-4.1290379925839));
#35026=CARTESIAN_POINT('Ctrl Pts',(97.7196138419051,-0.747982142955423,
-4.13203979866751));
#35027=CARTESIAN_POINT('Ctrl Pts',(97.6895821564042,-0.79444475791324,-4.13504160475113));
#35028=CARTESIAN_POINT('Ctrl Pts',(97.6595683204915,-0.840879757419996,
-4.13804162668572));
#35029=CARTESIAN_POINT('Ctrl Pts',(97.6268998394661,-0.885641776033794,
-4.14104164862032));
#35030=CARTESIAN_POINT('Ctrl Pts',(97.5917953392551,-0.928418010223474,
-4.14404167055491));
#35031=CARTESIAN_POINT('Ctrl Pts',(97.5566978390935,-0.971185714573505,
-4.147041094267));
#35032=CARTESIAN_POINT('Ctrl Pts',(97.5191656192783,-1.01196801287829,-4.15004051797909));
#35033=CARTESIAN_POINT('Ctrl Pts',(97.4794579233039,-1.05048473430816,-4.15303994169118));
#35034=CARTESIAN_POINT('Ctrl Pts',(97.4397137218542,-1.08903686628464,-4.15604212293894));
#35035=CARTESIAN_POINT('Ctrl Pts',(97.3977904283256,-1.1253188915866,-4.15904430418669));
#35036=CARTESIAN_POINT('Ctrl Pts',(97.3539834718479,-1.15908821609728,-4.16204648543445));
#35037=CARTESIAN_POINT('Ctrl Pts',(97.310156575416,-1.19287291165484,-4.16505003320847));
#35038=CARTESIAN_POINT('Ctrl Pts',(97.2644447435136,-1.2241423277905,-4.16805358098248));
#35039=CARTESIAN_POINT('Ctrl Pts',(97.2171730593664,-1.25269681127658,-4.1710571287565));
#35040=CARTESIAN_POINT('Ctrl Pts',(97.1698121578708,-1.28130518654472,-4.17406634522146));
#35041=CARTESIAN_POINT('Ctrl Pts',(97.1208859910793,-1.3071881456583,-4.17707556168643));
#35042=CARTESIAN_POINT('Ctrl Pts',(97.0707439034656,-1.33019223314197,-4.18008477815139));
#35043=CARTESIAN_POINT('Ctrl Pts',(97.0323831514559,-1.34779130284898,-4.18238695207452));
#35044=CARTESIAN_POINT('Ctrl Pts',(96.9933112546867,-1.36370635768066,-4.18468912599766));
#35045=CARTESIAN_POINT('Ctrl Pts',(96.9536907462404,-1.37788836502644,-4.18699129992079));
#35046=CARTESIAN_POINT('Ctrl Pts',(96.9018863074669,-1.39643156298229,-4.19000142858203));
#35047=CARTESIAN_POINT('Ctrl Pts',(96.8489258157292,-1.41208812463287,-4.19301155724327));
#35048=CARTESIAN_POINT('Ctrl Pts',(96.7951621861553,-1.42471776850098,-4.19602168590452));
#35049=CARTESIAN_POINT('Ctrl Pts',(96.7414941097001,-1.43732496593328,-4.19902646471897));
#35050=CARTESIAN_POINT('Ctrl Pts',(96.687026238061,-1.44691580181003,-4.20203124353341));
#35051=CARTESIAN_POINT('Ctrl Pts',(96.6321279739089,-1.45339930818685,-4.20503602234786));
#35052=CARTESIAN_POINT('Ctrl Pts',(96.577284022494,-1.45987640020825,-4.20803782843149));
#35053=CARTESIAN_POINT('Ctrl Pts',(96.5220110439524,-1.46325219091205,-4.21103963451512));
#35054=CARTESIAN_POINT('Ctrl Pts',(96.4666881584148,-1.46348683648281,-4.21404144059874));
#35055=CARTESIAN_POINT('Ctrl Pts',(96.4113981545055,-1.46372134258997,-4.21704146253335));
#35056=CARTESIAN_POINT('Ctrl Pts',(96.3560588294504,-1.46081840177854,-4.22004148446795));
#35057=CARTESIAN_POINT('Ctrl Pts',(96.3010516209737,-1.45479020452473,-4.22304150640256));
#35058=CARTESIAN_POINT('Ctrl Pts',(96.2460553812668,-1.44876320932988,-4.22604093011465));
#35059=CARTESIAN_POINT('Ctrl Pts',(96.1913916512949,-1.43961225283038,-4.22904035382675));
#35060=CARTESIAN_POINT('Ctrl Pts',(96.1374367312958,-1.42740137418846,-4.23203977753885));
#35061=CARTESIAN_POINT('Ctrl Pts',(96.0834322075626,-1.41517926941224,-4.23504195878662));
#35062=CARTESIAN_POINT('Ctrl Pts',(96.0301383119069,-1.39989173899873,-4.23804414003438));
#35063=CARTESIAN_POINT('Ctrl Pts',(95.9779196447471,-1.3816536603219,-4.24104632128215));
#35064=CARTESIAN_POINT('Ctrl Pts',(95.9256772088093,-1.36340728007651,-4.24404986905617));
#35065=CARTESIAN_POINT('Ctrl Pts',(95.8745114657393,-1.34220787684331,-4.2470534168302));
#35066=CARTESIAN_POINT('Ctrl Pts',(95.8247672546869,-1.31821862683288,-4.25005696460422));
#35067=CARTESIAN_POINT('Ctrl Pts',(95.7749291598078,-1.29418410115029,-4.25306618106919));
#35068=CARTESIAN_POINT('Ctrl Pts',(95.726518419494,-1.26734946696852,-4.25607539753417));
#35069=CARTESIAN_POINT('Ctrl Pts',(95.6798544372851,-1.23792346221688,-4.25908461399914));
#35070=CARTESIAN_POINT('Ctrl Pts',(95.6441545784552,-1.21541136260953,-4.26138678792221));
#35071=CARTESIAN_POINT('Ctrl Pts',(95.6094765607002,-1.19138352101,-4.26368896184529));
#35072=CARTESIAN_POINT('Ctrl Pts',(95.5759502575892,-1.1659492720233,-4.26599113576837));
#35073=CARTESIAN_POINT('Ctrl Pts',(95.5321140882677,-1.13269359091056,-4.2690012644296));
#35074=CARTESIAN_POINT('Ctrl Pts',(95.4900638917384,-1.0968924375822,-4.27201139309084));
#35075=CARTESIAN_POINT('Ctrl Pts',(95.4501099889542,-1.05876473870739,-4.27502152175207));
#35076=CARTESIAN_POINT('Ctrl Pts',(95.410227095513,-1.0207048034967,-4.27802630056651));
#35077=CARTESIAN_POINT('Ctrl Pts',(95.3724334811049,-0.98032689018171,-4.28103107938095));
#35078=CARTESIAN_POINT('Ctrl Pts',(95.3370071740009,-0.937890678913456,
-4.2840358581954));
#35079=CARTESIAN_POINT('Ctrl Pts',(95.3016159153585,-0.895496451245696,
-4.28703766427901));
#35080=CARTESIAN_POINT('Ctrl Pts',(95.2685876612969,-0.851048362947523,
-4.29003947036263));
#35081=CARTESIAN_POINT('Ctrl Pts',(95.2381629318349,-0.80484216682723,-4.29304127644625));
#35082=CARTESIAN_POINT('Ctrl Pts',(95.2077562855701,-0.75866343375327,-4.29604129838084));
#35083=CARTESIAN_POINT('Ctrl Pts',(95.1799503866571,-0.710729104212465,
-4.29904132031544));
#35084=CARTESIAN_POINT('Ctrl Pts',(95.1549434413191,-0.661365303392652,
-4.30204134225003));
#35085=CARTESIAN_POINT('Ctrl Pts',(95.1299414825171,-0.612011346013121,
-4.30504076596212));
#35086=CARTESIAN_POINT('Ctrl Pts',(95.1077376073965,-0.561228954292048,
-4.30804018967421));
#35087=CARTESIAN_POINT('Ctrl Pts',(95.0884837904084,-0.509368280552822,
-4.3110396133863));
#35088=CARTESIAN_POINT('Ctrl Pts',(95.0692122723243,-0.457459928435557,
-4.31404179463405));
#35089=CARTESIAN_POINT('Ctrl Pts',(95.0528964151029,-0.404471809923728,
-4.31704397588181));
#35090=CARTESIAN_POINT('Ctrl Pts',(95.0396392220891,-0.35077205622647,-4.32004615712956));
#35091=CARTESIAN_POINT('Ctrl Pts',(95.0263759946955,-0.297047859593382,
-4.32304970490358));
#35092=CARTESIAN_POINT('Ctrl Pts',(95.0161743042849,-0.242611902045981,
-4.3260532526776));
#35093=CARTESIAN_POINT('Ctrl Pts',(95.0090859051473,-0.187842154493746,
-4.32905680045161));
#35094=CARTESIAN_POINT('Ctrl Pts',(95.0019841278492,-0.132969038260377,
-4.33206601691658));
#35095=CARTESIAN_POINT('Ctrl Pts',(94.9980074177096,-0.0777614015979497,
-4.33507523338154));
#35096=CARTESIAN_POINT('Ctrl Pts',(94.997155471935,-0.022600807152141,-4.3380844498465));
#35097=CARTESIAN_POINT('Ctrl Pts',(94.996503698502,0.0195993082588217,-4.34038662376964));
#35098=CARTESIAN_POINT('Ctrl Pts',(94.9976797297326,0.061771799743154,-4.34268879769278));
#35099=CARTESIAN_POINT('Ctrl Pts',(95.0006629573609,0.10374815469235,-4.34499097161592));
#35100=CARTESIAN_POINT('Ctrl Pts',(95.0045635744675,0.158632899870289,-4.34800110027716));
#35101=CARTESIAN_POINT('Ctrl Pts',(95.0115719415834,0.213412680795123,-4.35101122893839));
#35102=CARTESIAN_POINT('Ctrl Pts',(95.0216742598818,0.267707974644417,-4.35402135759963));
#35103=CARTESIAN_POINT('Ctrl Pts',(95.031758623514,0.321906770457785,-4.35702613641407));
#35104=CARTESIAN_POINT('Ctrl Pts',(95.0449259300541,0.375622272989015,-4.36003091522852));
#35105=CARTESIAN_POINT('Ctrl Pts',(95.0611106039428,0.428479737863484,-4.36303569404296));
#35106=CARTESIAN_POINT('Ctrl Pts',(95.077279265778,0.481284909033545,-4.36603750012658));
#35107=CARTESIAN_POINT('Ctrl Pts',(95.0964592275933,0.533233221657604,-4.3690393062102));
#35108=CARTESIAN_POINT('Ctrl Pts',(95.1185342076463,0.583961635573341,-4.37204111229382));
#35109=CARTESIAN_POINT('Ctrl Pts',(95.1405960672468,0.634659898624063,-4.37504113422842));
#35110=CARTESIAN_POINT('Ctrl Pts',(95.16554932428,0.684139216791593,-4.37804115616302));
#35111=CARTESIAN_POINT('Ctrl Pts',(95.1932291392264,0.732055393507343,-4.38104117809761));
#35112=CARTESIAN_POINT('Ctrl Pts',(95.2209034346504,0.779962015447825,-4.3840406018097));
#35113=CARTESIAN_POINT('Ctrl Pts',(95.2513029442182,0.826305657917133,-4.38704002552179));
#35114=CARTESIAN_POINT('Ctrl Pts',(95.2842174441787,0.870767716367634,-4.39003944923389));
#35115=CARTESIAN_POINT('Ctrl Pts',(95.3171622042546,0.915270651241015,-4.39304163048164));
#35116=CARTESIAN_POINT('Ctrl Pts',(95.3526262592382,0.957888120715592,-4.3960438117294));
#35117=CARTESIAN_POINT('Ctrl Pts',(95.3903575699578,0.998332711270284,-4.39904599297716));
#35118=CARTESIAN_POINT('Ctrl Pts',(95.4281060551324,1.03879571130479,-4.40204954075118));
#35119=CARTESIAN_POINT('Ctrl Pts',(95.4681234710175,1.07708349509045,-4.4050530885252));
#35120=CARTESIAN_POINT('Ctrl Pts',(95.5101215351449,1.11294619519553,-4.40805663629922));
#35121=CARTESIAN_POINT('Ctrl Pts',(95.5521988635503,1.1488765801116,-4.41106585276419));
#35122=CARTESIAN_POINT('Ctrl Pts',(95.5962638862456,1.18237241782698,-4.41407506922915));
#35123=CARTESIAN_POINT('Ctrl Pts',(95.6419968688008,1.21322547760752,-4.41708428569412));
#35124=CARTESIAN_POINT('Ctrl Pts',(95.6769844747412,1.23682933279781,-4.41938645961724));
#35125=CARTESIAN_POINT('Ctrl Pts',(95.7129476501924,1.25888725878573,-4.42168863354036));
#35126=CARTESIAN_POINT('Ctrl Pts',(95.7497340010342,1.27932444092072,-4.42399080746349));
#35127=CARTESIAN_POINT('Ctrl Pts',(95.7978327341053,1.30604637842581,-4.42700093612473));
#35128=CARTESIAN_POINT('Ctrl Pts',(95.8475416191947,1.33010813960356,-4.43001106478597));
#35129=CARTESIAN_POINT('Ctrl Pts',(95.8985352560998,1.35131391156252,-4.43302119344721));
#35130=CARTESIAN_POINT('Ctrl Pts',(95.9494382629437,1.37248199488957,-4.43602597226165));
#35131=CARTESIAN_POINT('Ctrl Pts',(96.0016210065593,1.39080396100805,-4.43903075107609));
#35132=CARTESIAN_POINT('Ctrl Pts',(96.0547337982194,1.40612997235859,-4.44203552989054));
#35133=CARTESIAN_POINT('Ctrl Pts',(96.1077940435715,1.42144082116003,-4.44503733597416));
#35134=CARTESIAN_POINT('Ctrl Pts',(96.1617820093186,1.43376144103936,-4.44803914205778));
#35135=CARTESIAN_POINT('Ctrl Pts',(96.2163301036668,1.44299085736582,-4.4510409481414));
#35136=CARTESIAN_POINT('Ctrl Pts',(96.2708457768904,1.45221478811005,-4.454040970076));
#35137=CARTESIAN_POINT('Ctrl Pts',(96.3259203991757,1.45835106898929,-4.4570409920106));
#35138=CARTESIAN_POINT('Ctrl Pts',(96.3811756289667,1.4613496898836,-4.4600410139452));
#35139=CARTESIAN_POINT('Ctrl Pts',(96.4364198405309,1.46434771283477,-4.4630404376573));
#35140=CARTESIAN_POINT('Ctrl Pts',(96.4918440610336,1.46420928974961,-4.46603986136939));
#35141=CARTESIAN_POINT('Ctrl Pts',(96.5470665851594,1.46093640440328,-4.46903928508148));
#35142=CARTESIAN_POINT('Ctrl Pts',(96.6023398783976,1.45766051011292,-4.47204146632924));
#35143=CARTESIAN_POINT('Ctrl Pts',(96.6574105764688,1.4512444276434,-4.475043647577));
#35144=CARTESIAN_POINT('Ctrl Pts',(96.7119002495997,1.44174220496457,-4.47804582882476));
#35145=CARTESIAN_POINT('Ctrl Pts',(96.7664147252203,1.43223565708491,-4.48104937659878));
#35146=CARTESIAN_POINT('Ctrl Pts',(96.8203471335242,1.41964028905232,-4.4840529243728));
#35147=CARTESIAN_POINT('Ctrl Pts',(96.8733306874039,1.40406101860863,-4.48705647214682));
#35148=CARTESIAN_POINT('Ctrl Pts',(96.9264142388247,1.38845234491386,-4.49006568861178));
#35149=CARTESIAN_POINT('Ctrl Pts',(96.9785448598012,1.36984869672328,-4.49307490507675));
#35150=CARTESIAN_POINT('Ctrl Pts',(97.029373449852,1.34840408377119,-4.49608412154172));
#35151=CARTESIAN_POINT('Ctrl Pts',(97.0682594043608,1.33199807599333,-4.49838629546483));
#35152=CARTESIAN_POINT('Ctrl Pts',(97.1063836489081,1.3139303128472,-4.50068846938794));
#35153=CARTESIAN_POINT('Ctrl Pts',(97.1436002566615,1.29428755007857,-4.50299064331105));
#35154=CARTESIAN_POINT('Ctrl Pts',(97.1922615574208,1.26860432840617,-4.50600077197229));
#35155=CARTESIAN_POINT('Ctrl Pts',(97.2395746696548,1.24011905118202,-4.50901090063353));
#35156=CARTESIAN_POINT('Ctrl Pts',(97.2851977974036,1.20899725843814,-4.51202102929476));
#35157=CARTESIAN_POINT('Ctrl Pts',(97.3307398399993,1.17793077788913,-4.51502580810921));
#35158=CARTESIAN_POINT('Ctrl Pts',(97.3745974259837,1.14423737608224,-4.51803058692365));
#35159=CARTESIAN_POINT('Ctrl Pts',(97.4164539938206,1.10812805608364,-4.5210353657381));
#35160=CARTESIAN_POINT('Ctrl Pts',(97.458269151518,1.07205446027483,-4.52403717182171));
#35161=CARTESIAN_POINT('Ctrl Pts',(97.4980868147994,1.03357002432292,-4.52703897790533));
#35162=CARTESIAN_POINT('Ctrl Pts',(97.5356215639806,0.992927444106501,-4.53004078398895));
#35163=CARTESIAN_POINT('Ctrl Pts',(97.5731340040638,0.952309020153915,-4.53304080592355));
#35164=CARTESIAN_POINT('Ctrl Pts',(97.6083658618605,0.909535381553906,-4.53604082785815));
#35165=CARTESIAN_POINT('Ctrl Pts',(97.6410685282083,0.864896074208625,-4.53904084979275));
#35166=CARTESIAN_POINT('Ctrl Pts',(97.6737646734467,0.820265668211052,-4.54204027350484));
#35167=CARTESIAN_POINT('Ctrl Pts',(97.7039323168962,0.773770758081098,-4.54503969721693));
#35168=CARTESIAN_POINT('Ctrl Pts',(97.7313645577357,0.725732116220329,-4.54803912092901));
#35169=CARTESIAN_POINT('Ctrl Pts',(97.7588220185473,0.677649309786266,-4.55104130217677));
#35170=CARTESIAN_POINT('Ctrl Pts',(97.7835387900433,0.628020395763152,-4.55404348342453));
#35171=CARTESIAN_POINT('Ctrl Pts',(97.8053533663104,0.577191850869178,-4.55704566467229));
#35172=CARTESIAN_POINT('Ctrl Pts',(97.8271778720883,0.526340169949871,-4.56004921244631));
#35173=CARTESIAN_POINT('Ctrl Pts',(97.8460973685622,0.474288266867315,-4.56305276022033));
#35174=CARTESIAN_POINT('Ctrl Pts',(97.8619993161285,0.421400662337796,-4.56605630799434));
#35175=CARTESIAN_POINT('Ctrl Pts',(97.8779312759447,0.368413241355353,-4.56906552445931));
#35176=CARTESIAN_POINT('Ctrl Pts',(97.8908341865632,0.314587482958828,-4.57207474092428));
#35177=CARTESIAN_POINT('Ctrl Pts',(97.9006462881487,0.260299918510812,-4.57508395738924));
#35178=CARTESIAN_POINT('Ctrl Pts',(97.9081529479932,0.218767706828071,-4.57738613131237));
#35179=CARTESIAN_POINT('Ctrl Pts',(97.9138516476614,0.176965471128063,-4.57968830523549));
#35180=CARTESIAN_POINT('Ctrl Pts',(97.9177353135767,0.135062832059178,-4.58199047915861));
#35181=CARTESIAN_POINT('Ctrl Pts',(97.9218708719417,0.0904424107107279,
-4.58444197082477));
#35182=CARTESIAN_POINT('Ctrl Pts',(97.9239574360407,0.0456291932873014,
-4.58689346249092));
#35183=CARTESIAN_POINT('Ctrl Pts',(97.9239807519794,0.000760505223226176,
-4.58934495415707));
#35184=CARTESIAN_POINT('Origin',(96.460480949577,-8.32667268468867E-16,
1.18130019239114E-14));
#35185=CARTESIAN_POINT('',(97.9239808052395,0.000649981535139221,-5.16065504581337));
#35186=CARTESIAN_POINT('',(97.9239808315836,0.000587678971723037,-5.08934495412971));
#35187=CARTESIAN_POINT('',(97.923980949577,-1.01189432752408E-15,1.19922289829666E-14));
#35188=CARTESIAN_POINT('Ctrl Pts',(97.9239808052395,0.000649981535147704,
-5.16065504581337));
#35189=CARTESIAN_POINT('Ctrl Pts',(97.9239538366058,0.0613726164339911,
-5.15736868599221));
#35190=CARTESIAN_POINT('Ctrl Pts',(97.9201434793188,0.12197259959902,-5.15408232617104));
#35191=CARTESIAN_POINT('Ctrl Pts',(97.9126202744233,0.181998986906557,-5.15079596634988));
#35192=CARTESIAN_POINT('Ctrl Pts',(97.9050714331658,0.242229922436747,-5.14749840780278));
#35193=CARTESIAN_POINT('Ctrl Pts',(97.8937845435227,0.301883015490773,-5.14420084925568));
#35194=CARTESIAN_POINT('Ctrl Pts',(97.8788808603027,0.36051899152915,-5.14090329070857));
#35195=CARTESIAN_POINT('Ctrl Pts',(97.8639101969523,0.419418489360427,-5.13759091227445));
#35196=CARTESIAN_POINT('Ctrl Pts',(97.8452903207953,0.477291389051983,-5.13427853384032));
#35197=CARTESIAN_POINT('Ctrl Pts',(97.8231921632558,0.533713779205726,-5.13096615540619));
#35198=CARTESIAN_POINT('Ctrl Pts',(97.8166208628006,0.550492032208917,-5.12998115772604));
#35199=CARTESIAN_POINT('Ctrl Pts',(97.8097422965267,0.567142179412155,-5.12899616004589));
#35200=CARTESIAN_POINT('Ctrl Pts',(97.8025617387441,0.58365349767525,-5.12801116236573));
#35201=CARTESIAN_POINT('Ctrl Pts',(97.7806181309362,0.63411167980101,-5.12500103370449));
#35202=CARTESIAN_POINT('Ctrl Pts',(97.7557788480465,0.68343663933808,-5.12199090504325));
#35203=CARTESIAN_POINT('Ctrl Pts',(97.7281832053769,0.731275078639955,-5.11898077638201));
#35204=CARTESIAN_POINT('Ctrl Pts',(97.7006366079399,0.779028495555788,-5.11597599756757));
#35205=CARTESIAN_POINT('Ctrl Pts',(97.6703436342324,0.8253001814735,-5.11297121875312));
#35206=CARTESIAN_POINT('Ctrl Pts',(97.6374908347472,0.869758575819526,-5.10996643993868));
#35207=CARTESIAN_POINT('Ctrl Pts',(97.6046705376642,0.914172985949913,-5.10696463385506));
#35208=CARTESIAN_POINT('Ctrl Pts',(97.5692957439274,0.956777235594788,-5.10396282777143));
#35209=CARTESIAN_POINT('Ctrl Pts',(97.5315969248381,0.997267675972961,-5.10096102168781));
#35210=CARTESIAN_POINT('Ctrl Pts',(97.493920512363,1.03773405051294,-5.09796099975321));
#35211=CARTESIAN_POINT('Ctrl Pts',(97.4539231715251,1.07608872022588,-5.09496097781861));
#35212=CARTESIAN_POINT('Ctrl Pts',(97.4118748925435,1.11206196557868,-5.09196095588401));
#35213=CARTESIAN_POINT('Ctrl Pts',(97.3698349982429,1.1480280376489,-5.08896153217192));
#35214=CARTESIAN_POINT('Ctrl Pts',(97.3257453790662,1.18161328530533,-5.08596210845983));
#35215=CARTESIAN_POINT('Ctrl Pts',(97.279910305661,1.21258722588844,-5.08296268474774));
#35216=CARTESIAN_POINT('Ctrl Pts',(97.2340330935445,1.24358964252365,-5.07996050349998));
#35217=CARTESIAN_POINT('Ctrl Pts',(97.1864076597451,1.2719756594284,-5.07695832225222));
#35218=CARTESIAN_POINT('Ctrl Pts',(97.1373673266349,1.2975581229962,-5.07395614100446));
#35219=CARTESIAN_POINT('Ctrl Pts',(97.0883046714537,1.32315223113354,-5.07095259323044));
#35220=CARTESIAN_POINT('Ctrl Pts',(97.0378263153113,1.34594002441208,-5.06794904545642));
#35221=CARTESIAN_POINT('Ctrl Pts',(96.986287262866,1.36578181672822,-5.0649454976824));
#35222=CARTESIAN_POINT('Ctrl Pts',(96.9346509391329,1.38566105708812,-5.06193628121743));
#35223=CARTESIAN_POINT('Ctrl Pts',(96.8819504240829,1.40258302750709,-5.05892706475246));
#35224=CARTESIAN_POINT('Ctrl Pts',(96.8285565251034,1.41645777229713,-5.05591784828749));
#35225=CARTESIAN_POINT('Ctrl Pts',(96.7877080041297,1.42707252069334,-5.05361567436439));
#35226=CARTESIAN_POINT('Ctrl Pts',(96.7464539979934,1.4359047947553,-5.05131350044128));
#35227=CARTESIAN_POINT('Ctrl Pts',(96.7049631121538,1.44293476019595,-5.04901132651818));
#35228=CARTESIAN_POINT('Ctrl Pts',(96.6507131254815,1.45212655072403,-5.04600119785694));
#35229=CARTESIAN_POINT('Ctrl Pts',(96.5958300577282,1.45827394706614,-5.04299106919571));
#35230=CARTESIAN_POINT('Ctrl Pts',(96.5406859265152,1.46130058908985,-5.03998094053447));
#35231=CARTESIAN_POINT('Ctrl Pts',(96.4856398019612,1.46432185191787,-5.03697616172003));
#35232=CARTESIAN_POINT('Ctrl Pts',(96.4303340577829,1.46423333870561,-5.03397138290559));
#35233=CARTESIAN_POINT('Ctrl Pts',(96.3751483153409,1.46101012711559,-5.03096660409114));
#35234=CARTESIAN_POINT('Ctrl Pts',(96.3200171700481,1.45779010435944,-5.02796479800752));
#35235=CARTESIAN_POINT('Ctrl Pts',(96.265006315935,1.45144155732336,-5.0249629919239));
#35236=CARTESIAN_POINT('Ctrl Pts',(96.2104959956422,1.44199159942289,-5.02196118584028));
#35237=CARTESIAN_POINT('Ctrl Pts',(96.1560180740227,1.43254725818542,-5.01896116390569));
#35238=CARTESIAN_POINT('Ctrl Pts',(96.1020406158815,1.42000524975325,-5.01596114197109));
#35239=CARTESIAN_POINT('Ctrl Pts',(96.0489370401826,1.40444432450716,-5.01296112003649));
#35240=CARTESIAN_POINT('Ctrl Pts',(95.9958440536577,1.38888650220364,-5.0099616963244));
#35241=CARTESIAN_POINT('Ctrl Pts',(95.9436251100285,1.3703111070388,-5.00696227261231));
#35242=CARTESIAN_POINT('Ctrl Pts',(95.8926394970126,1.34884703904837,-5.00396284890022));
#35243=CARTESIAN_POINT('Ctrl Pts',(95.8416070101103,1.32736323795627,-5.00096066765246));
#35244=CARTESIAN_POINT('Ctrl Pts',(95.7918106069325,1.30298566361317,-4.9979584864047));
#35245=CARTESIAN_POINT('Ctrl Pts',(95.7435891596973,1.27589122248059,-4.99495630515695));
#35246=CARTESIAN_POINT('Ctrl Pts',(95.6953457631296,1.24878444855984,-4.99195275738293));
#35247=CARTESIAN_POINT('Ctrl Pts',(95.6486791973347,1.2189586275611,-4.98894920960891));
#35248=CARTESIAN_POINT('Ctrl Pts',(95.6039004263353,1.1866347615012,-4.98594566183489));
#35249=CARTESIAN_POINT('Ctrl Pts',(95.5590371429416,1.15424988958401,-4.98293644536992));
#35250=CARTESIAN_POINT('Ctrl Pts',(95.5160691827544,1.11935788811184,-4.97992722890496));
#35251=CARTESIAN_POINT('Ctrl Pts',(95.475274493784,1.08222016681624,-4.97691801243999));
#35252=CARTESIAN_POINT('Ctrl Pts',(95.4440648848233,1.05380828800113,-4.97461583851687));
#35253=CARTESIAN_POINT('Ctrl Pts',(95.4141265905881,1.02408286747061,-4.97231366459374));
#35254=CARTESIAN_POINT('Ctrl Pts',(95.3855683481887,0.993174279457893,-4.97001149067062));
#35255=CARTESIAN_POINT('Ctrl Pts',(95.3482279964901,0.952760813854431,-4.96700136200938));
#35256=CARTESIAN_POINT('Ctrl Pts',(95.3130914938384,0.910153680775445,-4.96399123334814));
#35257=CARTESIAN_POINT('Ctrl Pts',(95.2804260628675,0.865622732114266,-4.96098110468691));
#35258=CARTESIAN_POINT('Ctrl Pts',(95.2478186875715,0.821170927496311,-4.95797632587246));
#35259=CARTESIAN_POINT('Ctrl Pts',(95.2176739782589,0.774802515035211,-4.95497154705802));
#35260=CARTESIAN_POINT('Ctrl Pts',(95.1902202316792,0.7268218203698,-4.95196676824358));
#35261=CARTESIAN_POINT('Ctrl Pts',(95.1627936460333,0.678888594652632,-4.94896496215996));
#35262=CARTESIAN_POINT('Ctrl Pts',(95.1380530102981,0.629346702650633,-4.94596315607634));
#35263=CARTESIAN_POINT('Ctrl Pts',(95.1161833793443,0.578529422472609,-4.94296134999272));
#35264=CARTESIAN_POINT('Ctrl Pts',(95.094326746792,0.527742345978014,-4.93996132805812));
#35265=CARTESIAN_POINT('Ctrl Pts',(95.0753379451626,0.475681867920573,-4.93696130612352));
#35266=CARTESIAN_POINT('Ctrl Pts',(95.0593550535487,0.422703765631228,-4.93396128418892));
#35267=CARTESIAN_POINT('Ctrl Pts',(95.0433753490199,0.369736227495716,-4.93096186047683));
#35268=CARTESIAN_POINT('Ctrl Pts',(95.0304005165813,0.31585193384279,-4.92796243676475));
#35269=CARTESIAN_POINT('Ctrl Pts',(95.0205189123824,0.261422228279018,-4.92496301305265));
#35270=CARTESIAN_POINT('Ctrl Pts',(95.0106282234796,0.206942482484551,-4.9219608318049));
#35271=CARTESIAN_POINT('Ctrl Pts',(95.0038365388493,0.151916843731529,-4.91895865055714));
#35272=CARTESIAN_POINT('Ctrl Pts',(95.0001808530182,0.0967257876186296,
-4.91595646930938));
#35273=CARTESIAN_POINT('Ctrl Pts',(94.9965235032002,0.0415096097621443,
-4.91295292153536));
#35274=CARTESIAN_POINT('Ctrl Pts',(94.9960050026317,-0.0138716065345326,
-4.90994937376135));
#35275=CARTESIAN_POINT('Ctrl Pts',(94.9986101656971,-0.0690366658989129,
-4.90694582598733));
#35276=CARTESIAN_POINT('Ctrl Pts',(95.0012202455694,-0.124305840028945,
-4.90393660952236));
#35277=CARTESIAN_POINT('Ctrl Pts',(95.006965711078,-0.179357515711698,-4.90092739305739));
#35278=CARTESIAN_POINT('Ctrl Pts',(95.015779494239,-0.233816070756902,-4.89791817659243));
#35279=CARTESIAN_POINT('Ctrl Pts',(95.0225223995745,-0.275479097254243,
-4.89561600266931));
#35280=CARTESIAN_POINT('Ctrl Pts',(95.0310600728233,-0.316795077490998,
-4.89331382874618));
#35281=CARTESIAN_POINT('Ctrl Pts',(95.0413427355865,-0.357601705241623,
-4.89101165482306));
#35282=CARTESIAN_POINT('Ctrl Pts',(95.0547874790901,-0.410957013685889,
-4.88800152616182));
#35283=CARTESIAN_POINT('Ctrl Pts',(95.0712736526104,-0.463665150538443,
-4.88499139750058));
#35284=CARTESIAN_POINT('Ctrl Pts',(95.0907212573221,-0.515354863636512,
-4.88198126883934));
#35285=CARTESIAN_POINT('Ctrl Pts',(95.1101342981606,-0.566952709549832,
-4.8789764900249));
#35286=CARTESIAN_POINT('Ctrl Pts',(95.132498140675,-0.617535233426132,-4.87597171121045));
#35287=CARTESIAN_POINT('Ctrl Pts',(95.1576826444004,-0.666744948259141,
-4.872966932396));
#35288=CARTESIAN_POINT('Ctrl Pts',(95.1828422322318,-0.715905978232068,
-4.86996512631238));
#35289=CARTESIAN_POINT('Ctrl Pts',(95.2108167138578,-0.763696421811132,
-4.86696332022876));
#35290=CARTESIAN_POINT('Ctrl Pts',(95.2414280731478,-0.809779188711201,
-4.86396151414514));
#35291=CARTESIAN_POINT('Ctrl Pts',(95.2720212383156,-0.855834565926139,
-4.86096149221054));
#35292=CARTESIAN_POINT('Ctrl Pts',(95.3052478831216,-0.90018383917649,-4.85796147027594));
#35293=CARTESIAN_POINT('Ctrl Pts',(95.3408854803501,-0.942516968169074,
-4.85496144834134));
#35294=CARTESIAN_POINT('Ctrl Pts',(95.3765159712264,-0.984841655679857,
-4.85196202462925));
#35295=CARTESIAN_POINT('Ctrl Pts',(95.4145561198351,-1.0251505935611,-4.84896260091716));
#35296=CARTESIAN_POINT('Ctrl Pts',(95.4547431933651,-1.06316688047077,-4.84596317720506));
#35297=CARTESIAN_POINT('Ctrl Pts',(95.4949672130886,-1.10121811784998,-4.8429609959573));
#35298=CARTESIAN_POINT('Ctrl Pts',(95.5373417166254,-1.13697212951738,-4.83995881470954));
#35299=CARTESIAN_POINT('Ctrl Pts',(95.5815682590862,-1.17019004118742,-4.83695663346178));
#35300=CARTESIAN_POINT('Ctrl Pts',(95.6258149324874,-1.20342307291347,-4.83395308568776));
#35301=CARTESIAN_POINT('Ctrl Pts',(95.6719148849319,-1.2341174102732,-4.83094953791374));
#35302=CARTESIAN_POINT('Ctrl Pts',(95.7195405576755,-1.26207748797326,-4.82794599013972));
#35303=CARTESIAN_POINT('Ctrl Pts',(95.7672561158614,-1.2900903356145,-4.82493677367475));
#35304=CARTESIAN_POINT('Ctrl Pts',(95.8165026756475,-1.31535837310519,-4.82192755720979));
#35305=CARTESIAN_POINT('Ctrl Pts',(95.8669289976572,-1.33773253319647,-4.81891834074482));
#35306=CARTESIAN_POINT('Ctrl Pts',(95.9055072006282,-1.35484968263162,-4.81661616682171));
#35307=CARTESIAN_POINT('Ctrl Pts',(95.9447753971582,-1.37027404092256,-4.8143139928986));
#35308=CARTESIAN_POINT('Ctrl Pts',(95.9845704526933,-1.38395861533354,-4.81201181897549));
#35309=CARTESIAN_POINT('Ctrl Pts',(96.036603114535,-1.40185141189327,-4.80900169031426));
#35310=CARTESIAN_POINT('Ctrl Pts',(96.0897555781729,-1.41684331694314,-4.80599156165302));
#35311=CARTESIAN_POINT('Ctrl Pts',(96.1436731988852,-1.42879848092781,-4.80298143299179));
#35312=CARTESIAN_POINT('Ctrl Pts',(96.1974949927932,-1.44073239721747,-4.79997665417734));
#35313=CARTESIAN_POINT('Ctrl Pts',(96.2520787336219,-1.44964016971346,-4.7969718753629));
#35314=CARTESIAN_POINT('Ctrl Pts',(96.3070539081435,-1.45543546506087,-4.79396709654846));
#35315=CARTESIAN_POINT('Ctrl Pts',(96.3619746938377,-1.46122502692367,-4.79096529046484));
#35316=CARTESIAN_POINT('Ctrl Pts',(96.4172856234598,-1.46390815645121,-4.78796348438122));
#35317=CARTESIAN_POINT('Ctrl Pts',(96.4726071075089,-1.46344976213528,-4.78496167829761));
#35318=CARTESIAN_POINT('Ctrl Pts',(96.5278957107626,-1.46299164026993,-4.78196165636301));
#35319=CARTESIAN_POINT('Ctrl Pts',(96.5831943289659,-1.45939569982424,-4.77896163442842));
#35320=CARTESIAN_POINT('Ctrl Pts',(96.6381217070322,-1.45267890853097,-4.77596161249382));
#35321=CARTESIAN_POINT('Ctrl Pts',(96.6930381322474,-1.44596345660649,-4.77296218878173));
#35322=CARTESIAN_POINT('Ctrl Pts',(96.7475829404237,-1.43612845379554,-4.76996276506964));
#35323=CARTESIAN_POINT('Ctrl Pts',(96.8013806630584,-1.42324264809214,-4.76696334135755));
#35324=CARTESIAN_POINT('Ctrl Pts',(96.8552278449069,-1.41034499575678,-4.76396116010979));
#35325=CARTESIAN_POINT('Ctrl Pts',(96.9083260543104,-1.39439106024103,-4.76095897886203));
#35326=CARTESIAN_POINT('Ctrl Pts',(96.9603121585099,-1.3755002771998,-4.75795679761428));
#35327=CARTESIAN_POINT('Ctrl Pts',(97.0123219256299,-1.35660089549348,-4.75495324984026));
#35328=CARTESIAN_POINT('Ctrl Pts',(97.0632180922886,-1.33476221007533,-4.75194970206625));
#35329=CARTESIAN_POINT('Ctrl Pts',(97.1126578904773,-1.31015170410069,-4.74894615429223));
#35330=CARTESIAN_POINT('Ctrl Pts',(97.1621909979647,-1.2854947499378,-4.74593693782727));
#35331=CARTESIAN_POINT('Ctrl Pts',(97.2102617863444,-1.25805578723982,-4.7429277213623));
#35332=CARTESIAN_POINT('Ctrl Pts',(97.2565534919671,-1.22804753867779,-4.73991850489734));
#35333=CARTESIAN_POINT('Ctrl Pts',(97.2919685439525,-1.2050899986926,-4.7376163309742));
#35334=CARTESIAN_POINT('Ctrl Pts',(97.3263428475686,-1.18062963609603,-4.73531415705106));
#35335=CARTESIAN_POINT('Ctrl Pts',(97.3595479090547,-1.15477740382097,-4.73301198312793));
#35336=CARTESIAN_POINT('Ctrl Pts',(97.4030324702889,-1.12092193338683,-4.72999711074245));
#35337=CARTESIAN_POINT('Ctrl Pts',(97.4447047082584,-1.08452667630381,-4.72698223835697));
#35338=CARTESIAN_POINT('Ctrl Pts',(97.4842490377971,-1.04581602184234,-4.7239673659715));
#35339=CARTESIAN_POINT('Ctrl Pts',(97.5232220531078,-1.00766463714034,-4.72099605076627));
#35340=CARTESIAN_POINT('Ctrl Pts',(97.5601278206889,-0.967264685987466,
-4.71802473556104));
#35341=CARTESIAN_POINT('Ctrl Pts',(97.5946952874807,-0.924873010576951,
-4.71505342035581));
#35342=CARTESIAN_POINT('Ctrl Pts',(97.6292292884123,-0.882522375891087,
-4.71208498177501));
#35343=CARTESIAN_POINT('Ctrl Pts',(97.6614291294895,-0.838184251342567,
-4.70911654319421));
#35344=CARTESIAN_POINT('Ctrl Pts',(97.6910615717155,-0.792151237086225,
-4.70614810461341));
#35345=CARTESIAN_POINT('Ctrl Pts',(97.7206776781764,-0.746143599898085,
-4.70318130247267));
#35346=CARTESIAN_POINT('Ctrl Pts',(97.7477288975073,-0.698443378368204,
-4.70021450033193));
#35347=CARTESIAN_POINT('Ctrl Pts',(97.7720246603957,-0.649373039640524,
-4.69724769819118));
#35348=CARTESIAN_POINT('Ctrl Pts',(97.7969967336336,-0.59893675171043,-4.69419831049829));
#35349=CARTESIAN_POINT('Ctrl Pts',(97.8190573105785,-0.54705342191283,-4.6911489228054));
#35350=CARTESIAN_POINT('Ctrl Pts',(97.8380507198851,-0.494098955608387,
-4.68809953511251));
#35351=CARTESIAN_POINT('Ctrl Pts',(97.8565434550433,-0.442540391002808,
-4.68513053054418));
#35352=CARTESIAN_POINT('Ctrl Pts',(97.8721286571858,-0.389967029528204,
-4.68216152597585));
#35353=CARTESIAN_POINT('Ctrl Pts',(97.8847130788941,-0.33674187714174,-4.67919252140752));
#35354=CARTESIAN_POINT('Ctrl Pts',(97.8978085684271,-0.281355190162321,
-4.67610294215235));
#35355=CARTESIAN_POINT('Ctrl Pts',(97.9076541361318,-0.225263256882713,
-4.67301336289717));
#35356=CARTESIAN_POINT('Ctrl Pts',(97.9142039062054,-0.168884029356592,
-4.669923783642));
#35357=CARTESIAN_POINT('Ctrl Pts',(97.9207536762789,-0.112504801830471,
-4.66683420438683));
#35358=CARTESIAN_POINT('Ctrl Pts',(97.9240076811728,-0.0558389356524655,
-4.66374462513166));
#35359=CARTESIAN_POINT('Ctrl Pts',(97.9239807839468,0.000696275558458027,
-4.66065504587649));
#35360=CARTESIAN_POINT('Ctrl Pts',(97.9239807519797,0.000760504599684739,
-4.58934495419114));
#35361=CARTESIAN_POINT('Ctrl Pts',(97.9240091441741,-0.0538768649333986,
-4.59233017755843));
#35362=CARTESIAN_POINT('Ctrl Pts',(97.9209735154324,-0.108635686920582,
-4.59531540092572));
#35363=CARTESIAN_POINT('Ctrl Pts',(97.914859816964,-0.163139082068399,-4.59830062429302));
#35364=CARTESIAN_POINT('Ctrl Pts',(97.9087809889155,-0.217331608716174,
-4.60126882097953));
#35365=CARTESIAN_POINT('Ctrl Pts',(97.8996591242802,-0.271271069183976,
-4.60423701766605));
#35366=CARTESIAN_POINT('Ctrl Pts',(97.8875324670009,-0.324586223703797,
-4.60720521435256));
#35367=CARTESIAN_POINT('Ctrl Pts',(97.8754160378309,-0.377856410082728,
-4.61017090754288));
#35368=CARTESIAN_POINT('Ctrl Pts',(97.8602999526874,-0.430502806405192,
-4.61313660073319));
#35369=CARTESIAN_POINT('Ctrl Pts',(97.8422738547964,-0.482162438484627,
-4.61610229392351));
#35370=CARTESIAN_POINT('Ctrl Pts',(97.8242554245078,-0.53380009656151,-4.61906672562304));
#35371=CARTESIAN_POINT('Ctrl Pts',(97.8033296126891,-0.584451311009786,
-4.62203115732257));
#35372=CARTESIAN_POINT('Ctrl Pts',(97.7796357286456,-0.633768821306631,
-4.6249955890221));
#35373=CARTESIAN_POINT('Ctrl Pts',(97.7556610698103,-0.683670748816948,
-4.62799514952077));
#35374=CARTESIAN_POINT('Ctrl Pts',(97.7288524993572,-0.73220662233431,-4.63099471001945));
#35375=CARTESIAN_POINT('Ctrl Pts',(97.6994031308721,-0.779040485915271,
-4.63399427051812));
#35376=CARTESIAN_POINT('Ctrl Pts',(97.670268647178,-0.825373582515089,-4.63696175847908));
#35377=CARTESIAN_POINT('Ctrl Pts',(97.6385499376378,-0.870040477952918,
-4.63992924644005));
#35378=CARTESIAN_POINT('Ctrl Pts',(97.60447702287,-0.91274598563359,-4.64289673440101));
#35379=CARTESIAN_POINT('Ctrl Pts',(97.5698517192511,-0.956143833446764,
-4.64591233116854));
#35380=CARTESIAN_POINT('Ctrl Pts',(97.5327955634189,-0.997515679528127,
-4.64892792793607));
#35381=CARTESIAN_POINT('Ctrl Pts',(97.4935895731258,-1.0365899970331,-4.65194352470359));
#35382=CARTESIAN_POINT('Ctrl Pts',(97.4543835828327,-1.07566431453807,-4.65495912147112));
#35383=CARTESIAN_POINT('Ctrl Pts',(97.4130282385493,-1.11244077228239,-4.65797471823865));
#35384=CARTESIAN_POINT('Ctrl Pts',(97.3698377702358,-1.14669194761335,-4.66099031500617));
#35385=CARTESIAN_POINT('Ctrl Pts',(97.3267256181196,-1.18088101614369,-4.66400044366741));
#35386=CARTESIAN_POINT('Ctrl Pts',(97.2815920934796,-1.21270720915157,-4.66701057232865));
#35387=CARTESIAN_POINT('Ctrl Pts',(97.2347264161452,-1.24192439685295,-4.67002070098989));
#35388=CARTESIAN_POINT('Ctrl Pts',(97.1879440323248,-1.27108965737927,-4.67302547980433));
#35389=CARTESIAN_POINT('Ctrl Pts',(97.1394360496944,-1.29765483749973,-4.67603025861878));
#35390=CARTESIAN_POINT('Ctrl Pts',(97.0895231307834,-1.32141522023288,-4.67903503743322));
#35391=CARTESIAN_POINT('Ctrl Pts',(97.0396595924364,-1.34515209600379,-4.68203684351684));
#35392=CARTESIAN_POINT('Ctrl Pts',(96.9883943457357,-1.36608944541673,-4.68503864960047));
#35393=CARTESIAN_POINT('Ctrl Pts',(96.9360736651233,-1.38406785199257,-4.68804045568409));
#35394=CARTESIAN_POINT('Ctrl Pts',(96.8837840817532,-1.40203557294928,-4.69104047761869));
#35395=CARTESIAN_POINT('Ctrl Pts',(96.8304408062886,-1.41704766559507,-4.69404049955329));
#35396=CARTESIAN_POINT('Ctrl Pts',(96.7764090088346,-1.42899325098956,-4.69704052148789));
#35397=CARTESIAN_POINT('Ctrl Pts',(96.7223879856477,-1.4409364543621,-4.70003994519998));
#35398=CARTESIAN_POINT('Ctrl Pts',(96.6676792285092,-1.44981425091521,-4.70303936891206));
#35399=CARTESIAN_POINT('Ctrl Pts',(96.6126596829523,-1.45556651620883,-4.70603879262415));
#35400=CARTESIAN_POINT('Ctrl Pts',(96.5575895548922,-1.46132406987723,-4.70904097387191));
#35401=CARTESIAN_POINT('Ctrl Pts',(96.5022085939542,-1.46395029642693,-4.71204315511967));
#35402=CARTESIAN_POINT('Ctrl Pts',(96.4468989816342,-1.46343697511946,-4.71504533636743));
#35403=CARTESIAN_POINT('Ctrl Pts',(96.3915641936065,-1.46292342015954,-4.71804888414145));
#35404=CARTESIAN_POINT('Ctrl Pts',(96.336301346819,-1.45926750354694,-4.72105243191547));
#35405=CARTESIAN_POINT('Ctrl Pts',(96.2814894087509,-1.45251309058222,-4.72405597968949));
#35406=CARTESIAN_POINT('Ctrl Pts',(96.2265740223742,-1.44574592979974,-4.72706519615446));
#35407=CARTESIAN_POINT('Ctrl Pts',(96.1721117656645,-1.43586868506868,-4.73007441261943));
#35408=CARTESIAN_POINT('Ctrl Pts',(96.1184721394553,-1.42297653662988,-4.73308362908439));
#35409=CARTESIAN_POINT('Ctrl Pts',(96.0774356270801,-1.4131135147123,-4.73538580300751));
#35410=CARTESIAN_POINT('Ctrl Pts',(96.0368804091218,-1.40148697680282,-4.73768797693062));
#35411=CARTESIAN_POINT('Ctrl Pts',(95.9969645796261,-1.38815878947169,-4.73999015085374));
#35412=CARTESIAN_POINT('Ctrl Pts',(95.944774003929,-1.37073197463162,-4.74300027951497));
#35413=CARTESIAN_POINT('Ctrl Pts',(95.8934579300621,-1.35032113999202,-4.74601040817621));
#35414=CARTESIAN_POINT('Ctrl Pts',(95.8433805269229,-1.3270340305961,-4.74902053683745));
#35415=CARTESIAN_POINT('Ctrl Pts',(95.7933921254394,-1.30378830895515,-4.75202531565189));
#35416=CARTESIAN_POINT('Ctrl Pts',(95.7446385008558,-1.27767667814304,-4.75503009446634));
#35417=CARTESIAN_POINT('Ctrl Pts',(95.6974663179009,-1.24885584510312,-4.75803487328078));
#35418=CARTESIAN_POINT('Ctrl Pts',(95.650340804006,-1.22006352550266,-4.7610366793644));
#35419=CARTESIAN_POINT('Ctrl Pts',(95.6047940808374,-1.18856758721971,-4.76403848544802));
#35420=CARTESIAN_POINT('Ctrl Pts',(95.5611488669825,-1.15457093988041,-4.76704029153163));
#35421=CARTESIAN_POINT('Ctrl Pts',(95.5175295940325,-1.12059449873814,-4.77004031346623));
#35422=CARTESIAN_POINT('Ctrl Pts',(95.4758100061135,-1.08412061840237,-4.77304033540082));
#35423=CARTESIAN_POINT('Ctrl Pts',(95.4362824948339,-1.04539455484612,-4.77604035733542));
#35424=CARTESIAN_POINT('Ctrl Pts',(95.396762865579,-1.00667621350098,-4.77903978104751));
#35425=CARTESIAN_POINT('Ctrl Pts',(95.3594348219031,-0.965706950209886,
-4.7820392047596));
#35426=CARTESIAN_POINT('Ctrl Pts',(95.3245546812025,-0.922769615243584,
-4.78503862847169));
#35427=CARTESIAN_POINT('Ctrl Pts',(95.2896424732645,-0.879792805616806,
-4.78804080971945));
#35428=CARTESIAN_POINT('Ctrl Pts',(95.2571829981975,-0.834844720244155,
-4.79104299096721));
#35429=CARTESIAN_POINT('Ctrl Pts',(95.22739196356,-0.788240954634715,-4.79404517221497));
#35430=CARTESIAN_POINT('Ctrl Pts',(95.1975873687048,-0.741615976025689,
-4.79704871998899));
#35431=CARTESIAN_POINT('Ctrl Pts',(95.1704538947152,-0.693334276070171,
-4.80005226776301));
#35432=CARTESIAN_POINT('Ctrl Pts',(95.1461618695643,-0.643737218059181,
-4.80305581553703));
#35433=CARTESIAN_POINT('Ctrl Pts',(95.1218239973042,-0.594046553948072,
-4.80606503200199));
#35434=CARTESIAN_POINT('Ctrl Pts',(95.1003384923237,-0.543036060467608,
-4.80907424846695));
#35435=CARTESIAN_POINT('Ctrl Pts',(95.0818275324146,-0.491067210620215,
-4.81208346493192));
#35436=CARTESIAN_POINT('Ctrl Pts',(95.067665889445,-0.451308910635289,-4.81438563885505));
#35437=CARTESIAN_POINT('Ctrl Pts',(95.0552442159601,-0.410990129462408,
-4.81668781277818));
#35438=CARTESIAN_POINT('Ctrl Pts',(95.0445970790082,-0.370277078770857,
-4.8189899867013));
#35439=CARTESIAN_POINT('Ctrl Pts',(95.0306757797627,-0.317044123805158,
-4.82200011536254));
#35440=CARTESIAN_POINT('Ctrl Pts',(95.0197315017751,-0.262913130953223,
-4.82501024402378));
#35441=CARTESIAN_POINT('Ctrl Pts',(95.011872986128,-0.208247972936347,-4.82802037268502));
#35442=CARTESIAN_POINT('Ctrl Pts',(95.0040284372775,-0.153679970308288,
-4.83102515149946));
#35443=CARTESIAN_POINT('Ctrl Pts',(94.9992588417388,-0.0985802050447275,
-4.8340299303139));
#35444=CARTESIAN_POINT('Ctrl Pts',(94.9976223694762,-0.0433246422445049,
-4.83703470912835));
#35445=CARTESIAN_POINT('Ctrl Pts',(94.9959875162319,0.0118762543307089,
-4.84003651521197));
#35446=CARTESIAN_POINT('Ctrl Pts',(94.9974796614516,0.0672321178174589,
-4.84303832129558));
#35447=CARTESIAN_POINT('Ctrl Pts',(95.0021051950319,0.122361793690261,-4.8460401273792));
#35448=CARTESIAN_POINT('Ctrl Pts',(95.0067279793869,0.177458702770457,-4.84904014931379));
#35449=CARTESIAN_POINT('Ctrl Pts',(95.0144804167235,0.23232916548243,-4.85204017124839));
#35450=CARTESIAN_POINT('Ctrl Pts',(95.0253168601906,0.286594289084048,-4.85504019318298));
#35451=CARTESIAN_POINT('Ctrl Pts',(95.0361511428054,0.340848591892115,-4.85803961689508));
#35452=CARTESIAN_POINT('Ctrl Pts',(95.0500681068859,0.394497277710787,-4.86103904060717));
#35453=CARTESIAN_POINT('Ctrl Pts',(95.0669709085371,0.447171125544849,-4.86403846431926));
#35454=CARTESIAN_POINT('Ctrl Pts',(95.0838892498663,0.499893399352681,-4.86704064556702));
#35455=CARTESIAN_POINT('Ctrl Pts',(95.1037987512976,0.551638540699961,-4.87004282681477));
#35456=CARTESIAN_POINT('Ctrl Pts',(95.1265529548619,0.602053448553728,-4.87304500806253));
#35457=CARTESIAN_POINT('Ctrl Pts',(95.1493175156346,0.652491304154378,-4.87604855583654));
#35458=CARTESIAN_POINT('Ctrl Pts',(95.1749291150773,0.701597250182519,-4.87905210361056));
#35459=CARTESIAN_POINT('Ctrl Pts',(95.2031949187827,0.74904211281437,-4.88205565138457));
#35460=CARTESIAN_POINT('Ctrl Pts',(95.2315140694356,0.796576519639843,-4.88506486784954));
#35461=CARTESIAN_POINT('Ctrl Pts',(95.2624971349902,0.842443141689295,-4.8880740843145));
#35462=CARTESIAN_POINT('Ctrl Pts',(95.2959081295444,0.886342144344518,-4.89108330077947));
#35463=CARTESIAN_POINT('Ctrl Pts',(95.321468909669,0.919926680499025,-4.8933854747026));
#35464=CARTESIAN_POINT('Ctrl Pts',(95.3484498203687,0.952360190103343,-4.89568764862573));
#35465=CARTESIAN_POINT('Ctrl Pts',(95.3767305421968,0.983522904920491,-4.89798982254886));
#35466=CARTESIAN_POINT('Ctrl Pts',(95.4137080313777,1.02426864532291,-4.9009999512101));
#35467=CARTESIAN_POINT('Ctrl Pts',(95.4530642841859,1.06301173467717,-4.90401007987134));
#35468=CARTESIAN_POINT('Ctrl Pts',(95.4945539631249,1.09946228077349,-4.90702020853258));
#35469=CARTESIAN_POINT('Ctrl Pts',(95.535969903214,1.13584804397874,-4.91002498734703));
#35470=CARTESIAN_POINT('Ctrl Pts',(95.5795113512401,1.16994900404589,-4.91302976616147));
#35471=CARTESIAN_POINT('Ctrl Pts',(95.6248952101548,1.20151101621011,-4.91603454497592));
#35472=CARTESIAN_POINT('Ctrl Pts',(95.67023416926,1.23304180299228,-4.91903635105954));
#35473=CARTESIAN_POINT('Ctrl Pts',(95.7174114970096,1.2620383177162,-4.92203815714317));
#35474=CARTESIAN_POINT('Ctrl Pts',(95.7661114576449,1.28828694733509,-4.92503996322679));
#35475=CARTESIAN_POINT('Ctrl Pts',(95.8147824730437,1.31451997585735,-4.92803998516139));
#35476=CARTESIAN_POINT('Ctrl Pts',(95.8649738636181,1.33800810637278,-4.93104000709599));
#35477=CARTESIAN_POINT('Ctrl Pts',(95.9163433552392,1.35858254384057,-4.93404002903059));
#35478=CARTESIAN_POINT('Ctrl Pts',(95.9677026034731,1.37915287864111,-4.93703945274268));
#35479=CARTESIAN_POINT('Ctrl Pts',(96.0202389962309,1.39681047800454,-4.94003887645477));
#35480=CARTESIAN_POINT('Ctrl Pts',(96.0735903858681,1.41143471039685,-4.94303830016685));
#35481=CARTESIAN_POINT('Ctrl Pts',(96.126990824381,1.42607238765272,-4.94604048141462));
#35482=CARTESIAN_POINT('Ctrl Pts',(96.1812072462982,1.43767098648151,-4.94904266266238));
#35483=CARTESIAN_POINT('Ctrl Pts',(96.2358638959425,1.44616023635576,-4.95204484391014));
#35484=CARTESIAN_POINT('Ctrl Pts',(96.2905454240803,1.4546533503481,-4.95504839168416));
#35485=CARTESIAN_POINT('Ctrl Pts',(96.3456670528585,1.46003424267022,-4.95805193945818));
#35486=CARTESIAN_POINT('Ctrl Pts',(96.4008477263775,1.46228455804294,-4.9610554872322));
#35487=CARTESIAN_POINT('Ctrl Pts',(96.4561325441311,1.46453912050721,-4.96406470369717));
#35488=CARTESIAN_POINT('Ctrl Pts',(96.5114760998946,1.46365131149304,-4.96707392016214));
#35489=CARTESIAN_POINT('Ctrl Pts',(96.5664983323353,1.45965494708615,-4.97008313662711));
#35490=CARTESIAN_POINT('Ctrl Pts',(96.6085925951411,1.45659756453097,-4.97238531055022));
#35491=CARTESIAN_POINT('Ctrl Pts',(96.6504987960049,1.45172186801079,-4.97468748447332));
#35492=CARTESIAN_POINT('Ctrl Pts',(96.6920508837316,1.44506318740587,-4.97698965839643));
#35493=CARTESIAN_POINT('Ctrl Pts',(96.7463808928353,1.43635685764783,-4.97999978705767));
#35494=CARTESIAN_POINT('Ctrl Pts',(96.8003333748968,1.4245640086614,-4.9830099157189));
#35495=CARTESIAN_POINT('Ctrl Pts',(96.8535314859436,1.40973172123703,-4.98602004438014));
#35496=CARTESIAN_POINT('Ctrl Pts',(96.9066350489574,1.39492579496673,-4.98902482319459));
#35497=CARTESIAN_POINT('Ctrl Pts',(96.9589863970451,1.37709129113013,-4.99202960200903));
#35498=CARTESIAN_POINT('Ctrl Pts',(97.0102179940105,1.35632644742242,-4.99503438082347));
#35499=CARTESIAN_POINT('Ctrl Pts',(97.0613989057984,1.33558214708737,-4.99803618690708));
#35500=CARTESIAN_POINT('Ctrl Pts',(97.1114617739434,1.31191344723268,-5.0010379929907));
#35501=CARTESIAN_POINT('Ctrl Pts',(97.1600551749908,1.28546806772345,-5.00403979907431));
#35502=CARTESIAN_POINT('Ctrl Pts',(97.2086196941363,1.25903840625081,-5.00703982100891));
#35503=CARTESIAN_POINT('Ctrl Pts',(97.2557160143554,1.22983558815536,-5.01003984294351));
#35504=CARTESIAN_POINT('Ctrl Pts',(97.3010157480182,1.19805404828389,-5.01303986487811));
#35505=CARTESIAN_POINT('Ctrl Pts',(97.3463064486402,1.16627884584363,-5.0160392885902));
#35506=CARTESIAN_POINT('Ctrl Pts',(97.3898008420902,1.13192624597563,-5.01903871230228));
#35507=CARTESIAN_POINT('Ctrl Pts',(97.4312000201607,1.09523364448186,-5.02203813601437));
#35508=CARTESIAN_POINT('Ctrl Pts',(97.4726372587793,1.05850730945553,-5.02504031726212));
#35509=CARTESIAN_POINT('Ctrl Pts',(97.5119750375536,1.01943702584515,-5.02804249850988));
#35510=CARTESIAN_POINT('Ctrl Pts',(97.5489491915986,0.978299103602973,-5.03104467975764));
#35511=CARTESIAN_POINT('Ctrl Pts',(97.5859401754578,0.937142456291722,-5.03404822753166));
#35512=CARTESIAN_POINT('Ctrl Pts',(97.6205650591715,0.893916707146538,-5.03705177530568));
#35513=CARTESIAN_POINT('Ctrl Pts',(97.6526002622515,0.848930971486213,-5.0400553230797));
#35514=CARTESIAN_POINT('Ctrl Pts',(97.684695926386,0.803860332820683,-5.04306453954466));
#35515=CARTESIAN_POINT('Ctrl Pts',(97.7141918640548,0.757023520051016,-5.04607375600963));
#35516=CARTESIAN_POINT('Ctrl Pts',(97.7409087331197,0.708757321748395,-5.04908297247459));
#35517=CARTESIAN_POINT('Ctrl Pts',(97.7613482328981,0.671831701941769,-5.05138514639773));
#35518=CARTESIAN_POINT('Ctrl Pts',(97.7801620894879,0.63407006946034,-5.05368732032086));
#35519=CARTESIAN_POINT('Ctrl Pts',(97.7972891628933,0.595630800756833,-5.05598949424399));
#35520=CARTESIAN_POINT('Ctrl Pts',(97.8217753637232,0.540675022209471,-5.05928086175863));
#35521=CARTESIAN_POINT('Ctrl Pts',(97.8429012861721,0.484134691290987,-5.06257222927327));
#35522=CARTESIAN_POINT('Ctrl Pts',(97.8604806286845,0.426418982338702,-5.06586359678791));
#35523=CARTESIAN_POINT('Ctrl Pts',(97.8780070246564,0.368877105093971,-5.06914505116026));
#35524=CARTESIAN_POINT('Ctrl Pts',(97.8920079878108,0.310167235961735,-5.07242650553261));
#35525=CARTESIAN_POINT('Ctrl Pts',(97.9023453525958,0.25071755683876,-5.07570795990496));
#35526=CARTESIAN_POINT('Ctrl Pts',(97.9126346019441,0.191544587238597,-5.07897414069321));
#35527=CARTESIAN_POINT('Ctrl Pts',(97.9192941361081,0.131639017028875,-5.08224032148147));
#35528=CARTESIAN_POINT('Ctrl Pts',(97.9222362222824,0.071440693711251,-5.08550650226972));
#35529=CARTESIAN_POINT('Ctrl Pts',(97.923388746375,0.0478587814731765,-5.08678598622305));
#35530=CARTESIAN_POINT('Ctrl Pts',(97.9239713369921,0.0242321078176,-5.08806547017638));
#35531=CARTESIAN_POINT('Ctrl Pts',(97.9239808315836,0.000587678971723866,
-5.08934495412971));
#35532=CARTESIAN_POINT('Origin',(96.460480949577,-8.32667268468867E-16,
1.18130019239114E-14));
#35533=CARTESIAN_POINT('',(97.9239803738018,-0.00129818862389702,-5.66065504588482));
#35534=CARTESIAN_POINT('',(97.9239803690929,-0.00130348633276278,-5.58934495420992));
#35535=CARTESIAN_POINT('',(97.923980949577,-1.01189432752408E-15,1.19922289829666E-14));
#35536=CARTESIAN_POINT('Ctrl Pts',(97.9239803738025,-0.00129818785261365,
-5.6606550458429));
#35537=CARTESIAN_POINT('Ctrl Pts',(97.9240288523407,0.0533536197810905,
-5.65768502711363));
#35538=CARTESIAN_POINT('Ctrl Pts',(97.9210117416233,0.10807933482888,-5.65471500838436));
#35539=CARTESIAN_POINT('Ctrl Pts',(97.9149308469247,0.16250460333544,-5.65174498965509));
#35540=CARTESIAN_POINT('Ctrl Pts',(97.9088537700624,0.216895701416044,-5.64877683562595));
#35541=CARTESIAN_POINT('Ctrl Pts',(97.8997167787174,0.270986190441221,-5.64580868159681));
#35542=CARTESIAN_POINT('Ctrl Pts',(97.8875736481521,0.324405116595969,-5.64284052756767));
#35543=CARTESIAN_POINT('Ctrl Pts',(97.8754330899258,0.377812726756813,-5.63987300229719));
#35544=CARTESIAN_POINT('Ctrl Pts',(97.8602877763835,0.430548529546161,-5.63690547702672));
#35545=CARTESIAN_POINT('Ctrl Pts',(97.8422424151804,0.482252529462982,-5.63393795175625));
#35546=CARTESIAN_POINT('Ctrl Pts',(97.8241808024205,0.534003093728886,-5.6309677539482));
#35547=CARTESIAN_POINT('Ctrl Pts',(97.8032141053442,0.584719488164546,-5.62799755614015));
#35548=CARTESIAN_POINT('Ctrl Pts',(97.7794961401501,0.634059285112504,-5.6250273583321));
#35549=CARTESIAN_POINT('Ctrl Pts',(97.7557667425137,0.683422864639655,-5.62205572884072));
#35550=CARTESIAN_POINT('Ctrl Pts',(97.7292836989253,0.731408052320245,-5.61908409934935));
#35551=CARTESIAN_POINT('Ctrl Pts',(97.7002464014614,0.777697803979105,-5.61611246985798));
#35552=CARTESIAN_POINT('Ctrl Pts',(97.6711562336171,0.824071838852656,-5.61313542969842));
#35553=CARTESIAN_POINT('Ctrl Pts',(97.6395028433694,0.868743835850687,-5.61015838953886));
#35554=CARTESIAN_POINT('Ctrl Pts',(97.6055275969137,0.911427685240538,-5.60718134937931));
#35555=CARTESIAN_POINT('Ctrl Pts',(97.5858557269457,0.936141888153743,-5.60545762540324));
#35556=CARTESIAN_POINT('Ctrl Pts',(97.5654061942646,0.960190211352029,-5.60373390142718));
#35557=CARTESIAN_POINT('Ctrl Pts',(97.5442313569573,0.983522904920419,-5.60201017745112));
#35558=CARTESIAN_POINT('Ctrl Pts',(97.5072538677764,1.02426864532281,-5.59900004878988));
#35559=CARTESIAN_POINT('Ctrl Pts',(97.4678976149683,1.06301173467705,-5.59598992012864));
#35560=CARTESIAN_POINT('Ctrl Pts',(97.4264079360292,1.09946228077335,-5.5929797914674));
#35561=CARTESIAN_POINT('Ctrl Pts',(97.3849919959402,1.13584804397859,-5.58997501265296));
#35562=CARTESIAN_POINT('Ctrl Pts',(97.3414505479141,1.16994900404574,-5.58697023383851));
#35563=CARTESIAN_POINT('Ctrl Pts',(97.2960666889994,1.20151101620996,-5.58396545502407));
#35564=CARTESIAN_POINT('Ctrl Pts',(97.2507277298942,1.23304180299214,-5.58096364894044));
#35565=CARTESIAN_POINT('Ctrl Pts',(97.2035504021446,1.26203831771606,-5.57796184285682));
#35566=CARTESIAN_POINT('Ctrl Pts',(97.1548504415093,1.28828694733496,-5.5749600367732));
#35567=CARTESIAN_POINT('Ctrl Pts',(97.1061794261105,1.31451997585722,-5.5719600148386));
#35568=CARTESIAN_POINT('Ctrl Pts',(97.0559880355362,1.33800810637265,-5.568959992904));
#35569=CARTESIAN_POINT('Ctrl Pts',(97.0046185439151,1.35858254384045,-5.5659599709694));
#35570=CARTESIAN_POINT('Ctrl Pts',(96.9532592956811,1.37915287864104,-5.56296054725731));
#35571=CARTESIAN_POINT('Ctrl Pts',(96.9007229029232,1.39681047800451,-5.55996112354522));
#35572=CARTESIAN_POINT('Ctrl Pts',(96.8473715132859,1.41143471039685,-5.55696169983312));
#35573=CARTESIAN_POINT('Ctrl Pts',(96.7939710747731,1.42607238765271,-5.55395951858536));
#35574=CARTESIAN_POINT('Ctrl Pts',(96.7397546528558,1.4376709864815,-5.5509573373376));
#35575=CARTESIAN_POINT('Ctrl Pts',(96.6850980032116,1.44616023635575,-5.54795515608984));
#35576=CARTESIAN_POINT('Ctrl Pts',(96.6304164750737,1.45465335034809,-5.54495160831582));
#35577=CARTESIAN_POINT('Ctrl Pts',(96.5752948462955,1.46003424267022,-5.54194806054179));
#35578=CARTESIAN_POINT('Ctrl Pts',(96.5201141727766,1.46228455804294,-5.53894451276777));
#35579=CARTESIAN_POINT('Ctrl Pts',(96.4648293550229,1.46453912050721,-5.5359352963028));
#35580=CARTESIAN_POINT('Ctrl Pts',(96.4094857992594,1.46365131149304,-5.53292607983784));
#35581=CARTESIAN_POINT('Ctrl Pts',(96.3544635668188,1.45965494708616,-5.52991686337287));
#35582=CARTESIAN_POINT('Ctrl Pts',(96.312369304013,1.45659756453098,-5.52761468944977));
#35583=CARTESIAN_POINT('Ctrl Pts',(96.2704631031492,1.4517218680108,-5.52531251552666));
#35584=CARTESIAN_POINT('Ctrl Pts',(96.2289110154224,1.44506318740588,-5.52301034160356));
#35585=CARTESIAN_POINT('Ctrl Pts',(96.1745810063187,1.43635685764784,-5.52000021294232));
#35586=CARTESIAN_POINT('Ctrl Pts',(96.1206285242573,1.42456400866141,-5.51699008428108));
#35587=CARTESIAN_POINT('Ctrl Pts',(96.0674304132104,1.40973172123704,-5.51397995561984));
#35588=CARTESIAN_POINT('Ctrl Pts',(96.0143268501966,1.39492579496673,-5.5109751768054));
#35589=CARTESIAN_POINT('Ctrl Pts',(95.9619755021089,1.37709129113012,-5.50797039799096));
#35590=CARTESIAN_POINT('Ctrl Pts',(95.9107439051434,1.35632644742238,-5.50496561917651));
#35591=CARTESIAN_POINT('Ctrl Pts',(95.8595629933555,1.33558214708731,-5.5019638130929));
#35592=CARTESIAN_POINT('Ctrl Pts',(95.8095001252104,1.3119134472326,-5.49896200700928));
#35593=CARTESIAN_POINT('Ctrl Pts',(95.760906724163,1.28546806772334,-5.49596020092566));
#35594=CARTESIAN_POINT('Ctrl Pts',(95.7123422050175,1.25903840625068,-5.49296017899106));
#35595=CARTESIAN_POINT('Ctrl Pts',(95.6652458847984,1.22983558815522,-5.48996015705646));
#35596=CARTESIAN_POINT('Ctrl Pts',(95.6199461511356,1.19805404828372,-5.48696013512186));
#35597=CARTESIAN_POINT('Ctrl Pts',(95.5746554505134,1.16627884584334,-5.48396071140977));
#35598=CARTESIAN_POINT('Ctrl Pts',(95.5311610570632,1.13192624597521,-5.48096128769767));
#35599=CARTESIAN_POINT('Ctrl Pts',(95.4897618789926,1.09523364448129,-5.47796186398557));
#35600=CARTESIAN_POINT('Ctrl Pts',(95.4483246403741,1.0585073094549,-5.47495968273781));
#35601=CARTESIAN_POINT('Ctrl Pts',(95.4089868615997,1.01943702584445,-5.47195750149005));
#35602=CARTESIAN_POINT('Ctrl Pts',(95.3720127075547,0.978299103602208,-5.46895532024229));
#35603=CARTESIAN_POINT('Ctrl Pts',(95.3350217236955,0.937142456290982,-5.46595177246828));
#35604=CARTESIAN_POINT('Ctrl Pts',(95.300396839982,0.893916707145829,-5.46294822469426));
#35605=CARTESIAN_POINT('Ctrl Pts',(95.268361636902,0.848930971485543,-5.45994467692024));
#35606=CARTESIAN_POINT('Ctrl Pts',(95.2362659727676,0.803860332819978,-5.45693546045528));
#35607=CARTESIAN_POINT('Ctrl Pts',(95.2067700350987,0.757023520050274,-5.45392624399031));
#35608=CARTESIAN_POINT('Ctrl Pts',(95.1800531660339,0.708757321747617,-5.45091702752535));
#35609=CARTESIAN_POINT('Ctrl Pts',(95.1596136662556,0.67183170194124,-5.44861485360223));
#35610=CARTESIAN_POINT('Ctrl Pts',(95.140799809666,0.634070069460073,-5.44631267967911));
#35611=CARTESIAN_POINT('Ctrl Pts',(95.1236727362608,0.595630800756837,-5.44401050575599));
#35612=CARTESIAN_POINT('Ctrl Pts',(95.1012788180504,0.545370851550231,-5.44100037709476));
#35613=CARTESIAN_POINT('Ctrl Pts',(95.081676222055,0.493740629411957,-5.43799024843352));
#35614=CARTESIAN_POINT('Ctrl Pts',(95.0650314229126,0.441081476069969,-5.43498011977228));
#35615=CARTESIAN_POINT('Ctrl Pts',(95.0484162062683,0.38851591288124,-5.43197534095783));
#35616=CARTESIAN_POINT('Ctrl Pts',(95.0347485121264,0.334925547044205,-5.42897056214339));
#35617=CARTESIAN_POINT('Ctrl Pts',(95.0241468841081,0.280671876705698,-5.42596578332895));
#35618=CARTESIAN_POINT('Ctrl Pts',(95.0135557446443,0.226471881385568,-5.42296397724532));
#35619=CARTESIAN_POINT('Ctrl Pts',(95.0060247631399,0.171610397288745,-5.4199621711617));
#35620=CARTESIAN_POINT('Ctrl Pts',(95.0016222366284,0.116462464570799,-5.41696036507808));
#35621=CARTESIAN_POINT('Ctrl Pts',(94.997222326796,0.0613473094965147,-5.41396034314348));
#35622=CARTESIAN_POINT('Ctrl Pts',(94.9959472283989,0.0059465686443272,
-5.41096032120888));
#35623=CARTESIAN_POINT('Ctrl Pts',(94.9978135267317,-0.0493584860709382,
-5.40796029927428));
#35624=CARTESIAN_POINT('Ctrl Pts',(94.9996794529135,-0.104652512624003,
-5.40496087556219));
#35625=CARTESIAN_POINT('Ctrl Pts',(95.0046855139934,-0.159850363413252,
-5.4019614518501));
#35626=CARTESIAN_POINT('Ctrl Pts',(95.0127962068697,-0.214571982636142,
-5.39896202813801));
#35627=CARTESIAN_POINT('Ctrl Pts',(95.0209143563533,-0.269343910462044,
-5.39595984689025));
#35628=CARTESIAN_POINT('Ctrl Pts',(95.0321427624758,-0.323638208470656,
-5.39295766564249));
#35629=CARTESIAN_POINT('Ctrl Pts',(95.046394346872,-0.377082656788055,-5.38995548439472));
#35630=CARTESIAN_POINT('Ctrl Pts',(95.0606524182732,-0.43055143183191,-5.38695193662071));
#35631=CARTESIAN_POINT('Ctrl Pts',(95.077936245977,-0.483169083444685,-5.38394838884669));
#35632=CARTESIAN_POINT('Ctrl Pts',(95.0981091010857,-0.534579457553749,
-5.38094484107267));
#35633=CARTESIAN_POINT('Ctrl Pts',(95.1183200290636,-0.586086860091949,
-5.3779356246077));
#35634=CARTESIAN_POINT('Ctrl Pts',(95.1414306557218,-0.636381952346079,
-5.37492640814274));
#35635=CARTESIAN_POINT('Ctrl Pts',(95.1672569034086,-0.685130510495474,
-5.37191719167777));
#35636=CARTESIAN_POINT('Ctrl Pts',(95.187015041332,-0.722425155353208,-5.36961501775466));
#35637=CARTESIAN_POINT('Ctrl Pts',(95.2083616074269,-0.758815074333219,
-5.36731284383154));
#35638=CARTESIAN_POINT('Ctrl Pts',(95.2311973638051,-0.794162524771665,
-5.36501066990843));
#35639=CARTESIAN_POINT('Ctrl Pts',(95.2610554749082,-0.840379872904287,
-5.36200054124719));
#35640=CARTESIAN_POINT('Ctrl Pts',(95.2935863939703,-0.88500812530993,-5.35899041258595));
#35641=CARTESIAN_POINT('Ctrl Pts',(95.3285951991964,-0.927721347218681,
-5.35598028392472));
#35642=CARTESIAN_POINT('Ctrl Pts',(95.3635417839111,-0.970358655696832,
-5.35297550511027));
#35643=CARTESIAN_POINT('Ctrl Pts',(95.4009571831488,-1.01108728289679,-5.34997072629583));
#35644=CARTESIAN_POINT('Ctrl Pts',(95.4406034042517,-1.04961042417708,-5.34696594748138));
#35645=CARTESIAN_POINT('Ctrl Pts',(95.4802104019871,-1.08809545319132,-5.34396414139776));
#35646=CARTESIAN_POINT('Ctrl Pts',(95.5220434726716,-1.12437895242759,-5.34096233531414));
#35647=CARTESIAN_POINT('Ctrl Pts',(95.5658258273125,-1.1581988008135,-5.33796052923052));
#35648=CARTESIAN_POINT('Ctrl Pts',(95.6095821595379,-1.1919985480844,-5.33496050729593));
#35649=CARTESIAN_POINT('Ctrl Pts',(95.6552850622396,-1.22333722462838,-5.33196048536133));
#35650=CARTESIAN_POINT('Ctrl Pts',(95.7026242720679,-1.25199261433716,-5.32896046342673));
#35651=CARTESIAN_POINT('Ctrl Pts',(95.7499540421715,-1.28064228998804,-5.32596103971464));
#35652=CARTESIAN_POINT('Ctrl Pts',(95.7989190198661,-1.30660946809156,-5.32296161600254));
#35653=CARTESIAN_POINT('Ctrl Pts',(95.849181499433,-1.3297162224526,-5.31996219229045));
#35654=CARTESIAN_POINT('Ctrl Pts',(95.8994901880697,-1.35284422012747,-5.31696001104269));
#35655=CARTESIAN_POINT('Ctrl Pts',(95.951098280898,-1.37310631910394,-5.31395782979493));
#35656=CARTESIAN_POINT('Ctrl Pts',(96.0036464544788,-1.39037207037842,-5.31095564854717));
#35657=CARTESIAN_POINT('Ctrl Pts',(96.0562185468218,-1.4076456806396,-5.30795210077315));
#35658=CARTESIAN_POINT('Ctrl Pts',(96.1097310617508,-1.42192008806373,-5.30494855299913));
#35659=CARTESIAN_POINT('Ctrl Pts',(96.1638110025119,-1.43311520559528,-5.30194500522512));
#35660=CARTESIAN_POINT('Ctrl Pts',(96.21799301006,-1.44433145202711,-5.29893578876015));
#35661=CARTESIAN_POINT('Ctrl Pts',(96.2727440590942,-1.4524567211945,-5.29592657229519));
#35662=CARTESIAN_POINT('Ctrl Pts',(96.3276836488634,-1.45746256450146,-5.29291735583022));
#35663=CARTESIAN_POINT('Ctrl Pts',(96.3697146866388,-1.46129223978693,-5.2906151819071));
#35664=CARTESIAN_POINT('Ctrl Pts',(96.4118559030601,-1.46329722506164,-5.28831300798398));
#35665=CARTESIAN_POINT('Ctrl Pts',(96.4539377117467,-1.46348537267671,-5.28601083406087));
#35666=CARTESIAN_POINT('Ctrl Pts',(96.5089603393478,-1.46373137864655,-5.28300070539963));
#35667=CARTESIAN_POINT('Ctrl Pts',(96.5641124682866,-1.46087056035062,-5.27999057673839));
#35668=CARTESIAN_POINT('Ctrl Pts',(96.619014614918,-1.45488808055931,-5.27698044807715));
#35669=CARTESIAN_POINT('Ctrl Pts',(96.6738191849651,-1.44891623332027,-5.27397566926271));
#35670=CARTESIAN_POINT('Ctrl Pts',(96.7283741336371,-1.43983379151761,-5.27097089044826));
#35671=CARTESIAN_POINT('Ctrl Pts',(96.7823008408051,-1.42767790751623,-5.26796611163381));
#35672=CARTESIAN_POINT('Ctrl Pts',(96.8361741964306,-1.41553404974816,-5.2649643055502));
#35673=CARTESIAN_POINT('Ctrl Pts',(96.8894200291381,-1.40032288874674,-5.26196249946658));
#35674=CARTESIAN_POINT('Ctrl Pts',(96.941667569056,-1.38213302081762,-5.25896069338296));
#35675=CARTESIAN_POINT('Ctrl Pts',(96.9938840552034,-1.36395396419143,-5.25596067144835));
#35676=CARTESIAN_POINT('Ctrl Pts',(97.0451029268492,-1.34279988301938,-5.25296064951375));
#35677=CARTESIAN_POINT('Ctrl Pts',(97.0949685453458,-1.31880921319783,-5.24996062757914));
#35678=CARTESIAN_POINT('Ctrl Pts',(97.1448242203366,-1.29482332726092,-5.24696120386705));
#35679=CARTESIAN_POINT('Ctrl Pts',(97.193326702446,-1.26800220482898,-5.24396178015496));
#35680=CARTESIAN_POINT('Ctrl Pts',(97.2401424526182,-1.23853146535546,-5.24096235644287));
#35681=CARTESIAN_POINT('Ctrl Pts',(97.287001243092,-1.20903363180549,-5.23796017519511));
#35682=CARTESIAN_POINT('Ctrl Pts',(97.3321697556253,-1.17688159647601,-5.23495799394735));
#35683=CARTESIAN_POINT('Ctrl Pts',(97.3753424027505,-1.14230502559401,-5.23195581269959));
#35684=CARTESIAN_POINT('Ctrl Pts',(97.4185347011063,-1.10771271622452,-5.22895226492557));
#35685=CARTESIAN_POINT('Ctrl Pts',(97.4597289295779,-1.07069402497319,-5.22594871715155));
#35686=CARTESIAN_POINT('Ctrl Pts',(97.498654209139,-1.03151758740718,-5.22294516937753));
#35687=CARTESIAN_POINT('Ctrl Pts',(97.5376529536145,-0.992267210908366,
-5.21993595291257));
#35688=CARTESIAN_POINT('Ctrl Pts',(97.5743738434778,-0.950851349007003,
-5.2169267364476));
#35689=CARTESIAN_POINT('Ctrl Pts',(97.6085851481477,-0.907573137121431,
-5.21391751998263));
#35690=CARTESIAN_POINT('Ctrl Pts',(97.6347581983098,-0.874463531348052,
-5.21161534605952));
#35691=CARTESIAN_POINT('Ctrl Pts',(97.6594632226598,-0.840264644534702,
-5.20931317213641));
#35692=CARTESIAN_POINT('Ctrl Pts',(97.6826141364205,-0.805122800332881,
-5.2070109982133));
#35693=CARTESIAN_POINT('Ctrl Pts',(97.7134385129978,-0.758333051535094,
-5.20394575954988));
#35694=CARTESIAN_POINT('Ctrl Pts',(97.7416323362563,-0.709679539907104,
-5.20088052088647));
#35695=CARTESIAN_POINT('Ctrl Pts',(97.7669701794824,-0.659483238711326,
-5.19781528222305));
#35696=CARTESIAN_POINT('Ctrl Pts',(97.7925679753649,-0.608771950437985,
-5.19471859585804));
#35697=CARTESIAN_POINT('Ctrl Pts',(97.8152504927981,-0.556486417249488,
-5.19162190949302));
#35698=CARTESIAN_POINT('Ctrl Pts',(97.834829882593,-0.502988330200432,-5.18852522312801));
#35699=CARTESIAN_POINT('Ctrl Pts',(97.8541435920563,-0.450216179437119,
-5.18547055690095));
#35700=CARTESIAN_POINT('Ctrl Pts',(97.870437679572,-0.396264660733034,-5.18241589067389));
#35701=CARTESIAN_POINT('Ctrl Pts',(97.8835787106893,-0.341504044364106,
-5.17936122444683));
#35702=CARTESIAN_POINT('Ctrl Pts',(97.8969908948064,-0.285613493421438,
-5.17624352801284));
#35703=CARTESIAN_POINT('Ctrl Pts',(97.9071181978082,-0.22888056250821,-5.17312583157885));
#35704=CARTESIAN_POINT('Ctrl Pts',(97.9138720971347,-0.171716109322641,
-5.17000813514486));
#35705=CARTESIAN_POINT('Ctrl Pts',(97.9206259964612,-0.11455165613708,-5.16689043871087));
#35706=CARTESIAN_POINT('Ctrl Pts',(97.9240063897609,-0.0569562315344563,
-5.16377274227688));
#35707=CARTESIAN_POINT('Ctrl Pts',(97.9239808052397,0.000649980989679657,
-5.16065504584289));
#35708=CARTESIAN_POINT('Ctrl Pts',(97.9239808315838,0.000587678466145934,
-5.08934495415707));
#35709=CARTESIAN_POINT('Ctrl Pts',(97.9240035209153,-0.05591572584774,-5.09240255388167));
#35710=CARTESIAN_POINT('Ctrl Pts',(97.9207496103773,-0.112403252583685,
-5.09546015360626));
#35711=CARTESIAN_POINT('Ctrl Pts',(97.9142508208512,-0.168479706123258,
-5.09851775333086));
#35712=CARTESIAN_POINT('Ctrl Pts',(97.9077417371337,-0.224644985704266,
-5.10158019634462));
#35713=CARTESIAN_POINT('Ctrl Pts',(97.8979775678897,-0.280397394683033,
-5.10464263935838));
#35714=CARTESIAN_POINT('Ctrl Pts',(97.8850417680253,-0.335348661160212,
-5.10770508237214));
#35715=CARTESIAN_POINT('Ctrl Pts',(97.8720960647367,-0.390341997374302,
-5.11076986993918));
#35716=CARTESIAN_POINT('Ctrl Pts',(97.8559740363391,-0.444532490215592,
-5.11383465750622));
#35717=CARTESIAN_POINT('Ctrl Pts',(97.8368090965327,-0.497547065007448,
-5.11689944507326));
#35718=CARTESIAN_POINT('Ctrl Pts',(97.817598117962,-0.550688993474006,-5.11997159499226));
#35719=CARTESIAN_POINT('Ctrl Pts',(97.7953298137575,-0.602648896761696,
-5.12304374491126));
#35720=CARTESIAN_POINT('Ctrl Pts',(97.7701856592661,-0.653074133171955,
-5.12611589483027));
#35721=CARTESIAN_POINT('Ctrl Pts',(97.745977310828,-0.701622661359947,-5.12907370658403));
#35722=CARTESIAN_POINT('Ctrl Pts',(97.719103703838,-0.748748447528192,-5.13203151833779));
#35723=CARTESIAN_POINT('Ctrl Pts',(97.6897645353489,-0.794162524771699,
-5.13498933009155));
#35724=CARTESIAN_POINT('Ctrl Pts',(97.6599064242457,-0.840379872904354,
-5.13799945875279));
#35725=CARTESIAN_POINT('Ctrl Pts',(97.6273755051837,-0.885008125310025,
-5.14100958741403));
#35726=CARTESIAN_POINT('Ctrl Pts',(97.5923666999576,-0.927721347218802,
-5.14401971607527));
#35727=CARTESIAN_POINT('Ctrl Pts',(97.5574201152428,-0.970358655696963,
-5.14702449488971));
#35728=CARTESIAN_POINT('Ctrl Pts',(97.5200047160051,-1.01108728289694,-5.15002927370416));
#35729=CARTESIAN_POINT('Ctrl Pts',(97.4803584949022,-1.04961042417723,-5.15303405251861));
#35730=CARTESIAN_POINT('Ctrl Pts',(97.4407514971667,-1.0880954531915,-5.15603585860223));
#35731=CARTESIAN_POINT('Ctrl Pts',(97.3989184264822,-1.12437895242778,-5.15903766468585));
#35732=CARTESIAN_POINT('Ctrl Pts',(97.3551360718413,-1.15819880081371,-5.16203947076947));
#35733=CARTESIAN_POINT('Ctrl Pts',(97.3113797396159,-1.1919985480846,-5.16503949270407));
#35734=CARTESIAN_POINT('Ctrl Pts',(97.2656768369141,-1.22333722462856,-5.16803951463867));
#35735=CARTESIAN_POINT('Ctrl Pts',(97.2183376270859,-1.25199261433733,-5.17103953657327));
#35736=CARTESIAN_POINT('Ctrl Pts',(97.1710078569822,-1.28064228998816,-5.17403896028536));
#35737=CARTESIAN_POINT('Ctrl Pts',(97.1220428792877,-1.30660946809164,-5.17703838399745));
#35738=CARTESIAN_POINT('Ctrl Pts',(97.0717803997209,-1.32971622245264,-5.18003780770954));
#35739=CARTESIAN_POINT('Ctrl Pts',(97.0214717110841,-1.35284422012752,-5.1830399889573));
#35740=CARTESIAN_POINT('Ctrl Pts',(96.9698636182559,-1.37310631910399,-5.18604217020506));
#35741=CARTESIAN_POINT('Ctrl Pts',(96.9173154446751,-1.39037207037847,-5.18904435145282));
#35742=CARTESIAN_POINT('Ctrl Pts',(96.8647433523321,-1.40764568063965,-5.19204789922684));
#35743=CARTESIAN_POINT('Ctrl Pts',(96.811230837403,-1.42192008806378,-5.19505144700086));
#35744=CARTESIAN_POINT('Ctrl Pts',(96.7571508966418,-1.43311520559533,-5.19805499477488));
#35745=CARTESIAN_POINT('Ctrl Pts',(96.7029688890938,-1.44433145202716,-5.20106421123985));
#35746=CARTESIAN_POINT('Ctrl Pts',(96.6482178400595,-1.45245672119454,-5.20407342770482));
#35747=CARTESIAN_POINT('Ctrl Pts',(96.5932782502903,-1.4574625645015,-5.20708264416979));
#35748=CARTESIAN_POINT('Ctrl Pts',(96.551247212515,-1.46129223978694,-5.2093848180929));
#35749=CARTESIAN_POINT('Ctrl Pts',(96.5091059960939,-1.46329722506164,-5.211686992016));
#35750=CARTESIAN_POINT('Ctrl Pts',(96.4670241874073,-1.46348537267671,-5.21398916593911));
#35751=CARTESIAN_POINT('Ctrl Pts',(96.4120015598063,-1.46373137864655,-5.21699929460035));
#35752=CARTESIAN_POINT('Ctrl Pts',(96.3568494308675,-1.46087056035062,-5.22000942326159));
#35753=CARTESIAN_POINT('Ctrl Pts',(96.3019472842361,-1.45488808055932,-5.22301955192283));
#35754=CARTESIAN_POINT('Ctrl Pts',(96.2471427141891,-1.44891623332029,-5.22602433073727));
#35755=CARTESIAN_POINT('Ctrl Pts',(96.192587765517,-1.43983379151764,-5.22902910955171));
#35756=CARTESIAN_POINT('Ctrl Pts',(96.138661058349,-1.42767790751627,-5.23203388836616));
#35757=CARTESIAN_POINT('Ctrl Pts',(96.0847877027236,-1.41553404974821,-5.23503569444978));
#35758=CARTESIAN_POINT('Ctrl Pts',(96.0315418700161,-1.4003228887468,-5.2380375005334));
#35759=CARTESIAN_POINT('Ctrl Pts',(95.9792943300983,-1.38213302081769,-5.24103930661701));
#35760=CARTESIAN_POINT('Ctrl Pts',(95.9270778439509,-1.36395396419155,-5.24403932855161));
#35761=CARTESIAN_POINT('Ctrl Pts',(95.8758589723052,-1.34279988301956,-5.24703935048621));
#35762=CARTESIAN_POINT('Ctrl Pts',(95.8259933538087,-1.31880921319808,-5.25003937242081));
#35763=CARTESIAN_POINT('Ctrl Pts',(95.776137678818,-1.29482332726122,-5.25303879613289));
#35764=CARTESIAN_POINT('Ctrl Pts',(95.7276351967086,-1.26800220482933,-5.25603821984498));
#35765=CARTESIAN_POINT('Ctrl Pts',(95.6808194465364,-1.23853146535586,-5.25903764355707));
#35766=CARTESIAN_POINT('Ctrl Pts',(95.6339606560627,-1.20903363180593,-5.26203982480482));
#35767=CARTESIAN_POINT('Ctrl Pts',(95.5887921435294,-1.17688159647649,-5.26504200605258));
#35768=CARTESIAN_POINT('Ctrl Pts',(95.5456194964042,-1.14230502559454,-5.26804418730034));
#35769=CARTESIAN_POINT('Ctrl Pts',(95.5024271980484,-1.10771271622507,-5.27104773507436));
#35770=CARTESIAN_POINT('Ctrl Pts',(95.4612329695767,-1.07069402497377,-5.27405128284838));
#35771=CARTESIAN_POINT('Ctrl Pts',(95.4223076900156,-1.03151758740778,-5.27705483062239));
#35772=CARTESIAN_POINT('Ctrl Pts',(95.3833089455401,-0.992267210909005,
-5.28006404708736));
#35773=CARTESIAN_POINT('Ctrl Pts',(95.3465880556767,-0.950851349007679,
-5.28307326355232));
#35774=CARTESIAN_POINT('Ctrl Pts',(95.3123767510069,-0.907573137122142,
-5.28608248001729));
#35775=CARTESIAN_POINT('Ctrl Pts',(95.2862037008445,-0.874463531348529,
-5.28838465394042));
#35776=CARTESIAN_POINT('Ctrl Pts',(95.2614986764943,-0.840264644534928,
-5.29068682786355));
#35777=CARTESIAN_POINT('Ctrl Pts',(95.2383477627335,-0.805122800332843,
-5.29298900178667));
#35778=CARTESIAN_POINT('Ctrl Pts',(95.2080775783894,-0.759174285592585,
-5.29599913044791));
#35779=CARTESIAN_POINT('Ctrl Pts',(95.1803386839591,-0.711419753414071,
-5.29900925910915));
#35780=CARTESIAN_POINT('Ctrl Pts',(95.1553508543956,-0.662168924559175,
-5.30201938777039));
#35781=CARTESIAN_POINT('Ctrl Pts',(95.1304074352461,-0.613005628304544,
-5.30502416658483));
#35782=CARTESIAN_POINT('Ctrl Pts',(95.1082056148983,-0.562351780010962,
-5.30802894539927));
#35783=CARTESIAN_POINT('Ctrl Pts',(95.0889211537989,-0.510544784132586,
-5.31103372421372));
#35784=CARTESIAN_POINT('Ctrl Pts',(95.0696557714787,-0.458789042693585,
-5.31403553029734));
#35785=CARTESIAN_POINT('Ctrl Pts',(95.0533022142256,-0.405882906141247,
-5.31703733638096));
#35786=CARTESIAN_POINT('Ctrl Pts',(95.0399888674516,-0.35218531289517,-5.32003914246458));
#35787=CARTESIAN_POINT('Ctrl Pts',(95.0266834335787,-0.298519635271133,
-5.32303916439918));
#35788=CARTESIAN_POINT('Ctrl Pts',(95.016414755477,-0.244063944907904,-5.32603918633378));
#35789=CARTESIAN_POINT('Ctrl Pts',(95.0092612089185,-0.189191739574413,
-5.32903920826838));
#35790=CARTESIAN_POINT('Ctrl Pts',(95.0021090888205,-0.134330476090436,
-5.33203863198046));
#35791=CARTESIAN_POINT('Ctrl Pts',(94.9980709348699,-0.0790533859721265,
-5.33503805569255));
#35792=CARTESIAN_POINT('Ctrl Pts',(94.9971735302096,-0.0237412388959985,
-5.33803747940464));
#35793=CARTESIAN_POINT('Ctrl Pts',(94.9962753005157,0.0316217596880619,
-5.3410396606524));
#35794=CARTESIAN_POINT('Ctrl Pts',(94.9985235974758,0.0870193504396207,
-5.34404184190015));
#35795=CARTESIAN_POINT('Ctrl Pts',(95.0038930412365,0.142070106905398,-5.34704402314791));
#35796=CARTESIAN_POINT('Ctrl Pts',(95.0092649290487,0.19714592125349,-5.35004757092193));
#35797=CARTESIAN_POINT('Ctrl Pts',(95.0177607145291,0.251874063834909,-5.35305111869595));
#35798=CARTESIAN_POINT('Ctrl Pts',(95.0293034153971,0.305880884755493,-5.35605466646997));
#35799=CARTESIAN_POINT('Ctrl Pts',(95.0408679011704,0.359989634461566,-5.35906388293494));
#35800=CARTESIAN_POINT('Ctrl Pts',(95.055490650066,0.413373832349386,-5.3620730993999));
#35801=CARTESIAN_POINT('Ctrl Pts',(95.0730443946928,0.465673765817796,-5.36508231586487));
#35802=CARTESIAN_POINT('Ctrl Pts',(95.0864737287415,0.505685358341554,-5.36738448978799));
#35803=CARTESIAN_POINT('Ctrl Pts',(95.1016174885178,0.545062618622844,-5.36968666371111));
#35804=CARTESIAN_POINT('Ctrl Pts',(95.1184001604099,0.58365349767525,-5.37198883763424));
#35805=CARTESIAN_POINT('Ctrl Pts',(95.1403437682178,0.634111679801023,-5.37499896629548));
#35806=CARTESIAN_POINT('Ctrl Pts',(95.1651830511075,0.683436639338107,-5.37800909495672));
#35807=CARTESIAN_POINT('Ctrl Pts',(95.1927786937771,0.731275078639996,-5.38101922361796));
#35808=CARTESIAN_POINT('Ctrl Pts',(95.2203252912141,0.779028495555819,-5.3840240024324));
#35809=CARTESIAN_POINT('Ctrl Pts',(95.2506182649216,0.825300181473522,-5.38702878124685));
#35810=CARTESIAN_POINT('Ctrl Pts',(95.2834710644068,0.86975857581954,-5.3900335600613));
#35811=CARTESIAN_POINT('Ctrl Pts',(95.3162913614897,0.914172985949891,-5.39303536614492));
#35812=CARTESIAN_POINT('Ctrl Pts',(95.3516661552266,0.956777235594734,-5.39603717222854));
#35813=CARTESIAN_POINT('Ctrl Pts',(95.3893649743159,0.997267675972879,-5.39903897831215));
#35814=CARTESIAN_POINT('Ctrl Pts',(95.4270413867909,1.03773405051287,-5.40203900024676));
#35815=CARTESIAN_POINT('Ctrl Pts',(95.4670387276289,1.07608872022583,-5.40503902218136));
#35816=CARTESIAN_POINT('Ctrl Pts',(95.5090870066105,1.11206196557865,-5.40803904411596));
#35817=CARTESIAN_POINT('Ctrl Pts',(95.5511269009111,1.14802803764882,-5.41103846782805));
#35818=CARTESIAN_POINT('Ctrl Pts',(95.5952165200877,1.18161328530521,-5.41403789154014));
#35819=CARTESIAN_POINT('Ctrl Pts',(95.6410515934928,1.21258722588828,-5.41703731525223));
#35820=CARTESIAN_POINT('Ctrl Pts',(95.6869288056093,1.24358964252351,-5.42003949649999));
#35821=CARTESIAN_POINT('Ctrl Pts',(95.7345542394087,1.27197565942828,-5.42304167774775));
#35822=CARTESIAN_POINT('Ctrl Pts',(95.7835945725189,1.2975581229961,-5.42604385899551));
#35823=CARTESIAN_POINT('Ctrl Pts',(95.8326572277,1.3231522311334,-5.42904740676953));
#35824=CARTESIAN_POINT('Ctrl Pts',(95.8831355838423,1.34594002441192,-5.43205095454354));
#35825=CARTESIAN_POINT('Ctrl Pts',(95.9346746362876,1.36578181672804,-5.43505450231756));
#35826=CARTESIAN_POINT('Ctrl Pts',(95.9863109600207,1.38566105708795,-5.43806371878253));
#35827=CARTESIAN_POINT('Ctrl Pts',(96.0390114750706,1.40258302750693,-5.44107293524749));
#35828=CARTESIAN_POINT('Ctrl Pts',(96.0924053740501,1.41645777229698,-5.44408215171246));
#35829=CARTESIAN_POINT('Ctrl Pts',(96.133253895024,1.42707252069326,-5.44638432563558));
#35830=CARTESIAN_POINT('Ctrl Pts',(96.1745079011604,1.43590479475527,-5.44868649955869));
#35831=CARTESIAN_POINT('Ctrl Pts',(96.2159987870002,1.44293476019596,-5.45098867348181));
#35832=CARTESIAN_POINT('Ctrl Pts',(96.2702487736725,1.45212655072404,-5.45399880214304));
#35833=CARTESIAN_POINT('Ctrl Pts',(96.3251318414259,1.45827394706615,-5.45700893080428));
#35834=CARTESIAN_POINT('Ctrl Pts',(96.380275972639,1.46130058908986,-5.46001905946552));
#35835=CARTESIAN_POINT('Ctrl Pts',(96.435322097193,1.46432185191788,-5.46302383827997));
#35836=CARTESIAN_POINT('Ctrl Pts',(96.4906278413713,1.46423333870561,-5.46602861709441));
#35837=CARTESIAN_POINT('Ctrl Pts',(96.5458135838134,1.46101012711558,-5.46903339590885));
#35838=CARTESIAN_POINT('Ctrl Pts',(96.6009447291061,1.45779010435941,-5.47203520199247));
#35839=CARTESIAN_POINT('Ctrl Pts',(96.6559555832192,1.45144155732333,-5.47503700807609));
#35840=CARTESIAN_POINT('Ctrl Pts',(96.710465903512,1.44199159942286,-5.47803881415971));
#35841=CARTESIAN_POINT('Ctrl Pts',(96.7649438251316,1.43254725818537,-5.48103883609431));
#35842=CARTESIAN_POINT('Ctrl Pts',(96.8189212832728,1.42000524975318,-5.48403885802891));
#35843=CARTESIAN_POINT('Ctrl Pts',(96.8720248589717,1.40444432450706,-5.48703887996351));
#35844=CARTESIAN_POINT('Ctrl Pts',(96.9251178454966,1.38888650220354,-5.4900383036756));
#35845=CARTESIAN_POINT('Ctrl Pts',(96.9773367891258,1.37031110703871,-5.49303772738769));
#35846=CARTESIAN_POINT('Ctrl Pts',(97.0283224021416,1.34884703904829,-5.49603715109977));
#35847=CARTESIAN_POINT('Ctrl Pts',(97.0793548890439,1.32736323795619,-5.49903933234753));
#35848=CARTESIAN_POINT('Ctrl Pts',(97.1291512922216,1.30298566361309,-5.50204151359529));
#35849=CARTESIAN_POINT('Ctrl Pts',(97.1773727394569,1.2758912224805,-5.50504369484304));
#35850=CARTESIAN_POINT('Ctrl Pts',(97.2256161360245,1.24878444855975,-5.50804724261706));
#35851=CARTESIAN_POINT('Ctrl Pts',(97.2722827018194,1.218958627561,-5.51105079039108));
#35852=CARTESIAN_POINT('Ctrl Pts',(97.3170614728188,1.18663476150111,-5.5140543381651));
#35853=CARTESIAN_POINT('Ctrl Pts',(97.3619247562125,1.15424988958391,-5.51706355463006));
#35854=CARTESIAN_POINT('Ctrl Pts',(97.4048927163997,1.11935788811173,-5.52007277109503));
#35855=CARTESIAN_POINT('Ctrl Pts',(97.4456874053701,1.08222016681613,-5.52308198755999));
#35856=CARTESIAN_POINT('Ctrl Pts',(97.4768970143308,1.05380828800104,-5.52538416148312));
#35857=CARTESIAN_POINT('Ctrl Pts',(97.506835308566,1.02408286747054,-5.52768633540624));
#35858=CARTESIAN_POINT('Ctrl Pts',(97.5353935509653,0.993174279457849,-5.52998850932936));
#35859=CARTESIAN_POINT('Ctrl Pts',(97.5722927650602,0.953238257117894,-5.5329630764363));
#35860=CARTESIAN_POINT('Ctrl Pts',(97.6070498726323,0.911149160200333,-5.53593764354323));
#35861=CARTESIAN_POINT('Ctrl Pts',(97.6394002965644,0.867168624489368,-5.53891221065017));
#35862=CARTESIAN_POINT('Ctrl Pts',(97.6717038201296,0.823251850021986,-5.54188246534719));
#35863=CARTESIAN_POINT('Ctrl Pts',(97.7016072483117,0.777449496312327,-5.54485272004423));
#35864=CARTESIAN_POINT('Ctrl Pts',(97.7288843008441,0.730058345952218,-5.54782297474125));
#35865=CARTESIAN_POINT('Ctrl Pts',(97.7561332027838,0.682716104430883,-5.550790164062));
#35866=CARTESIAN_POINT('Ctrl Pts',(97.7807608285218,0.633788780753312,-5.55375735338275));
#35867=CARTESIAN_POINT('Ctrl Pts',(97.8025839793593,0.583602353875609,-5.5567245427035));
#35868=CARTESIAN_POINT('Ctrl Pts',(97.8244001929085,0.533431880593121,-5.55969078879438));
#35869=CARTESIAN_POINT('Ctrl Pts',(97.8434134677593,0.482003586648015,-5.56265703488525));
#35870=CARTESIAN_POINT('Ctrl Pts',(97.8594874089156,0.429666355128056,-5.56562328097612));
#35871=CARTESIAN_POINT('Ctrl Pts',(97.8755578133273,0.377340639353834,-5.56858887440473));
#35872=CARTESIAN_POINT('Ctrl Pts',(97.8886900146702,0.324106902664976,-5.57155446783335));
#35873=CARTESIAN_POINT('Ctrl Pts',(97.8987973994405,0.270329502740709,-5.57452006126196));
#35874=CARTESIAN_POINT('Ctrl Pts',(97.9089129448949,0.21650868304136,-5.57748804910532));
#35875=CARTESIAN_POINT('Ctrl Pts',(97.9159987049772,0.162143858228707,-5.58045603694869));
#35876=CARTESIAN_POINT('Ctrl Pts',(97.9200194895277,0.107608087050669,-5.58342402479205));
#35877=CARTESIAN_POINT('Ctrl Pts',(97.9226932180571,0.0713430632866484,
-5.58539766791373));
#35878=CARTESIAN_POINT('Ctrl Pts',(97.9240127055925,0.0350025971491351,
-5.5873713110354));
#35879=CARTESIAN_POINT('Ctrl Pts',(97.9239803690938,-0.00130348536077301,
-5.58934495415708));
#35880=CARTESIAN_POINT('Origin',(96.460480949577,-8.32667268468867E-16,
1.18130019239114E-14));
#35881=CARTESIAN_POINT('',(97.9239808258401,0.000601812115854682,-6.16065504587429));
#35882=CARTESIAN_POINT('',(97.923980796324,0.000669754741461998,-6.08934495418968));
#35883=CARTESIAN_POINT('',(97.923980949577,-1.01189432752408E-15,1.19922289829666E-14));
#35884=CARTESIAN_POINT('Ctrl Pts',(97.9239808258399,0.000601812690350752,
-6.16065504584289));
#35885=CARTESIAN_POINT('Ctrl Pts',(97.9239666682132,0.0350306063101608,
-6.15877304002328));
#35886=CARTESIAN_POINT('Ctrl Pts',(97.922737702697,0.0694328740323531,-6.15689103420366));
#35887=CARTESIAN_POINT('Ctrl Pts',(97.9202989417931,0.103748154692315,-6.15500902838404));
#35888=CARTESIAN_POINT('Ctrl Pts',(97.9163983246865,0.158632899870198,-6.1519988997228));
#35889=CARTESIAN_POINT('Ctrl Pts',(97.9093899575706,0.21341268079498,-6.14898877106156));
#35890=CARTESIAN_POINT('Ctrl Pts',(97.8992876392723,0.267707974644227,-6.14597864240033));
#35891=CARTESIAN_POINT('Ctrl Pts',(97.8892032756401,0.321906770457557,-6.14297386358588));
#35892=CARTESIAN_POINT('Ctrl Pts',(97.8760359690999,0.375622272988754,-6.13996908477144));
#35893=CARTESIAN_POINT('Ctrl Pts',(97.8598512952113,0.428479737863195,-6.13696430595699));
#35894=CARTESIAN_POINT('Ctrl Pts',(97.8436826333761,0.481284909033203,-6.13396249987338));
#35895=CARTESIAN_POINT('Ctrl Pts',(97.8245026715609,0.533233221657217,-6.13096069378976));
#35896=CARTESIAN_POINT('Ctrl Pts',(97.8024276915079,0.583961635572912,-6.12795888770614));
#35897=CARTESIAN_POINT('Ctrl Pts',(97.7803658319074,0.634659898623632,-6.12495886577155));
#35898=CARTESIAN_POINT('Ctrl Pts',(97.7554125748742,0.684139216791161,-6.12195884383695));
#35899=CARTESIAN_POINT('Ctrl Pts',(97.7277327599278,0.732055393506915,-6.11895882190236));
#35900=CARTESIAN_POINT('Ctrl Pts',(97.7000584645039,0.779962015447368,-6.11595939819027));
#35901=CARTESIAN_POINT('Ctrl Pts',(97.6696589549361,0.826305657916654,-6.11295997447818));
#35902=CARTESIAN_POINT('Ctrl Pts',(97.6367444549757,0.870767716367136,-6.1099605507661));
#35903=CARTESIAN_POINT('Ctrl Pts',(97.6037996948998,0.915270651240504,-6.10695836951834));
#35904=CARTESIAN_POINT('Ctrl Pts',(97.5683356399163,0.957888120715072,-6.10395618827059));
#35905=CARTESIAN_POINT('Ctrl Pts',(97.5306043291967,0.998332711269761,-6.10095400702284));
#35906=CARTESIAN_POINT('Ctrl Pts',(97.4928558440221,1.03879571130427,-6.09795045924882));
#35907=CARTESIAN_POINT('Ctrl Pts',(97.4528384281371,1.07708349508994,-6.09494691147481));
#35908=CARTESIAN_POINT('Ctrl Pts',(97.4108403640097,1.11294619519502,-6.0919433637008));
#35909=CARTESIAN_POINT('Ctrl Pts',(97.3687630356043,1.14887658011109,-6.08893414723584));
#35910=CARTESIAN_POINT('Ctrl Pts',(97.3246980129091,1.18237241782646,-6.08592493077087));
#35911=CARTESIAN_POINT('Ctrl Pts',(97.2789650303539,1.21322547760701,-6.08291571430591));
#35912=CARTESIAN_POINT('Ctrl Pts',(97.2439774244133,1.23682933279751,-6.08061354038278));
#35913=CARTESIAN_POINT('Ctrl Pts',(97.2080142489618,1.2588872587856,-6.07831136645964));
#35914=CARTESIAN_POINT('Ctrl Pts',(97.1712278981197,1.27932444092076,-6.0760091925365));
#35915=CARTESIAN_POINT('Ctrl Pts',(97.1231291650486,1.30604637842591,-6.07299906387526));
#35916=CARTESIAN_POINT('Ctrl Pts',(97.073420279959,1.33010813960371,-6.06998893521401));
#35917=CARTESIAN_POINT('Ctrl Pts',(97.0224266430538,1.35131391156271,-6.06697880655277));
#35918=CARTESIAN_POINT('Ctrl Pts',(96.9715236362098,1.3724819948898,-6.06397402773831));
#35919=CARTESIAN_POINT('Ctrl Pts',(96.9193408925939,1.3908039610083,-6.06096924892386));
#35920=CARTESIAN_POINT('Ctrl Pts',(96.8662281009337,1.40612997235885,-6.05796447010941));
#35921=CARTESIAN_POINT('Ctrl Pts',(96.8131678555815,1.42144082116029,-6.05496266402578));
#35922=CARTESIAN_POINT('Ctrl Pts',(96.7591798898342,1.43376144103961,-6.05196085794215));
#35923=CARTESIAN_POINT('Ctrl Pts',(96.7046317954859,1.44299085736604,-6.04895905185852));
#35924=CARTESIAN_POINT('Ctrl Pts',(96.6501161222621,1.45221478811025,-6.04595902992391));
#35925=CARTESIAN_POINT('Ctrl Pts',(96.5950414999767,1.45835106898945,-6.04295900798931));
#35926=CARTESIAN_POINT('Ctrl Pts',(96.5397862701856,1.46134968988369,-6.0399589860547));
#35927=CARTESIAN_POINT('Ctrl Pts',(96.4845420586212,1.46434771283481,-6.03695956234259));
#35928=CARTESIAN_POINT('Ctrl Pts',(96.4291178381183,1.46420928974957,-6.03396013863049));
#35929=CARTESIAN_POINT('Ctrl Pts',(96.3738953139924,1.46093640440315,-6.03096071491839));
#35930=CARTESIAN_POINT('Ctrl Pts',(96.3186220207541,1.4576605101127,-6.02795853367062));
#35931=CARTESIAN_POINT('Ctrl Pts',(96.2635513226828,1.45124442764307,-6.02495635242285));
#35932=CARTESIAN_POINT('Ctrl Pts',(96.2090616495517,1.44174220496412,-6.02195417117508));
#35933=CARTESIAN_POINT('Ctrl Pts',(96.154547173931,1.43223565708433,-6.01895062340105));
#35934=CARTESIAN_POINT('Ctrl Pts',(96.1006147656269,1.4196402890516,-6.01594707562702));
#35935=CARTESIAN_POINT('Ctrl Pts',(96.0476312117472,1.40406101860775,-6.01294352785299));
#35936=CARTESIAN_POINT('Ctrl Pts',(95.9945476603262,1.38845234491283,-6.00993431138801));
#35937=CARTESIAN_POINT('Ctrl Pts',(95.9424170393497,1.36984869672209,-6.00692509492304));
#35938=CARTESIAN_POINT('Ctrl Pts',(95.8915884492988,1.34840408376983,-6.00391587845806));
#35939=CARTESIAN_POINT('Ctrl Pts',(95.8527024947912,1.33199807599234,-6.00161370453501));
#35940=CARTESIAN_POINT('Ctrl Pts',(95.814578250245,1.31393031284668,-5.99931153061197));
#35941=CARTESIAN_POINT('Ctrl Pts',(95.7773616424926,1.29428755007862,-5.99700935668892));
#35942=CARTESIAN_POINT('Ctrl Pts',(95.7287003417334,1.26860432840625,-5.99399922802769));
#35943=CARTESIAN_POINT('Ctrl Pts',(95.6813872294994,1.24011905118213,-5.99098909936645));
#35944=CARTESIAN_POINT('Ctrl Pts',(95.6357641017506,1.2089972584383,-5.98797897070522));
#35945=CARTESIAN_POINT('Ctrl Pts',(95.590222059155,1.17793077788934,-5.98497419189078));
#35946=CARTESIAN_POINT('Ctrl Pts',(95.5463644731706,1.14423737608251,-5.98196941307634));
#35947=CARTESIAN_POINT('Ctrl Pts',(95.5045079053338,1.10812805608397,-5.9789646342619));
#35948=CARTESIAN_POINT('Ctrl Pts',(95.4626927476364,1.07205446027521,-5.97596282817829));
#35949=CARTESIAN_POINT('Ctrl Pts',(95.4228750843551,1.03357002432336,-5.97296102209467));
#35950=CARTESIAN_POINT('Ctrl Pts',(95.3853403351739,0.992927444106999,-5.96995921601105));
#35951=CARTESIAN_POINT('Ctrl Pts',(95.3478278950906,0.952309020154461,-5.96695919407646));
#35952=CARTESIAN_POINT('Ctrl Pts',(95.312596037294,0.909535381554504,-5.96395917214186));
#35953=CARTESIAN_POINT('Ctrl Pts',(95.2798933709462,0.864896074209275,-5.96095915020727));
#35954=CARTESIAN_POINT('Ctrl Pts',(95.2471972257077,0.820265668211757,-5.95795972649518));
#35955=CARTESIAN_POINT('Ctrl Pts',(95.2170295822583,0.773770758081859,-5.9549603027831));
#35956=CARTESIAN_POINT('Ctrl Pts',(95.1895973414188,0.725732116221149,-5.95196087907101));
#35957=CARTESIAN_POINT('Ctrl Pts',(95.1621398806071,0.677649309787143,-5.94895869782326));
#35958=CARTESIAN_POINT('Ctrl Pts',(95.1374231091112,0.62802039576409,-5.9459565165755));
#35959=CARTESIAN_POINT('Ctrl Pts',(95.1156085328441,0.577191850870175,-5.94295433532775));
#35960=CARTESIAN_POINT('Ctrl Pts',(95.0937840270661,0.526340169950935,-5.93995078755373));
#35961=CARTESIAN_POINT('Ctrl Pts',(95.0748645305922,0.474288266868446,-5.93694723977972));
#35962=CARTESIAN_POINT('Ctrl Pts',(95.0589625830258,0.421400662338995,-5.9339436920057));
#35963=CARTESIAN_POINT('Ctrl Pts',(95.0430306232096,0.368413241356617,-5.93093447554074));
#35964=CARTESIAN_POINT('Ctrl Pts',(95.0301277125911,0.314587482960157,-5.92792525907578));
#35965=CARTESIAN_POINT('Ctrl Pts',(95.0203156110056,0.260299918512206,-5.92491604261082));
#35966=CARTESIAN_POINT('Ctrl Pts',(95.0128089511609,0.218767706829014,-5.92261386868767));
#35967=CARTESIAN_POINT('Ctrl Pts',(95.0071102514927,0.176965471128548,-5.92031169476452));
#35968=CARTESIAN_POINT('Ctrl Pts',(95.0032265855773,0.135062832059204,-5.91800952084137));
#35969=CARTESIAN_POINT('Ctrl Pts',(94.9981486312295,0.0802744715553483,
-5.91499939218014));
#35970=CARTESIAN_POINT('Ctrl Pts',(94.9961541187356,0.0250842230714438,
-5.9119892635189));
#35971=CARTESIAN_POINT('Ctrl Pts',(94.9972911598343,-0.0301311996537504,
-5.90897913485766));
#35972=CARTESIAN_POINT('Ctrl Pts',(94.9984261800905,-0.0852484890147449,
-5.90597435604322));
#35973=CARTESIAN_POINT('Ctrl Pts',(95.0026816980782,-0.140390340093219,
-5.90296957722878));
#35974=CARTESIAN_POINT('Ctrl Pts',(95.0100539610316,-0.195176332835741,
-5.89996479841433));
#35975=CARTESIAN_POINT('Ctrl Pts',(95.0174189303522,-0.249908123915031,
-5.89696299233071));
#35976=CARTESIAN_POINT('Ctrl Pts',(95.027894466283,-0.304284233252548,-5.8939611862471));
#35977=CARTESIAN_POINT('Ctrl Pts',(95.0414248814198,-0.357927542145374,
-5.89095938016348));
#35978=CARTESIAN_POINT('Ctrl Pts',(95.0549472546391,-0.411538967680527,
-5.88795935822888));
#35979=CARTESIAN_POINT('Ctrl Pts',(95.0715207793374,-0.464417944996317,
-5.88495933629428));
#35980=CARTESIAN_POINT('Ctrl Pts',(95.0910387920996,-0.516198050484219,
-5.88195931435968));
#35981=CARTESIAN_POINT('Ctrl Pts',(95.1105529128521,-0.567967830706091,
-5.87895989064759));
#35982=CARTESIAN_POINT('Ctrl Pts',(95.1330101694463,-0.61863868036885,-5.8759604669355));
#35983=CARTESIAN_POINT('Ctrl Pts',(95.1582549561594,-0.667862045685692,
-5.87296104322341));
#35984=CARTESIAN_POINT('Ctrl Pts',(95.1835229517974,-0.717130664757451,
-5.86995886197565));
#35985=CARTESIAN_POINT('Ctrl Pts',(95.2115833560347,-0.764948669884523,
-5.86695668072789));
#35986=CARTESIAN_POINT('Ctrl Pts',(95.2422342314922,-0.810991481999388,
-5.86395449948013));
#35987=CARTESIAN_POINT('Ctrl Pts',(95.2728990585477,-0.857055251780253,
-5.86095095170611));
#35988=CARTESIAN_POINT('Ctrl Pts',(95.3061563896463,-0.901341794764974,
-5.85794740393209));
#35989=CARTESIAN_POINT('Ctrl Pts',(95.3417624200753,-0.943557683318552,
-5.85494385615807));
#35990=CARTESIAN_POINT('Ctrl Pts',(95.3774356508944,-0.985853247257124,
-5.85193463969311));
#35991=CARTESIAN_POINT('Ctrl Pts',(95.4154660724507,-1.02606996524403,-5.84892542322814));
#35992=CARTESIAN_POINT('Ctrl Pts',(95.455572074926,-1.06395037649674,-5.84591620676318));
#35993=CARTESIAN_POINT('Ctrl Pts',(95.4862548104933,-1.09293044356687,-5.84361403284005));
#35994=CARTESIAN_POINT('Ctrl Pts',(95.5181515607852,-1.12054383539475,-5.84131185891693));
#35995=CARTESIAN_POINT('Ctrl Pts',(95.5511241289182,-1.14669194761334,-5.8390096849938));
#35996=CARTESIAN_POINT('Ctrl Pts',(95.5942362810344,-1.1808810161437,-5.83599955633256));
#35997=CARTESIAN_POINT('Ctrl Pts',(95.6393698056744,-1.21270720915158,-5.83298942767132));
#35998=CARTESIAN_POINT('Ctrl Pts',(95.6862354830088,-1.24192439685297,-5.82997929901008));
#35999=CARTESIAN_POINT('Ctrl Pts',(95.7330178668292,-1.2710896573793,-5.82697452019564));
#36000=CARTESIAN_POINT('Ctrl Pts',(95.7815258494597,-1.29765483749976,-5.82396974138119));
#36001=CARTESIAN_POINT('Ctrl Pts',(95.8314387683707,-1.32141522023292,-5.82096496256675));
#36002=CARTESIAN_POINT('Ctrl Pts',(95.8813023067177,-1.34515209600382,-5.81796315648312));
#36003=CARTESIAN_POINT('Ctrl Pts',(95.9325675534184,-1.36608944541675,-5.81496135039951));
#36004=CARTESIAN_POINT('Ctrl Pts',(95.9848882340308,-1.38406785199259,-5.81195954431588));
#36005=CARTESIAN_POINT('Ctrl Pts',(96.0371778174009,-1.40203557294931,-5.80895952238128));
#36006=CARTESIAN_POINT('Ctrl Pts',(96.0905210928655,-1.41704766559509,-5.80595950044668));
#36007=CARTESIAN_POINT('Ctrl Pts',(96.1445528903195,-1.42899325098958,-5.80295947851208));
#36008=CARTESIAN_POINT('Ctrl Pts',(96.1985739135064,-1.44093645436212,-5.79996005479999));
#36009=CARTESIAN_POINT('Ctrl Pts',(96.253282670645,-1.44981425091524,-5.7969606310879));
#36010=CARTESIAN_POINT('Ctrl Pts',(96.308302216202,-1.45556651620885,-5.79396120737581));
#36011=CARTESIAN_POINT('Ctrl Pts',(96.3633723442621,-1.46132406987725,-5.79095902612805));
#36012=CARTESIAN_POINT('Ctrl Pts',(96.4187533052,-1.46395029642693,-5.78795684488029));
#36013=CARTESIAN_POINT('Ctrl Pts',(96.4740629175201,-1.46343697511946,-5.78495466363253));
#36014=CARTESIAN_POINT('Ctrl Pts',(96.5293977055478,-1.46292342015952,-5.78195111585851));
#36015=CARTESIAN_POINT('Ctrl Pts',(96.5846605523354,-1.45926750354692,-5.77894756808449));
#36016=CARTESIAN_POINT('Ctrl Pts',(96.6394724904034,-1.45251309058218,-5.77594402031047));
#36017=CARTESIAN_POINT('Ctrl Pts',(96.6943878767801,-1.44574592979969,-5.7729348038455));
#36018=CARTESIAN_POINT('Ctrl Pts',(96.7488501334898,-1.43586868506862,-5.76992558738053));
#36019=CARTESIAN_POINT('Ctrl Pts',(96.802489759699,-1.42297653662981,-5.76691637091556));
#36020=CARTESIAN_POINT('Ctrl Pts',(96.8435262720741,-1.41311351471224,-5.76461419699245));
#36021=CARTESIAN_POINT('Ctrl Pts',(96.8840814900324,-1.40148697680278,-5.76231202306935));
#36022=CARTESIAN_POINT('Ctrl Pts',(96.923997319528,-1.38815878947168,-5.76000984914624));
#36023=CARTESIAN_POINT('Ctrl Pts',(96.976187895225,-1.3707319746316,-5.756999720485));
#36024=CARTESIAN_POINT('Ctrl Pts',(97.027503969092,-1.350321139992,-5.75398959182376));
#36025=CARTESIAN_POINT('Ctrl Pts',(97.0775813722312,-1.32703403059606,-5.75097946316252));
#36026=CARTESIAN_POINT('Ctrl Pts',(97.1275697737147,-1.30378830895512,-5.74797468434808));
#36027=CARTESIAN_POINT('Ctrl Pts',(97.1763233982983,-1.27767667814301,-5.74496990553364));
#36028=CARTESIAN_POINT('Ctrl Pts',(97.2234955812531,-1.2488558451031,-5.74196512671919));
#36029=CARTESIAN_POINT('Ctrl Pts',(97.2706210951481,-1.22006352550264,-5.73896332063557));
#36030=CARTESIAN_POINT('Ctrl Pts',(97.3161678183167,-1.18856758721968,-5.73596151455196));
#36031=CARTESIAN_POINT('Ctrl Pts',(97.3598130321715,-1.15457093988038,-5.73295970846834));
#36032=CARTESIAN_POINT('Ctrl Pts',(97.4034323051216,-1.12059449873807,-5.72995968653374));
#36033=CARTESIAN_POINT('Ctrl Pts',(97.4451518930407,-1.08412061840226,-5.72695966459914));
#36034=CARTESIAN_POINT('Ctrl Pts',(97.4846794043202,-1.04539455484597,-5.72395964266454));
#36035=CARTESIAN_POINT('Ctrl Pts',(97.5241990335751,-1.00667621350084,-5.72096021895246));
#36036=CARTESIAN_POINT('Ctrl Pts',(97.561527077251,-0.965706950209761,-5.71796079524037));
#36037=CARTESIAN_POINT('Ctrl Pts',(97.5964072179516,-0.922769615243472,
-5.71496137152828));
#36038=CARTESIAN_POINT('Ctrl Pts',(97.6313194258896,-0.879792805616685,
-5.71195919028052));
#36039=CARTESIAN_POINT('Ctrl Pts',(97.6637789009566,-0.834844720244027,
-5.70895700903276));
#36040=CARTESIAN_POINT('Ctrl Pts',(97.6935699355941,-0.788240954634579,
-5.705954827785));
#36041=CARTESIAN_POINT('Ctrl Pts',(97.7233745304493,-0.741615976025545,
-5.70295128001098));
#36042=CARTESIAN_POINT('Ctrl Pts',(97.7505080044389,-0.69333427607002,-5.69994773223696));
#36043=CARTESIAN_POINT('Ctrl Pts',(97.7748000295898,-0.643737218059023,
-5.69694418446294));
#36044=CARTESIAN_POINT('Ctrl Pts',(97.7991379018499,-0.594046553947895,
-5.69393496799798));
#36045=CARTESIAN_POINT('Ctrl Pts',(97.8206234068304,-0.543036060467411,
-5.69092575153301));
#36046=CARTESIAN_POINT('Ctrl Pts',(97.8391343667395,-0.491067210619997,
-5.68791653506804));
#36047=CARTESIAN_POINT('Ctrl Pts',(97.853296009709,-0.451308910635165,-5.68561436114492));
#36048=CARTESIAN_POINT('Ctrl Pts',(97.8657176831939,-0.41099012946238,-5.6833121872218));
#36049=CARTESIAN_POINT('Ctrl Pts',(97.8763648201458,-0.370277078770926,
-5.68101001329868));
#36050=CARTESIAN_POINT('Ctrl Pts',(97.8941165227751,-0.302397237243981,
-5.67717165684012));
#36051=CARTESIAN_POINT('Ctrl Pts',(97.9069947864868,-0.233194083262063,
-5.67333330038157));
#36052=CARTESIAN_POINT('Ctrl Pts',(97.9148439409853,-0.163280553715951,
-5.66949494392301));
#36053=CARTESIAN_POINT('Ctrl Pts',(97.9208695864408,-0.10960927718987,-5.66654831124361));
#36054=CARTESIAN_POINT('Ctrl Pts',(97.923932276957,-0.055519665670863,-5.66360167856421));
#36055=CARTESIAN_POINT('Ctrl Pts',(97.9239803738018,-0.00129818862390677,
-5.66065504588482));
#36056=CARTESIAN_POINT('Ctrl Pts',(97.9239803690929,-0.00130348633276346,
-5.58934495420992));
#36057=CARTESIAN_POINT('Ctrl Pts',(97.9239165941649,-0.0729072828784039,
-5.59323742430783));
#36058=CARTESIAN_POINT('Ctrl Pts',(97.9185940325572,-0.144280430134909,
-5.59712989440575));
#36059=CARTESIAN_POINT('Ctrl Pts',(97.9081361102898,-0.214771473109514,
-5.60102236450367));
#36060=CARTESIAN_POINT('Ctrl Pts',(97.9010020279403,-0.262858358116362,
-5.60367769139475));
#36061=CARTESIAN_POINT('Ctrl Pts',(97.8914791845124,-0.310535349866628,
-5.60633301828584));
#36062=CARTESIAN_POINT('Ctrl Pts',(97.8796191635676,-0.357601705241597,
-5.60898834517693));
#36063=CARTESIAN_POINT('Ctrl Pts',(97.8661744200639,-0.410957013685808,
-5.61199847383816));
#36064=CARTESIAN_POINT('Ctrl Pts',(97.8496882465437,-0.463665150538308,
-5.6150086024994));
#36065=CARTESIAN_POINT('Ctrl Pts',(97.8302406418319,-0.51535486363633,-5.61801873116064));
#36066=CARTESIAN_POINT('Ctrl Pts',(97.8108276009935,-0.566952709549609,
-5.62102350997508));
#36067=CARTESIAN_POINT('Ctrl Pts',(97.7884637584791,-0.617535233425873,
-5.62402828878952));
#36068=CARTESIAN_POINT('Ctrl Pts',(97.7632792547537,-0.666744948258849,
-5.62703306760397));
#36069=CARTESIAN_POINT('Ctrl Pts',(97.7381196669224,-0.715905978231743,
-5.63003487368758));
#36070=CARTESIAN_POINT('Ctrl Pts',(97.7101451852964,-0.763696421810779,
-5.6330366797712));
#36071=CARTESIAN_POINT('Ctrl Pts',(97.6795338260064,-0.809779188710823,
-5.63603848585482));
#36072=CARTESIAN_POINT('Ctrl Pts',(97.6489406608386,-0.855834565925755,
-5.63903850778942));
#36073=CARTESIAN_POINT('Ctrl Pts',(97.6157140160327,-0.900183839176101,
-5.64203852972402));
#36074=CARTESIAN_POINT('Ctrl Pts',(97.5800764188042,-0.942516968168683,
-5.64503855165861));
#36075=CARTESIAN_POINT('Ctrl Pts',(97.544445927928,-0.984841655679431,-5.6480379753707));
#36076=CARTESIAN_POINT('Ctrl Pts',(97.5064057793194,-1.02515059356064,-5.65103739908279));
#36077=CARTESIAN_POINT('Ctrl Pts',(97.4662187057894,-1.06316688047029,-5.65403682279488));
#36078=CARTESIAN_POINT('Ctrl Pts',(97.4259946860659,-1.10121811784949,-5.65703900404263));
#36079=CARTESIAN_POINT('Ctrl Pts',(97.3836201825292,-1.13697212951688,-5.66004118529039));
#36080=CARTESIAN_POINT('Ctrl Pts',(97.3393936400685,-1.17019004118692,-5.66304336653815));
#36081=CARTESIAN_POINT('Ctrl Pts',(97.2951469666673,-1.20342307291299,-5.66604691431216));
#36082=CARTESIAN_POINT('Ctrl Pts',(97.2490470142228,-1.23411741027274,-5.66905046208618));
#36083=CARTESIAN_POINT('Ctrl Pts',(97.2014213414792,-1.26207748797282,-5.6720540098602));
#36084=CARTESIAN_POINT('Ctrl Pts',(97.1537057832934,-1.29009033561407,-5.67506322632516));
#36085=CARTESIAN_POINT('Ctrl Pts',(97.1044592235074,-1.31535837310478,-5.67807244279013));
#36086=CARTESIAN_POINT('Ctrl Pts',(97.0540329014977,-1.33773253319607,-5.6810816592551));
#36087=CARTESIAN_POINT('Ctrl Pts',(97.0154546985263,-1.35484968263142,-5.68338383317823));
#36088=CARTESIAN_POINT('Ctrl Pts',(96.976186501996,-1.37027404092252,-5.68568600710135));
#36089=CARTESIAN_POINT('Ctrl Pts',(96.9363914464605,-1.38395861533362,-5.68798818102448));
#36090=CARTESIAN_POINT('Ctrl Pts',(96.8843587846187,-1.40185141189338,-5.69099830968572));
#36091=CARTESIAN_POINT('Ctrl Pts',(96.8312063209807,-1.41684331694327,-5.69400843834697));
#36092=CARTESIAN_POINT('Ctrl Pts',(96.7772887002682,-1.42879848092794,-5.69701856700821));
#36093=CARTESIAN_POINT('Ctrl Pts',(96.7234669063601,-1.4407323972176,-5.70002334582266));
#36094=CARTESIAN_POINT('Ctrl Pts',(96.6688831655312,-1.44964016971358,-5.70302812463711));
#36095=CARTESIAN_POINT('Ctrl Pts',(96.6139079910096,-1.45543546506097,-5.70603290345156));
#36096=CARTESIAN_POINT('Ctrl Pts',(96.5589872053152,-1.46122502692374,-5.70903470953518));
#36097=CARTESIAN_POINT('Ctrl Pts',(96.503676275693,-1.46390815645125,-5.71203651561881));
#36098=CARTESIAN_POINT('Ctrl Pts',(96.4483547916438,-1.46344976213527,-5.71503832170243));
#36099=CARTESIAN_POINT('Ctrl Pts',(96.39306618839,-1.46299164026986,-5.71803834363704));
#36100=CARTESIAN_POINT('Ctrl Pts',(96.3377675701865,-1.45939569982411,-5.72103836557164));
#36101=CARTESIAN_POINT('Ctrl Pts',(96.2828401921201,-1.45267890853076,-5.72403838750624));
#36102=CARTESIAN_POINT('Ctrl Pts',(96.2279237669048,-1.4459634566062,-5.72703781121834));
#36103=CARTESIAN_POINT('Ctrl Pts',(96.1733789587284,-1.43612845379516,-5.73003723493044));
#36104=CARTESIAN_POINT('Ctrl Pts',(96.1195812360937,-1.42324264809166,-5.73303665864253));
#36105=CARTESIAN_POINT('Ctrl Pts',(96.065734054245,-1.4103449957562,-5.7360388398903));
#36106=CARTESIAN_POINT('Ctrl Pts',(96.0126358448415,-1.39439106024033,-5.73904102113806));
#36107=CARTESIAN_POINT('Ctrl Pts',(95.9606497406419,-1.37550027719898,-5.74204320238583));
#36108=CARTESIAN_POINT('Ctrl Pts',(95.9086399735217,-1.35660089549253,-5.74504675015985));
#36109=CARTESIAN_POINT('Ctrl Pts',(95.857743806863,-1.33476221007424,-5.74805029793388));
#36110=CARTESIAN_POINT('Ctrl Pts',(95.8083040086742,-1.31015170409946,-5.7510538457079));
#36111=CARTESIAN_POINT('Ctrl Pts',(95.7587709011868,-1.28549474993643,-5.75406306217287));
#36112=CARTESIAN_POINT('Ctrl Pts',(95.710700112807,-1.25805578723829,-5.75707227863784));
#36113=CARTESIAN_POINT('Ctrl Pts',(95.6644084071843,-1.2280475386761,-5.76008149510281));
#36114=CARTESIAN_POINT('Ctrl Pts',(95.6289933551998,-1.2050899986914,-5.76238366902589));
#36115=CARTESIAN_POINT('Ctrl Pts',(95.5946190515846,-1.18062963609541,-5.76468584294898));
#36116=CARTESIAN_POINT('Ctrl Pts',(95.5614139900993,-1.15477740382099,-5.76698801687206));
#36117=CARTESIAN_POINT('Ctrl Pts',(95.5179978492627,-1.12097520297683,-5.76999814553329));
#36118=CARTESIAN_POINT('Ctrl Pts',(95.4763994278315,-1.08465010225798,-5.77300827419453));
#36119=CARTESIAN_POINT('Ctrl Pts',(95.4369262799483,-1.04602489849969,-5.77601840285576));
#36120=CARTESIAN_POINT('Ctrl Pts',(95.3975232869712,-1.00746834261188,-5.7790231816702));
#36121=CARTESIAN_POINT('Ctrl Pts',(95.3602384460574,-0.966620162582308,
-5.78202796048465));
#36122=CARTESIAN_POINT('Ctrl Pts',(95.3253465106882,-0.923743501004823,
-5.78503273929909));
#36123=CARTESIAN_POINT('Ctrl Pts',(95.2904890951085,-0.880909258780438,
-5.7880345453827));
#36124=CARTESIAN_POINT('Ctrl Pts',(95.2580202271021,-0.836050918083252,
-5.79103635146632));
#36125=CARTESIAN_POINT('Ctrl Pts',(95.2281767029648,-0.789467221473735,
-5.79403815754994));
#36126=CARTESIAN_POINT('Ctrl Pts',(95.1983509165803,-0.742911212281183,
-5.79703817948454));
#36127=CARTESIAN_POINT('Ctrl Pts',(95.1711476655756,-0.694632323544357,
-5.80003820141913));
#36128=CARTESIAN_POINT('Ctrl Pts',(95.1467610553005,-0.644959137761565,
-5.80303822335373));
#36129=CARTESIAN_POINT('Ctrl Pts',(95.1223793078629,-0.59529585711228,-5.80603764706582));
#36130=CARTESIAN_POINT('Ctrl Pts',(95.1008133183402,-0.544239305376108,
-5.8090370707779));
#36131=CARTESIAN_POINT('Ctrl Pts',(95.0822106629532,-0.49214151116318,-5.81203649448999));
#36132=CARTESIAN_POINT('Ctrl Pts',(95.063590905119,-0.439995820574301,-5.81503867573775));
#36133=CARTESIAN_POINT('Ctrl Pts',(95.0479401023057,-0.386807473433288,
-5.8180408569855));
#36134=CARTESIAN_POINT('Ctrl Pts',(95.035356638252,-0.332945862371634,-5.82104303823326));
#36135=CARTESIAN_POINT('Ctrl Pts',(95.0227674464847,-0.279059734700263,
-5.82404658600728));
#36136=CARTESIAN_POINT('Ctrl Pts',(95.0132484676021,-0.224500253376058,
-5.82705013378129));
#36137=CARTESIAN_POINT('Ctrl Pts',(95.0068467170481,-0.169646007969578,
-5.83005368155531));
#36138=CARTESIAN_POINT('Ctrl Pts',(95.0004328842673,-0.114688234406487,
-5.83306289802027));
#36139=CARTESIAN_POINT('Ctrl Pts',(94.9971480639266,-0.0594351139089585,
-5.83607211448524));
#36140=CARTESIAN_POINT('Ctrl Pts',(94.9969871734786,-0.00426817539066629,
-5.8390813309502));
#36141=CARTESIAN_POINT('Ctrl Pts',(94.996864085692,0.0379367934957089,-5.84138350487334));
#36142=CARTESIAN_POINT('Ctrl Pts',(94.9985683131112,0.0800912439885254,
-5.84368567879648));
#36143=CARTESIAN_POINT('Ctrl Pts',(95.0020771381554,0.122026934858111,-5.84598785271961));
#36144=CARTESIAN_POINT('Ctrl Pts',(95.0066649821607,0.17685851111159,-5.84899798138085));
#36145=CARTESIAN_POINT('Ctrl Pts',(95.0143590174573,0.231546201030424,-5.85200811004209));
#36146=CARTESIAN_POINT('Ctrl Pts',(95.0251406920756,0.285710684426911,-5.85501823870333));
#36147=CARTESIAN_POINT('Ctrl Pts',(95.0359032046201,0.339778902274502,-5.85802301751777));
#36148=CARTESIAN_POINT('Ctrl Pts',(95.0497423640299,0.393325245198479,-5.86102779633221));
#36149=CARTESIAN_POINT('Ctrl Pts',(95.0665879055246,0.445975819683366,-5.86403257514666));
#36150=CARTESIAN_POINT('Ctrl Pts',(95.0834167811468,0.498574305147611,-5.86703438123028));
#36151=CARTESIAN_POINT('Ctrl Pts',(95.103245986732,0.55027827719602,-5.87003618731389));
#36152=CARTESIAN_POINT('Ctrl Pts',(95.1259547019121,0.600726180795795,-5.87303799339751));
#36153=CARTESIAN_POINT('Ctrl Pts',(95.1486499199739,0.651144100254258,-5.87603801533211));
#36154=CARTESIAN_POINT('Ctrl Pts',(95.1742210390583,0.700306950371653,-5.87903803726671));
#36155=CARTESIAN_POINT('Ctrl Pts',(95.2024989208809,0.747872626506352,-5.88203805920131));
#36156=CARTESIAN_POINT('Ctrl Pts',(95.2307711639229,0.795428817757702,-5.8850374829134));
#36157=CARTESIAN_POINT('Ctrl Pts',(95.2617488280683,0.841388013827451,-5.88803690662549));
#36158=CARTESIAN_POINT('Ctrl Pts',(95.2952177149497,0.885434268608315,-5.89103633033758));
#36159=CARTESIAN_POINT('Ctrl Pts',(95.328717371625,0.929521017540821,-5.89403851158534));
#36160=CARTESIAN_POINT('Ctrl Pts',(95.3647125065922,0.97169089018698,-5.8970406928331));
#36161=CARTESIAN_POINT('Ctrl Pts',(95.4029475000694,1.01165965283419,-5.90004287408086));
#36162=CARTESIAN_POINT('Ctrl Pts',(95.4411998972669,1.0516466083749,-5.90304642185487));
#36163=CARTESIAN_POINT('Ctrl Pts',(95.4816937985382,1.08943009578894,-5.90604996962889));
#36164=CARTESIAN_POINT('Ctrl Pts',(95.5241378139832,1.12476387852135,-5.90905351740291));
#36165=CARTESIAN_POINT('Ctrl Pts',(95.5666619353643,1.16016434782222,-5.91206273386788));
#36166=CARTESIAN_POINT('Ctrl Pts',(95.6111430978656,1.19310556139912,-5.91507195033284));
#36167=CARTESIAN_POINT('Ctrl Pts',(95.6572589836699,1.2233833101217,-5.91808116679781));
#36168=CARTESIAN_POINT('Ctrl Pts',(95.6925395262884,1.24654702877457,-5.92038334072093));
#36169=CARTESIAN_POINT('Ctrl Pts',(95.7287761962478,1.26815271871225,-5.92268551464406));
#36170=CARTESIAN_POINT('Ctrl Pts',(95.7658156741933,1.28812748017271,-5.92498768856718));
#36171=CARTESIAN_POINT('Ctrl Pts',(95.8142453749389,1.31424479536318,-5.92799781722842));
#36172=CARTESIAN_POINT('Ctrl Pts',(95.8642517777346,1.33768197282213,-5.93100794588966));
#36173=CARTESIAN_POINT('Ctrl Pts',(95.9155070549913,1.35824729126183,-5.9340180745509));
#36174=CARTESIAN_POINT('Ctrl Pts',(95.9666712371782,1.37877605933599,-5.93702285336535));
#36175=CARTESIAN_POINT('Ctrl Pts',(96.0190794028408,1.3964429024492,-5.94002763217979));
#36176=CARTESIAN_POINT('Ctrl Pts',(96.0723800136972,1.41110237529713,-5.94303241099424));
#36177=CARTESIAN_POINT('Ctrl Pts',(96.1256278924296,1.42574734502538,-5.94603421707786));
#36178=CARTESIAN_POINT('Ctrl Pts',(96.179765960616,1.43739069904301,-5.94903602316148));
#36179=CARTESIAN_POINT('Ctrl Pts',(96.2344253904109,1.44593607540932,-5.9520378292451));
#36180=CARTESIAN_POINT('Ctrl Pts',(96.2890523329081,1.45447637275838,-5.9550378511797));
#36181=CARTESIAN_POINT('Ctrl Pts',(96.3441995020836,1.45992226064108,-5.95803787311431));
#36182=CARTESIAN_POINT('Ctrl Pts',(96.3994879595983,1.46222847228929,-5.96103789504891));
#36183=CARTESIAN_POINT('Ctrl Pts',(96.4547653922605,1.46453422406495,-5.964037318761));
#36184=CARTESIAN_POINT('Ctrl Pts',(96.5101835299486,1.46370152095764,-5.96703674247309));
#36185=CARTESIAN_POINT('Ctrl Pts',(96.5653607221479,1.45973712815201,-5.97003616618518));
#36186=CARTESIAN_POINT('Ctrl Pts',(96.6205886417835,1.4557690906614,-5.97303834743294));
#36187=CARTESIAN_POINT('Ctrl Pts',(96.6755746454829,1.44866364926276,-5.9760405286807));
#36188=CARTESIAN_POINT('Ctrl Pts',(96.7299410102169,1.43847958821803,-5.97904270992846));
#36189=CARTESIAN_POINT('Ctrl Pts',(96.7843321213133,1.42829089161479,-5.98204625770248));
#36190=CARTESIAN_POINT('Ctrl Pts',(96.8381025175785,1.41502090868982,-5.98504980547651));
#36191=CARTESIAN_POINT('Ctrl Pts',(96.8908867549732,1.39877914363966,-5.98805335325053));
#36192=CARTESIAN_POINT('Ctrl Pts',(96.9437706137327,1.38250672499134,-5.99106256971549));
#36193=CARTESIAN_POINT('Ctrl Pts',(96.995664099223,1.36325150406159,-5.99407178618046));
#36194=CARTESIAN_POINT('Ctrl Pts',(97.0462200676117,1.34117185162974,-5.99708100264543));
#36195=CARTESIAN_POINT('Ctrl Pts',(97.0848974553757,1.32428001262397,-5.99938317656853));
#36196=CARTESIAN_POINT('Ctrl Pts',(97.1227923763854,1.30573609046428,-6.00168535049163));
#36197=CARTESIAN_POINT('Ctrl Pts',(97.1597600020344,1.28562866209272,-6.00398752441473));
#36198=CARTESIAN_POINT('Ctrl Pts',(97.2080957547711,1.25933788282639,-6.00699765307597));
#36199=CARTESIAN_POINT('Ctrl Pts',(97.255048323838,1.23026215642407,-6.0100077817372));
#36200=CARTESIAN_POINT('Ctrl Pts',(97.300278013789,1.19857129155549,-6.01301791039844));
#36201=CARTESIAN_POINT('Ctrl Pts',(97.3454273178366,1.16693675028329,-6.01602268921288));
#36202=CARTESIAN_POINT('Ctrl Pts',(97.3888593903943,1.13269659480702,-6.01902746802733));
#36203=CARTESIAN_POINT('Ctrl Pts',(97.4302603379682,1.09606577715551,-6.02203224684177));
#36204=CARTESIAN_POINT('Ctrl Pts',(97.4716203261636,1.0594711996293,-6.02503405292539));
#36205=CARTESIAN_POINT('Ctrl Pts',(97.5109527764421,1.02049099343675,-6.02803585900901));
#36206=CARTESIAN_POINT('Ctrl Pts',(97.5479754569982,0.979381410038397,-6.03103766509263));
#36207=CARTESIAN_POINT('Ctrl Pts',(97.5849761328086,0.938296260471195,-6.03403768702722));
#36208=CARTESIAN_POINT('Ctrl Pts',(97.6196694072262,0.895084633875136,-6.03703770896183));
#36209=CARTESIAN_POINT('Ctrl Pts',(97.6518103176934,0.850039167723047,-6.04003773089642));
#36210=CARTESIAN_POINT('Ctrl Pts',(97.6839448190689,0.80500268390918,-6.04303715460851));
#36211=CARTESIAN_POINT('Ctrl Pts',(97.7135276606886,0.758133516421528,-6.0460365783206));
#36212=CARTESIAN_POINT('Ctrl Pts',(97.7403559762338,0.709755004308052,-6.04903600203269));
#36213=CARTESIAN_POINT('Ctrl Pts',(97.7672089565293,0.661332015159835,-6.05203818328045));
#36214=CARTESIAN_POINT('Ctrl Pts',(97.7913020946972,0.61139737193975,-6.05504036452821));
#36215=CARTESIAN_POINT('Ctrl Pts',(97.8124782377585,0.560299547340323,-6.05804254577597));
#36216=CARTESIAN_POINT('Ctrl Pts',(97.8336640197302,0.509178464145439,-6.06104609354998));
#36217=CARTESIAN_POINT('Ctrl Pts',(97.8519299853338,0.456893643576719,-6.064049641324));
#36218=CARTESIAN_POINT('Ctrl Pts',(97.8671681700926,0.403810987515378,-6.06705318909802));
#36219=CARTESIAN_POINT('Ctrl Pts',(97.8824351143606,0.350628146874156,-6.07006240556298));
#36220=CARTESIAN_POINT('Ctrl Pts',(97.8946627453756,0.29664497904243,-6.07307162202795));
#36221=CARTESIAN_POINT('Ctrl Pts',(97.9037940249,0.242238759494788,-6.07608083849291));
#36222=CARTESIAN_POINT('Ctrl Pts',(97.9107798279656,0.200615771797842,-6.07838301241604));
#36223=CARTESIAN_POINT('Ctrl Pts',(97.9159544301644,0.158745429316313,-6.08068518633917));
#36224=CARTESIAN_POINT('Ctrl Pts',(97.9193128832873,0.116797427999095,-6.0829873602623));
#36225=CARTESIAN_POINT('Ctrl Pts',(97.9224044077598,0.0781834387904871,
-6.08510655822723));
#36226=CARTESIAN_POINT('Ctrl Pts',(97.9239630511916,0.0394451060571853,
-6.08722575619215));
#36227=CARTESIAN_POINT('Ctrl Pts',(97.9239807963238,0.000669755337866506,
-6.08934495415708));
#36228=CARTESIAN_POINT('Origin',(96.460480949577,-8.32667268468867E-16,
1.18130019239114E-14));
#36229=CARTESIAN_POINT('',(97.9239807654655,0.000734094157886227,-6.66065504581088));
#36230=CARTESIAN_POINT('',(97.9239807941682,0.000674448999180449,-6.58934495412678));
#36231=CARTESIAN_POINT('',(97.923980949577,-1.01189432752408E-15,1.19922289829666E-14));
#36232=CARTESIAN_POINT('Ctrl Pts',(97.9239807654655,0.00073409415789471,
-6.66065504581088));
#36233=CARTESIAN_POINT('Ctrl Pts',(97.9239500697605,0.0619294573548053,
-6.65734240038256));
#36234=CARTESIAN_POINT('Ctrl Pts',(97.920076940596,0.122993979023221,-6.65402975495424));
#36235=CARTESIAN_POINT('Ctrl Pts',(97.9124351738156,0.183469835983322,-6.65071710952592));
#36236=CARTESIAN_POINT('Ctrl Pts',(97.9047640051462,0.244178375316814,-6.6473917186114));
#36237=CARTESIAN_POINT('Ctrl Pts',(97.8932952909286,0.304293403245994,-6.64406632769688));
#36238=CARTESIAN_POINT('Ctrl Pts',(97.8781534976419,0.363368678428781,-6.64074093678236));
#36239=CARTESIAN_POINT('Ctrl Pts',(97.8629398160292,0.422724423867994,-6.63739975798975));
#36240=CARTESIAN_POINT('Ctrl Pts',(97.8440182538604,0.481030224079548,-6.63405857919715));
#36241=CARTESIAN_POINT('Ctrl Pts',(97.82156295279,0.537855027428008,-6.63071740040454));
#36242=CARTESIAN_POINT('Ctrl Pts',(97.8177335533478,0.547545606484042,-6.6301476147595));
#36243=CARTESIAN_POINT('Ctrl Pts',(97.8138014947121,0.557193171847244,-6.62957782911446));
#36244=CARTESIAN_POINT('Ctrl Pts',(97.8097677733136,0.566795657438289,-6.62900804346942));
#36245=CARTESIAN_POINT('Ctrl Pts',(97.788457969357,0.61752476468832,-6.62599791480819));
#36246=CARTESIAN_POINT('Ctrl Pts',(97.7642385218159,0.667157011953622,-6.62298778614695));
#36247=CARTESIAN_POINT('Ctrl Pts',(97.7372443093545,0.715337384127,-6.61997765748572));
#36248=CARTESIAN_POINT('Ctrl Pts',(97.7102980732148,0.763432126203284,-6.61697287867128));
#36249=CARTESIAN_POINT('Ctrl Pts',(97.6805871148748,0.810079656987014,-6.61396809985684));
#36250=CARTESIAN_POINT('Ctrl Pts',(97.6482938167803,0.854946105030219,-6.61096332104239));
#36251=CARTESIAN_POINT('Ctrl Pts',(97.6160324675541,0.899768165156256,-6.60796151495878));
#36252=CARTESIAN_POINT('Ctrl Pts',(97.5811941465018,0.942812206625132,-6.60495970887516));
#36253=CARTESIAN_POINT('Ctrl Pts',(97.5440055030784,0.983771717401802,-6.60195790279155));
#36254=CARTESIAN_POINT('Ctrl Pts',(97.5068389630419,1.0247068835443,-6.59895788085695));
#36255=CARTESIAN_POINT('Ctrl Pts',(97.467325223743,1.06355958447362,-6.59595785892235));
#36256=CARTESIAN_POINT('Ctrl Pts',(97.4257308754801,1.10005673969302,-6.59295783698776));
#36257=CARTESIAN_POINT('Ctrl Pts',(97.3841448213818,1.13654661715901,-6.58995841327567));
#36258=CARTESIAN_POINT('Ctrl Pts',(97.3404793790073,1.17068153361597,-6.58695898956358));
#36259=CARTESIAN_POINT('Ctrl Pts',(97.2950359079084,1.20222721293624,-6.5839595658515));
#36260=CARTESIAN_POINT('Ctrl Pts',(97.2495506581198,1.23380189393962,-6.58095738460374));
#36261=CARTESIAN_POINT('Ctrl Pts',(97.2022845485745,1.26278228021625,-6.57795520335599));
#36262=CARTESIAN_POINT('Ctrl Pts',(97.1535685310457,1.28897705736522,-6.57495302210823));
#36263=CARTESIAN_POINT('Ctrl Pts',(97.1048303390671,1.31518375779526,-6.57194947433421));
#36264=CARTESIAN_POINT('Ctrl Pts',(97.0546414029244,1.33860209783461,-6.5689459265602));
#36265=CARTESIAN_POINT('Ctrl Pts',(97.0033549495939,1.35908795525001,-6.56594237878618));
#36266=CARTESIAN_POINT('Ctrl Pts',(96.9519717017138,1.37961247627365,-6.56293316232122));
#36267=CARTESIAN_POINT('Ctrl Pts',(96.8994873007415,1.39719329036052,-6.55992394585626));
#36268=CARTESIAN_POINT('Ctrl Pts',(96.8462713981076,1.41173580383248,-6.55691472939129));
#36269=CARTESIAN_POINT('Ctrl Pts',(96.8055590516326,1.42286142263786,-6.55461255546815));
#36270=CARTESIAN_POINT('Ctrl Pts',(96.7644189230227,1.43220978642083,-6.55231038154501));
#36271=CARTESIAN_POINT('Ctrl Pts',(96.7230193560468,1.43975895035534,-6.55000820762187));
#36272=CARTESIAN_POINT('Ctrl Pts',(96.6688887702276,1.44962960109082,-6.54699807896063));
#36273=CARTESIAN_POINT('Ctrl Pts',(96.614087016333,1.45646402702743,-6.54398795029939));
#36274=CARTESIAN_POINT('Ctrl Pts',(96.5589851262422,1.46018121381543,-6.54097782163815));
#36275=CARTESIAN_POINT('Ctrl Pts',(96.5039811677362,1.46389179411512,-6.5379730428237));
#36276=CARTESIAN_POINT('Ctrl Pts',(96.4486786542793,1.46449609459621,-6.53496826400925));
#36277=CARTESIAN_POINT('Ctrl Pts',(96.3934568652473,1.46196443941696,-6.5319634851948));
#36278=CARTESIAN_POINT('Ctrl Pts',(96.3382897090267,1.45943528889109,-6.52896167911118));
#36279=CARTESIAN_POINT('Ctrl Pts',(96.2832036439936,1.45377635269247,-6.52595987302756));
#36280=CARTESIAN_POINT('Ctrl Pts',(96.2285792225989,1.44500997886678,-6.52295806694393));
#36281=CARTESIAN_POINT('Ctrl Pts',(96.1739872676945,1.43624881541007,-6.51995804500933));
#36282=CARTESIAN_POINT('Ctrl Pts',(96.1198569329886,1.42438395858338,-6.51695802307473));
#36283=CARTESIAN_POINT('Ctrl Pts',(96.0665625946391,1.40948947482519,-6.51395800114012));
#36284=CARTESIAN_POINT('Ctrl Pts',(96.0132788835028,1.39459796111709,-6.51095857742803));
#36285=CARTESIAN_POINT('Ctrl Pts',(95.9608313459994,1.37667816231465,-6.50795915371594));
#36286=CARTESIAN_POINT('Ctrl Pts',(95.9095808563667,1.35585446759632,-6.50495973000384));
#36287=CARTESIAN_POINT('Ctrl Pts',(95.8582832493319,1.33501162850679,-6.50195754875608));
#36288=CARTESIAN_POINT('Ctrl Pts',(95.8081853791708,1.31125975898834,-6.49895536750831));
#36289=CARTESIAN_POINT('Ctrl Pts',(95.7596283075926,1.28477150662033,-6.49595318626055));
#36290=CARTESIAN_POINT('Ctrl Pts',(95.7110491339133,1.25827119738783,-6.49294963848653));
#36291=CARTESIAN_POINT('Ctrl Pts',(95.664012606188,1.22903230170261,-6.4899460907125));
#36292=CARTESIAN_POINT('Ctrl Pts',(95.6188324324989,1.19727190884122,-6.48694254293848));
#36293=CARTESIAN_POINT('Ctrl Pts',(95.5735669888356,1.16545157358335,-6.48393332647351));
#36294=CARTESIAN_POINT('Ctrl Pts',(95.5301653132286,1.13110056306101,-6.48092411000854));
#36295=CARTESIAN_POINT('Ctrl Pts',(95.48890860652,1.0944767846815,-6.47791489354357));
#36296=CARTESIAN_POINT('Ctrl Pts',(95.4573455350552,1.06645809326073,-6.47561271962048));
#36297=CARTESIAN_POINT('Ctrl Pts',(95.4270372240236,1.03711003762185,-6.47331054569739));
#36298=CARTESIAN_POINT('Ctrl Pts',(95.3980940351819,1.00656161963493,-6.4710083717743));
#36299=CARTESIAN_POINT('Ctrl Pts',(95.360250359947,0.966619082011855,-6.46799824311307));
#36300=CARTESIAN_POINT('Ctrl Pts',(95.3245828810931,0.924455441751405,-6.46498811445183));
#36301=CARTESIAN_POINT('Ctrl Pts',(95.2913621806809,0.88033718211545,-6.4619779857906));
#36302=CARTESIAN_POINT('Ctrl Pts',(95.258200522814,0.836297333058049,-6.45897320697615));
#36303=CARTESIAN_POINT('Ctrl Pts',(95.2274773286411,0.790310177095552,-6.45596842816171));
#36304=CARTESIAN_POINT('Ctrl Pts',(95.1994246892403,0.742677156149086,-6.45296364934727));
#36305=CARTESIAN_POINT('Ctrl Pts',(95.1713998032787,0.695091260185318,-6.44996184326365));
#36306=CARTESIAN_POINT('Ctrl Pts',(95.1460405049562,0.645863177668212,-6.44696003718003));
#36307=CARTESIAN_POINT('Ctrl Pts',(95.1235360095484,0.595323842401656,-6.44395823109641));
#36308=CARTESIAN_POINT('Ctrl Pts',(95.1010448898792,0.544814545619602,-6.44095820916181));
#36309=CARTESIAN_POINT('Ctrl Pts',(95.0814054244011,0.49299602230385,-6.43795818722721));
#36310=CARTESIAN_POINT('Ctrl Pts',(95.0647601381418,0.440222292173557,-6.43495816529262));
#36311=CARTESIAN_POINT('Ctrl Pts',(95.0481181710531,0.38745908544404,-6.43195874158052));
#36312=CARTESIAN_POINT('Ctrl Pts',(95.0344693562214,0.333741553548245,-6.42895931786843));
#36313=CARTESIAN_POINT('Ctrl Pts',(95.0239066946291,0.2794399041314,-6.42595989415634));
#36314=CARTESIAN_POINT('Ctrl Pts',(95.0133343221994,0.225088332212951,-6.42295771290859));
#36315=CARTESIAN_POINT('Ctrl Pts',(95.0058538725625,0.170152089407996,-6.41995553166083));
#36316=CARTESIAN_POINT('Ctrl Pts',(95.0015071035033,0.115011158036669,-6.41695335041307));
#36317=CARTESIAN_POINT('Ctrl Pts',(94.9971583558914,0.0598451277374262,
-6.41394980263905));
#36318=CARTESIAN_POINT('Ctrl Pts',(94.9959461438304,0.00447475205460546,
-6.41094625486504));
#36319=CARTESIAN_POINT('Ctrl Pts',(94.9978600580734,-0.050718613321517,
-6.40794270709102));
#36320=CARTESIAN_POINT('Ctrl Pts',(94.9997775845075,-0.106016146886121,
-6.40493349062605));
#36321=CARTESIAN_POINT('Ctrl Pts',(95.0048329751331,-0.161135475574066,
-6.40192427416109));
#36322=CARTESIAN_POINT('Ctrl Pts',(95.0129638725916,-0.21570016651737,-6.39891505769612));
#36323=CARTESIAN_POINT('Ctrl Pts',(95.0191843423779,-0.257444391326635,
-6.39661288377299));
#36324=CARTESIAN_POINT('Ctrl Pts',(95.027203786649,-0.298864079893977,-6.39431070984987));
#36325=CARTESIAN_POINT('Ctrl Pts',(95.0369744640976,-0.339796315162534,
-6.39200853592674));
#36326=CARTESIAN_POINT('Ctrl Pts',(95.0497497787392,-0.393315857414546,
-6.3889984072655));
#36327=CARTESIAN_POINT('Ctrl Pts',(95.0655743917758,-0.446226378391436,
-6.38598827860426));
#36328=CARTESIAN_POINT('Ctrl Pts',(95.0843729612793,-0.498155652927122,
-6.38297814994303));
#36329=CARTESIAN_POINT('Ctrl Pts',(95.1031381204279,-0.549992634509871,
-6.37997337112859));
#36330=CARTESIAN_POINT('Ctrl Pts',(95.1248665685073,-0.600851337971165,
-6.37696859231414));
#36331=CARTESIAN_POINT('Ctrl Pts',(95.1494326534498,-0.650372674104561,
-6.3739638134997));
#36332=CARTESIAN_POINT('Ctrl Pts',(95.1739744343211,-0.699845017080219,
-6.37096200741608));
#36333=CARTESIAN_POINT('Ctrl Pts',(95.2013480572489,-0.747982142955453,
-6.36796020133246));
#36334=CARTESIAN_POINT('Ctrl Pts',(95.2313797427498,-0.794444757913278,
-6.36495839524884));
#36335=CARTESIAN_POINT('Ctrl Pts',(95.2613935786625,-0.84087975742006,-6.36195837331425));
#36336=CARTESIAN_POINT('Ctrl Pts',(95.2940620596879,-0.885641776033881,
-6.35895835137965));
#36337=CARTESIAN_POINT('Ctrl Pts',(95.329166559899,-0.928418010223583,-6.35595832944505));
#36338=CARTESIAN_POINT('Ctrl Pts',(95.3642640600605,-0.971185714573611,
-6.35295890573296));
#36339=CARTESIAN_POINT('Ctrl Pts',(95.4017962798758,-1.0119680128784,-6.34995948202087));
#36340=CARTESIAN_POINT('Ctrl Pts',(95.4415039758503,-1.05048473430826,-6.34696005830879));
#36341=CARTESIAN_POINT('Ctrl Pts',(95.4812481772999,-1.08903686628473,-6.34395787706103));
#36342=CARTESIAN_POINT('Ctrl Pts',(95.5231714708285,-1.12531889158668,-6.34095569581327));
#36343=CARTESIAN_POINT('Ctrl Pts',(95.5669784273062,-1.15908821609735,-6.33795351456551));
#36344=CARTESIAN_POINT('Ctrl Pts',(95.6108053237381,-1.19287291165491,-6.3349499667915));
#36345=CARTESIAN_POINT('Ctrl Pts',(95.6565171556405,-1.22414232779057,-6.33194641901748));
#36346=CARTESIAN_POINT('Ctrl Pts',(95.7037888397877,-1.25269681127665,-6.32894287124346));
#36347=CARTESIAN_POINT('Ctrl Pts',(95.7511497412833,-1.28130518654478,-6.3259336547785));
#36348=CARTESIAN_POINT('Ctrl Pts',(95.8000759080748,-1.30718814565836,-6.32292443831353));
#36349=CARTESIAN_POINT('Ctrl Pts',(95.8502179956886,-1.33019223314202,-6.31991522184857));
#36350=CARTESIAN_POINT('Ctrl Pts',(95.8885787476981,-1.347791302849,-6.31761304792544));
#36351=CARTESIAN_POINT('Ctrl Pts',(95.9276506444673,-1.36370635768065,-6.31531087400231));
#36352=CARTESIAN_POINT('Ctrl Pts',(95.9672711529135,-1.37788836502641,-6.31300870007918));
#36353=CARTESIAN_POINT('Ctrl Pts',(96.019075591687,-1.39643156298224,-6.30999857141794));
#36354=CARTESIAN_POINT('Ctrl Pts',(96.0720360834246,-1.41208812463281,-6.3069884427567));
#36355=CARTESIAN_POINT('Ctrl Pts',(96.1257997129984,-1.42471776850091,-6.30397831409546));
#36356=CARTESIAN_POINT('Ctrl Pts',(96.1794677894535,-1.43732496593321,-6.30097353528102));
#36357=CARTESIAN_POINT('Ctrl Pts',(96.2339356610926,-1.44691580180996,-6.29796875646657));
#36358=CARTESIAN_POINT('Ctrl Pts',(96.2888339252446,-1.45339930818679,-6.29496397765213));
#36359=CARTESIAN_POINT('Ctrl Pts',(96.3436778766594,-1.4598764002082,-6.29196217156851));
#36360=CARTESIAN_POINT('Ctrl Pts',(96.3989508552009,-1.46325219091202,-6.28896036548488));
#36361=CARTESIAN_POINT('Ctrl Pts',(96.4542737407385,-1.4634868364828,-6.28595855940126));
#36362=CARTESIAN_POINT('Ctrl Pts',(96.5095637446478,-1.46372134258999,-6.28295853746666));
#36363=CARTESIAN_POINT('Ctrl Pts',(96.5649030697027,-1.4608184017786,-6.27995851553206));
#36364=CARTESIAN_POINT('Ctrl Pts',(96.6199102781794,-1.45479020452483,-6.27695849359746));
#36365=CARTESIAN_POINT('Ctrl Pts',(96.6749065178862,-1.44876320933003,-6.27395906988537));
#36366=CARTESIAN_POINT('Ctrl Pts',(96.729570247858,-1.43961225283058,-6.27095964617328));
#36367=CARTESIAN_POINT('Ctrl Pts',(96.7835251678571,-1.42740137418871,-6.26796022246119));
#36368=CARTESIAN_POINT('Ctrl Pts',(96.8375296915902,-1.41517926941256,-6.26495804121343));
#36369=CARTESIAN_POINT('Ctrl Pts',(96.8908235872459,-1.39989173899911,-6.26195585996567));
#36370=CARTESIAN_POINT('Ctrl Pts',(96.9430422544056,-1.38165366032234,-6.2589536787179));
#36371=CARTESIAN_POINT('Ctrl Pts',(96.9952846903434,-1.36340728007702,-6.25595013094388));
#36372=CARTESIAN_POINT('Ctrl Pts',(97.0464504334134,-1.3422078768439,-6.25294658316986));
#36373=CARTESIAN_POINT('Ctrl Pts',(97.0961946444657,-1.31821862683356,-6.24994303539584));
#36374=CARTESIAN_POINT('Ctrl Pts',(97.1460327393448,-1.29418410115106,-6.24693381893088));
#36375=CARTESIAN_POINT('Ctrl Pts',(97.1944434796585,-1.26734946696937,-6.24392460246591));
#36376=CARTESIAN_POINT('Ctrl Pts',(97.2411074618674,-1.23792346221783,-6.24091538600094));
#36377=CARTESIAN_POINT('Ctrl Pts',(97.2768073206978,-1.2154113626102,-6.23861321207783));
#36378=CARTESIAN_POINT('Ctrl Pts',(97.3114853384534,-1.19138352101034,-6.23631103815472));
#36379=CARTESIAN_POINT('Ctrl Pts',(97.3450116415648,-1.16594927202327,-6.23400886423161));
#36380=CARTESIAN_POINT('Ctrl Pts',(97.3895217877492,-1.13218228803036,-6.23095245513339));
#36381=CARTESIAN_POINT('Ctrl Pts',(97.4322008967868,-1.09578275819487,-6.22789604603517));
#36382=CARTESIAN_POINT('Ctrl Pts',(97.472718199951,-1.05698060481507,-6.22483963693695));
#36383=CARTESIAN_POINT('Ctrl Pts',(97.5121538043451,-1.01921436049912,-6.22186482542061));
#36384=CARTESIAN_POINT('Ctrl Pts',(97.5495411637813,-0.979172570374641,
-6.21889001390427));
#36385=CARTESIAN_POINT('Ctrl Pts',(97.5846061097723,-0.937109851733445,
-6.21591520238793));
#36386=CARTESIAN_POINT('Ctrl Pts',(97.6196372587544,-0.895087674836593,
-6.21294325811489));
#36387=CARTESIAN_POINT('Ctrl Pts',(97.6523500816875,-0.851048838165583,
-6.20997131384185));
#36388=CARTESIAN_POINT('Ctrl Pts',(97.682507860416,-0.805284098430678,-6.20699936956881));
#36389=CARTESIAN_POINT('Ctrl Pts',(97.7126490811507,-0.759544485621851,
-6.2040290570285));
#36390=CARTESIAN_POINT('Ctrl Pts',(97.7402377405751,-0.712081297143327,
-6.2010587444882));
#36391=CARTESIAN_POINT('Ctrl Pts',(97.7650794754836,-0.663215603105351,
-6.19808843194789));
#36392=CARTESIAN_POINT('Ctrl Pts',(97.7911684880299,-0.611896413461828,
-6.19496898310842));
#36393=CARTESIAN_POINT('Ctrl Pts',(97.8142270779522,-0.559030689985845,
-6.19184953426896));
#36394=CARTESIAN_POINT('Ctrl Pts',(97.8340851191835,-0.505018648407742,
-6.18873008542949));
#36395=CARTESIAN_POINT('Ctrl Pts',(97.8530084023842,-0.453549062504344,
-6.18575747533509));
#36396=CARTESIAN_POINT('Ctrl Pts',(97.8690256010605,-0.401039230351928,
-6.18278486524069));
#36397=CARTESIAN_POINT('Ctrl Pts',(97.8820403515782,-0.347852147588492,
-6.17981225514629));
#36398=CARTESIAN_POINT('Ctrl Pts',(97.8950625388923,-0.294634673039838,
-6.17683794646414));
#36399=CARTESIAN_POINT('Ctrl Pts',(97.9050787684695,-0.240739708873497,
-6.17386363778198));
#36400=CARTESIAN_POINT('Ctrl Pts',(97.9120440368436,-0.18653914786186,-6.17088932909983));
#36401=CARTESIAN_POINT('Ctrl Pts',(97.919020403135,-0.132252227889061,-6.1679102813854));
#36402=CARTESIAN_POINT('Ctrl Pts',(97.9229360828988,-0.0776592775315085,
-6.16493123367097));
#36403=CARTESIAN_POINT('Ctrl Pts',(97.9237980922905,-0.0231341704168234,
-6.16195218595654));
#36404=CARTESIAN_POINT('Ctrl Pts',(97.9239232046351,-0.0152203772959857,
-6.16151980592912));
#36405=CARTESIAN_POINT('Ctrl Pts',(97.9239840784704,-0.00730800547042104,
-6.16108742590171));
#36406=CARTESIAN_POINT('Ctrl Pts',(97.9239808258401,0.000601812115853528,
-6.16065504587429));
#36407=CARTESIAN_POINT('Ctrl Pts',(97.923980796324,0.000669754741469797,
-6.08934495418968));
#36408=CARTESIAN_POINT('Ctrl Pts',(97.9240061409169,-0.0547114251152243,
-6.09237171426968));
#36409=CARTESIAN_POINT('Ctrl Pts',(97.9208833585887,-0.110218119586203,
-6.09539847434969));
#36410=CARTESIAN_POINT('Ctrl Pts',(97.914597801083,-0.165458249012885,-6.0984252344297));
#36411=CARTESIAN_POINT('Ctrl Pts',(97.9084269093797,-0.219690647022858,
-6.10139677810715));
#36412=CARTESIAN_POINT('Ctrl Pts',(97.8992077170686,-0.273665561285684,
-6.10436832178461));
#36413=CARTESIAN_POINT('Ctrl Pts',(97.8869787414137,-0.327011161713091,
-6.10733986546207));
#36414=CARTESIAN_POINT('Ctrl Pts',(97.8747603913136,-0.380310411030574,
-6.11030882721437));
#36415=CARTESIAN_POINT('Ctrl Pts',(97.8595375552866,-0.432980903985484,
-6.11327778896667));
#36416=CARTESIAN_POINT('Ctrl Pts',(97.8414001466125,-0.484659077351177,
-6.11624675071897));
#36417=CARTESIAN_POINT('Ctrl Pts',(97.8232709470958,-0.536313860701884,
-6.11921436869197));
#36418=CARTESIAN_POINT('Ctrl Pts',(97.8022299677344,-0.586976704809362,
-6.12218198666496));
#36419=CARTESIAN_POINT('Ctrl Pts',(97.7784167915995,-0.636299745648629,
-6.12514960463796));
#36420=CARTESIAN_POINT('Ctrl Pts',(97.7537836778224,-0.687321082321191,
-6.12821940392729));
#36421=CARTESIAN_POINT('Ctrl Pts',(97.7261841503896,-0.736908073167478,
-6.13128920321661));
#36422=CARTESIAN_POINT('Ctrl Pts',(97.6958254384189,-0.784701372426493,
-6.13435900250594));
#36423=CARTESIAN_POINT('Ctrl Pts',(97.6664480597674,-0.830949772249572,
-6.13732957175122));
#36424=CARTESIAN_POINT('Ctrl Pts',(97.6344875686607,-0.875518274432512,
-6.1403001409965));
#36425=CARTESIAN_POINT('Ctrl Pts',(97.600175234414,-0.918111750883227,-6.14327071024178));
#36426=CARTESIAN_POINT('Ctrl Pts',(97.5641436264403,-0.962839440776835,
-6.14639012455313));
#36427=CARTESIAN_POINT('Ctrl Pts',(97.5255186926607,-1.00538843252877,-6.14950953886447));
#36428=CARTESIAN_POINT('Ctrl Pts',(97.4846125658143,-1.04546003396744,-6.15262895317582));
#36429=CARTESIAN_POINT('Ctrl Pts',(97.4437064389679,-1.0855316354061,-6.15574836748717));
#36430=CARTESIAN_POINT('Ctrl Pts',(97.4005196863332,-1.12312546069117,-6.15886778179852));
#36431=CARTESIAN_POINT('Ctrl Pts',(97.3554019806568,-1.15799334977843,-6.16198719610987));
#36432=CARTESIAN_POINT('Ctrl Pts',(97.3118649299702,-1.19163967624316,-6.1649973247711));
#36433=CARTESIAN_POINT('Ctrl Pts',(97.2663362647515,-1.22289799115632,-6.16800745343234));
#36434=CARTESIAN_POINT('Ctrl Pts',(97.2191082653678,-1.25152580705956,-6.17101758209358));
#36435=CARTESIAN_POINT('Ctrl Pts',(97.1719642034464,-1.2801027432675,-6.17402236090802));
#36436=CARTESIAN_POINT('Ctrl Pts',(97.123127248929,-1.30605818676541,-6.17702713972246));
#36437=CARTESIAN_POINT('Ctrl Pts',(97.0729206036436,-1.3291914535261,-6.18003191853691));
#36438=CARTESIAN_POINT('Ctrl Pts',(97.0227636295158,-1.3523018337519,-6.18303372462052));
#36439=CARTESIAN_POINT('Ctrl Pts',(96.971240126264,-1.37259534829198,-6.18603553070414));
#36440=CARTESIAN_POINT('Ctrl Pts',(96.9186983381466,-1.3899169309036,-6.18903733678776));
#36441=CARTESIAN_POINT('Ctrl Pts',(96.8661877786886,-1.40722821828501,-6.19203735872236));
#36442=CARTESIAN_POINT('Ctrl Pts',(96.8126606345249,-1.42157090982353,-6.19503738065695));
#36443=CARTESIAN_POINT('Ctrl Pts',(96.7584834360717,-1.43283870970985,-6.19803740259155));
#36444=CARTESIAN_POINT('Ctrl Pts',(96.7043170408793,-1.44410426272875,-6.20103682630364));
#36445=CARTESIAN_POINT('Ctrl Pts',(96.6495013655885,-1.45229603431262,-6.20403625001572));
#36446=CARTESIAN_POINT('Ctrl Pts',(96.5944140793254,-1.45735862667903,-6.20703567372781));
#36447=CARTESIAN_POINT('Ctrl Pts',(96.5392761482814,-1.46242587336587,-6.21003785497557));
#36448=CARTESIAN_POINT('Ctrl Pts',(96.4838666344131,-1.46435814487389,-6.21304003622333));
#36449=CARTESIAN_POINT('Ctrl Pts',(96.4285677922088,-1.46315200863984,-6.21604221747108));
#36450=CARTESIAN_POINT('Ctrl Pts',(96.3732437791991,-1.46194532339935,-6.2190457652451));
#36451=CARTESIAN_POINT('Ctrl Pts',(96.318031065677,-1.45759742426576,-6.22204931301913));
#36452=CARTESIAN_POINT('Ctrl Pts',(96.2633080398926,-1.45015692036642,-6.22505286079315));
#36453=CARTESIAN_POINT('Ctrl Pts',(96.2084817336066,-1.44270237376816,-6.22806207725811));
#36454=CARTESIAN_POINT('Ctrl Pts',(96.1541474809876,-1.4321436635384,-6.23107129372307));
#36455=CARTESIAN_POINT('Ctrl Pts',(96.1006735615679,-1.41858059113119,-6.23408051018804));
#36456=CARTESIAN_POINT('Ctrl Pts',(96.0597638216776,-1.40820428488106,-6.23638268411117));
#36457=CARTESIAN_POINT('Ctrl Pts',(96.0193574297397,-1.39607063011449,-6.2386848580343));
#36458=CARTESIAN_POINT('Ctrl Pts',(95.9796116924021,-1.38224346896778,-6.24098703195743));
#36459=CARTESIAN_POINT('Ctrl Pts',(95.9276435148809,-1.36416423800564,-6.24399716061866));
#36460=CARTESIAN_POINT('Ctrl Pts',(95.8765871509405,-1.34311217613533,-6.2470072892799));
#36461=CARTESIAN_POINT('Ctrl Pts',(95.8268053911985,-1.319199581835,-6.25001741794114));
#36462=CARTESIAN_POINT('Ctrl Pts',(95.7771121076705,-1.29532948695258,-6.25302219675559));
#36463=CARTESIAN_POINT('Ctrl Pts',(95.7286894049705,-1.26860917563456,-6.25602697557003));
#36464=CARTESIAN_POINT('Ctrl Pts',(95.6818819575821,-1.23919968514544,-6.25903175438448));
#36465=CARTESIAN_POINT('Ctrl Pts',(95.6351208184082,-1.20981929047479,-6.2620335604681));
#36466=CARTESIAN_POINT('Ctrl Pts',(95.5899722139074,-1.17775526653278,-6.26503536655172));
#36467=CARTESIAN_POINT('Ctrl Pts',(95.5467562955269,-1.14321454967169,-6.26803717263534));
#36468=CARTESIAN_POINT('Ctrl Pts',(95.5035660628957,-1.10869436237996,-6.27103719456994));
#36469=CARTESIAN_POINT('Ctrl Pts',(95.4623066512841,-1.07170072892293,-6.27403721650454));
#36470=CARTESIAN_POINT('Ctrl Pts',(95.4232673570736,-1.03248254877558,-6.27703723843914));
#36471=CARTESIAN_POINT('Ctrl Pts',(95.3842358475343,-0.993272188970415,
-6.28003666215123));
#36472=CARTESIAN_POINT('Ctrl Pts',(95.3474239485744,-0.951838537499062,
-6.28303608586332));
#36473=CARTESIAN_POINT('Ctrl Pts',(95.3130844142555,-0.908467633288195,
-6.28603550957541));
#36474=CARTESIAN_POINT('Ctrl Pts',(95.2787133097086,-0.865056855812712,
-6.28903769082317));
#36475=CARTESIAN_POINT('Ctrl Pts',(95.2468194394562,-0.819705682281835,
-6.29203987207093));
#36476=CARTESIAN_POINT('Ctrl Pts',(95.2176145407144,-0.772732385577921,
-6.29504205331869));
#36477=CARTESIAN_POINT('Ctrl Pts',(95.188396348551,-0.725737707672089,-6.29804560109271));
#36478=CARTESIAN_POINT('Ctrl Pts',(95.1618698211654,-0.677119899142627,
-6.30104914886673));
#36479=CARTESIAN_POINT('Ctrl Pts',(95.1382009969599,-0.627222430168735,
-6.30405269664075));
#36480=CARTESIAN_POINT('Ctrl Pts',(95.1144875018319,-0.577230788119558,
-6.30706191310572));
#36481=CARTESIAN_POINT('Ctrl Pts',(95.0936426834794,-0.525955151436571,
-6.31007112957069));
#36482=CARTESIAN_POINT('Ctrl Pts',(95.0757841819897,-0.473758495262404,
-6.31308034603565));
#36483=CARTESIAN_POINT('Ctrl Pts',(95.0621216964509,-0.433825914101524,
-6.31538251995877));
#36484=CARTESIAN_POINT('Ctrl Pts',(95.0502060649354,-0.39335469206665,-6.31768469388188));
#36485=CARTESIAN_POINT('Ctrl Pts',(95.0400697696705,-0.352511460801641,
-6.319986867805));
#36486=CARTESIAN_POINT('Ctrl Pts',(95.0268164039759,-0.299108292685668,
-6.32299699646623));
#36487=CARTESIAN_POINT('Ctrl Pts',(95.0165510755356,-0.244844449845191,
-6.32600712512747));
#36488=CARTESIAN_POINT('Ctrl Pts',(95.0093779587212,-0.190085138633783,
-6.3290172537887));
#36489=CARTESIAN_POINT('Ctrl Pts',(95.0022175905566,-0.135423150147869,
-6.33202203260315));
#36490=CARTESIAN_POINT('Ctrl Pts',(94.998138595741,-0.0802679602288693,
-6.33502681141759));
#36491=CARTESIAN_POINT('Ctrl Pts',(94.9971944300164,-0.0249962331622791,
-6.33803159023204));
#36492=CARTESIAN_POINT('Ctrl Pts',(94.9962511983874,0.0302208116874317,
-6.34103339631566));
#36493=CARTESIAN_POINT('Ctrl Pts',(94.9984366611126,0.0855536398493844,
-6.34403520239928));
#36494=CARTESIAN_POINT('Ctrl Pts',(95.0037524329219,0.140621046659748,-6.3470370084829));
#36495=CARTESIAN_POINT('Ctrl Pts',(95.0090650452568,0.195655723687715,-6.35003703041749));
#36496=CARTESIAN_POINT('Ctrl Pts',(95.0175042283483,0.250424767422655,-6.35303705235209));
#36497=CARTESIAN_POINT('Ctrl Pts',(95.0290195925948,0.30454988666314,-6.35603707428669));
#36498=CARTESIAN_POINT('Ctrl Pts',(95.0405326606079,0.358664213027637,-6.35903649799878));
#36499=CARTESIAN_POINT('Ctrl Pts',(95.055120581734,0.412134353634326,-6.36203592171087));
#36500=CARTESIAN_POINT('Ctrl Pts',(95.072681894501,0.464592329607494,-6.36503534542295));
#36501=CARTESIAN_POINT('Ctrl Pts',(95.0902593523515,0.517098533091617,-6.36803752667071));
#36502=CARTESIAN_POINT('Ctrl Pts',(95.110815495214,0.568590210971758,-6.37103970791847));
#36503=CARTESIAN_POINT('Ctrl Pts',(95.1341994533675,0.618716124577668,-6.37404188916623));
#36504=CARTESIAN_POINT('Ctrl Pts',(95.1575940553797,0.668864854386714,-6.37704543694025));
#36505=CARTESIAN_POINT('Ctrl Pts',(95.1838187880407,0.717646114704595,-6.38004898471427));
#36506=CARTESIAN_POINT('Ctrl Pts',(95.2126767085625,0.764733173143499,-6.38305253248829));
#36507=CARTESIAN_POINT('Ctrl Pts',(95.2415890935527,0.8119091004808,-6.38606174895325));
#36508=CARTESIAN_POINT('Ctrl Pts',(95.2731442923336,0.857384003441493,-6.38907096541822));
#36509=CARTESIAN_POINT('Ctrl Pts',(95.3071025815364,0.900861027093556,-6.39208018188318));
#36510=CARTESIAN_POINT('Ctrl Pts',(95.3330820644971,0.934122732016443,-6.39438235580631));
#36511=CARTESIAN_POINT('Ctrl Pts',(95.3604671478669,0.966215710941009,-6.39668452972943));
#36512=CARTESIAN_POINT('Ctrl Pts',(95.3891360213213,0.997021712251413,-6.39898670365255));
#36513=CARTESIAN_POINT('Ctrl Pts',(95.4266210248666,1.03730104412603,-6.40199683231379));
#36514=CARTESIAN_POINT('Ctrl Pts',(95.466459518483,1.07554808367407,-6.40500696097503));
#36515=CARTESIAN_POINT('Ctrl Pts',(95.508402552488,1.11147603473779,-6.40801708963627));
#36516=CARTESIAN_POINT('Ctrl Pts',(95.5502710419033,1.14734013170907,-6.41102186845071));
#36517=CARTESIAN_POINT('Ctrl Pts',(95.594236251094,1.1808929788986,-6.41402664726515));
#36518=CARTESIAN_POINT('Ctrl Pts',(95.6400119215914,1.21188399779696,-6.4170314260796));
#36519=CARTESIAN_POINT('Ctrl Pts',(95.6857423046466,1.24284435621649,-6.42003323216322));
#36520=CARTESIAN_POINT('Ctrl Pts',(95.7332791656549,1.27124761245924,-6.42303503824684));
#36521=CARTESIAN_POINT('Ctrl Pts',(95.7823041177332,1.2968841254138,-6.42603684433046));
#36522=CARTESIAN_POINT('Ctrl Pts',(95.8312999314135,1.32250540108844,-6.42903686626505));
#36523=CARTESIAN_POINT('Ctrl Pts',(95.8817816160496,1.34536294862071,-6.43203688819965));
#36524=CARTESIAN_POINT('Ctrl Pts',(95.9334048098988,1.36529227383073,-6.43503691013424));
#36525=CARTESIAN_POINT('Ctrl Pts',(95.9850177097712,1.38521762501287,-6.43803633384634));
#36526=CARTESIAN_POINT('Ctrl Pts',(96.0377711744047,1.40221572339034,-6.44103575755843));
#36527=CARTESIAN_POINT('Ctrl Pts',(96.0913015734375,1.4161704834635,-6.44403518127053));
#36528=CARTESIAN_POINT('Ctrl Pts',(96.1448811859189,1.43013807291734,-6.44703736251828));
#36529=CARTESIAN_POINT('Ctrl Pts',(96.1992386477005,1.44105660070103,-6.45003954376604));
#36530=CARTESIAN_POINT('Ctrl Pts',(96.2539973523197,1.44886050883572,-6.4530417250138));
#36531=CARTESIAN_POINT('Ctrl Pts',(96.3087809818858,1.45666796913615,-6.45604527278782));
#36532=CARTESIAN_POINT('Ctrl Pts',(96.3639656912268,1.46135793888933,-6.45904882056184));
#36533=CARTESIAN_POINT('Ctrl Pts',(96.4191702244085,1.46291683768629,-6.46205236833586));
#36534=CARTESIAN_POINT('Ctrl Pts',(96.4744789468561,1.46447867864238,-6.46506158480083));
#36535=CARTESIAN_POINT('Ctrl Pts',(96.5298070386893,1.46289765888103,-6.46807080126579));
#36536=CARTESIAN_POINT('Ctrl Pts',(96.5847748920056,1.45821235280584,-6.47108001773076));
#36537=CARTESIAN_POINT('Ctrl Pts',(96.6268275525529,1.45462790163933,-6.47338219165387));
#36538=CARTESIAN_POINT('Ctrl Pts',(96.6686693881686,1.44922763500379,-6.475684365577));
#36539=CARTESIAN_POINT('Ctrl Pts',(96.7101348032585,1.44204896010572,-6.47798653950011));
#36540=CARTESIAN_POINT('Ctrl Pts',(96.7643514865242,1.43266272962009,-6.48099666816135));
#36541=CARTESIAN_POINT('Ctrl Pts',(96.8181520080073,1.42019495131144,-6.48400679682259));
#36542=CARTESIAN_POINT('Ctrl Pts',(96.8711601430782,1.4046974229439,-6.48701692548383));
#36543=CARTESIAN_POINT('Ctrl Pts',(96.9240740677568,1.38922743805102,-6.49002170429828));
#36544=CARTESIAN_POINT('Ctrl Pts',(96.9761978979951,1.3707385361097,-6.49302648311272));
#36545=CARTESIAN_POINT('Ctrl Pts',(97.027165357044,1.3493335511777,-6.49603126192716));
#36546=CARTESIAN_POINT('Ctrl Pts',(97.0780823922361,1.32794974293203,-6.49903306801079));
#36547=CARTESIAN_POINT('Ctrl Pts',(97.1278448379982,1.30365577019171,-6.50203487409441));
#36548=CARTESIAN_POINT('Ctrl Pts',(97.1761031489141,1.27660374345996,-6.50503668017803));
#36549=CARTESIAN_POINT('Ctrl Pts',(97.2243327770917,1.2495677953308,-6.50803670211263));
#36550=CARTESIAN_POINT('Ctrl Pts',(97.2710595826273,1.21977730007934,-6.51103672404723));
#36551=CARTESIAN_POINT('Ctrl Pts',(97.3159576393139,1.1874307909587,-6.51403674598183));
#36552=CARTESIAN_POINT('Ctrl Pts',(97.3608467430567,1.15509073192744,-6.51703616969392));
#36553=CARTESIAN_POINT('Ctrl Pts',(97.4039073939027,1.12019597977156,-6.52003559340602));
#36554=CARTESIAN_POINT('Ctrl Pts',(97.4448436809194,1.08298765604419,-6.52303501711812));
#36555=CARTESIAN_POINT('Ctrl Pts',(97.4858176029228,1.04574512465248,-6.52603719836588));
#36556=CARTESIAN_POINT('Ctrl Pts',(97.5246628675223,1.00618512821049,-6.52903937961364));
#36557=CARTESIAN_POINT('Ctrl Pts',(97.5611187918536,0.964587264143905,-6.5320415608614));
#36558=CARTESIAN_POINT('Ctrl Pts',(97.5975913101124,0.922970465653054,-6.53504510863541));
#36559=CARTESIAN_POINT('Ctrl Pts',(97.6316719945516,0.879314367459454,-6.53804865640943));
#36560=CARTESIAN_POINT('Ctrl Pts',(97.6631411544674,0.833930861386641,-6.54105220418344));
#36561=CARTESIAN_POINT('Ctrl Pts',(97.6946697071265,0.788461701583791,-6.54406142064841));
#36562=CARTESIAN_POINT('Ctrl Pts',(97.7235766127074,0.741259072640851,-6.54707063711337));
#36563=CARTESIAN_POINT('Ctrl Pts',(97.7496867620436,0.692661983295228,-6.55007985357834));
#36564=CARTESIAN_POINT('Ctrl Pts',(97.769662096364,0.655483218280092,-6.55238202750145));
#36565=CARTESIAN_POINT('Ctrl Pts',(97.7880014424451,0.61748887037511,-6.55468420142456));
#36566=CARTESIAN_POINT('Ctrl Pts',(97.8046456490466,0.578838069497681,-6.55698637534768));
#36567=CARTESIAN_POINT('Ctrl Pts',(97.8286351980216,0.523130080359468,-6.56030453375556));
#36568=CARTESIAN_POINT('Ctrl Pts',(97.8491882128639,0.465858031256992,-6.56362269216345));
#36569=CARTESIAN_POINT('Ctrl Pts',(97.8661211561645,0.40744062098,-6.56694085057134));
#36570=CARTESIAN_POINT('Ctrl Pts',(97.8829986720517,0.349214431207237,-6.57024814749254));
#36571=CARTESIAN_POINT('Ctrl Pts',(97.8962796017182,0.289850665694475,-6.57355544441374));
#36572=CARTESIAN_POINT('Ctrl Pts',(97.9058288493017,0.229786202286622,-6.57686274133495));
#36573=CARTESIAN_POINT('Ctrl Pts',(97.9153293820534,0.170028153621295,-6.58015316630763));
#36574=CARTESIAN_POINT('Ctrl Pts',(97.9211360715741,0.109576858096741,-6.58344359128031));
#36575=CARTESIAN_POINT('Ctrl Pts',(97.9231644409405,0.0488799968574776,
-6.58673401625299));
#36576=CARTESIAN_POINT('Ctrl Pts',(97.9237009416909,0.0328257652465272,
-6.58760432887759));
#36577=CARTESIAN_POINT('Ctrl Pts',(97.9239733837609,0.0167544342987488,
-6.58847464150218));
#36578=CARTESIAN_POINT('Ctrl Pts',(97.9239807941682,0.000674448999165355,
-6.58934495412678));
#36579=CARTESIAN_POINT('Origin',(96.460480949577,-8.32667268468867E-16,
1.18130019239114E-14));
#36580=CARTESIAN_POINT('',(97.9239803863197,-0.00128399919636206,-7.16065504587409));
#36581=CARTESIAN_POINT('',(97.9239803766892,-0.00129492944526685,-7.08934495420499));
#36582=CARTESIAN_POINT('',(97.923980949577,-1.01189432752408E-15,1.19922289829666E-14));
#36583=CARTESIAN_POINT('Ctrl Pts',(97.9239803863202,-0.00128399862218805,
-7.1606550458429));
#36584=CARTESIAN_POINT('Ctrl Pts',(97.9240284084967,0.0534515961901013,
-7.15768174384173));
#36585=CARTESIAN_POINT('Ctrl Pts',(97.9210014401702,0.108255387245641,-7.15470844184055));
#36586=CARTESIAN_POINT('Ctrl Pts',(97.9149031712147,0.162752115827591,-7.15173513983938));
#36587=CARTESIAN_POINT('Ctrl Pts',(97.9088083138335,0.217218357129264,-7.14876350120212));
#36588=CARTESIAN_POINT('Ctrl Pts',(97.8996456193441,0.271377341401932,-7.14579186256485));
#36589=CARTESIAN_POINT('Ctrl Pts',(97.8874707313403,0.324857526837941,-7.14282022392758));
#36590=CARTESIAN_POINT('Ctrl Pts',(97.8752976171332,0.378329920581715,-7.13984901823746));
#36591=CARTESIAN_POINT('Ctrl Pts',(97.8601133014658,0.431123186603639,-7.13687781254734));
#36592=CARTESIAN_POINT('Ctrl Pts',(97.8420242977194,0.482877031140819,-7.13390660685723));
#36593=CARTESIAN_POINT('Ctrl Pts',(97.8239180353275,0.53468025381267,-7.13093256635172));
#36594=CARTESIAN_POINT('Ctrl Pts',(97.8029017321617,0.585441565881671,-7.12795852584622));
#36595=CARTESIAN_POINT('Ctrl Pts',(97.7791309073797,0.6348185085415,-7.12498448534072));
#36596=CARTESIAN_POINT('Ctrl Pts',(97.7553473168163,0.684221968382254,-7.12200884766929));
#36597=CARTESIAN_POINT('Ctrl Pts',(97.7288065230378,0.732239107887783,-7.11903320999787));
#36598=CARTESIAN_POINT('Ctrl Pts',(97.6997094827783,0.778553076225247,-7.11605757232644));
#36599=CARTESIAN_POINT('Ctrl Pts',(97.6705602221932,0.824950164030577,-7.11307659429165));
#36600=CARTESIAN_POINT('Ctrl Pts',(97.6388458752375,0.869637543718845,-7.11009561625686));
#36601=CARTESIAN_POINT('Ctrl Pts',(97.6048091565678,0.912329548291191,-7.10711463822207));
#36602=CARTESIAN_POINT('Ctrl Pts',(97.5891757490176,0.931938415793702,-7.10574544499965));
#36603=CARTESIAN_POINT('Ctrl Pts',(97.5730529323351,0.951126822072045,-7.10437625177722));
#36604=CARTESIAN_POINT('Ctrl Pts',(97.5564667651661,0.969869755187462,-7.1030070585548));
#36605=CARTESIAN_POINT('Ctrl Pts',(97.5200025931577,1.01107550996509,-7.09999692989356));
#36606=CARTESIAN_POINT('Ctrl Pts',(97.4811347572606,1.05030856924528,-7.09698680123233));
#36607=CARTESIAN_POINT('Ctrl Pts',(97.440104944285,1.08727599025841,-7.09397667257109));
#36608=CARTESIAN_POINT('Ctrl Pts',(97.3991480528479,1.12417770974811,-7.09097189375665));
#36609=CARTESIAN_POINT('Ctrl Pts',(97.3560371988642,1.15882143129324,-7.08796711494221));
#36610=CARTESIAN_POINT('Ctrl Pts',(97.311052273536,1.190949483756,-7.08496233612777));
#36611=CARTESIAN_POINT('Ctrl Pts',(97.2661118533386,1.22304575083361,-7.08196053004415));
#36612=CARTESIAN_POINT('Ctrl Pts',(97.2193014622973,1.25263097367006,-7.07895872396053));
#36613=CARTESIAN_POINT('Ctrl Pts',(97.1709341354984,1.27948760080513,-7.07595691787692));
#36614=CARTESIAN_POINT('Ctrl Pts',(97.1225955562323,1.30632826547508,-7.07295689594232));
#36615=CARTESIAN_POINT('Ctrl Pts',(97.0727023361604,1.33044329302545,-7.06995687400772));
#36616=CARTESIAN_POINT('Ctrl Pts',(97.0215946080853,1.3516596140432,-7.06695685207312));
#36617=CARTESIAN_POINT('Ctrl Pts',(96.9704970712002,1.37287170439828,-7.06395742836103));
#36618=CARTESIAN_POINT('Ctrl Pts',(96.9181859947554,1.39118603377388,-7.06095800464894));
#36619=CARTESIAN_POINT('Ctrl Pts',(96.8650219868468,1.40647744353213,-7.05795858093685));
#36620=CARTESIAN_POINT('Ctrl Pts',(96.8118091023332,1.42178291152684,-7.05495639968909));
#36621=CARTESIAN_POINT('Ctrl Pts',(96.7577422283616,1.43405976125443,-7.05195421844133));
#36622=CARTESIAN_POINT('Ctrl Pts',(96.7031962108579,1.44323302066623,-7.04895203719357));
#36623=CARTESIAN_POINT('Ctrl Pts',(96.6486253652178,1.45241045554207,-7.04594848941955));
#36624=CARTESIAN_POINT('Ctrl Pts',(96.5935754671363,1.45848142601986,-7.04294494164554));
#36625=CARTESIAN_POINT('Ctrl Pts',(96.5384273126797,1.46142280483064,-7.03994139387152));
#36626=CARTESIAN_POINT('Ctrl Pts',(96.4831750753627,1.46436973499891,-7.03693217740656));
#36627=CARTESIAN_POINT('Ctrl Pts',(96.4278247406292,1.46417527605419,-7.03392296094159));
#36628=CARTESIAN_POINT('Ctrl Pts',(96.3727567635999,1.46086848045765,-7.03091374447663));
#36629=CARTESIAN_POINT('Ctrl Pts',(96.3306275043085,1.45833864630311,-7.0286115705535));
#36630=CARTESIAN_POINT('Ctrl Pts',(96.2886635144571,1.45398828503214,-7.02630939663037));
#36631=CARTESIAN_POINT('Ctrl Pts',(96.2470312747839,1.44785064365449,-7.02400722270724));
#36632=CARTESIAN_POINT('Ctrl Pts',(96.1925964657486,1.43982558089201,-7.020997094046));
#36633=CARTESIAN_POINT('Ctrl Pts',(96.1385004897705,1.42870951185745,-7.01798696538476));
#36634=CARTESIAN_POINT('Ctrl Pts',(96.0851207510273,1.41454479297927,-7.01497683672353));
#36635=CARTESIAN_POINT('Ctrl Pts',(96.0318358831207,1.4004052487977,-7.01197205790908));
#36636=CARTESIAN_POINT('Ctrl Pts',(95.9792652325821,1.38322794180095,-7.00896727909463));
#36637=CARTESIAN_POINT('Ctrl Pts',(95.9277775373783,1.36310649790536,-7.00596250028019));
#36638=CARTESIAN_POINT('Ctrl Pts',(95.8763407807187,1.34300496084492,-7.00296069419656));
#36639=CARTESIAN_POINT('Ctrl Pts',(95.8259853464624,1.31996524816035,-6.99995888811294));
#36640=CARTESIAN_POINT('Ctrl Pts',(95.7770644809546,1.29413066589723,-6.99695708202932));
#36641=CARTESIAN_POINT('Ctrl Pts',(95.7281726919799,1.26831143863818,-6.99395706009472));
#36642=CARTESIAN_POINT('Ctrl Pts',(95.6807142478144,1.23970088044208,-6.99095703816012));
#36643=CARTESIAN_POINT('Ctrl Pts',(95.6350199459775,1.20848929723705,-6.98795701622552));
#36644=CARTESIAN_POINT('Ctrl Pts',(95.5893347558606,1.1772839378104,-6.98495759251343));
#36645=CARTESIAN_POINT('Ctrl Pts',(95.5454134452998,1.143478881119,-6.98195816880133));
#36646=CARTESIAN_POINT('Ctrl Pts',(95.5035578728706,1.10730775995957,-6.97895874508924));
#36647=CARTESIAN_POINT('Ctrl Pts',(95.4616638203048,1.07110338469324,-6.97595656384148));
#36648=CARTESIAN_POINT('Ctrl Pts',(95.4218397005595,1.03252894514053,-6.97295438259372));
#36649=CARTESIAN_POINT('Ctrl Pts',(95.3843531190853,0.991857420419462,-6.96995220134596));
#36650=CARTESIAN_POINT('Ctrl Pts',(95.3468494745513,0.951167382923188,-6.96694865357194));
#36651=CARTESIAN_POINT('Ctrl Pts',(95.3116858251814,0.908378766162068,-6.96394510579792));
#36652=CARTESIAN_POINT('Ctrl Pts',(95.2790896061615,0.863797860441274,-6.9609415580239));
#36653=CARTESIAN_POINT('Ctrl Pts',(95.246431867264,0.819132815763593,-6.95793234155893));
#36654=CARTESIAN_POINT('Ctrl Pts',(95.2163515262493,0.772669169180109,-6.95492312509396));
#36655=CARTESIAN_POINT('Ctrl Pts',(95.1890321300838,0.724741436244182,-6.951913908629));
#36656=CARTESIAN_POINT('Ctrl Pts',(95.1681316723801,0.688074756314977,-6.94961173470589));
#36657=CARTESIAN_POINT('Ctrl Pts',(95.1488462577054,0.650551765119949,-6.94730956078278));
#36658=CARTESIAN_POINT('Ctrl Pts',(95.131239005216,0.612330060793418,-6.94500738685968));
#36659=CARTESIAN_POINT('Ctrl Pts',(95.1082172452907,0.562354580435533,-6.94199725819844));
#36660=CARTESIAN_POINT('Ctrl Pts',(95.0879694233587,0.510973968189141,-6.93898712953721));
#36661=CARTESIAN_POINT('Ctrl Pts',(95.0706662769323,0.458527453596354,-6.93597700087597));
#36662=CARTESIAN_POINT('Ctrl Pts',(95.0533938830727,0.406174151237822,-6.93297222206153));
#36663=CARTESIAN_POINT('Ctrl Pts',(95.039055942892,0.352759203469606,-6.92996744324708));
#36664=CARTESIAN_POINT('Ctrl Pts',(95.0277755191432,0.298642595095792,-6.92696266443264));
#36665=CARTESIAN_POINT('Ctrl Pts',(95.0165062555048,0.244579526140235,-6.92396085834902));
#36666=CARTESIAN_POINT('Ctrl Pts',(95.0082886233428,0.189816686172077,-6.9209590522654));
#36667=CARTESIAN_POINT('Ctrl Pts',(95.0031956124036,0.134728230373038,-6.91795724618177));
#36668=CARTESIAN_POINT('Ctrl Pts',(94.9981056285388,0.0796725168670466,
-6.91495722424717));
#36669=CARTESIAN_POINT('Ctrl Pts',(94.9961366334338,0.0242920959479925,
-6.91195720231257));
#36670=CARTESIAN_POINT('Ctrl Pts',(94.9973099872178,-0.0310319981469414,
-6.90895718037797));
#36671=CARTESIAN_POINT('Ctrl Pts',(94.9984831070281,-0.0863450602830034,
-6.90595775666589));
#36672=CARTESIAN_POINT('Ctrl Pts',(95.0027973201282,-0.141601290199693,
-6.9029583329538));
#36673=CARTESIAN_POINT('Ctrl Pts',(95.0102218871038,-0.196420217173161,
-6.89995890924171));
#36674=CARTESIAN_POINT('Ctrl Pts',(95.0176532798934,-0.251289542210087,
-6.89695672799395));
#36675=CARTESIAN_POINT('Ctrl Pts',(95.0282006684755,-0.305720236624135,
-6.89395454674619));
#36676=CARTESIAN_POINT('Ctrl Pts',(95.0417816440599,-0.359339018929665,
-6.89095236549844));
#36677=CARTESIAN_POINT('Ctrl Pts',(95.0553688014029,-0.412982207314665,
-6.88794881772442));
#36678=CARTESIAN_POINT('Ctrl Pts',(95.0719921395309,-0.465812242245802,
-6.88494526995039));
#36679=CARTESIAN_POINT('Ctrl Pts',(95.0915194017629,-0.517471284813382,
-6.88194172217638));
#36680=CARTESIAN_POINT('Ctrl Pts',(95.111083518416,-0.569227825129932,-6.87893250571141));
#36681=CARTESIAN_POINT('Ctrl Pts',(95.1335622926563,-0.619808474374922,
-6.87592328924644));
#36682=CARTESIAN_POINT('Ctrl Pts',(95.1587758480468,-0.668876729039158,
-6.87291407278148));
#36683=CARTESIAN_POINT('Ctrl Pts',(95.1780652512535,-0.706415954833038,
-6.87061189885836));
#36684=CARTESIAN_POINT('Ctrl Pts',(95.1989542913622,-0.743070423738718,
-6.86830972493524));
#36685=CARTESIAN_POINT('Ctrl Pts',(95.2213454637532,-0.778701160762088,
-6.86600755101212));
#36686=CARTESIAN_POINT('Ctrl Pts',(95.2506222742913,-0.825288910565812,
-6.86299742235088));
#36687=CARTESIAN_POINT('Ctrl Pts',(95.2825915894323,-0.870321171193206,
-6.85998729368965));
#36688=CARTESIAN_POINT('Ctrl Pts',(95.3170625856117,-0.913469591692483,
-6.85697716502841));
#36689=CARTESIAN_POINT('Ctrl Pts',(95.3514723171179,-0.956541325290622,
-6.85397238621397));
#36690=CARTESIAN_POINT('Ctrl Pts',(95.3883745791975,-0.997735453842079,
-6.85096760739953));
#36691=CARTESIAN_POINT('Ctrl Pts',(95.4275351158937,-1.0367522146956,-6.84796282858509));
#36692=CARTESIAN_POINT('Ctrl Pts',(95.4666569097267,-1.07573037492832,-6.84496102250147));
#36693=CARTESIAN_POINT('Ctrl Pts',(95.5080321800748,-1.11253506380543,-6.84195921641785));
#36694=CARTESIAN_POINT('Ctrl Pts',(95.5513874432147,-1.14690071352749,-6.83895741033423));
#36695=CARTESIAN_POINT('Ctrl Pts',(95.5947169377845,-1.18124593773287,-6.83595738839963));
#36696=CARTESIAN_POINT('Ctrl Pts',(95.6400236795582,-1.21315466871284,-6.83295736646503));
#36697=CARTESIAN_POINT('Ctrl Pts',(95.687000213198,-1.24240082117273,-6.82995734453043));
#36698=CARTESIAN_POINT('Ctrl Pts',(95.7339673794331,-1.27164114177298,-6.82695792081835));
#36699=CARTESIAN_POINT('Ctrl Pts',(95.7826032281977,-1.29821965930536,-6.82395849710626));
#36700=CARTESIAN_POINT('Ctrl Pts',(95.8325723091258,-1.32195423114674,-6.82095907339417));
#36701=CARTESIAN_POINT('Ctrl Pts',(95.8825873293864,-1.34571062348925,-6.81795689214642));
#36702=CARTESIAN_POINT('Ctrl Pts',(95.9339375525643,-1.36661761944449,-6.81495471089866));
#36703=CARTESIAN_POINT('Ctrl Pts',(95.9862653175298,-1.38454027905369,-6.8119525296509));
#36704=CARTESIAN_POINT('Ctrl Pts',(96.0386169009323,-1.40247109665969,-6.80894898187689));
#36705=CARTESIAN_POINT('Ctrl Pts',(96.0919464036947,-1.41741472729072,-6.80594543410287));
#36706=CARTESIAN_POINT('Ctrl Pts',(96.1458818615687,-1.42928641770092,-6.80294188632886));
#36707=CARTESIAN_POINT('Ctrl Pts',(96.1999191135424,-1.44118051392886,-6.7999326698639));
#36708=CARTESIAN_POINT('Ctrl Pts',(96.2545640825608,-1.44999100372019,-6.79692345339893));
#36709=CARTESIAN_POINT('Ctrl Pts',(96.3094366540997,-1.45568467423538,-6.79391423693396));
#36710=CARTESIAN_POINT('Ctrl Pts',(96.3514164201826,-1.46004056552456,-6.79161206301083));
#36711=CARTESIAN_POINT('Ctrl Pts',(96.393529213884,-1.46257329016689,-6.78930988908769));
#36712=CARTESIAN_POINT('Ctrl Pts',(96.4356053637645,-1.46328857551424,-6.78700771516456));
#36713=CARTESIAN_POINT('Ctrl Pts',(96.490620592387,-1.46422382237087,-6.78399758650331));
#36714=CARTESIAN_POINT('Ctrl Pts',(96.5458042309069,-1.46205411097958,-6.78098745784207));
#36715=CARTESIAN_POINT('Ctrl Pts',(96.6007770113185,-1.45675985154034,-6.77797732918083));
#36716=CARTESIAN_POINT('Ctrl Pts',(96.6556520896096,-1.45147500149188,-6.77497255036638));
#36717=CARTESIAN_POINT('Ctrl Pts',(96.7103165320628,-1.44307667398022,-6.77196777155193));
#36718=CARTESIAN_POINT('Ctrl Pts',(96.7643912828551,-1.43159727553765,-6.76896299273748));
#36719=CARTESIAN_POINT('Ctrl Pts',(96.8184125356401,-1.420129234058,-6.76596118665386));
#36720=CARTESIAN_POINT('Ctrl Pts',(96.871844738392,-1.40558626913275,-6.76295938057023));
#36721=CARTESIAN_POINT('Ctrl Pts',(96.9243160404985,-1.38805232553742,-6.75995757448661));
#36722=CARTESIAN_POINT('Ctrl Pts',(96.9767561558396,-1.37052880339086,-6.75695755255201));
#36723=CARTESIAN_POINT('Ctrl Pts',(97.0282360026413,-1.35001799316396,-6.7539575306174));
#36724=CARTESIAN_POINT('Ctrl Pts',(97.0783982359955,-1.32665386485894,-6.7509575086828));
#36725=CARTESIAN_POINT('Ctrl Pts',(97.1285504666972,-1.30329439550231,-6.7479580849707));
#36726=CARTESIAN_POINT('Ctrl Pts',(97.1773851272762,-1.27708296087088,-6.7449586612586));
#36727=CARTESIAN_POINT('Ctrl Pts',(97.2245663796204,-1.24820098765999,-6.7419592375465));
#36728=CARTESIAN_POINT('Ctrl Pts',(97.2717910082924,-1.21929246165803,-6.73895705629874));
#36729=CARTESIAN_POINT('Ctrl Pts',(97.3173587404368,-1.1877087682782,-6.73595487505097));
#36730=CARTESIAN_POINT('Ctrl Pts',(97.3609611355696,-1.15367572767863,-6.73295269380321));
#36731=CARTESIAN_POINT('Ctrl Pts',(97.4045833775446,-1.11962719599447,-6.72994914602919));
#36732=CARTESIAN_POINT('Ctrl Pts',(97.4462381013335,-1.08312744329101,-6.72694559825516));
#36733=CARTESIAN_POINT('Ctrl Pts',(97.4856510840067,-1.04444169079626,-6.72394205048114));
#36734=CARTESIAN_POINT('Ctrl Pts',(97.5251384520517,-1.00568292545424,-6.72093283401617));
#36735=CARTESIAN_POINT('Ctrl Pts',(97.5623752709247,-0.964730310279934,
-6.7179236175512));
#36736=CARTESIAN_POINT('Ctrl Pts',(97.5971260308949,-0.921884054052279,
-6.71491440108623));
#36737=CARTESIAN_POINT('Ctrl Pts',(97.6237117864701,-0.889104912060561,
-6.71261222716315));
#36738=CARTESIAN_POINT('Ctrl Pts',(97.6488432766803,-0.855218184759521,
-6.71031005324007));
#36739=CARTESIAN_POINT('Ctrl Pts',(97.6724325905286,-0.820369105948431,
-6.70800787931698));
#36740=CARTESIAN_POINT('Ctrl Pts',(97.7037292966424,-0.774133705253864,
-6.70495351066697));
#36741=CARTESIAN_POINT('Ctrl Pts',(97.732438933426,-0.726012933133433,-6.70189914201697));
#36742=CARTESIAN_POINT('Ctrl Pts',(97.758333054594,-0.676322529199528,-6.69884477336696));
#36743=CARTESIAN_POINT('Ctrl Pts',(97.7853132466074,-0.624547972702387,
-6.69566229607329));
#36744=CARTESIAN_POINT('Ctrl Pts',(97.8092360930233,-0.571069584415693,
-6.69247981877961));
#36745=CARTESIAN_POINT('Ctrl Pts',(97.8298924651478,-0.516279334297092,
-6.68929734148594));
#36746=CARTESIAN_POINT('Ctrl Pts',(97.8496510794807,-0.463870352953487,
-6.68625317956389));
#36747=CARTESIAN_POINT('Ctrl Pts',(97.8664210779866,-0.41026171723104,-6.68320901764185));
#36748=CARTESIAN_POINT('Ctrl Pts',(97.8800668537132,-0.3558203349695,-6.6801648557198));
#36749=CARTESIAN_POINT('Ctrl Pts',(97.8937003451011,-0.30142796248155,-6.67712343424409));
#36750=CARTESIAN_POINT('Ctrl Pts',(97.9042150716696,-0.246204821887107,
-6.67408201276838));
#36751=CARTESIAN_POINT('Ctrl Pts',(97.9115251914004,-0.190533089701565,
-6.67104059129267));
#36752=CARTESIAN_POINT('Ctrl Pts',(97.9188312553177,-0.134892245404056,
-6.66800085726376));
#36753=CARTESIAN_POINT('Ctrl Pts',(97.9229361774325,-0.0788038064188046,
-6.66496112323484));
#36754=CARTESIAN_POINT('Ctrl Pts',(97.9238055394607,-0.0226582135575034,
-6.66192138920592));
#36755=CARTESIAN_POINT('Ctrl Pts',(97.9239262639303,-0.0148615227717745,
-6.66149927475158));
#36756=CARTESIAN_POINT('Ctrl Pts',(97.9239846768685,-0.00706373686963602,
-6.66107716029724));
#36757=CARTESIAN_POINT('Ctrl Pts',(97.9239807654658,0.000734093566312587,
-6.6606550458429));
#36758=CARTESIAN_POINT('Ctrl Pts',(97.9239807941685,0.000674448439337589,
-6.58934495415708));
#36759=CARTESIAN_POINT('Ctrl Pts',(97.9240067388656,-0.0556234952178808,
-6.59239202230983));
#36760=CARTESIAN_POINT('Ctrl Pts',(97.9207798368809,-0.111913354676098,
-6.59543909046258));
#36761=CARTESIAN_POINT('Ctrl Pts',(97.9143291626584,-0.167802334071808,
-6.59848615861533));
#36762=CARTESIAN_POINT('Ctrl Pts',(97.9077134966479,-0.22512081096258,-6.60161116299699));
#36763=CARTESIAN_POINT('Ctrl Pts',(97.8977069013895,-0.28201705927344,-6.60473616737865));
#36764=CARTESIAN_POINT('Ctrl Pts',(97.8843968830571,-0.338076417961225,
-6.60786117176031));
#36765=CARTESIAN_POINT('Ctrl Pts',(97.8713913919585,-0.392853163732691,
-6.61091467744706));
#36766=CARTESIAN_POINT('Ctrl Pts',(97.8552322800615,-0.446830443496005,
-6.61396818313381));
#36767=CARTESIAN_POINT('Ctrl Pts',(97.8360516456787,-0.499637378531921,
-6.61702168882056));
#36768=CARTESIAN_POINT('Ctrl Pts',(97.8161973313687,-0.554299047433307,
-6.62018244254967));
#36769=CARTESIAN_POINT('Ctrl Pts',(97.7931054900853,-0.607706069216668,
-6.62334319627879));
#36770=CARTESIAN_POINT('Ctrl Pts',(97.7669754134871,-0.659472869625587,
-6.6265039500079));
#36771=CARTESIAN_POINT('Ctrl Pts',(97.740845336889,-0.7112396700345,-6.62966470373701));
#36772=CARTESIAN_POINT('Ctrl Pts',(97.7116773880182,-0.761365777376917,
-6.63282545746612));
#36773=CARTESIAN_POINT('Ctrl Pts',(97.6797197261331,-0.809499262348027,
-6.63598621119524));
#36774=CARTESIAN_POINT('Ctrl Pts',(97.6492850000422,-0.855338956007879,
-6.63899633985647));
#36775=CARTESIAN_POINT('Ctrl Pts',(97.6161975820751,-0.899556196763912,
-6.64200646851771));
#36776=CARTESIAN_POINT('Ctrl Pts',(97.5806564616684,-0.941827517176423,
-6.64501659717895));
#36777=CARTESIAN_POINT('Ctrl Pts',(97.5451785078471,-0.984023709541822,
-6.64802137599339));
#36778=CARTESIAN_POINT('Ctrl Pts',(97.5072558429796,-1.0242804439233,-6.65102615480783));
#36779=CARTESIAN_POINT('Ctrl Pts',(97.4671301590771,-1.06230392026613,-6.65403093362228));
#36780=CARTESIAN_POINT('Ctrl Pts',(97.427044172891,-1.10028977867862,-6.6570327397059));
#36781=CARTESIAN_POINT('Ctrl Pts',(97.3847598666553,-1.13604639437271,-6.66003454578952));
#36782=CARTESIAN_POINT('Ctrl Pts',(97.3405572911961,-1.16931513413723,-6.66303635187314));
#36783=CARTESIAN_POINT('Ctrl Pts',(97.2963809879142,-1.20256410034279,-6.66603637380774));
#36784=CARTESIAN_POINT('Ctrl Pts',(97.250289096355,-1.23332780453114,-6.66903639574234));
#36785=CARTESIAN_POINT('Ctrl Pts',(97.2025946391917,-1.26138793465233,-6.67203641767694));
#36786=CARTESIAN_POINT('Ctrl Pts',(97.1549096925914,-1.289442469414,-6.67503584138903));
#36787=CARTESIAN_POINT('Ctrl Pts',(97.1056232699489,-1.31479423310814,-6.67803526510112));
#36788=CARTESIAN_POINT('Ctrl Pts',(97.05507527934,-1.33726954388924,-6.68103468881322));
#36789=CARTESIAN_POINT('Ctrl Pts',(97.004480817175,-1.35976551746326,-6.68403687006098));
#36790=CARTESIAN_POINT('Ctrl Pts',(96.9526229534576,-1.37937953976783,-6.68703905130873));
#36791=CARTESIAN_POINT('Ctrl Pts',(96.8998626175477,-1.39598567322567,-6.69004123255649));
#36792=CARTESIAN_POINT('Ctrl Pts',(96.847078266304,-1.41259936542684,-6.69304478033051));
#36793=CARTESIAN_POINT('Ctrl Pts',(96.7933911368269,-1.42620230958813,-6.69604832810453));
#36794=CARTESIAN_POINT('Ctrl Pts',(96.7391751998421,-1.43671909741228,-6.69905187587855));
#36795=CARTESIAN_POINT('Ctrl Pts',(96.6848569394005,-1.44725573390355,-6.70206109234352));
#36796=CARTESIAN_POINT('Ctrl Pts',(96.6300084023298,-1.45469450736379,-6.70507030880848));
#36797=CARTESIAN_POINT('Ctrl Pts',(96.5750104158968,-1.45901173790498,-6.70807952527345));
#36798=CARTESIAN_POINT('Ctrl Pts',(96.5329347022804,-1.46231459620304,-6.71038169919656));
#36799=CARTESIAN_POINT('Ctrl Pts',(96.4907716762808,-1.46379152747159,-6.71268387311968));
#36800=CARTESIAN_POINT('Ctrl Pts',(96.4486908126069,-1.46345250782874,-6.7149860470428));
#36801=CARTESIAN_POINT('Ctrl Pts',(96.3936694206248,-1.46300923430651,-6.71799617570403));
#36802=CARTESIAN_POINT('Ctrl Pts',(96.3385574561869,-1.45945775804877,-6.72100630436527));
#36803=CARTESIAN_POINT('Ctrl Pts',(96.2837345590264,-1.4527879967247,-6.72401643302651));
#36804=CARTESIAN_POINT('Ctrl Pts',(96.2290090976017,-1.44613008944583,-6.72702121184096));
#36805=CARTESIAN_POINT('Ctrl Pts',(96.1745722039164,-1.43636495864269,-6.7300259906554));
#36806=CARTESIAN_POINT('Ctrl Pts',(96.1208020029894,-1.42353449668251,-6.73303076946985));
#36807=CARTESIAN_POINT('Ctrl Pts',(96.0670849987679,-1.41071672833879,-6.73603257555347));
#36808=CARTESIAN_POINT('Ctrl Pts',(96.0140338918733,-1.39483975832009,-6.73903438163709));
#36809=CARTESIAN_POINT('Ctrl Pts',(95.9620183132523,-1.37599682055892,-6.74203618772071));
#36810=CARTESIAN_POINT('Ctrl Pts',(95.9100336505337,-1.35716508225835,-6.7450362096553));
#36811=CARTESIAN_POINT('Ctrl Pts',(95.8590837917253,-1.33537104981141,-6.74803623158991));
#36812=CARTESIAN_POINT('Ctrl Pts',(95.8095226134042,-1.31075760328414,-6.75103625352451));
#36813=CARTESIAN_POINT('Ctrl Pts',(95.7599713178817,-1.28614906482688,-6.7540356772366));
#36814=CARTESIAN_POINT('Ctrl Pts',(95.7118086256451,-1.25872246358268,-6.75703510094869));
#36815=CARTESIAN_POINT('Ctrl Pts',(95.6653657243524,-1.22866758263416,-6.76003452466078));
#36816=CARTESIAN_POINT('Ctrl Pts',(95.6188801255389,-1.19858507057577,-6.76303670590854));
#36817=CARTESIAN_POINT('Ctrl Pts',(95.5741179208266,-1.16586973885513,-6.7660388871563));
#36818=CARTESIAN_POINT('Ctrl Pts',(95.5313817967113,-1.13075506372699,-6.76904106840406));
#36819=CARTESIAN_POINT('Ctrl Pts',(95.488626220061,-1.09562440517822,-6.77204461617808));
#36820=CARTESIAN_POINT('Ctrl Pts',(95.4478989514394,-1.05809258465265,-6.7750481639521));
#36821=CARTESIAN_POINT('Ctrl Pts',(95.4094674834614,-1.01843160990004,-6.77805171172612));
#36822=CARTESIAN_POINT('Ctrl Pts',(95.3709634825552,-0.978695781732232,
-6.78106092819108));
#36823=CARTESIAN_POINT('Ctrl Pts',(95.3347642842418,-0.936823172417153,
-6.78407014465605));
#36824=CARTESIAN_POINT('Ctrl Pts',(95.301097803588,-0.893119796442088,-6.78707936112102));
#36825=CARTESIAN_POINT('Ctrl Pts',(95.2753415661268,-0.859684922715582,
-6.78938153504414));
#36826=CARTESIAN_POINT('Ctrl Pts',(95.2510668845504,-0.825179243157309,
-6.79168370896725));
#36827=CARTESIAN_POINT('Ctrl Pts',(95.228358003907,-0.789750148308691,-6.79398588289037));
#36828=CARTESIAN_POINT('Ctrl Pts',(95.1986657848254,-0.743426048823991,
-6.7969960115516));
#36829=CARTESIAN_POINT('Ctrl Pts',(95.1715272807514,-0.695327782696951,
-6.80000614021284));
#36830=CARTESIAN_POINT('Ctrl Pts',(95.1471583695683,-0.645767799475315,
-6.80301626887408));
#36831=CARTESIAN_POINT('Ctrl Pts',(95.1228327688067,-0.596295898308325,
-6.80602104768852));
#36832=CARTESIAN_POINT('Ctrl Pts',(95.1012672236512,-0.545367905653447,
-6.80902582650297));
#36833=CARTESIAN_POINT('Ctrl Pts',(95.0826332541428,-0.493323401215417,
-6.81203060531741));
#36834=CARTESIAN_POINT('Ctrl Pts',(95.0640177198601,-0.441330386192153,
-6.81503241140103));
#36835=CARTESIAN_POINT('Ctrl Pts',(95.0483281929976,-0.388223542315368,
-6.81803421748465));
#36836=CARTESIAN_POINT('Ctrl Pts',(95.0356885525259,-0.334363388105666,
-6.82103602356827));
#36837=CARTESIAN_POINT('Ctrl Pts',(95.0230564245323,-0.280535246137478,
-6.82403604550287));
#36838=CARTESIAN_POINT('Ctrl Pts',(95.0134707104046,-0.225955194401009,
-6.82703606743747));
#36839=CARTESIAN_POINT('Ctrl Pts',(95.0070051010148,-0.170997683160566,
-6.83003608937207));
#36840=CARTESIAN_POINT('Ctrl Pts',(95.0005407809065,-0.116051130780047,
-6.83303551308416));
#36841=CARTESIAN_POINT('Ctrl Pts',(94.997195391609,-0.0607277925787329,
-6.83603493679625));
#36842=CARTESIAN_POINT('Ctrl Pts',(94.9969909443191,-0.00540874386480694,
-6.83903436050834));
#36843=CARTESIAN_POINT('Ctrl Pts',(94.9967863090695,0.0499611627019756,
-6.8420365417561));
#36844=CARTESIAN_POINT('Ctrl Pts',(94.9997283869156,0.10532624265535,-6.84503872300386));
#36845=CARTESIAN_POINT('Ctrl Pts',(95.0057870219234,0.160305417399915,-6.84804090425161));
#36846=CARTESIAN_POINT('Ctrl Pts',(95.0118484146874,0.21530961744437,-6.85104445202563));
#36847=CARTESIAN_POINT('Ctrl Pts',(95.0210291047738,0.269927040405136,-6.85404799979965));
#36848=CARTESIAN_POINT('Ctrl Pts',(95.0332474352863,0.323785030051596,-6.85705154757367));
#36849=CARTESIAN_POINT('Ctrl Pts',(95.0454888258415,0.377744667589589,-6.86006076403863));
#36850=CARTESIAN_POINT('Ctrl Pts',(95.0607791632033,0.430941499757943,-6.8630699805036));
#36851=CARTESIAN_POINT('Ctrl Pts',(95.0789866839011,0.483017436439501,-6.86607919696856));
#36852=CARTESIAN_POINT('Ctrl Pts',(95.0929161834379,0.522857662241198,-6.86838137089169));
#36853=CARTESIAN_POINT('Ctrl Pts',(95.108552027997,0.56204212921919,-6.8706835448148));
#36854=CARTESIAN_POINT('Ctrl Pts',(95.1258168051965,0.600419746265118,-6.87298571873793));
#36855=CARTESIAN_POINT('Ctrl Pts',(95.1483907732866,0.650599084958767,-6.87599584739916));
#36856=CARTESIAN_POINT('Ctrl Pts',(95.1738459935429,0.699609016294267,-6.8790059760604));
#36857=CARTESIAN_POINT('Ctrl Pts',(95.2020387358882,0.747098015528137,-6.88201610472164));
#36858=CARTESIAN_POINT('Ctrl Pts',(95.2301813717866,0.794502613429398,-6.88502088353609));
#36859=CARTESIAN_POINT('Ctrl Pts',(95.261051607042,0.840391193152243,-6.88802566235053));
#36860=CARTESIAN_POINT('Ctrl Pts',(95.2944587523897,0.884434557028695,-6.89103044116498));
#36861=CARTESIAN_POINT('Ctrl Pts',(95.3278328469018,0.928434347293419,-6.8940322472486));
#36862=CARTESIAN_POINT('Ctrl Pts',(95.3637385620232,0.970592119309378,-6.89703405333222));
#36863=CARTESIAN_POINT('Ctrl Pts',(95.4019416407734,1.01060713520026,-6.90003585941584));
#36864=CARTESIAN_POINT('Ctrl Pts',(95.4401220131984,1.05059836782555,-6.90303588135044));
#36865=CARTESIAN_POINT('Ctrl Pts',(95.4805966788677,1.08844898739582,-6.90603590328504));
#36866=CARTESIAN_POINT('Ctrl Pts',(95.5230922900105,1.12389267766819,-6.90903592521964));
#36867=CARTESIAN_POINT('Ctrl Pts',(95.5655794272716,1.15932930025439,-6.91203534893172));
#36868=CARTESIAN_POINT('Ctrl Pts',(95.6100863043492,1.1923596086404,-6.91503477264381));
#36869=CARTESIAN_POINT('Ctrl Pts',(95.6563057872485,1.22275694980396,-6.9180341963559));
#36870=CARTESIAN_POINT('Ctrl Pts',(95.702567762268,1.25318223692004,-6.92103637760366));
#36871=CARTESIAN_POINT('Ctrl Pts',(95.7505450465516,1.28096942988863,-6.92403855885142));
#36872=CARTESIAN_POINT('Ctrl Pts',(95.7999019994357,1.30593556526737,-6.92704074009918));
#36873=CARTESIAN_POINT('Ctrl Pts',(95.8492814185092,1.33091306467673,-6.9300442878732));
#36874=CARTESIAN_POINT('Ctrl Pts',(95.9000412731775,1.35306673514891,-6.93304783564722));
#36875=CARTESIAN_POINT('Ctrl Pts',(95.9518248368109,1.37226134863066,-6.93605138342124));
#36876=CARTESIAN_POINT('Ctrl Pts',(96.0037061332057,1.39149218871501,-6.93906059988621));
#36877=CARTESIAN_POINT('Ctrl Pts',(96.0566144921403,1.4077526599331,-6.94206981635118));
#36878=CARTESIAN_POINT('Ctrl Pts',(96.1101780084611,1.42095745870365,-6.94507903281614));
#36879=CARTESIAN_POINT('Ctrl Pts',(96.1511562936526,1.43105967093846,-6.94738120673926));
#36880=CARTESIAN_POINT('Ctrl Pts',(96.1925177034025,1.43937446924748,-6.94968338066238));
#36881=CARTESIAN_POINT('Ctrl Pts',(96.2340933970198,1.44588413299515,-6.9519855545855));
#36882=CARTESIAN_POINT('Ctrl Pts',(96.2884542711968,1.45439562086543,-6.95499568324673));
#36883=CARTESIAN_POINT('Ctrl Pts',(96.3434100401121,1.45985502291366,-6.95800581190796));
#36884=CARTESIAN_POINT('Ctrl Pts',(96.3985877587826,1.46219064520783,-6.9610159405692));
#36885=CARTESIAN_POINT('Ctrl Pts',(96.4536674110997,1.46452211644307,-6.96402071938364));
#36886=CARTESIAN_POINT('Ctrl Pts',(96.508967706973,1.46374080342766,-6.96702549819809));
#36887=CARTESIAN_POINT('Ctrl Pts',(96.5641087426303,1.45982654123937,-6.97003027701254));
#36888=CARTESIAN_POINT('Ctrl Pts',(96.6191952253683,1.45591615156502,-6.97303208309616));
#36889=CARTESIAN_POINT('Ctrl Pts',(96.6741222358115,1.448878989957,-6.97603388917977));
#36890=CARTESIAN_POINT('Ctrl Pts',(96.7285099008003,1.43874693094586,-6.97903569526339));
#36891=CARTESIAN_POINT('Ctrl Pts',(96.7828652400171,1.42862089401031,-6.98203571719799));
#36892=CARTESIAN_POINT('Ctrl Pts',(96.8366813510123,1.41540370216642,-6.98503573913259));
#36893=CARTESIAN_POINT('Ctrl Pts',(96.8895858306163,1.39917877737916,-6.98803576106719));
#36894=CARTESIAN_POINT('Ctrl Pts',(96.9424797607473,1.38295708793995,-6.99103518477928));
#36895=CARTESIAN_POINT('Ctrl Pts',(96.9944619158818,1.36372901141448,-6.99403460849137));
#36896=CARTESIAN_POINT('Ctrl Pts',(97.0451746512045,1.34162793846771,-6.99703403220346));
#36897=CARTESIAN_POINT('Ctrl Pts',(97.0959340095421,1.31950654678549,-7.00003621345122));
#36898=CARTESIAN_POINT('Ctrl Pts',(97.1454211312806,1.29450709314458,-7.00303839469898));
#36899=CARTESIAN_POINT('Ctrl Pts',(97.1932993868719,1.26681071512705,-7.00604057594674));
#36900=CARTESIAN_POINT('Ctrl Pts',(97.2411994355822,1.23910173033309,-7.00904412372076));
#36901=CARTESIAN_POINT('Ctrl Pts',(97.2874887161502,1.20869366453079,-7.01204767149478));
#36902=CARTESIAN_POINT('Ctrl Pts',(97.3318590574115,1.17581139779589,-7.01505121926879));
#36903=CARTESIAN_POINT('Ctrl Pts',(97.3763131402248,1.14286707131635,-7.01806043573376));
#36904=CARTESIAN_POINT('Ctrl Pts',(97.4188406421111,1.10743955443045,-7.02106965219873));
#36905=CARTESIAN_POINT('Ctrl Pts',(97.4591669115095,1.06979371817143,-7.0240788686637));
#36906=CARTESIAN_POINT('Ctrl Pts',(97.4900181603,1.04099311058523,-7.02638104258681));
#36907=CARTESIAN_POINT('Ctrl Pts',(97.5195817395779,1.01089498991801,-7.02868321650993));
#36908=CARTESIAN_POINT('Ctrl Pts',(97.5477505539431,0.97963108230674,-7.03098539043305));
#36909=CARTESIAN_POINT('Ctrl Pts',(97.584188794614,0.939189132032247,-7.03396340599271));
#36910=CARTESIAN_POINT('Ctrl Pts',(97.6184523334827,0.896617035648177,-7.03694142155236));
#36911=CARTESIAN_POINT('Ctrl Pts',(97.6502795702539,0.852180434083894,-7.03991943711201));
#36912=CARTESIAN_POINT('Ctrl Pts',(97.6820603240518,0.80780873119042,-7.04289310334601));
#36913=CARTESIAN_POINT('Ctrl Pts',(97.7114115077978,0.761578348566087,-7.04586676958));
#36914=CARTESIAN_POINT('Ctrl Pts',(97.7381102812762,0.713789563374084,-7.04884043581399));
#36915=CARTESIAN_POINT('Ctrl Pts',(97.7647811609684,0.666050705949744,-7.05181099528316));
#36916=CARTESIAN_POINT('Ctrl Pts',(97.7888048572825,0.616757140291628,-7.05478155475234));
#36917=CARTESIAN_POINT('Ctrl Pts',(97.8100019850866,0.566237781075439,-7.05775211422151));
#36918=CARTESIAN_POINT('Ctrl Pts',(97.8311912990912,0.51573704457758,-7.06072157866704));
#36919=CARTESIAN_POINT('Ctrl Pts',(97.8495558883255,0.4640119020712,-7.06369104311258));
#36920=CARTESIAN_POINT('Ctrl Pts',(97.8649634682578,0.411413544648343,-7.06666050755811));
#36921=CARTESIAN_POINT('Ctrl Pts',(97.880367471045,0.358827398874208,-7.06962928258941));
#36922=CARTESIAN_POINT('Ctrl Pts',(97.892815681147,0.305368960812963,-7.0725980576207));
#36923=CARTESIAN_POINT('Ctrl Pts',(97.9022257719699,0.251404290144893,-7.075566832652));
#36924=CARTESIAN_POINT('Ctrl Pts',(97.9116425082685,0.197401509227816,-7.07853770425415));
#36925=CARTESIAN_POINT('Ctrl Pts',(97.9180167573192,0.142892316245049,-7.08150857585629));
#36926=CARTESIAN_POINT('Ctrl Pts',(97.9213177137636,0.088250769973256,-7.08447944745844));
#36927=CARTESIAN_POINT('Ctrl Pts',(97.9231197467293,0.0584212737836033,
-7.08610128302465));
#36928=CARTESIAN_POINT('Ctrl Pts',(97.924006786112,0.0285524121465811,-7.08772311859086));
#36929=CARTESIAN_POINT('Ctrl Pts',(97.92398037669,-0.00129492856329451,
-7.08934495415707));
#36930=CARTESIAN_POINT('Origin',(96.460480949577,-8.32667268468867E-16,
1.18130019239114E-14));
#36931=CARTESIAN_POINT('',(97.9239808632502,0.000502671547986457,-7.66065504587107));
#36932=CARTESIAN_POINT('',(97.9239808370566,0.000573887927501785,-7.58934495418715));
#36933=CARTESIAN_POINT('',(97.923980949577,-1.01189432752408E-15,1.19922289829666E-14));
#36934=CARTESIAN_POINT('Ctrl Pts',(97.92398086325,0.000502672062914034,
-7.66065504584291));
#36935=CARTESIAN_POINT('Ctrl Pts',(97.9239711281533,0.0288458290411993,
-7.65910533372452));
#36936=CARTESIAN_POINT('Ctrl Pts',(97.9231380787271,0.0571737031003787,
-7.65755562160613));
#36937=CARTESIAN_POINT('Ctrl Pts',(97.9214840360923,0.0854530935234917,
-7.65600590948774));
#36938=CARTESIAN_POINT('Ctrl Pts',(97.918271258001,0.140382394666001,-7.65299578082649));
#36939=CARTESIAN_POINT('Ctrl Pts',(97.9119496588756,0.195245670108786,-7.64998565216525));
#36940=CARTESIAN_POINT('Ctrl Pts',(97.9025282822349,0.249663253952477,-7.646975523504));
#36941=CARTESIAN_POINT('Ctrl Pts',(97.8931236500352,0.303984122416502,-7.64397074468955));
#36942=CARTESIAN_POINT('Ctrl Pts',(97.8806302626854,0.357860355082166,-7.6409659658751));
#36943=CARTESIAN_POINT('Ctrl Pts',(97.8651089962332,0.410916415523629,-7.63796118706064));
#36944=CARTESIAN_POINT('Ctrl Pts',(97.8496030855027,0.463919985783276,-7.63495938097702));
#36945=CARTESIAN_POINT('Ctrl Pts',(97.8310753773326,0.51610448683195,-7.63195757489339));
#36946=CARTESIAN_POINT('Ctrl Pts',(97.8096375965919,0.567105450349019,-7.62895576880977));
#36947=CARTESIAN_POINT('Ctrl Pts',(97.7882125575788,0.618076101008883,-7.62595574687516));
#36948=CARTESIAN_POINT('Ctrl Pts',(97.7638810784644,0.667864122530152,-7.62295572494056));
#36949=CARTESIAN_POINT('Ctrl Pts',(97.7368036741354,0.716123280431402,-7.61995570300596));
#36950=CARTESIAN_POINT('Ctrl Pts',(97.7097316692045,0.764372815164853,-7.61695627929387));
#36951=CARTESIAN_POINT('Ctrl Pts',(97.6799150847523,0.811093631412987,-7.61395685558177));
#36952=CARTESIAN_POINT('Ctrl Pts',(97.6475601369233,0.855964516185827,-7.61095743186968));
#36953=CARTESIAN_POINT('Ctrl Pts',(97.6151754434061,0.900876653238153,-7.60795525062192));
#36954=CARTESIAN_POINT('Ctrl Pts',(97.5802480337135,0.943935031661751,-7.60495306937416));
#36955=CARTESIAN_POINT('Ctrl Pts',(97.5430263268552,0.984849103230332,-7.6019508881264));
#36956=CARTESIAN_POINT('Ctrl Pts',(97.5057876775023,1.02578179797606,-7.59894734035238));
#36957=CARTESIAN_POINT('Ctrl Pts',(97.4662530268612,1.06456786970337,-7.59594379257836));
#36958=CARTESIAN_POINT('Ctrl Pts',(97.4247075047286,1.10095385931496,-7.59294024480434));
#36959=CARTESIAN_POINT('Ctrl Pts',(97.3830835724148,1.13740852135842,-7.58993102833937));
#36960=CARTESIAN_POINT('Ctrl Pts',(97.3394416045668,1.17145372677336,-7.5869218118744));
#36961=CARTESIAN_POINT('Ctrl Pts',(97.2940987020515,1.20287725589913,-7.58391259540943));
#36962=CARTESIAN_POINT('Ctrl Pts',(97.2594095233291,1.22691754351777,-7.58161042148635));
#36963=CARTESIAN_POINT('Ctrl Pts',(97.2237254860201,1.24942424404664,-7.57930824756327));
#36964=CARTESIAN_POINT('Ctrl Pts',(97.1871980350955,1.27032063968725,-7.57700607364019));
#36965=CARTESIAN_POINT('Ctrl Pts',(97.139437817743,1.29764300608345,-7.57399594497896));
#36966=CARTESIAN_POINT('Ctrl Pts',(97.0900342510819,1.32232557501299,-7.57098581631772));
#36967=CARTESIAN_POINT('Ctrl Pts',(97.0393102568641,1.34416847270924,-7.56797568765649));
#36968=CARTESIAN_POINT('Ctrl Pts',(96.9886764134766,1.36597254942163,-7.56497090884205));
#36969=CARTESIAN_POINT('Ctrl Pts',(96.9367272808478,1.38494676331364,-7.56196613002761));
#36970=CARTESIAN_POINT('Ctrl Pts',(96.8838106432748,1.40093690808463,-7.55896135121318));
#36971=CARTESIAN_POINT('Ctrl Pts',(96.8309463579478,1.41691123325652,-7.55595954512956));
#36972=CARTESIAN_POINT('Ctrl Pts',(96.7771169668699,1.42990718554583,-7.55295773904595));
#36973=CARTESIAN_POINT('Ctrl Pts',(96.7226887680985,1.4398191934775,-7.54995593296233));
#36974=CARTESIAN_POINT('Ctrl Pts',(96.6682929191908,1.44972531012279,-7.54695591102774));
#36975=CARTESIAN_POINT('Ctrl Pts',(96.6132994865528,1.45655102104358,-7.54395588909314));
#36976=CARTESIAN_POINT('Ctrl Pts',(96.558086155585,1.46024158061607,-7.54095586715855));
#36977=CARTESIAN_POINT('Ctrl Pts',(96.5028838344892,1.46393140426868,-7.53795644344646));
#36978=CARTESIAN_POINT('Ctrl Pts',(96.4474622287907,1.46448728292819,-7.53495701973437));
#36979=CARTESIAN_POINT('Ctrl Pts',(96.3922030387056,1.46190641864896,-7.53195759602229));
#36980=CARTESIAN_POINT('Ctrl Pts',(96.3368930457988,1.45932318163884,-7.52895541477453));
#36981=CARTESIAN_POINT('Ctrl Pts',(96.2817462954972,1.45359746496226,-7.52595323352677));
#36982=CARTESIAN_POINT('Ctrl Pts',(96.2271418649315,1.44477857181534,-7.52295105227902));
#36983=CARTESIAN_POINT('Ctrl Pts',(96.1725125796411,1.43595566450402,-7.519947504505));
#36984=CARTESIAN_POINT('Ctrl Pts',(96.1184266228099,1.42403688793133,-7.51694395673099));
#36985=CARTESIAN_POINT('Ctrl Pts',(96.0652520670549,1.40912255691983,-7.51394040895697));
#36986=CARTESIAN_POINT('Ctrl Pts',(96.0119771532747,1.39418007761852,-7.51093119249201));
#36987=CARTESIAN_POINT('Ctrl Pts',(95.9596175775726,1.37623092160277,-7.50792197602704));
#36988=CARTESIAN_POINT('Ctrl Pts',(95.9085243422947,1.35542471339334,-7.50491275956208));
#36989=CARTESIAN_POINT('Ctrl Pts',(95.8694359233405,1.3395071114072,-7.50261058563893));
#36990=CARTESIAN_POINT('Ctrl Pts',(95.8310883380211,1.32191834261455,-7.50030841171577));
#36991=CARTESIAN_POINT('Ctrl Pts',(95.7936285884951,1.30274332795046,-7.49800623779262));
#36992=CARTESIAN_POINT('Ctrl Pts',(95.7446493760397,1.2776716942917,-7.49499610913138));
#36993=CARTESIAN_POINT('Ctrl Pts',(95.6969831453964,1.24978133638675,-7.49198598047014));
#36994=CARTESIAN_POINT('Ctrl Pts',(95.6509737394014,1.21923349965204,-7.48897585180891));
#36995=CARTESIAN_POINT('Ctrl Pts',(95.6050461050849,1.18873995503065,-7.48597107299446));
#36996=CARTESIAN_POINT('Ctrl Pts',(95.5607698881623,1.15559859433539,-7.48296629418001));
#36997=CARTESIAN_POINT('Ctrl Pts',(95.5184642685352,1.12001643855746,-7.47996151536557));
#36998=CARTESIAN_POINT('Ctrl Pts',(95.4762005033097,1.08446948542766,-7.47695970928195));
#36999=CARTESIAN_POINT('Ctrl Pts',(95.4359038755366,1.04648685900662,-7.47395790319833));
#37000=CARTESIAN_POINT('Ctrl Pts',(95.3978629479879,1.00631765993588,-7.47095609711471));
#37001=CARTESIAN_POINT('Ctrl Pts',(95.3598446303887,0.966172335770845,-7.46795607518011));
#37002=CARTESIAN_POINT('Ctrl Pts',(95.3240797180821,0.923843397553606,-7.46495605324551));
#37003=CARTESIAN_POINT('Ctrl Pts',(95.2908204278217,0.879617254177741,-7.46195603131091));
#37004=CARTESIAN_POINT('Ctrl Pts',(95.2575677696649,0.835399929762189,-7.45895660759881));
#37005=CARTESIAN_POINT('Ctrl Pts',(95.2268200585374,0.789286573348786,-7.45595718388672));
#37006=CARTESIAN_POINT('Ctrl Pts',(95.1987881972936,0.741595340354497,-7.45295776017463));
#37007=CARTESIAN_POINT('Ctrl Pts',(95.1707305648135,0.693860262179053,-7.44995557892687));
#37008=CARTESIAN_POINT('Ctrl Pts',(95.145394038746,0.644544865525138,-7.44695339767911));
#37009=CARTESIAN_POINT('Ctrl Pts',(95.1229444525937,0.593993576764662,-7.44395121643135));
#37010=CARTESIAN_POINT('Ctrl Pts',(95.1004846478881,0.543419278179704,-7.44094766865733));
#37011=CARTESIAN_POINT('Ctrl Pts',(95.0809145895451,0.491608460990693,-7.43794412088331));
#37012=CARTESIAN_POINT('Ctrl Pts',(95.064351374634,0.438924207545438,-7.43494057310929));
#37013=CARTESIAN_POINT('Ctrl Pts',(95.0477568994422,0.386140521438198,-7.43193135664432));
#37014=CARTESIAN_POINT('Ctrl Pts',(95.0341807340498,0.332480619252014,-7.42892214017936));
#37015=CARTESIAN_POINT('Ctrl Pts',(95.0236893501979,0.278320229149122,-7.42591292371439));
#37016=CARTESIAN_POINT('Ctrl Pts',(95.0156630115804,0.236885311052697,-7.42361074979128));
#37017=CARTESIAN_POINT('Ctrl Pts',(95.0094411087291,0.195157742080686,-7.42130857586817));
#37018=CARTESIAN_POINT('Ctrl Pts',(95.0050328394778,0.153307040962721,-7.41900640194506));
#37019=CARTESIAN_POINT('Ctrl Pts',(94.9992689580063,0.0985865901473129,
-7.41599627328382));
#37020=CARTESIAN_POINT('Ctrl Pts',(94.9965832420588,0.0434256570727678,
-7.41298614462259));
#37021=CARTESIAN_POINT('Ctrl Pts',(94.9970285186357,-0.0117996767691671,
-7.40997601596135));
#37022=CARTESIAN_POINT('Ctrl Pts',(94.9974730038305,-0.0669268596320551,
-7.4069712371469));
#37023=CARTESIAN_POINT('Ctrl Pts',(95.001037434229,-0.122117692291472,-7.40396645833246));
#37024=CARTESIAN_POINT('Ctrl Pts',(95.0077228228246,-0.176991737532955,
-7.40096167951802));
#37025=CARTESIAN_POINT('Ctrl Pts',(95.0144015973358,-0.231811493997847,
-7.3979598734344));
#37026=CARTESIAN_POINT('Ctrl Pts',(95.0241951499612,-0.286314562229797,
-7.39495806735078));
#37027=CARTESIAN_POINT('Ctrl Pts',(95.0370525217755,-0.340123155528405,
-7.39195626126716));
#37028=CARTESIAN_POINT('Ctrl Pts',(95.0499022517013,-0.393899767231153,
-7.38895623933256));
#37029=CARTESIAN_POINT('Ctrl Pts',(95.0658120689693,-0.446982209501575,
-7.38595621739796));
#37030=CARTESIAN_POINT('Ctrl Pts',(95.0846799086669,-0.499002751325654,
-7.38295619546336));
#37031=CARTESIAN_POINT('Ctrl Pts',(95.1035439860032,-0.55101291993925,-7.37995677175127));
#37032=CARTESIAN_POINT('Ctrl Pts',(95.1253647343889,-0.601961112440803,
-7.37695734803918));
#37033=CARTESIAN_POINT('Ctrl Pts',(95.1499909265914,-0.65149685314294,-7.37395792432708));
#37034=CARTESIAN_POINT('Ctrl Pts',(95.1746397590108,-0.701078134783912,
-7.37095574307932));
#37035=CARTESIAN_POINT('Ctrl Pts',(95.2020989525488,-0.749243896384251,
-7.36795356183157));
#37036=CARTESIAN_POINT('Ctrl Pts',(95.2321706516241,-0.795667054705019,
-7.36495138058381));
#37037=CARTESIAN_POINT('Ctrl Pts',(95.2622560386694,-0.842111343816925,
-7.36194783280979));
#37038=CARTESIAN_POINT('Ctrl Pts',(95.2949559893923,-0.886811021489771,
-7.35894428503577));
#37039=CARTESIAN_POINT('Ctrl Pts',(95.3300303939341,-0.929469629007074,
-7.35594073726175));
#37040=CARTESIAN_POINT('Ctrl Pts',(95.3651709955116,-0.972208747466919,
-7.35293152079679));
#37041=CARTESIAN_POINT('Ctrl Pts',(95.4026946442625,-1.01289871126401,-7.34992230433182));
#37042=CARTESIAN_POINT('Ctrl Pts',(95.4423229776373,-1.05127855213337,-7.34691308786686));
#37043=CARTESIAN_POINT('Ctrl Pts',(95.4726402767663,-1.0806407033284,-7.34461091394374));
#37044=CARTESIAN_POINT('Ctrl Pts',(95.5041886154988,-1.10865149429615,-7.34230874002061));
#37045=CARTESIAN_POINT('Ctrl Pts',(95.5368310429968,-1.13521059723487,-7.34000656609749));
#37046=CARTESIAN_POINT('Ctrl Pts',(95.5795115310335,-1.16993704260449,-7.33699643743626));
#37047=CARTESIAN_POINT('Ctrl Pts',(95.6242428323756,-1.20232611928237,-7.33398630877502));
#37048=CARTESIAN_POINT('Ctrl Pts',(95.6707388331178,-1.23212809378348,-7.33097618011378));
#37049=CARTESIAN_POINT('Ctrl Pts',(95.7171521973655,-1.26187710177862,-7.32797140129934));
#37050=CARTESIAN_POINT('Ctrl Pts',(95.7653235958424,-1.2890478496978,-7.32496662248489));
#37051=CARTESIAN_POINT('Ctrl Pts',(95.8149349556383,-1.31343161973118,-7.32196184367045));
#37052=CARTESIAN_POINT('Ctrl Pts',(95.864497233213,-1.33779126606386,-7.31896003758683));
#37053=CARTESIAN_POINT('Ctrl Pts',(95.9154961784037,-1.35936916469073,-7.31595823150321));
#37054=CARTESIAN_POINT('Ctrl Pts',(95.9675875409249,-1.37800157391323,-7.31295642541959));
#37055=CARTESIAN_POINT('Ctrl Pts',(96.019647942501,-1.39662290880455,-7.30995640348499));
#37056=CARTESIAN_POINT('Ctrl Pts',(96.0727989782063,-1.41230204673811,-7.30695638155039));
#37057=CARTESIAN_POINT('Ctrl Pts',(96.1266768955525,-1.42492354304251,-7.30395635961579));
#37058=CARTESIAN_POINT('Ctrl Pts',(96.1805440693163,-1.43754252254425,-7.3009569359037));
#37059=CARTESIAN_POINT('Ctrl Pts',(96.23513732296,-1.44710495089071,-7.29795751219161));
#37060=CARTESIAN_POINT('Ctrl Pts',(96.2900804936969,-1.45354598641937,-7.29495808847952));
#37061=CARTESIAN_POINT('Ctrl Pts',(96.3450741767213,-1.45999294354728,-7.29195590723176));
#37062=CARTESIAN_POINT('Ctrl Pts',(96.4004178938987,-1.46331271300988,-7.288953725984));
#37063=CARTESIAN_POINT('Ctrl Pts',(96.4557295967009,-1.46349228718359,-7.28595154473624));
#37064=CARTESIAN_POINT('Ctrl Pts',(96.5110664761623,-1.46367194309547,-7.28294799696222));
#37065=CARTESIAN_POINT('Ctrl Pts',(96.5663707839206,-1.46070858272003,-7.2799444491882));
#37066=CARTESIAN_POINT('Ctrl Pts',(96.6212630327378,-1.45464132064728,-7.27694090141418));
#37067=CARTESIAN_POINT('Ctrl Pts',(96.6762588814367,-1.44856260763845,-7.27393168494921));
#37068=CARTESIAN_POINT('Ctrl Pts',(96.7308405955774,-1.43936837842359,-7.27092246848425));
#37069=CARTESIAN_POINT('Ctrl Pts',(96.7846375110102,-1.4271491770939,-7.26791325201928));
#37070=CARTESIAN_POINT('Ctrl Pts',(96.8257943560879,-1.41780098729431,-7.26561107809616));
#37071=CARTESIAN_POINT('Ctrl Pts',(96.8664920358128,-1.40668339077259,-7.26330890417304));
#37072=CARTESIAN_POINT('Ctrl Pts',(96.9065716935508,-1.39385626882433,-7.26100673024993));
#37073=CARTESIAN_POINT('Ctrl Pts',(96.9589764772547,-1.37708460486363,-7.25799660158869));
#37074=CARTESIAN_POINT('Ctrl Pts',(97.0105442081131,-1.35731820048866,-7.25498647292745));
#37075=CARTESIAN_POINT('Ctrl Pts',(97.0609093960967,-1.33466023039945,-7.25197634426622));
#37076=CARTESIAN_POINT('Ctrl Pts',(97.1111850709499,-1.31204252990742,-7.24897156545177));
#37077=CARTESIAN_POINT('Ctrl Pts',(97.1602619666023,-1.28654367725036,-7.24596678663733));
#37078=CARTESIAN_POINT('Ctrl Pts',(97.2077914824816,-1.25831602445883,-7.24296200782288));
#37079=CARTESIAN_POINT('Ctrl Pts',(97.2552739757793,-1.23011629825316,-7.23996020173926));
#37080=CARTESIAN_POINT('Ctrl Pts',(97.301211670054,-1.19919338822766,-7.23695839565564));
#37081=CARTESIAN_POINT('Ctrl Pts',(97.3452793302217,-1.16574614544011,-7.23395658957202));
#37082=CARTESIAN_POINT('Ctrl Pts',(97.3893207984002,-1.13231878230627,-7.23095656763743));
#37083=CARTESIAN_POINT('Ctrl Pts',(97.4314940156502,-1.09637037886917,-7.22795654570282));
#37084=CARTESIAN_POINT('Ctrl Pts',(97.4715035410207,-1.0581425091123,-7.22495652376823));
#37085=CARTESIAN_POINT('Ctrl Pts',(97.51150508825,-1.01992226222374,-7.22195710005614));
#37086=CARTESIAN_POINT('Ctrl Pts',(97.5493434188221,-0.979423816342423,
-7.21895767634405));
#37087=CARTESIAN_POINT('Ctrl Pts',(97.5847586922295,-0.936926788695987,
-7.21595825263196));
#37088=CARTESIAN_POINT('Ctrl Pts',(97.6202065248513,-0.894390691187875,
-7.2129560713842));
#37089=CARTESIAN_POINT('Ctrl Pts',(97.6532265109286,-0.849852747592014,
-7.20995389013644));
#37090=CARTESIAN_POINT('Ctrl Pts',(97.6835990064107,-0.8036258265184,-7.20695170888868));
#37091=CARTESIAN_POINT('Ctrl Pts',(97.7139853267784,-0.757377863976492,
-7.20394816111467));
#37092=CARTESIAN_POINT('Ctrl Pts',(97.7417214893671,-0.709439849351401,
-7.20094461334065));
#37093=CARTESIAN_POINT('Ctrl Pts',(97.7666329033613,-0.660150985476467,
-7.19794106556663));
#37094=CARTESIAN_POINT('Ctrl Pts',(97.791591333457,-0.610769097165929,-7.19493184910166));
#37095=CARTESIAN_POINT('Ctrl Pts',(97.8137141533856,-0.560031751868831,
-7.1919226326367));
#37096=CARTESIAN_POINT('Ctrl Pts',(97.8328746668239,-0.508298863722117,
-7.18891341617173));
#37097=CARTESIAN_POINT('Ctrl Pts',(97.8475332448641,-0.468721084108819,
-7.18661124224861));
#37098=CARTESIAN_POINT('Ctrl Pts',(97.8604590110083,-0.428561070948875,
-7.18430906832549));
#37099=CARTESIAN_POINT('Ctrl Pts',(97.8716153188119,-0.387984589853705,
-7.18200689440237));
#37100=CARTESIAN_POINT('Ctrl Pts',(97.8898814412655,-0.321549082204936,
-7.17823756573832));
#37101=CARTESIAN_POINT('Ctrl Pts',(97.9034650875488,-0.253774761264491,
-7.17446823707427));
#37102=CARTESIAN_POINT('Ctrl Pts',(97.9122095811533,-0.185246404179905,
-7.17069890841022));
#37103=CARTESIAN_POINT('Ctrl Pts',(97.919976524955,-0.124378854568375,-7.16735095423151));
#37104=CARTESIAN_POINT('Ctrl Pts',(97.9239263130642,-0.0629165758066123,
-7.1640030000528));
#37105=CARTESIAN_POINT('Ctrl Pts',(97.9239803863197,-0.00128399919637083,
-7.16065504587409));
#37106=CARTESIAN_POINT('Ctrl Pts',(97.9239803766892,-0.00129492944525746,
-7.08934495420499));
#37107=CARTESIAN_POINT('Ctrl Pts',(97.923918208247,-0.0715562706037072,
-7.0931627932256));
#37108=CARTESIAN_POINT('Ctrl Pts',(97.9187924004044,-0.141595414215573,
-7.0969806322462));
#37109=CARTESIAN_POINT('Ctrl Pts',(97.9087212224606,-0.210789852692321,
-7.1007984712668));
#37110=CARTESIAN_POINT('Ctrl Pts',(97.900643228254,-0.266290041077624,-7.10386072293807));
#37111=CARTESIAN_POINT('Ctrl Pts',(97.8893846145948,-0.321247370882346,
-7.10692297460935));
#37112=CARTESIAN_POINT('Ctrl Pts',(97.8750281893846,-0.375350977556835,
-7.10998522628062));
#37113=CARTESIAN_POINT('Ctrl Pts',(97.8609161268772,-0.428533679244946,
-7.11299535494185));
#37114=CARTESIAN_POINT('Ctrl Pts',(97.8437709800176,-0.48103116058418,-7.11600548360309));
#37115=CARTESIAN_POINT('Ctrl Pts',(97.8236773919737,-0.532473200674981,
-7.11901561226433));
#37116=CARTESIAN_POINT('Ctrl Pts',(97.8036195158975,-0.583823813765773,
-7.12202039107877));
#37117=CARTESIAN_POINT('Ctrl Pts',(97.7806237884638,-0.634122220236565,
-7.12502516989322));
#37118=CARTESIAN_POINT('Ctrl Pts',(97.7548248181123,-0.683012591381024,
-7.12802994870766));
#37119=CARTESIAN_POINT('Ctrl Pts',(97.7290513715678,-0.731854593603062,
-7.13103175479128));
#37120=CARTESIAN_POINT('Ctrl Pts',(97.7004804212265,-0.779290855221356,
-7.1340335608749));
#37121=CARTESIAN_POINT('Ctrl Pts',(97.6692941919306,-0.824986542381567,
-7.13703536695852));
#37122=CARTESIAN_POINT('Ctrl Pts',(97.6381264984357,-0.870655069920795,
-7.14003538889312));
#37123=CARTESIAN_POINT('Ctrl Pts',(97.6043469040442,-0.914584638159508,
-7.14303541082771));
#37124=CARTESIAN_POINT('Ctrl Pts',(97.5681818023395,-0.956468018696541,
-7.14603543276231));
#37125=CARTESIAN_POINT('Ctrl Pts',(97.5320239121746,-0.998343047434352,
-7.1490348564744));
#37126=CARTESIAN_POINT('Ctrl Pts',(97.4934818043415,-1.03817229928613,-7.15203428018649));
#37127=CARTESIAN_POINT('Ctrl Pts',(97.4528216597379,-1.07568218585111,-7.15503370389859));
#37128=CARTESIAN_POINT('Ctrl Pts',(97.4121241340205,-1.11322655732384,-7.15803588514634));
#37129=CARTESIAN_POINT('Ctrl Pts',(97.3693050702268,-1.14844694454677,-7.1610380663941));
#37130=CARTESIAN_POINT('Ctrl Pts',(97.3246658821713,-1.1811082305517,-7.16404024764186));
#37131=CARTESIAN_POINT('Ctrl Pts',(97.2800063753483,-1.21378438324898,-7.16704379541587));
#37132=CARTESIAN_POINT('Ctrl Pts',(97.2335255367407,-1.24389882502807,-7.17004734318989));
#37133=CARTESIAN_POINT('Ctrl Pts',(97.1855533492081,-1.27126010921966,-7.17305089096391));
#37134=CARTESIAN_POINT('Ctrl Pts',(97.137490622245,-1.29867303323045,-7.17606010742887));
#37135=CARTESIAN_POINT('Ctrl Pts',(97.0879313976346,-1.32332218383262,-7.17906932389384));
#37136=CARTESIAN_POINT('Ctrl Pts',(97.0372287545369,-1.34506290539661,-7.1820785403588));
#37137=CARTESIAN_POINT('Ctrl Pts',(96.9984391546088,-1.36169544839816,-7.18438071428192));
#37138=CARTESIAN_POINT('Ctrl Pts',(96.9589808206018,-1.3766266896331,-7.18668288820505));
#37139=CARTESIAN_POINT('Ctrl Pts',(96.9190174629403,-1.38981168361495,-7.18898506212817));
#37140=CARTESIAN_POINT('Ctrl Pts',(96.8667647434183,-1.40705127089564,-7.19199519078941));
#37141=CARTESIAN_POINT('Ctrl Pts',(96.8134286489963,-1.42137616669333,-7.19500531945064));
#37142=CARTESIAN_POINT('Ctrl Pts',(96.7593654983363,-1.43265497469313,-7.19801544811188));
#37143=CARTESIAN_POINT('Ctrl Pts',(96.7053984331283,-1.44391373707309,-7.20102022692632));
#37144=CARTESIAN_POINT('Ctrl Pts',(96.6507073888337,-1.4521370483083,-7.20402500574077));
#37145=CARTESIAN_POINT('Ctrl Pts',(96.5956639310935,-1.45724322318147,-7.20702978455521));
#37146=CARTESIAN_POINT('Ctrl Pts',(96.5406749297354,-1.46234434634056,-7.21003159063883));
#37147=CARTESIAN_POINT('Ctrl Pts',(96.485334728873,-1.46433439363332,-7.21303339672245));
#37148=CARTESIAN_POINT('Ctrl Pts',(96.4300233278089,-1.4631830313656,-7.21603520280607));
#37149=CARTESIAN_POINT('Ctrl Pts',(96.3747448015473,-1.46203235341986,-7.21903522474067));
#37150=CARTESIAN_POINT('Ctrl Pts',(96.3194955681037,-1.457743977644,-7.22203524667527));
#37151=CARTESIAN_POINT('Ctrl Pts',(96.2646566400979,-1.45033964636461,-7.22503526860987));
#37152=CARTESIAN_POINT('Ctrl Pts',(96.2098286473058,-1.44293679155364,-7.22803469232196));
#37153=CARTESIAN_POINT('Ctrl Pts',(96.1554113205392,-1.43241928581964,-7.23103411603405));
#37154=CARTESIAN_POINT('Ctrl Pts',(96.1017792376444,-1.41886057519992,-7.23403353974614));
#37155=CARTESIAN_POINT('Ctrl Pts',(96.0480978478174,-1.40528939930961,-7.2370357209939));
#37156=CARTESIAN_POINT('Ctrl Pts',(95.9952036572684,-1.3886715623126,-7.24003790224166));
#37157=CARTESIAN_POINT('Ctrl Pts',(95.9434582741108,-1.3691310394019,-7.24304008348942));
#37158=CARTESIAN_POINT('Ctrl Pts',(95.8916893376034,-1.34958162207895,-7.24604363126344));
#37159=CARTESIAN_POINT('Ctrl Pts',(95.8410707343959,-1.32710708157954,-7.24904717903746));
#37160=CARTESIAN_POINT('Ctrl Pts',(95.7919431075654,-1.30187918172096,-7.25205072681147));
#37161=CARTESIAN_POINT('Ctrl Pts',(95.7427227606071,-1.27660366844707,-7.25505994327644));
#37162=CARTESIAN_POINT('Ctrl Pts',(95.6949994678199,-1.24856468317754,-7.25806915974141));
#37163=CARTESIAN_POINT('Ctrl Pts',(95.6490873032538,-1.21797889994298,-7.26107837620637));
#37164=CARTESIAN_POINT('Ctrl Pts',(95.6139626157317,-1.19457952226423,-7.26338055012949));
#37165=CARTESIAN_POINT('Ctrl Pts',(95.5798974205506,-1.16969047719016,-7.26568272405262));
#37166=CARTESIAN_POINT('Ctrl Pts',(95.5470188114984,-1.14342431856985,-7.26798489797574));
#37167=CARTESIAN_POINT('Ctrl Pts',(95.5040295123601,-1.10908090251014,-7.27099502663698));
#37168=CARTESIAN_POINT('Ctrl Pts',(95.4628893939892,-1.0722375548306,-7.27400515529821));
#37169=CARTESIAN_POINT('Ctrl Pts',(95.4239031954539,-1.03312090756948,-7.27701528395945));
#37170=CARTESIAN_POINT('Ctrl Pts',(95.3849862863786,-0.994073781612414,
-7.2800200627739));
#37171=CARTESIAN_POINT('Ctrl Pts',(95.348216069999,-0.95276174509638,-7.28302484158834));
#37172=CARTESIAN_POINT('Ctrl Pts',(95.3138639818906,-0.909451361763583,
-7.28602962040278));
#37173=CARTESIAN_POINT('Ctrl Pts',(95.2795458794822,-0.866183826879712,
-7.2890314264864));
#37174=CARTESIAN_POINT('Ctrl Pts',(95.2476414928095,-0.820922273318624,
-7.29203323257002));
#37175=CARTESIAN_POINT('Ctrl Pts',(95.218383857285,-0.773968386511854,-7.29503503865364));
#37176=CARTESIAN_POINT('Ctrl Pts',(95.1891436112855,-0.727042407147746,
-7.29803506058824));
#37177=CARTESIAN_POINT('Ctrl Pts',(95.1625472771441,-0.678426535530184,
-7.30103508252284));
#37178=CARTESIAN_POINT('Ctrl Pts',(95.138784828877,-0.628451759904116,-7.30403510445744));
#37179=CARTESIAN_POINT('Ctrl Pts',(95.1150271189857,-0.578486949550379,
-7.30703452816953));
#37180=CARTESIAN_POINT('Ctrl Pts',(95.094102399371,-0.527164250007825,-7.31003395188162));
#37181=CARTESIAN_POINT('Ctrl Pts',(95.0761538248649,-0.474837510930137,
-7.31303337559372));
#37182=CARTESIAN_POINT('Ctrl Pts',(95.0581887492442,-0.422462664994863,
-7.31603555684147));
#37183=CARTESIAN_POINT('Ctrl Pts',(95.0432054568902,-0.369082435972016,
-7.31903773808924));
#37184=CARTESIAN_POINT('Ctrl Pts',(95.0312976964958,-0.315067419947357,
-7.322039919337));
#37185=CARTESIAN_POINT('Ctrl Pts',(95.0193845159533,-0.261027817486447,
-7.32504346711101));
#37186=CARTESIAN_POINT('Ctrl Pts',(95.0105497423939,-0.206353374302305,
-7.32804701488503));
#37187=CARTESIAN_POINT('Ctrl Pts',(95.0048356450383,-0.15142323921522,-7.33105056265905));
#37188=CARTESIAN_POINT('Ctrl Pts',(94.9991107632855,-0.0963894327425316,
-7.33405977912402));
#37189=CARTESIAN_POINT('Ctrl Pts',(94.9965183482246,-0.0410994991782647,
-7.33706899558898));
#37190=CARTESIAN_POINT('Ctrl Pts',(94.9970485383513,0.0140651261685238,
-7.34007821205395));
#37191=CARTESIAN_POINT('Ctrl Pts',(94.9974541555272,0.0562683253835064,
-7.34238038597707));
#37192=CARTESIAN_POINT('Ctrl Pts',(94.9996863116939,0.0983981196657594,
-7.34468255990019));
#37193=CARTESIAN_POINT('Ctrl Pts',(95.0037201835205,0.140286565566228,-7.34698473382331));
#37194=CARTESIAN_POINT('Ctrl Pts',(95.0089945344629,0.195056368279004,-7.34999486248454));
#37195=CARTESIAN_POINT('Ctrl Pts',(95.0173730305296,0.249643385155405,-7.35300499114578));
#37196=CARTESIAN_POINT('Ctrl Pts',(95.0288323695198,0.303668558168467,-7.35601511980702));
#37197=CARTESIAN_POINT('Ctrl Pts',(95.0402713420357,0.35759771322645,-7.35901989862146));
#37198=CARTESIAN_POINT('Ctrl Pts',(95.054780182562,0.410966493616192,-7.3620246774359));
#37199=CARTESIAN_POINT('Ctrl Pts',(95.0722839481235,0.463401915355771,-7.36502945625035));
#37200=CARTESIAN_POINT('Ctrl Pts',(95.0897703966089,0.515785460932704,-7.36803126233397));
#37201=CARTESIAN_POINT('Ctrl Pts',(95.110245734204,0.567236978598275,-7.37103306841759));
#37202=CARTESIAN_POINT('Ctrl Pts',(95.1335846208753,0.617396455187357,-7.37403487450121));
#37203=CARTESIAN_POINT('Ctrl Pts',(95.1569096358805,0.667526119064179,-7.37703489643581));
#37204=CARTESIAN_POINT('Ctrl Pts',(95.1830946041882,0.716364786097731,-7.38003491837041));
#37205=CARTESIAN_POINT('Ctrl Pts',(95.2119661152921,0.763572497259179,-7.38303494030501));
#37206=CARTESIAN_POINT('Ctrl Pts',(95.2408318692422,0.81077079491767,-7.3860343640171));
#37207=CARTESIAN_POINT('Ctrl Pts',(95.2723828266986,0.85633833229758,-7.38903378772919));
#37208=CARTESIAN_POINT('Ctrl Pts',(95.3064008482915,0.899961871312809,-7.39203321144128));
#37209=CARTESIAN_POINT('Ctrl Pts',(95.3404501445281,0.943625515853741,-7.39503539268904));
#37210=CARTESIAN_POINT('Ctrl Pts',(95.3769707108299,0.985341174032579,-7.3980375739368));
#37211=CARTESIAN_POINT('Ctrl Pts',(95.4157033869191,1.02482783654945,-7.40103975518456));
#37212=CARTESIAN_POINT('Ctrl Pts',(95.4544536932627,1.06433247251854,-7.40404330295858));
#37213=CARTESIAN_POINT('Ctrl Pts',(95.4954177252884,1.10160573426926,-7.4070468507326));
#37214=CARTESIAN_POINT('Ctrl Pts',(95.5383010313913,1.13640505476484,-7.41005039850662));
#37215=CARTESIAN_POINT('Ctrl Pts',(95.5812652725176,1.17127005312137,-7.41305961497158));
#37216=CARTESIAN_POINT('Ctrl Pts',(95.6261555944798,1.20365147315702,-7.41606883143655));
#37217=CARTESIAN_POINT('Ctrl Pts',(95.6726471466537,1.2333491593914,-7.41907804790152));
#37218=CARTESIAN_POINT('Ctrl Pts',(95.7082150894409,1.25606910646787,-7.42138022182463));
#37219=CARTESIAN_POINT('Ctrl Pts',(95.7447195673557,1.27721916981486,-7.42368239574775));
#37220=CARTESIAN_POINT('Ctrl Pts',(95.7820063598691,1.29672837599889,-7.42598456967087));
#37221=CARTESIAN_POINT('Ctrl Pts',(95.8307594283072,1.32223697033352,-7.4289946983321));
#37222=CARTESIAN_POINT('Ctrl Pts',(95.8810555013984,1.34504588612142,-7.43200482699334));
#37223=CARTESIAN_POINT('Ctrl Pts',(95.9325643756122,1.36496752376505,-7.43501495565458));
#37224=CARTESIAN_POINT('Ctrl Pts',(95.983981704043,1.38485375504527,-7.43801973446902));
#37225=CARTESIAN_POINT('Ctrl Pts',(96.0366070674375,1.4018627027287,-7.44102451328347));
#37226=CARTESIAN_POINT('Ctrl Pts',(96.0900871331254,1.41585333659049,-7.44402929209791));
#37227=CARTESIAN_POINT('Ctrl Pts',(96.1435142891485,1.42983012903794,-7.44703109818153));
#37228=CARTESIAN_POINT('Ctrl Pts',(96.1977939639886,1.44079439002421,-7.45003290426515));
#37229=CARTESIAN_POINT('Ctrl Pts',(96.2525561516286,1.44865438542052,-7.45303471034876));
#37230=CARTESIAN_POINT('Ctrl Pts',(96.3072857908958,1.45650970916161,-7.45603473228336));
#37231=CARTESIAN_POINT('Ctrl Pts',(96.3624968528197,1.46126434943482,-7.45903475421796));
#37232=CARTESIAN_POINT('Ctrl Pts',(96.4178098617443,1.4628777899275,-7.46203477615256));
#37233=CARTESIAN_POINT('Ctrl Pts',(96.4731118409207,1.4644909086904,-7.46503419986465));
#37234=CARTESIAN_POINT('Ctrl Pts',(96.5285151991299,1.46296405623551,-7.46803362357674));
#37235=CARTESIAN_POINT('Ctrl Pts',(96.5836384005495,1.45830877809535,-7.47103304728883));
#37236=CARTESIAN_POINT('Ctrl Pts',(96.6388122797687,1.45364922010121,-7.47403522853659));
#37237=CARTESIAN_POINT('Ctrl Pts',(96.6937049602461,1.44585553481708,-7.47703740978434));
#37238=CARTESIAN_POINT('Ctrl Pts',(96.7479394849717,1.43499123357209,-7.4800395910321));
#37239=CARTESIAN_POINT('Ctrl Pts',(96.802198696049,1.42412198713835,-7.48304313880612));
#37240=CARTESIAN_POINT('Ctrl Pts',(96.8557986421881,1.41017947175455,-7.48604668658014));
#37241=CARTESIAN_POINT('Ctrl Pts',(96.9083752797664,1.39327776088768,-7.48905023435416));
#37242=CARTESIAN_POINT('Ctrl Pts',(96.9610511468999,1.37634415088598,-7.49205945081912));
#37243=CARTESIAN_POINT('Ctrl Pts',(97.012699353357,1.35644037890279,-7.49506866728409));
#37244=CARTESIAN_POINT('Ctrl Pts',(97.0629747664302,1.33372915190965,-7.49807788374906));
#37245=CARTESIAN_POINT('Ctrl Pts',(97.1014375178803,1.31635413248035,-7.50038005767218));
#37246=CARTESIAN_POINT('Ctrl Pts',(97.1390971685741,1.29733696136971,-7.5026822315953));
#37247=CARTESIAN_POINT('Ctrl Pts',(97.1758100108592,1.27676802281589,-7.50498440551843));
#37248=CARTESIAN_POINT('Ctrl Pts',(97.2238126303345,1.24987381171822,-7.50799453417966));
#37249=CARTESIAN_POINT('Ctrl Pts',(97.2703972880558,1.22021219893684,-7.5110046628409));
#37250=CARTESIAN_POINT('Ctrl Pts',(97.3152264423986,1.18795723513143,-7.51401479150214));
#37251=CARTESIAN_POINT('Ctrl Pts',(97.3599759227027,1.15575959748515,-7.51701957031658));
#37252=CARTESIAN_POINT('Ctrl Pts',(97.4029756661203,1.12097806158275,-7.52002434913103));
#37253=CARTESIAN_POINT('Ctrl Pts',(97.4439144964584,1.08383149468368,-7.52302912794547));
#37254=CARTESIAN_POINT('Ctrl Pts',(97.4848128246064,1.04672167815837,-7.52603093402909));
#37255=CARTESIAN_POINT('Ctrl Pts',(97.5236538895144,1.0072518188157,-7.52903274011271));
#37256=CARTESIAN_POINT('Ctrl Pts',(97.5601586915457,0.965681683485103,-7.53203454619633));
#37257=CARTESIAN_POINT('Ctrl Pts',(97.5966417966368,0.924136255718623,-7.53503456813093));
#37258=CARTESIAN_POINT('Ctrl Pts',(97.6307910433249,0.880493422245896,-7.53803459006553));
#37259=CARTESIAN_POINT('Ctrl Pts',(97.6623651540989,0.835048866187381,-7.54103461200013));
#37260=CARTESIAN_POINT('Ctrl Pts',(97.6939329688043,0.789613372048033,-7.54403403571222));
#37261=CARTESIAN_POINT('Ctrl Pts',(97.7229263662146,0.742377302293105,-7.54703345942431));
#37262=CARTESIAN_POINT('Ctrl Pts',(97.7491465463483,0.693666511875963,-7.5500328831364));
#37263=CARTESIAN_POINT('Ctrl Pts',(97.7753908321398,0.644910938942282,-7.55303506438416));
#37264=CARTESIAN_POINT('Ctrl Pts',(97.7988565560888,0.594678402674946,-7.55603724563191));
#37265=CARTESIAN_POINT('Ctrl Pts',(97.8193909428121,0.543319317055657,-7.55903942687967));
#37266=CARTESIAN_POINT('Ctrl Pts',(97.8399346763324,0.491936853920694,-7.56204297465369));
#37267=CARTESIAN_POINT('Ctrl Pts',(97.8575442446221,0.439427320824427,-7.56504652242771));
#37268=CARTESIAN_POINT('Ctrl Pts',(97.8721162752737,0.386157943392706,-7.56805007020172));
#37269=CARTESIAN_POINT('Ctrl Pts',(97.8867158081807,0.332788028975941,-7.57105928666669));
#37270=CARTESIAN_POINT('Ctrl Pts',(97.898266240733,0.278655923186091,-7.57406850313166));
#37271=CARTESIAN_POINT('Ctrl Pts',(97.9067152652418,0.224139586404613,-7.57707771959663));
#37272=CARTESIAN_POINT('Ctrl Pts',(97.9131791152594,0.182432354510986,-7.57937989351975));
#37273=CARTESIAN_POINT('Ctrl Pts',(97.9178288079481,0.140500475882384,-7.58168206744287));
#37274=CARTESIAN_POINT('Ctrl Pts',(97.9206615212428,0.0985136951381394,
-7.58398424136599));
#37275=CARTESIAN_POINT('Ctrl Pts',(97.9228602202261,0.065924342623426,-7.58577114562968));
#37276=CARTESIAN_POINT('Ctrl Pts',(97.9239680194875,0.0332605710567664,
-7.58755804989338));
#37277=CARTESIAN_POINT('Ctrl Pts',(97.9239808370563,0.000573888477526073,
-7.58934495415708));
#37278=CARTESIAN_POINT('Origin',(96.460480949577,-8.32667268468867E-16,
1.18130019239114E-14));
#37279=CARTESIAN_POINT('',(97.9239807231656,0.000814067757715891,-8.16065504580903));
#37280=CARTESIAN_POINT('',(97.9239807535762,0.000757426072927294,-8.08934495412446));
#37281=CARTESIAN_POINT('',(97.923980949577,-1.01189432752408E-15,1.19922289829666E-14));
#37282=CARTESIAN_POINT('Ctrl Pts',(97.9239807231655,0.000814067757716574,
-8.16065504580903));
#37283=CARTESIAN_POINT('Ctrl Pts',(97.9239464028604,0.0625137952283417,
-8.15731430388859));
#37284=CARTESIAN_POINT('Ctrl Pts',(97.9200061480074,0.124074536863195,-8.15397356196815));
#37285=CARTESIAN_POINT('Ctrl Pts',(97.9122370551678,0.185030970056225,-8.1506328200477));
#37286=CARTESIAN_POINT('Ctrl Pts',(97.9042418234276,0.24776169286938,-8.14719483746861));
#37287=CARTESIAN_POINT('Ctrl Pts',(97.8921915595825,0.30985203107941,-8.14375685488951));
#37288=CARTESIAN_POINT('Ctrl Pts',(97.8762243240005,0.370813899113717,-8.14031887231041));
#37289=CARTESIAN_POINT('Ctrl Pts',(97.8602570884185,0.43177576714803,-8.13688088973131));
#37290=CARTESIAN_POINT('Ctrl Pts',(97.840373094531,0.491608884166954,-8.13344290715221));
#37291=CARTESIAN_POINT('Ctrl Pts',(97.8167620668367,0.549848871022543,-8.13000492457311));
#37292=CARTESIAN_POINT('Ctrl Pts',(97.7960894108393,0.600840942572633,-8.12699479591192));
#37293=CARTESIAN_POINT('Ctrl Pts',(97.7724935993597,0.650772688870189,-8.12398466725073));
#37294=CARTESIAN_POINT('Ctrl Pts',(97.746105053258,0.699287433059187,-8.12097453858954));
#37295=CARTESIAN_POINT('Ctrl Pts',(97.7197634070382,0.747715952877777,-8.11796975977514));
#37296=CARTESIAN_POINT('Ctrl Pts',(97.6906391265511,0.794732008217593,-8.11496498096075));
#37297=CARTESIAN_POINT('Ctrl Pts',(97.6589103975745,0.839999469150084,-8.11196020214635));
#37298=CARTESIAN_POINT('Ctrl Pts',(97.6272130589186,0.885222145429594,-8.10895839606278));
#37299=CARTESIAN_POINT('Ctrl Pts',(97.5929166776638,0.928699223901486,-8.10595658997921));
#37300=CARTESIAN_POINT('Ctrl Pts',(97.5562440458509,0.970121377377232,-8.10295478389564));
#37301=CARTESIAN_POINT('Ctrl Pts',(97.5195932107292,1.01151891124313,-8.09995476196109));
#37302=CARTESIAN_POINT('Ctrl Pts',(97.4805692737868,1.05086354630713,-8.09695474002655));
#37303=CARTESIAN_POINT('Ctrl Pts',(97.4394353835665,1.08787888396288,-8.093954718092));
#37304=CARTESIAN_POINT('Ctrl Pts',(97.3983096956925,1.12488684053655,-8.09095529437996));
#37305=CARTESIAN_POINT('Ctrl Pts',(97.355075282457,1.15956606906559,-8.08795587066792));
#37306=CARTESIAN_POINT('Ctrl Pts',(97.3100305450237,1.1916785367188,-8.08495644695589));
#37307=CARTESIAN_POINT('Ctrl Pts',(97.2649443954787,1.22382052713489,-8.08195426570818));
#37308=CARTESIAN_POINT('Ctrl Pts',(97.2180450275701,1.25339073494585,-8.07895208446047));
#37309=CARTESIAN_POINT('Ctrl Pts',(97.1696609705368,1.28019371497892,-8.07594990321276));
#37310=CARTESIAN_POINT('Ctrl Pts',(97.1212548901547,1.30700889513351,-8.07294635543879));
#37311=CARTESIAN_POINT('Ctrl Pts',(97.0713632500681,1.33105410693777,-8.06994280766482));
#37312=CARTESIAN_POINT('Ctrl Pts',(97.02033744414,1.35218081464558,-8.06693925989085));
#37313=CARTESIAN_POINT('Ctrl Pts',(96.9692153355905,1.37334739545873,-8.06393004342593));
#37314=CARTESIAN_POINT('Ctrl Pts',(96.9169552849752,1.39158429428975,-8.06092082696102));
#37315=CARTESIAN_POINT('Ctrl Pts',(96.8639257297596,1.40679229431478,-8.0579116104961));
#37316=CARTESIAN_POINT('Ctrl Pts',(96.8233559466894,1.41842703760911,-8.05560943657258));
#37317=CARTESIAN_POINT('Ctrl Pts',(96.7823361516432,1.42829002409365,-8.05330726264907));
#37318=CARTESIAN_POINT('Ctrl Pts',(96.7410344002811,1.43635720184709,-8.05100508872556));
#37319=CARTESIAN_POINT('Ctrl Pts',(96.6870317099268,1.44690516380721,-8.04799496006434));
#37320=CARTESIAN_POINT('Ctrl Pts',(96.6323198698276,1.45442554682468,-8.04498483140311));
#37321=CARTESIAN_POINT('Ctrl Pts',(96.5772688678957,1.45883269504587,-8.04197470274189));
#37322=CARTESIAN_POINT('Ctrl Pts',(96.5223157071059,1.46323201052287,-8.03896992392746));
#37323=CARTESIAN_POINT('Ctrl Pts',(96.4670251028906,1.46452902986565,-8.03596514511304));
#37324=CARTESIAN_POINT('Ctrl Pts',(96.4117759331206,1.46268932838521,-8.03296036629861));
#37325=CARTESIAN_POINT('Ctrl Pts',(96.3565814232508,1.4608514469846,-8.02995856021501));
#37326=CARTESIAN_POINT('Ctrl Pts',(96.3014287918509,1.45588300966986,-8.0269567541314));
#37327=CARTESIAN_POINT('Ctrl Pts',(96.2466988414626,1.44780159560975,-8.0239549480478));
#37328=CARTESIAN_POINT('Ctrl Pts',(96.1920014202866,1.43972498480695,-8.02095492611322));
#37329=CARTESIAN_POINT('Ctrl Pts',(96.1377267035879,1.42853914151573,-8.01795490417863));
#37330=CARTESIAN_POINT('Ctrl Pts',(96.0842499659686,1.41431343660911,-8.01495488224405));
#37331=CARTESIAN_POINT('Ctrl Pts',(96.030783891934,1.40009056839403,-8.01195545853197));
#37332=CARTESIAN_POINT('Ctrl Pts',(95.9781159910503,1.38282917807471,-8.0089560348199));
#37333=CARTESIAN_POINT('Ctrl Pts',(95.9266086674442,1.36264912445217,-8.00595661110783));
#37334=CARTESIAN_POINT('Ctrl Pts',(95.8750539903143,1.34245051819319,-8.00295442986008));
#37335=CARTESIAN_POINT('Ctrl Pts',(95.8246625149347,1.3193280808361,-7.99995224861234));
#37336=CARTESIAN_POINT('Ctrl Pts',(95.7757774389838,1.29345017398482,-7.9969500673646));
#37337=CARTESIAN_POINT('Ctrl Pts',(95.7268701116316,1.26756048808478,-7.9939465195906));
#37338=CARTESIAN_POINT('Ctrl Pts',(95.6794710033299,1.23891310611856,-7.9909429718166));
#37339=CARTESIAN_POINT('Ctrl Pts',(95.6338965169911,1.20772117055498,-7.98793942404259));
#37340=CARTESIAN_POINT('Ctrl Pts',(95.5882360164793,1.17647036546241,-7.98493020757765));
#37341=CARTESIAN_POINT('Ctrl Pts',(95.5444074363961,1.14266573653001,-7.9819209911127));
#37342=CARTESIAN_POINT('Ctrl Pts',(95.5026951862869,1.10656164836794,-7.97891177464775));
#37343=CARTESIAN_POINT('Ctrl Pts',(95.4707836054484,1.07894054125991,-7.9766096007245));
#37344=CARTESIAN_POINT('Ctrl Pts',(95.4401100338438,1.04997445604544,-7.97430742680124));
#37345=CARTESIAN_POINT('Ctrl Pts',(95.4107864405577,1.01979100198748,-7.97200525287799));
#37346=CARTESIAN_POINT('Ctrl Pts',(95.372445380523,0.980325660451858,-7.96899512421673));
#37347=CARTESIAN_POINT('Ctrl Pts',(95.3362525226972,0.938612129670457,-7.96598499555547));
#37348=CARTESIAN_POINT('Ctrl Pts',(95.3024817661057,0.894913482454971,-7.96297486689421));
#37349=CARTESIAN_POINT('Ctrl Pts',(95.2687710296642,0.851292500048519,-7.95997008807975));
#37350=CARTESIAN_POINT('Ctrl Pts',(95.237474171964,0.805693817262215,-7.95696530926528));
#37351=CARTESIAN_POINT('Ctrl Pts',(95.20882704199,0.758415944994775,-7.95396053045082));
#37352=CARTESIAN_POINT('Ctrl Pts',(95.1802082536051,0.711184846349246,-7.95095872436717));
#37353=CARTESIAN_POINT('Ctrl Pts',(95.1542342722823,0.662278298587115,-7.94795691828353));
#37354=CARTESIAN_POINT('Ctrl Pts',(95.1310984440087,0.612024839274533,-7.94495511219989));
#37355=CARTESIAN_POINT('Ctrl Pts',(95.1079763667118,0.561801248533632,-7.94195509026527));
#37356=CARTESIAN_POINT('Ctrl Pts',(95.0876893193695,0.510232811742635,-7.93895506833065));
#37357=CARTESIAN_POINT('Ctrl Pts',(95.0703842505783,0.457671735453273,-7.93595504639603));
#37358=CARTESIAN_POINT('Ctrl Pts',(95.0530826325224,0.40512114016024,-7.93295562268392));
#37359=CARTESIAN_POINT('Ctrl Pts',(95.0387619771807,0.351578799812521,-7.92995619897181));
#37360=CARTESIAN_POINT('Ctrl Pts',(95.0275199157738,0.297413727998022,-7.92695677525969));
#37361=CARTESIAN_POINT('Ctrl Pts',(95.0162675189198,0.243198859245237,-7.92395459401191));
#37362=CARTESIAN_POINT('Ctrl Pts',(95.0080994781695,0.188360633429305,-7.92095241276413));
#37363=CARTESIAN_POINT('Ctrl Pts',(95.0030623080127,0.133278479961912,-7.91795023151635));
#37364=CARTESIAN_POINT('Ctrl Pts',(94.998022845048,0.0781712543209931,-7.91494668374231));
#37365=CARTESIAN_POINT('Ctrl Pts',(94.9961171117249,0.0228204084206592,
-7.91194313596827));
#37366=CARTESIAN_POINT('Ctrl Pts',(94.997339476799,-0.0323926015764528,
-7.90893958819422));
#37367=CARTESIAN_POINT('Ctrl Pts',(94.9985641488813,-0.0877098168379549,
-7.90593037172924));
#37368=CARTESIAN_POINT('Ctrl Pts',(95.0029286712914,-0.142888148758757,
-7.90292115526425));
#37369=CARTESIAN_POINT('Ctrl Pts',(95.0103754070814,-0.197550412866063,
-7.89991193879926));
#37370=CARTESIAN_POINT('Ctrl Pts',(95.0160724651516,-0.239369285140981,
-7.89760976487632));
#37371=CARTESIAN_POINT('Ctrl Pts',(95.0235724219682,-0.280886182121544,
-7.89530759095337));
#37372=CARTESIAN_POINT('Ctrl Pts',(95.0328295808075,-0.32193760148588,-7.89300541703043));
#37373=CARTESIAN_POINT('Ctrl Pts',(95.0449334617809,-0.375612978824334,
-7.8899952883692));
#37374=CARTESIAN_POINT('Ctrl Pts',(95.060094031007,-0.428717580776824,-7.88698515970797));
#37375=CARTESIAN_POINT('Ctrl Pts',(95.078240615278,-0.480878267586556,-7.88397503104674));
#37376=CARTESIAN_POINT('Ctrl Pts',(95.0963549479557,-0.532946250158535,
-7.8809702522323));
#37377=CARTESIAN_POINT('Ctrl Pts',(95.1174445917954,-0.584073152043974,
-7.87796547341787));
#37378=CARTESIAN_POINT('Ctrl Pts',(95.1413884028453,-0.633898338187454,
-7.87496069460343));
#37379=CARTESIAN_POINT('Ctrl Pts',(95.165308525461,-0.683674230563958,-7.87195888851982));
#37380=CARTESIAN_POINT('Ctrl Pts',(95.1920769939993,-0.73215048466659,-7.8689570824362));
#37381=CARTESIAN_POINT('Ctrl Pts',(95.221524292895,-0.778985656391256,-7.86595527635259));
#37382=CARTESIAN_POINT('Ctrl Pts',(95.2509540895377,-0.825792991232581,
-7.862955254418));
#37383=CARTESIAN_POINT('Ctrl Pts',(95.2830592801791,-0.870960730790322,
-7.85995523248341));
#37384=CARTESIAN_POINT('Ctrl Pts',(95.3176251744894,-0.914173357383019,
-7.85695521054882));
#37385=CARTESIAN_POINT('Ctrl Pts',(95.3521841761514,-0.957377367116765,
-7.85395578683673));
#37386=CARTESIAN_POINT('Ctrl Pts',(95.3892025773124,-0.998626625955611,
-7.85095636312465));
#37387=CARTESIAN_POINT('Ctrl Pts',(95.428424664477,-1.03763773754891,-7.84795693941257));
#37388=CARTESIAN_POINT('Ctrl Pts',(95.4676828106698,-1.07668471420897,-7.84495475816482));
#37389=CARTESIAN_POINT('Ctrl Pts',(95.5091483152464,-1.11348905947541,-7.84195257691706));
#37390=CARTESIAN_POINT('Ctrl Pts',(95.5525288111977,-1.14780449747004,-7.83895039566931));
#37391=CARTESIAN_POINT('Ctrl Pts',(95.5959290529877,-1.18213555509029,-7.8359468478953));
#37392=CARTESIAN_POINT('Ctrl Pts',(95.641245590876,-1.21397514295113,-7.83294330012129));
#37393=CARTESIAN_POINT('Ctrl Pts',(95.6881558681701,-1.24311955122177,-7.82993975234728));
#37394=CARTESIAN_POINT('Ctrl Pts',(95.735154680718,-1.27231896465823,-7.82693053588232));
#37395=CARTESIAN_POINT('Ctrl Pts',(95.7837527766234,-1.29881278363055,-7.82392131941736));
#37396=CARTESIAN_POINT('Ctrl Pts',(95.8336027611374,-1.3224431885184,-7.8209121029524));
#37397=CARTESIAN_POINT('Ctrl Pts',(95.8717400423052,-1.3405214167085,-7.81860992902922));
#37398=CARTESIAN_POINT('Ctrl Pts',(95.9106095078347,-1.3569246705614,-7.81630775510604));
#37399=CARTESIAN_POINT('Ctrl Pts',(95.9500492516203,-1.37160188528635,-7.81400558118287));
#37400=CARTESIAN_POINT('Ctrl Pts',(96.0016173377522,-1.39079257468904,-7.81099545252163));
#37401=CARTESIAN_POINT('Ctrl Pts',(96.0543775465989,-1.40711133598547,-7.8079853238604));
#37402=CARTESIAN_POINT('Ctrl Pts',(96.1079787480087,-1.42041347779071,-7.80497519519916));
#37403=CARTESIAN_POINT('Ctrl Pts',(96.1614846849804,-1.43369197794184,-7.80197041638472));
#37404=CARTESIAN_POINT('Ctrl Pts',(96.215828139889,-1.44396437212751,-7.79896563757028));
#37405=CARTESIAN_POINT('Ctrl Pts',(96.2706408785899,-1.45113507208929,-7.79596085875583));
#37406=CARTESIAN_POINT('Ctrl Pts',(96.3253993891668,-1.45829867783146,-7.79295905267221));
#37407=CARTESIAN_POINT('Ctrl Pts',(96.380625742743,-1.4623665999551,-7.78995724658859));
#37408=CARTESIAN_POINT('Ctrl Pts',(96.4359413480525,-1.46329424859015,-7.78695544050498));
#37409=CARTESIAN_POINT('Ctrl Pts',(96.4912240760606,-1.46422134586934,-7.78395541857038));
#37410=CARTESIAN_POINT('Ctrl Pts',(96.5465954236708,-1.46201186024535,-7.78095539663578));
#37411=CARTESIAN_POINT('Ctrl Pts',(96.6016738303798,-1.45667320302483,-7.77795537470119));
#37412=CARTESIAN_POINT('Ctrl Pts',(96.6567412541216,-1.45133561036482,-7.7749559509891));
#37413=CARTESIAN_POINT('Ctrl Pts',(96.7115153276124,-1.44287013621937,-7.77195652727701));
#37414=CARTESIAN_POINT('Ctrl Pts',(96.7656189779315,-1.43133610086938,-7.76895710356492));
#37415=CARTESIAN_POINT('Ctrl Pts',(96.8197723687206,-1.41979146164447,-7.76595492231716));
#37416=CARTESIAN_POINT('Ctrl Pts',(96.8732535873175,-1.40517273537686,-7.7629527410694));
#37417=CARTESIAN_POINT('Ctrl Pts',(96.92569662286,-1.38759022313211,-7.75995055982164));
#37418=CARTESIAN_POINT('Ctrl Pts',(96.9781635293082,-1.36999970771809,-7.75694701204763));
#37419=CARTESIAN_POINT('Ctrl Pts',(97.0295908194455,-1.34944291345266,-7.75394346427361));
#37420=CARTESIAN_POINT('Ctrl Pts',(97.0796316370957,-1.3260786839947,-7.75093991649959));
#37421=CARTESIAN_POINT('Ctrl Pts',(97.1297668983678,-1.30267035848568,-7.74793070003463));
#37422=CARTESIAN_POINT('Ctrl Pts',(97.178509993609,-1.27644426392918,-7.74492148356967));
#37423=CARTESIAN_POINT('Ctrl Pts',(97.2255389295129,-1.24760512075593,-7.74191226710471));
#37424=CARTESIAN_POINT('Ctrl Pts',(97.2615179928775,-1.22554199430688,-7.73961009318157));
#37425=CARTESIAN_POINT('Ctrl Pts',(97.2964942828172,-1.20195044434721,-7.73730791925843));
#37426=CARTESIAN_POINT('Ctrl Pts',(97.330336566335,-1.17693816999641,-7.7350057453353));
#37427=CARTESIAN_POINT('Ctrl Pts',(97.3758768095831,-1.14328012627949,-7.73190779952429));
#37428=CARTESIAN_POINT('Ctrl Pts',(97.4195684264721,-1.10689512752576,-7.72880985371328));
#37429=CARTESIAN_POINT('Ctrl Pts',(97.4610650931287,-1.06801854931123,-7.72571190790227));
#37430=CARTESIAN_POINT('Ctrl Pts',(97.5009660260385,-1.03063695064124,-7.7227330920618));
#37431=CARTESIAN_POINT('Ctrl Pts',(97.5388373000252,-0.990952309552827,
-7.71975427622134));
#37432=CARTESIAN_POINT('Ctrl Pts',(97.5744015893822,-0.949217076445578,
-7.71677546038087));
#37433=CARTESIAN_POINT('Ctrl Pts',(97.6099317286148,-0.907521919027523,
-7.71379950490775));
#37434=CARTESIAN_POINT('Ctrl Pts',(97.6431589216179,-0.863780475734517,
-7.71082354943462));
#37435=CARTESIAN_POINT('Ctrl Pts',(97.6738429280665,-0.818281711365913,
-7.7078475939615));
#37436=CARTESIAN_POINT('Ctrl Pts',(97.704510123906,-0.77280787405331,-7.70487326890207));
#37437=CARTESIAN_POINT('Ctrl Pts',(97.7326365934287,-0.725579068743478,
-7.70189894384265));
#37438=CARTESIAN_POINT('Ctrl Pts',(97.7580241324221,-0.676915015827166,
-7.69892461878322));
#37439=CARTESIAN_POINT('Ctrl Pts',(97.7834082307919,-0.628257558063158,
-7.69595069681655));
#37440=CARTESIAN_POINT('Ctrl Pts',(97.8060538882951,-0.578165716678501,
-7.69297677484987));
#37441=CARTESIAN_POINT('Ctrl Pts',(97.8258089713965,-0.526983531843833,
-7.69000285288319));
#37442=CARTESIAN_POINT('Ctrl Pts',(97.8455819994866,-0.475754854482134,
-7.68702622948538));
#37443=CARTESIAN_POINT('Ctrl Pts',(97.8624590207538,-0.42343436066911,-7.68404960608758));
#37444=CARTESIAN_POINT('Ctrl Pts',(97.8763368191506,-0.37038413383133,-7.68107298268977));
#37445=CARTESIAN_POINT('Ctrl Pts',(97.8902221992464,-0.31730492466961,-7.67809473310733));
#37446=CARTESIAN_POINT('Ctrl Pts',(97.9011049906649,-0.263495717065944,
-7.67511648352489));
#37447=CARTESIAN_POINT('Ctrl Pts',(97.9089331718106,-0.209328473711563,
-7.67213823394245));
#37448=CARTESIAN_POINT('Ctrl Pts',(97.9167743489373,-0.155071304427995,
-7.66915504000906));
#37449=CARTESIAN_POINT('Ctrl Pts',(97.9215507579237,-0.100455449451422,
-7.66617184607568));
#37450=CARTESIAN_POINT('Ctrl Pts',(97.9232623684937,-0.0458559753144874,
-7.66318865214229));
#37451=CARTESIAN_POINT('Ctrl Pts',(97.9237469215567,-0.0303989882543154,
-7.66234411671855));
#37452=CARTESIAN_POINT('Ctrl Pts',(97.9239861685101,-0.0149432940640844,
-7.66149958129481));
#37453=CARTESIAN_POINT('Ctrl Pts',(97.9239808632502,0.000502671547976529,
-7.66065504587106));
#37454=CARTESIAN_POINT('Ctrl Pts',(97.9239808370565,0.00057388792750276,
-7.58934495418714));
#37455=CARTESIAN_POINT('Ctrl Pts',(97.9240028461078,-0.0555524784163405,
-7.59241325097991));
#37456=CARTESIAN_POINT('Ctrl Pts',(97.9207913233707,-0.111807974811069,
-7.59548154777268));
#37457=CARTESIAN_POINT('Ctrl Pts',(97.9143311632191,-0.167785000202359,
-7.59854984456545));
#37458=CARTESIAN_POINT('Ctrl Pts',(97.9080666489641,-0.222066761843438,
-7.60152521801527));
#37459=CARTESIAN_POINT('Ctrl Pts',(97.8987475302933,-0.276086097553949,
-7.60450059146509));
#37460=CARTESIAN_POINT('Ctrl Pts',(97.8864127316492,-0.329470488627234,
-7.6074759649149));
#37461=CARTESIAN_POINT('Ctrl Pts',(97.874088928565,-0.382807291468012,-7.61044868603956));
#37462=CARTESIAN_POINT('Ctrl Pts',(97.8587548885398,-0.435509746893538,
-7.61342140716422));
#37463=CARTESIAN_POINT('Ctrl Pts',(97.8405009258672,-0.487213623619121,
-7.61639412828888));
#37464=CARTESIAN_POINT('Ctrl Pts',(97.8222556758174,-0.538892822066113,
-7.6193654305327));
#37465=CARTESIAN_POINT('Ctrl Pts',(97.8010934439899,-0.589573878319355,
-7.62233673277652));
#37466=CARTESIAN_POINT('Ctrl Pts',(97.7771542131249,-0.638908261848428,
-7.62530803502034));
#37467=CARTESIAN_POINT('Ctrl Pts',(97.7532164953648,-0.688239527144512,
-7.62827914945979));
#37468=CARTESIAN_POINT('Ctrl Pts',(97.7265023650285,-0.736223804873542,
-7.63125026389924));
#37469=CARTESIAN_POINT('Ctrl Pts',(97.6971986597833,-0.782535338027751,
-7.63422137833869));
#37470=CARTESIAN_POINT('Ctrl Pts',(97.6678656785182,-0.828893138961163,
-7.63719546108555));
#37471=CARTESIAN_POINT('Ctrl Pts',(97.6359382520737,-0.873574406303675,
-7.64016954383241));
#37472=CARTESIAN_POINT('Ctrl Pts',(97.6016466922879,-0.916282160506793,
-7.64314362657927));
#37473=CARTESIAN_POINT('Ctrl Pts',(97.5673341391361,-0.959016060488219,
-7.64611953006593));
#37474=CARTESIAN_POINT('Ctrl Pts',(97.5306549364374,-0.99977364518832,-7.64909543355259));
#37475=CARTESIAN_POINT('Ctrl Pts',(97.4918776007987,-1.03829340643611,-7.65207133703926));
#37476=CARTESIAN_POINT('Ctrl Pts',(97.4530340547581,-1.07687893829012,-7.65505232173541));
#37477=CARTESIAN_POINT('Ctrl Pts',(97.4120856380219,-1.11321867435527,-7.65803330643157));
#37478=CARTESIAN_POINT('Ctrl Pts',(97.3693340381951,-1.14709124018506,-7.66101429112772));
#37479=CARTESIAN_POINT('Ctrl Pts',(97.3599175181445,-1.15455205326792,-7.66167088648966));
#37480=CARTESIAN_POINT('Ctrl Pts',(97.3504136240353,-1.16189334111058,-7.6623274818516));
#37481=CARTESIAN_POINT('Ctrl Pts',(97.3408257528014,-1.16911303022237,-7.66298407721354));
#37482=CARTESIAN_POINT('Ctrl Pts',(97.296870635732,-1.20221133456666,-7.66599420587478));
#37483=CARTESIAN_POINT('Ctrl Pts',(97.2509539746627,-1.23289686607644,-7.66900433453601));
#37484=CARTESIAN_POINT('Ctrl Pts',(97.2033710646308,-1.26093081767217,-7.67201446319725));
#37485=CARTESIAN_POINT('Ctrl Pts',(97.1558727228374,-1.28891494503684,-7.67501924201169));
#37486=CARTESIAN_POINT('Ctrl Pts',(97.1067144603246,-1.31425657877322,-7.67802402082613));
#37487=CARTESIAN_POINT('Ctrl Pts',(97.0562219674992,-1.33675909930136,-7.68102879964058));
#37488=CARTESIAN_POINT('Ctrl Pts',(97.0057794286303,-1.35923935731351,-7.6840306057242));
#37489=CARTESIAN_POINT('Ctrl Pts',(96.954005754314,-1.37888585235764,-7.68703241180782));
#37490=CARTESIAN_POINT('Ctrl Pts',(96.9012511039757,-1.39554789276162,-7.69003421789144));
#37491=CARTESIAN_POINT('Ctrl Pts',(96.8485278088132,-1.41220002993994,-7.69303423982604));
#37492=CARTESIAN_POINT('Ctrl Pts',(96.7948251958644,-1.42587106959957,-7.69603426176064));
#37493=CARTESIAN_POINT('Ctrl Pts',(96.7405110983378,-1.43645931574306,-7.69903428369524));
#37494=CARTESIAN_POINT('Ctrl Pts',(96.6862078313705,-1.44704545052625,-7.70203370740733));
#37495=CARTESIAN_POINT('Ctrl Pts',(96.6312938400482,-1.45454991162153,-7.70503313111942));
#37496=CARTESIAN_POINT('Ctrl Pts',(96.5761474578232,-1.45892203659761,-7.70803255483151));
#37497=CARTESIAN_POINT('Ctrl Pts',(96.5209503764872,-1.46329818110936,-7.71103473607927));
#37498=CARTESIAN_POINT('Ctrl Pts',(96.4655210049996,-1.46453619434792,-7.71403691732703));
#37499=CARTESIAN_POINT('Ctrl Pts',(96.4102416108544,-1.46263743246395,-7.71703909857478));
#37500=CARTESIAN_POINT('Ctrl Pts',(96.3549370547562,-1.46073780630571,-7.7200426463488));
#37501=CARTESIAN_POINT('Ctrl Pts',(96.2997831389271,-1.45569860695874,-7.72304619412282));
#37502=CARTESIAN_POINT('Ctrl Pts',(96.2451576130081,-1.44757317974907,-7.72604974189684));
#37503=CARTESIAN_POINT('Ctrl Pts',(96.190428990602,-1.439432417163,-7.7290589583618));
#37504=CARTESIAN_POINT('Ctrl Pts',(96.1362312686457,-1.42819389839307,-7.73206817482677));
#37505=CARTESIAN_POINT('Ctrl Pts',(96.0829314475773,-1.41396203044488,-7.73507739129173));
#37506=CARTESIAN_POINT('Ctrl Pts',(96.0421549000608,-1.4030740681965,-7.73737956521486));
#37507=CARTESIAN_POINT('Ctrl Pts',(96.0019036750428,-1.39043520068455,-7.73968173913799));
#37508=CARTESIAN_POINT('Ctrl Pts',(95.9623342670875,-1.37611123559279,-7.74198391306112));
#37509=CARTESIAN_POINT('Ctrl Pts',(95.9105966430106,-1.35738242564838,-7.74499404172235));
#37510=CARTESIAN_POINT('Ctrl Pts',(95.8598080011761,-1.33569244020792,-7.74800417038358));
#37511=CARTESIAN_POINT('Ctrl Pts',(95.8103296969894,-1.31115811356174,-7.75101429904482));
#37512=CARTESIAN_POINT('Ctrl Pts',(95.7609393296906,-1.28666739132701,-7.75401907785926));
#37513=CARTESIAN_POINT('Ctrl Pts',(95.712855147758,-1.25934259267138,-7.7570238566737));
#37514=CARTESIAN_POINT('Ctrl Pts',(95.666419781341,-1.22934905990919,-7.76002863548815));
#37515=CARTESIAN_POINT('Ctrl Pts',(95.6200303550259,-1.19938520077853,-7.76303044157177));
#37516=CARTESIAN_POINT('Ctrl Pts',(95.5752869542786,-1.16675812292454,-7.76603224765539));
#37517=CARTESIAN_POINT('Ctrl Pts',(95.5325071131653,-1.13167875695152,-7.76903405373901));
#37518=CARTESIAN_POINT('Ctrl Pts',(95.4897526986151,-1.0966202406986,-7.7720340756736));
#37519=CARTESIAN_POINT('Ctrl Pts',(95.4489599380729,-1.05911265946183,-7.7750340976082));
#37520=CARTESIAN_POINT('Ctrl Pts',(95.4104149872946,-1.01940851715886,-7.77803411954279));
#37521=CARTESIAN_POINT('Ctrl Pts',(95.3718777226125,-0.979712292101841,
-7.78103354325488));
#37522=CARTESIAN_POINT('Ctrl Pts',(95.3355877451907,-0.937820754555388,
-7.78403296696697));
#37523=CARTESIAN_POINT('Ctrl Pts',(95.3017942060922,-0.894023087214553,
-7.78703239067905));
#37524=CARTESIAN_POINT('Ctrl Pts',(95.2679695987292,-0.850185154262212,
-7.79003457192681));
#37525=CARTESIAN_POINT('Ctrl Pts',(95.2366463383367,-0.804438009447662,
-7.79303675317457));
#37526=CARTESIAN_POINT('Ctrl Pts',(95.2080321585604,-0.757102553080574,
-7.79603893442233));
#37527=CARTESIAN_POINT('Ctrl Pts',(95.1794049542447,-0.709745550664493,
-7.79904248219635));
#37528=CARTESIAN_POINT('Ctrl Pts',(95.1534895362214,-0.660799263062481,
-7.80204602997037));
#37529=CARTESIAN_POINT('Ctrl Pts',(95.1304476272651,-0.610609213441792,
-7.80504957774439));
#37530=CARTESIAN_POINT('Ctrl Pts',(95.1073622305835,-0.560324438549092,
-7.80805879420935));
#37531=CARTESIAN_POINT('Ctrl Pts',(95.0871613699973,-0.508791705252998,
-7.81106801067432));
#37532=CARTESIAN_POINT('Ctrl Pts',(95.069958129428,-0.45637543387533,-7.81407722713928));
#37533=CARTESIAN_POINT('Ctrl Pts',(95.056796945348,-0.41627483808297,-7.81637940106241));
#37534=CARTESIAN_POINT('Ctrl Pts',(95.0453892256993,-0.375657526258463,
-7.81868157498554));
#37535=CARTESIAN_POINT('Ctrl Pts',(95.035765362791,-0.334690523871059,-7.82098374890867));
#37536=CARTESIAN_POINT('Ctrl Pts',(95.0231820104731,-0.281125523063627,
-7.82399387756991));
#37537=CARTESIAN_POINT('Ctrl Pts',(95.0135972424989,-0.226737345757492,
-7.82700400623114));
#37538=CARTESIAN_POINT('Ctrl Pts',(95.007110650181,-0.171892474627354,-7.83001413489238));
#37539=CARTESIAN_POINT('Ctrl Pts',(95.0006355863653,-0.117145078286787,
-7.83301891370682));
#37540=CARTESIAN_POINT('Ctrl Pts',(94.9972478323819,-0.0619431191127279,
-7.83602369252127));
#37541=CARTESIAN_POINT('Ctrl Pts',(94.9969961213614,-0.00666390146810231,
-7.83902847133572));
#37542=CARTESIAN_POINT('Ctrl Pts',(94.9967446593672,0.0485606265489857,
-7.84203027741934));
#37543=CARTESIAN_POINT('Ctrl Pts',(94.9996230966375,0.103861736109363,-7.84503208350295));
#37544=CARTESIAN_POINT('Ctrl Pts',(95.0056282724815,0.158858232232584,-7.84803388958658));
#37545=CARTESIAN_POINT('Ctrl Pts',(95.0116298790981,0.213822040719754,-7.85103391152118));
#37546=CARTESIAN_POINT('Ctrl Pts',(95.0207544835995,0.268481070674426,-7.85403393345578));
#37547=CARTESIAN_POINT('Ctrl Pts',(95.0329469615407,0.32245769180041,-7.85703395539038));
#37548=CARTESIAN_POINT('Ctrl Pts',(95.0451370082282,0.376423549661888,-7.86003337910247));
#37549=CARTESIAN_POINT('Ctrl Pts',(95.0603935971449,0.429706754088005,-7.86303280281456));
#37550=CARTESIAN_POINT('Ctrl Pts',(95.0786106651637,0.481940626068776,-7.86603222652665));
#37551=CARTESIAN_POINT('Ctrl Pts',(95.0968444811381,0.534222519529316,-7.86903440777442));
#37552=CARTESIAN_POINT('Ctrl Pts',(95.118044039595,0.585452653450035,-7.87203658902218));
#37553=CARTESIAN_POINT('Ctrl Pts',(95.1420540827371,0.635281706642631,-7.87503877026994));
#37554=CARTESIAN_POINT('Ctrl Pts',(95.1660750547179,0.685133440914093,-7.87804231804396));
#37555=CARTESIAN_POINT('Ctrl Pts',(95.192908805199,0.733582360370158,-7.88104586581798));
#37556=CARTESIAN_POINT('Ctrl Pts',(95.222354313918,0.780304225332474,-7.884049413592));
#37557=CARTESIAN_POINT('Ctrl Pts',(95.2518553960792,0.827114269951953,-7.88705863005697));
#37558=CARTESIAN_POINT('Ctrl Pts',(95.2839777761885,0.872190317532797,-7.89006784652194));
#37559=CARTESIAN_POINT('Ctrl Pts',(95.3184780310294,0.915238539414054,-7.89307706298691));
#37560=CARTESIAN_POINT('Ctrl Pts',(95.3448721399146,0.948172193408378,-7.89537923691002));
#37561=CARTESIAN_POINT('Ctrl Pts',(95.3726570984648,0.979919605362234,-7.89768141083313));
#37562=CARTESIAN_POINT('Ctrl Pts',(95.4017096245929,1.01036405883792,-7.89998358475624));
#37563=CARTESIAN_POINT('Ctrl Pts',(95.4396962600516,1.0501706612249,-7.90299371341748));
#37564=CARTESIAN_POINT('Ctrl Pts',(95.4800107426962,1.08791564893066,-7.90600384207871));
#37565=CARTESIAN_POINT('Ctrl Pts',(95.5224005497256,1.12331536685595,-7.90901397073995));
#37566=CARTESIAN_POINT('Ctrl Pts',(95.5647150181239,1.15865216950793,-7.9120187495544));
#37567=CARTESIAN_POINT('Ctrl Pts',(95.6090970891016,1.19165163843458,-7.91502352836885));
#37568=CARTESIAN_POINT('Ctrl Pts',(95.6552573876917,1.22206680070472,-7.91802830718329));
#37569=CARTESIAN_POINT('Ctrl Pts',(95.7013720183138,1.2524518722108,-7.92103011326692));
#37570=CARTESIAN_POINT('Ctrl Pts',(95.7492609527108,1.28025741270279,-7.92403191935054));
#37571=CARTESIAN_POINT('Ctrl Pts',(95.7986032028385,1.30527778590322,-7.92703372543416));
#37572=CARTESIAN_POINT('Ctrl Pts',(95.8479161259795,1.33028328803166,-7.93003374736876));
#37573=CARTESIAN_POINT('Ctrl Pts',(95.8986801826815,1.35250666558881,-7.93303376930337));
#37574=CARTESIAN_POINT('Ctrl Pts',(95.9505489776281,1.37178775106951,-7.93603379123797));
#37575=CARTESIAN_POINT('Ctrl Pts',(96.0024074296236,1.39106499178524,-7.93903321495007));
#37576=CARTESIAN_POINT('Ctrl Pts',(96.0553696876308,1.40740092169702,-7.94203263866216));
#37577=CARTESIAN_POINT('Ctrl Pts',(96.109070695634,1.42068401955668,-7.94503206237426));
#37578=CARTESIAN_POINT('Ctrl Pts',(96.1628210739361,1.43397932930088,-7.94803424362202));
#37579=CARTESIAN_POINT('Ctrl Pts',(96.2173110453676,1.44421607261537,-7.95103642486978));
#37580=CARTESIAN_POINT('Ctrl Pts',(96.2721632117813,1.45133341435782,-7.95403860611754));
#37581=CARTESIAN_POINT('Ctrl Pts',(96.3270403456836,1.45845399575624,-7.95704215389157));
#37582=CARTESIAN_POINT('Ctrl Pts',(96.3822794755548,1.46245230695228,-7.96004570166559));
#37583=CARTESIAN_POINT('Ctrl Pts',(96.4374992052558,1.46331954453836,-7.96304924943961));
#37584=CARTESIAN_POINT('Ctrl Pts',(96.4928231529035,1.46418841888944,-7.96605846590458));
#37585=CARTESIAN_POINT('Ctrl Pts',(96.5481270982729,1.46191443648731,-7.96906768236955));
#37586=CARTESIAN_POINT('Ctrl Pts',(96.603031946463,1.45654092400001,-7.97207689883452));
#37587=CARTESIAN_POINT('Ctrl Pts',(96.6450364055061,1.45242996672336,-7.97437907275761));
#37588=CARTESIAN_POINT('Ctrl Pts',(96.6868073097122,1.44650597742622,-7.97668124668071));
#37589=CARTESIAN_POINT('Ctrl Pts',(96.728179545075,1.43880843477108,-7.97898342060381));
#37590=CARTESIAN_POINT('Ctrl Pts',(96.7822743943803,1.42874377652141,-7.98199354926504));
#37591=CARTESIAN_POINT('Ctrl Pts',(96.8359145124702,1.41560302543563,-7.98500367792627));
#37592=CARTESIAN_POINT('Ctrl Pts',(96.8887243530978,1.39944268812301,-7.9880138065875));
#37593=CARTESIAN_POINT('Ctrl Pts',(96.9414403357584,1.38331107228327,-7.99101858540194));
#37594=CARTESIAN_POINT('Ctrl Pts',(96.9933284684523,1.36417067366595,-7.99402336421638));
#37595=CARTESIAN_POINT('Ctrl Pts',(97.0440237913569,1.34212890655383,-7.99702814303082));
#37596=CARTESIAN_POINT('Ctrl Pts',(97.0946689596385,1.32010894611851,-8.00002994911443));
#37597=CARTESIAN_POINT('Ctrl Pts',(97.1441231738903,1.2951935129002,-8.00303175519805));
#37598=CARTESIAN_POINT('Ctrl Pts',(97.1920388215885,1.26753908416982,-8.00603356128167));
#37599=CARTESIAN_POINT('Ctrl Pts',(97.2399259902132,1.23990109208476,-8.00903358321626));
#37600=CARTESIAN_POINT('Ctrl Pts',(97.2862759483156,1.2095275946438,-8.01203360515086));
#37601=CARTESIAN_POINT('Ctrl Pts',(97.3307652822583,1.17662119235098,-8.01503362708546));
#37602=CARTESIAN_POINT('Ctrl Pts',(97.3752457447589,1.14372135179367,-8.01803305079755));
#37603=CARTESIAN_POINT('Ctrl Pts',(97.4178658955736,1.10828992331808,-8.02103247450964));
#37604=CARTESIAN_POINT('Ctrl Pts',(97.4583328674818,1.07057171638976,-8.02403189822173));
#37605=CARTESIAN_POINT('Ctrl Pts',(97.4988370429094,1.03281883303333,-8.02703407946948));
#37606=CARTESIAN_POINT('Ctrl Pts',(97.5371836974197,0.992775331835817,-8.03003626071724));
#37607=CARTESIAN_POINT('Ctrl Pts',(97.5731156710776,0.950724053819656,-8.03303844196499));
#37608=CARTESIAN_POINT('Ctrl Pts',(97.6090640001723,0.908653634995189,-8.036041989739));
#37609=CARTESIAN_POINT('Ctrl Pts',(97.6425951371194,0.864574038622622,-8.03904553751302));
#37610=CARTESIAN_POINT('Ctrl Pts',(97.673493315475,0.818799884085621,-8.04204908528704));
#37611=CARTESIAN_POINT('Ctrl Pts',(97.7044498089422,0.77293933853546,-8.045058301752));
#37612=CARTESIAN_POINT('Ctrl Pts',(97.7327631461288,0.725378300839316,-8.04806751821696));
#37613=CARTESIAN_POINT('Ctrl Pts',(97.7582624783195,0.676457946700814,-8.05107673468192));
#37614=CARTESIAN_POINT('Ctrl Pts',(97.7777705124909,0.63903187086994,-8.05337890860507));
#37615=CARTESIAN_POINT('Ctrl Pts',(97.7956324701048,0.600810769922016,-8.05568108252822));
#37616=CARTESIAN_POINT('Ctrl Pts',(97.8117911979588,0.561954502267177,-8.05798325645138));
#37617=CARTESIAN_POINT('Ctrl Pts',(97.8352823864444,0.505466150240102,-8.06133010417628));
#37618=CARTESIAN_POINT('Ctrl Pts',(97.8552563046488,0.447434047055465,-8.06467695190118));
#37619=CARTESIAN_POINT('Ctrl Pts',(97.8715321197142,0.388287065525512,-8.06802379962608));
#37620=CARTESIAN_POINT('Ctrl Pts',(97.8877496688976,0.329351824607984,-8.07135866595195));
#37621=CARTESIAN_POINT('Ctrl Pts',(97.9002953787761,0.26930995292303,-8.07469353227782));
#37622=CARTESIAN_POINT('Ctrl Pts',(97.9090371646527,0.208607626336123,-8.0780283986037));
#37623=CARTESIAN_POINT('Ctrl Pts',(97.9177299795459,0.148245350703205,-8.08134458319957));
#37624=CARTESIAN_POINT('Ctrl Pts',(97.9226612352516,0.0872302985620028,
-8.08466076779545));
#37625=CARTESIAN_POINT('Ctrl Pts',(97.923749648434,0.0260185500224431,-8.08797695239133));
#37626=CARTESIAN_POINT('Ctrl Pts',(97.9238993135162,0.0176014695223185,
-8.08843295296904));
#37627=CARTESIAN_POINT('Ctrl Pts',(97.9239763941621,0.00918069264905495,
-8.08888895354675));
#37628=CARTESIAN_POINT('Ctrl Pts',(97.9239807535762,0.000757426072930723,
-8.08934495412446));
#37629=CARTESIAN_POINT('Origin',(96.460480949577,-8.32667268468867E-16,
1.18130019239114E-14));
#37630=CARTESIAN_POINT('',(97.9239804054011,-0.00126206278290129,-8.66065504588342));
#37631=CARTESIAN_POINT('',(97.9239803911303,-0.00127850425146132,-8.58934495419103));
#37632=CARTESIAN_POINT('',(97.923980949577,-1.01189432752408E-15,1.19922289829666E-14));
#37633=CARTESIAN_POINT('Ctrl Pts',(97.9239804054018,-0.0012620620365945,
-8.6606550458429));
#37634=CARTESIAN_POINT('Ctrl Pts',(97.9240276872323,0.053566410110067,-8.65767794005104));
#37635=CARTESIAN_POINT('Ctrl Pts',(97.9209895412013,0.1084571276113,-8.65470083425919));
#37636=CARTESIAN_POINT('Ctrl Pts',(97.914871620017,0.163033823904847,-8.65172372846733));
#37637=CARTESIAN_POINT('Ctrl Pts',(97.9087566825499,0.217583903081169,-8.64874807461337));
#37638=CARTESIAN_POINT('Ctrl Pts',(97.8995650059973,0.271819731168011,-8.64577242075942));
#37639=CARTESIAN_POINT('Ctrl Pts',(97.8873541773523,0.325369085590568,-8.64279676690547));
#37640=CARTESIAN_POINT('Ctrl Pts',(97.8751442845461,0.378914335987086,-8.63982134110582));
#37641=CARTESIAN_POINT('Ctrl Pts',(97.8599158208427,0.431772693885009,-8.63684591530617));
#37642=CARTESIAN_POINT('Ctrl Pts',(97.8417771765689,0.483583481208858,-8.63387048950652));
#37643=CARTESIAN_POINT('Ctrl Pts',(97.8236202153823,0.535446588521609,-8.63089205903829));
#37644=CARTESIAN_POINT('Ctrl Pts',(97.8025473891416,0.586259506865642,-8.62791362857006));
#37645=CARTESIAN_POINT('Ctrl Pts',(97.7787159875234,0.635679663612517,-8.62493519810183));
#37646=CARTESIAN_POINT('Ctrl Pts',(97.7548704339337,0.685129167884049,-8.62195499893096));
#37647=CARTESIAN_POINT('Ctrl Pts',(97.7282633079905,0.733183795884246,-8.61897479976009));
#37648=CARTESIAN_POINT('Ctrl Pts',(97.6990971959579,0.779526807878603,-8.61599460058922));
#37649=CARTESIAN_POINT('Ctrl Pts',(97.6698794337128,0.825951888624783,-8.61300912378931));
#37650=CARTESIAN_POINT('Ctrl Pts',(97.6380939598203,0.870658871980485,-8.6100236469894));
#37651=CARTESIAN_POINT('Ctrl Pts',(97.6039849017055,0.913362448027296,-8.60703817018948));
#37652=CARTESIAN_POINT('Ctrl Pts',(97.592429545286,0.927829427442212,-8.60602676001248));
#37653=CARTESIAN_POINT('Ctrl Pts',(97.5806078299067,0.94206678369978,-8.60501534983548));
#37654=CARTESIAN_POINT('Ctrl Pts',(97.568530182405,0.956064405586448,-8.60400393965848));
#37655=CARTESIAN_POINT('Ctrl Pts',(97.5325850498447,0.997723708374557,-8.60099381099893));
#37656=CARTESIAN_POINT('Ctrl Pts',(97.4942117303392,1.03744058079032,-8.59798368233938));
#37657=CARTESIAN_POINT('Ctrl Pts',(97.4536482220841,1.07491907547536,-8.59497355367983));
#37658=CARTESIAN_POINT('Ctrl Pts',(97.4131568066128,1.11233096031496,-8.59196877486707));
#37659=CARTESIAN_POINT('Ctrl Pts',(97.3704833120042,1.14751200675001,-8.58896399605431));
#37660=CARTESIAN_POINT('Ctrl Pts',(97.3259043796911,1.18020105770567,-8.58595921724156));
#37661=CARTESIAN_POINT('Ctrl Pts',(97.2813695508459,1.2128577682611,-8.58295741115963));
#37662=CARTESIAN_POINT('Ctrl Pts',(97.2349334424098,1.24302705644912,-8.57995560507771));
#37663=CARTESIAN_POINT('Ctrl Pts',(97.1869063396721,1.27048746653605,-8.57695379899578));
#37664=CARTESIAN_POINT('Ctrl Pts',(97.138907782252,1.2979315552943,-8.57395377706286));
#37665=CARTESIAN_POINT('Ctrl Pts',(97.089320562364,1.32266969555262,-8.57095375512995));
#37666=CARTESIAN_POINT('Ctrl Pts',(97.0384826181072,1.34452457068523,-8.56795373319704));
#37667=CARTESIAN_POINT('Ctrl Pts',(96.9876548112437,1.36637508782369,-8.56495430948662));
#37668=CARTESIAN_POINT('Ctrl Pts',(96.935577260224,1.38534327318383,-8.56195488577621));
#37669=CARTESIAN_POINT('Ctrl Pts',(96.8826089770052,1.40129946066485,-8.5589554620658));
#37670=CARTESIAN_POINT('Ctrl Pts',(96.8295919971214,1.41727031754929,-8.5559532808197));
#37671=CARTESIAN_POINT('Ctrl Pts',(96.7756831557414,1.43022349160527,-8.5529510995736));
#37672=CARTESIAN_POINT('Ctrl Pts',(96.721256330215,1.44007932102821,-8.5499489183275));
#37673=CARTESIAN_POINT('Ctrl Pts',(96.6668047308057,1.44993963660596,-8.54694537055513));
#37674=CARTESIAN_POINT('Ctrl Pts',(96.6118352023302,1.45669973255281,-8.54394182278276));
#37675=CARTESIAN_POINT('Ctrl Pts',(96.5567282212643,1.46033171323941,-8.54093827501039));
#37676=CARTESIAN_POINT('Ctrl Pts',(96.5015172350449,1.46397054867837,-8.53792905854703));
#37677=CARTESIAN_POINT('Ctrl Pts',(96.4461688073963,1.46446947034548,-8.53491984208368));
#37678=CARTESIAN_POINT('Ctrl Pts',(96.3910637275223,1.46185276251824,-8.53191062562032));
#37679=CARTESIAN_POINT('Ctrl Pts',(96.3489060827673,1.45985087377657,-8.52960845168386));
#37680=CARTESIAN_POINT('Ctrl Pts',(96.3068908890163,1.45602653043792,-8.52730627774739));
#37681=CARTESIAN_POINT('Ctrl Pts',(96.2651850304279,1.45041089142481,-8.52500410381093));
#37682=CARTESIAN_POINT('Ctrl Pts',(96.2106539638432,1.44306835502095,-8.52199397515112));
#37683=CARTESIAN_POINT('Ctrl Pts',(96.1564229831566,1.43263081037034,-8.51898384649131));
#37684=CARTESIAN_POINT('Ctrl Pts',(96.1028699935255,1.4191358828921,-8.5159737178315));
#37685=CARTESIAN_POINT('Ctrl Pts',(96.0494121826475,1.40566493970267,-8.51296893901853));
#37686=CARTESIAN_POINT('Ctrl Pts',(95.9966304794966,1.38914752516248,-8.50996416020556));
#37687=CARTESIAN_POINT('Ctrl Pts',(95.9448947659446,1.36967263871603,-8.50695938139259));
#37688=CARTESIAN_POINT('Ctrl Pts',(95.8932102363104,1.35021701944346,-8.50395757531048));
#37689=CARTESIAN_POINT('Ctrl Pts',(95.8425701381476,1.32780990952714,-8.50095576922837));
#37690=CARTESIAN_POINT('Ctrl Pts',(95.7933294852573,1.30259017870396,-8.49795396314626));
#37691=CARTESIAN_POINT('Ctrl Pts',(95.7441180989689,1.27738543744288,-8.49495394121319));
#37692=CARTESIAN_POINT('Ctrl Pts',(95.696304978438,1.24937162897091,-8.49195391928012));
#37693=CARTESIAN_POINT('Ctrl Pts',(95.6502232791616,1.21873490043279,-8.48895389734706));
#37694=CARTESIAN_POINT('Ctrl Pts',(95.6041507688549,1.18810428104376,-8.48595447363652));
#37695=CARTESIAN_POINT('Ctrl Pts',(95.5598094336834,1.15485207252031,-8.48295504992598));
#37696=CARTESIAN_POINT('Ctrl Pts',(95.5175040352204,1.11920810798997,-8.47995562621545));
#37697=CARTESIAN_POINT('Ctrl Pts',(95.4751597430713,1.08353137399718,-8.47695344496927));
#37698=CARTESIAN_POINT('Ctrl Pts',(95.4348555318852,1.04545883194678,-8.47395126372309));
#37699=CARTESIAN_POINT('Ctrl Pts',(95.3968624056838,1.00526008728411,-8.47094908247691));
#37700=CARTESIAN_POINT('Ctrl Pts',(95.3588519858549,0.965043045045409,-8.46794553470448));
#37701=CARTESIAN_POINT('Ctrl Pts',(95.3231550889943,0.92269827543808,-8.46494198693206));
#37702=CARTESIAN_POINT('Ctrl Pts',(95.2900029692953,0.878529195687755,-8.46193843915963));
#37703=CARTESIAN_POINT('Ctrl Pts',(95.2567882805497,0.83427675423281,-8.45892922269626));
#37704=CARTESIAN_POINT('Ctrl Pts',(95.2261282566351,0.788193565322302,-8.4559200062329));
#37705=CARTESIAN_POINT('Ctrl Pts',(95.1982106205418,0.740611818996549,-8.45291078976953));
#37706=CARTESIAN_POINT('Ctrl Pts',(95.1768524846503,0.704209832790175,-8.45060861583415));
#37707=CARTESIAN_POINT('Ctrl Pts',(95.1570985381993,0.666931371096175,-8.44830644189875));
#37708=CARTESIAN_POINT('Ctrl Pts',(95.139013869602,0.628933229001528,-8.44600426796337));
#37709=CARTESIAN_POINT('Ctrl Pts',(95.1153678807133,0.579250060027472,-8.4429941393009));
#37710=CARTESIAN_POINT('Ctrl Pts',(95.0944780102903,0.528127120712406,-8.43998401063843));
#37711=CARTESIAN_POINT('Ctrl Pts',(95.0765192319262,0.475901475178343,-8.43697388197596));
#37712=CARTESIAN_POINT('Ctrl Pts',(95.0585923713712,0.423768649331462,-8.43396910316026));
#37713=CARTESIAN_POINT('Ctrl Pts',(95.0435864351764,0.370537501915542,-8.43096432434456));
#37714=CARTESIAN_POINT('Ctrl Pts',(95.031628985914,0.316566447900545,-8.42795954552886));
#37715=CARTESIAN_POINT('Ctrl Pts',(95.0196833665665,0.262648789301595,-8.42495773944396));
#37716=CARTESIAN_POINT('Ctrl Pts',(95.0107803733285,0.207993187268241,-8.42195593335907));
#37717=CARTESIAN_POINT('Ctrl Pts',(95.0049976772048,0.152972853293195,-8.41895412727417));
#37718=CARTESIAN_POINT('Ctrl Pts',(94.9992184180757,0.0979852211221702,
-8.41595410533829));
#37719=CARTESIAN_POINT('Ctrl Pts',(94.9965558352626,0.042633810859308,-8.4129540834024));
#37720=CARTESIAN_POINT('Ctrl Pts',(94.9970360603772,-0.012700640730549,
-8.40995406146651));
#37721=CARTESIAN_POINT('Ctrl Pts',(94.997516189732,-0.0680240582965324,
-8.40695463775312));
#37722=CARTESIAN_POINT('Ctrl Pts',(95.0011378778449,-0.123329996105209,
-8.40395521403973));
#37723=CARTESIAN_POINT('Ctrl Pts',(95.0078751538129,-0.178237628217731,
-8.40095579032634));
#37724=CARTESIAN_POINT('Ctrl Pts',(95.0146186237304,-0.233195739945271,
-8.39795360907727));
#37725=CARTESIAN_POINT('Ctrl Pts',(95.0244833396089,-0.287754289076616,
-8.39495142782821));
#37726=CARTESIAN_POINT('Ctrl Pts',(95.0373915751653,-0.341538991092539,
-8.39194924657914));
#37727=CARTESIAN_POINT('Ctrl Pts',(95.050305686264,-0.395348174711013,-8.38894569880381));
#37728=CARTESIAN_POINT('Ctrl Pts',(95.0662659261699,-0.44838230245804,-8.38594215102847));
#37729=CARTESIAN_POINT('Ctrl Pts',(95.0851445311735,-0.500281906741627,
-8.38293860325314));
#37730=CARTESIAN_POINT('Ctrl Pts',(95.1040587663669,-0.552279462793791,
-8.37992938678686));
#37731=CARTESIAN_POINT('Ctrl Pts',(95.1259021606642,-0.603137731515617,
-8.37692017032059));
#37732=CARTESIAN_POINT('Ctrl Pts',(95.1504990670713,-0.652517982516026,
-8.37391095385432));
#37733=CARTESIAN_POINT('Ctrl Pts',(95.1693167084412,-0.690295898108604,
-8.37160877994148));
#37734=CARTESIAN_POINT('Ctrl Pts',(95.1897449444011,-0.727209164653124,
-8.36930660602864));
#37735=CARTESIAN_POINT('Ctrl Pts',(95.2116880189019,-0.763117596636237,
-8.3670044321158));
#37736=CARTESIAN_POINT('Ctrl Pts',(95.2403789345166,-0.810068437177948,
-8.36399430345488));
#37737=CARTESIAN_POINT('Ctrl Pts',(95.2717816288482,-0.855497639194487,
-8.36098417479396));
#37738=CARTESIAN_POINT('Ctrl Pts',(95.3057094065078,-0.899074487079725,
-8.35797404613304));
#37739=CARTESIAN_POINT('Ctrl Pts',(95.3395768849468,-0.942573886627629,
-8.35496926731891));
#37740=CARTESIAN_POINT('Ctrl Pts',(95.3759602188609,-0.984227052009934,
-8.35196448850478));
#37741=CARTESIAN_POINT('Ctrl Pts',(95.4146289257559,-1.02373130960683,-8.34895970969066));
#37742=CARTESIAN_POINT('Ctrl Pts',(95.4532593763718,-1.06319648428564,-8.34595790360735));
#37743=CARTESIAN_POINT('Ctrl Pts',(95.4941703534348,-1.10051658711055,-8.34295609752405));
#37744=CARTESIAN_POINT('Ctrl Pts',(95.537091721408,-1.13542264523016,-8.33995429144075));
#37745=CARTESIAN_POINT('Ctrl Pts',(95.5799875787004,-1.17030795663668,-8.33695426950647));
#37746=CARTESIAN_POINT('Ctrl Pts',(95.6248910496381,-1.20278173467422,-8.3339542475722));
#37747=CARTESIAN_POINT('Ctrl Pts',(95.6714975351442,-1.23261406034087,-8.33095422563792));
#37748=CARTESIAN_POINT('Ctrl Pts',(95.7180947270356,-1.26244043726151,-8.32795480192614));
#37749=CARTESIAN_POINT('Ctrl Pts',(95.7663938145319,-1.28962612330611,-8.32495537821437));
#37750=CARTESIAN_POINT('Ctrl Pts',(95.8160616552611,-1.31398478800686,-8.32195595450259));
#37751=CARTESIAN_POINT('Ctrl Pts',(95.865775158376,-1.33836584697168,-8.31895377325515));
#37752=CARTESIAN_POINT('Ctrl Pts',(95.9168594536031,-1.3599144590114,-8.31595159200771));
#37753=CARTESIAN_POINT('Ctrl Pts',(95.9689585982489,-1.378491214388,-8.31294941076028));
#37754=CARTESIAN_POINT('Ctrl Pts',(96.0210814572689,-1.39707642549129,-8.30994586298657));
#37755=CARTESIAN_POINT('Ctrl Pts',(96.0742195789598,-1.41268693425598,-8.30694231521287));
#37756=CARTESIAN_POINT('Ctrl Pts',(96.12800208995,-1.42523333454601,-8.30393876743917));
#37757=CARTESIAN_POINT('Ctrl Pts',(96.1818861063786,-1.43780341405514,-8.30092955097451));
#37758=CARTESIAN_POINT('Ctrl Pts',(96.2364164200425,-1.4472977418607,-8.29792033450986));
#37759=CARTESIAN_POINT('Ctrl Pts',(96.2912133622951,-1.45367834609166,-8.2949111180452));
#37760=CARTESIAN_POINT('Ctrl Pts',(96.3331352689248,-1.45855976983201,-8.29260894411955));
#37761=CARTESIAN_POINT('Ctrl Pts',(96.37521303127,-1.46161983639158,-8.29030677019389));
#37762=CARTESIAN_POINT('Ctrl Pts',(96.4172769194585,-1.46286214722424,-8.28800459626824));
#37763=CARTESIAN_POINT('Ctrl Pts',(96.4722761156628,-1.46448648820115,-8.28499446760714));
#37764=CARTESIAN_POINT('Ctrl Pts',(96.5274826038959,-1.46300822420361,-8.28198433894605));
#37765=CARTESIAN_POINT('Ctrl Pts',(96.5825173913096,-1.45840301593532,-8.27897421028495));
#37766=CARTESIAN_POINT('Ctrl Pts',(96.6374543663989,-1.45380599241975,-8.27596943147066));
#37767=CARTESIAN_POINT('Ctrl Pts',(96.6922197242421,-1.44609309713388,-8.27296465265636));
#37768=CARTESIAN_POINT('Ctrl Pts',(96.7464340328068,-1.43529198569189,-8.26995987384207));
#37769=CARTESIAN_POINT('Ctrl Pts',(96.800594705295,-1.42450156016022,-8.2669580677586));
#37770=CARTESIAN_POINT('Ctrl Pts',(96.8542048930735,-1.41062907351296,-8.26395626167513));
#37771=CARTESIAN_POINT('Ctrl Pts',(96.9068917231434,-1.39375380582219,-8.26095445559167));
#37772=CARTESIAN_POINT('Ctrl Pts',(96.959547238347,-1.37688856809057,-8.25795443365723));
#37773=CARTESIAN_POINT('Ctrl Pts',(97.011279981667,-1.3570242475339,-8.25495441172278));
#37774=CARTESIAN_POINT('Ctrl Pts',(97.0617309580119,-1.33429032723655,-8.25195438978834));
#37775=CARTESIAN_POINT('Ctrl Pts',(97.112171874127,-1.31156094022041,-8.24895496607641));
#37776=CARTESIAN_POINT('Ctrl Pts',(97.161331049642,-1.28596330670351,-8.24595554236449));
#37777=CARTESIAN_POINT('Ctrl Pts',(97.2088704000913,-1.25767463215211,-8.24295611865257));
#37778=CARTESIAN_POINT('Ctrl Pts',(97.2564534560878,-1.22935995026172,-8.23995393740497));
#37779=CARTESIAN_POINT('Ctrl Pts',(97.3024132569838,-1.19834955520426,-8.23695175615737));
#37780=CARTESIAN_POINT('Ctrl Pts',(97.3464385576812,-1.16486538563146,-8.23394957490977));
#37781=CARTESIAN_POINT('Ctrl Pts',(97.3904838977182,-1.13136597480799,-8.23094602713592));
#37782=CARTESIAN_POINT('Ctrl Pts',(97.4325925800262,-1.0953908884934,-8.22794247936206));
#37783=CARTESIAN_POINT('Ctrl Pts',(97.4724870808059,-1.0572018919559,-8.2249389315882));
#37784=CARTESIAN_POINT('Ctrl Pts',(97.5124568757418,-1.0189408201144,-8.2219297151234));
#37785=CARTESIAN_POINT('Ctrl Pts',(97.5502037801204,-0.978457878287744,
-8.2189204986586));
#37786=CARTESIAN_POINT('Ctrl Pts',(97.5854885420198,-0.936050301504208,
-8.2159112821938));
#37787=CARTESIAN_POINT('Ctrl Pts',(97.6124828309726,-0.903606767245738,
-8.21360910826943));
#37788=CARTESIAN_POINT('Ctrl Pts',(97.6380368432212,-0.870037517218503,
-8.21130693434505));
#37789=CARTESIAN_POINT('Ctrl Pts',(97.6620608553443,-0.835486672578546,
-8.20900476042068));
#37790=CARTESIAN_POINT('Ctrl Pts',(97.6938285605627,-0.789799006340861,
-8.20596052358728));
#37791=CARTESIAN_POINT('Ctrl Pts',(97.7230514378139,-0.742204285146314,
-8.20291628675389));
#37792=CARTESIAN_POINT('Ctrl Pts',(97.7494980213216,-0.693013159147089,
-8.19987204992049));
#37793=CARTESIAN_POINT('Ctrl Pts',(97.7759001255963,-0.643904765329677,
-8.19683293304217));
#37794=CARTESIAN_POINT('Ctrl Pts',(97.7995349562016,-0.593205739149372,
-8.19379381616385));
#37795=CARTESIAN_POINT('Ctrl Pts',(97.8202141814697,-0.541255751088821,
-8.19075469928553));
#37796=CARTESIAN_POINT('Ctrl Pts',(97.8408626648377,-0.489382992291977,
-8.18772010038243));
#37797=CARTESIAN_POINT('Ctrl Pts',(97.8585640806866,-0.436263438544642,
-8.18468550147933));
#37798=CARTESIAN_POINT('Ctrl Pts',(97.8731769705423,-0.382259339125534,
-8.18165090257623));
#37799=CARTESIAN_POINT('Ctrl Pts',(97.8877772492243,-0.328301846167547,
-8.17861892258387));
#37800=CARTESIAN_POINT('Ctrl Pts',(97.8992941568264,-0.27346181511333,-8.1755869425915));
#37801=CARTESIAN_POINT('Ctrl Pts',(97.9076357256374,-0.218117638272708,
-8.17255496259914));
#37802=CARTESIAN_POINT('Ctrl Pts',(97.9159735880353,-0.162798052535111,
-8.16952432980781));
#37803=CARTESIAN_POINT('Ctrl Pts',(97.9211388342734,-0.106975271404341,
-8.16649369701649));
#37804=CARTESIAN_POINT('Ctrl Pts',(97.9230907703806,-0.0510368698973246,
-8.16346306422516));
#37805=CARTESIAN_POINT('Ctrl Pts',(97.9236936227492,-0.0337603833765289,
-8.16252705809774));
#37806=CARTESIAN_POINT('Ctrl Pts',(97.9239903389913,-0.016472908141087,
-8.16159105197031));
#37807=CARTESIAN_POINT('Ctrl Pts',(97.9239807231659,0.000814067132374142,
-8.16065504584289));
#37808=CARTESIAN_POINT('Ctrl Pts',(97.9239807535765,0.000757425470412684,
-8.08934495415708));
#37809=CARTESIAN_POINT('Ctrl Pts',(97.9240097899909,-0.0553468229746924,
-8.09238220454818));
#37810=CARTESIAN_POINT('Ctrl Pts',(97.9208082948967,-0.111450673046662,
-8.09541945493928));
#37811=CARTESIAN_POINT('Ctrl Pts',(97.9144027461864,-0.167163570625104,
-8.09845670533038));
#37812=CARTESIAN_POINT('Ctrl Pts',(97.9079948428155,-0.222896948098714,
-8.10149507220567));
#37813=CARTESIAN_POINT('Ctrl Pts',(97.8983806086794,-0.278238582411924,
-8.10453343908097));
#37814=CARTESIAN_POINT('Ctrl Pts',(97.8856381128755,-0.332805213148775,
-8.10757180595627));
#37815=CARTESIAN_POINT('Ctrl Pts',(97.8728767166415,-0.387452780368249,
-8.11061467951861));
#37816=CARTESIAN_POINT('Ctrl Pts',(97.8569779203156,-0.441322554640103,
-8.11365755308095));
#37817=CARTESIAN_POINT('Ctrl Pts',(97.8380701510059,-0.494044777430771,
-8.11670042664329));
#37818=CARTESIAN_POINT('Ctrl Pts',(97.8191457289805,-0.546813434476251,
-8.11974598016787));
#37819=CARTESIAN_POINT('Ctrl Pts',(97.7972072600667,-0.598432060855823,
-8.12279153369245));
#37820=CARTESIAN_POINT('Ctrl Pts',(97.7724307275929,-0.648552256926193,
-8.12583708721703));
#37821=CARTESIAN_POINT('Ctrl Pts',(97.7476053007107,-0.698771360999091,
-8.12888865088602));
#37822=CARTESIAN_POINT('Ctrl Pts',(97.7199308884093,-0.747485693921532,
-8.131940214555));
#37823=CARTESIAN_POINT('Ctrl Pts',(97.6896280054007,-0.794373819533371,
-8.13499177822398));
#37824=CARTESIAN_POINT('Ctrl Pts',(97.6830365696656,-0.804572851309346,
-8.1356555495823));
#37825=CARTESIAN_POINT('Ctrl Pts',(97.6763209229621,-0.814685599609082,
-8.13631932094062));
#37826=CARTESIAN_POINT('Ctrl Pts',(97.6694835840665,-0.824708966725532,
-8.13698309229894));
#37827=CARTESIAN_POINT('Ctrl Pts',(97.6384770190523,-0.870163812375409,
-8.13999322096016));
#37828=CARTESIAN_POINT('Ctrl Pts',(97.6048382945268,-0.913963102553137,
-8.14300334962138));
#37829=CARTESIAN_POINT('Ctrl Pts',(97.5687704363409,-0.955785887910356,
-8.1460134782826));
#37830=CARTESIAN_POINT('Ctrl Pts',(97.5327666809018,-0.997534342393602,
-8.14901825709703));
#37831=CARTESIAN_POINT('Ctrl Pts',(97.4943427015374,-1.03731286654272,-8.15202303591145));
#37832=CARTESIAN_POINT('Ctrl Pts',(97.4537438516837,-1.07483071099524,-8.15502781472588));
#37833=CARTESIAN_POINT('Ctrl Pts',(97.4131851676658,-1.11231143775637,-8.15802962080948));
#37834=CARTESIAN_POINT('Ctrl Pts',(97.370456261476,-1.14753555868958,-8.16103142689308));
#37835=CARTESIAN_POINT('Ctrl Pts',(97.3258404018259,-1.18024796903173,-8.16403323297668));
#37836=CARTESIAN_POINT('Ctrl Pts',(97.2812510599921,-1.21294093647409,-8.16703325491126));
#37837=CARTESIAN_POINT('Ctrl Pts',(97.2347774126897,-1.24312484061645,-8.17003327684584));
#37838=CARTESIAN_POINT('Ctrl Pts',(97.1867351927932,-1.27058530772654,-8.17303329878042));
#37839=CARTESIAN_POINT('Ctrl Pts',(97.1387025528057,-1.2980402990535,-8.1760327224925));
#37840=CARTESIAN_POINT('Ctrl Pts',(97.0891024196415,-1.3227726699336,-8.17903214620457));
#37841=CARTESIAN_POINT('Ctrl Pts',(97.038276850392,-1.34461301012647,-8.18203156991665));
#37842=CARTESIAN_POINT('Ctrl Pts',(96.9874045543932,-1.36647342934882,-8.18503375116439));
#37843=CARTESIAN_POINT('Ctrl Pts',(96.935305057744,-1.38543629698991,-8.18803593241213));
#37844=CARTESIAN_POINT('Ctrl Pts',(96.8823408390857,-1.4013802066619,-8.19103811365987));
#37845=CARTESIAN_POINT('Ctrl Pts',(96.8293525122906,-1.41733137364766,-8.19404166143388));
#37846=CARTESIAN_POINT('Ctrl Pts',(96.7754991932863,-1.4302607198618,-8.19704520920788));
#37847=CARTESIAN_POINT('Ctrl Pts',(96.7211557680833,-1.44009752759898,-8.20004875698189));
#37848=CARTESIAN_POINT('Ctrl Pts',(96.666709778811,-1.4499529006553,-8.20305797344684));
#37849=CARTESIAN_POINT('Ctrl Pts',(96.6117723609819,-1.45670401105588,-8.20606718991179));
#37850=CARTESIAN_POINT('Ctrl Pts',(96.5567246086163,-1.46033195133666,-8.20907640637675));
#37851=CARTESIAN_POINT('Ctrl Pts',(96.5146108220191,-1.46310747433635,-8.21137858029999));
#37852=CARTESIAN_POINT('Ctrl Pts',(96.4724326030032,-1.46405611982685,-8.21368075422325));
#37853=CARTESIAN_POINT('Ctrl Pts',(96.4303592880104,-1.46318998612773,-8.2159829281465));
#37854=CARTESIAN_POINT('Ctrl Pts',(96.3753477660521,-1.46205750267555,-8.21899305680768));
#37855=CARTESIAN_POINT('Ctrl Pts',(96.3202846147334,-1.45781592578264,-8.22200318546886));
#37856=CARTESIAN_POINT('Ctrl Pts',(96.2655495702991,-1.45045992959917,-8.22501331413004));
#37857=CARTESIAN_POINT('Ctrl Pts',(96.2109118054615,-1.44311700709362,-8.22801809294442));
#37858=CARTESIAN_POINT('Ctrl Pts',(96.1566015094434,-1.432670719714,-8.23102287175881));
#37859=CARTESIAN_POINT('Ctrl Pts',(96.102996252815,-1.4191676932558,-8.2340276505732));
#37860=CARTESIAN_POINT('Ctrl Pts',(96.049444029707,-1.40567802580518,-8.23702945665676));
#37861=CARTESIAN_POINT('Ctrl Pts',(95.9965959738366,-1.38913773831285,-8.24003126274032));
#37862=CARTESIAN_POINT('Ctrl Pts',(95.9448205192203,-1.36964468770713,-8.24303306882389));
#37863=CARTESIAN_POINT('Ctrl Pts',(95.8930758377866,-1.35016322296212,-8.24603309075843));
#37864=CARTESIAN_POINT('Ctrl Pts',(95.842402987282,-1.32773265933758,-8.24903311269297));
#37865=CARTESIAN_POINT('Ctrl Pts',(95.7931540266796,-1.30250029864732,-8.25203313462751));
#37866=CARTESIAN_POINT('Ctrl Pts',(95.7439148866177,-1.27727296944229,-8.25503255833954));
#37867=CARTESIAN_POINT('Ctrl Pts',(95.6960995423354,-1.24924519339181,-8.25803198205157));
#37868=CARTESIAN_POINT('Ctrl Pts',(95.6500367781202,-1.21861088742537,-8.2610314057636));
#37869=CARTESIAN_POINT('Ctrl Pts',(95.6039316658649,-1.18794841765161,-8.26403358701131));
#37870=CARTESIAN_POINT('Ctrl Pts',(95.5595827934227,-1.15467492349639,-8.26703576825901));
#37871=CARTESIAN_POINT('Ctrl Pts',(95.5172898988173,-1.1190276546032,-8.27003794950671));
#37872=CARTESIAN_POINT('Ctrl Pts',(95.4749777534251,-1.08336415986454,-8.27304149728068));
#37873=CARTESIAN_POINT('Ctrl Pts',(95.4347238359076,-1.04532509986401,-8.27604504505464));
#37874=CARTESIAN_POINT('Ctrl Pts',(95.3967922104908,-1.00518581184832,-8.2790485928286));
#37875=CARTESIAN_POINT('Ctrl Pts',(95.3587889955147,-0.964970767681657,
-8.28205780929351));
#37876=CARTESIAN_POINT('Ctrl Pts',(95.3231171694233,-0.922647981944113,
-8.28506702575842));
#37877=CARTESIAN_POINT('Ctrl Pts',(95.2900007960032,-0.878526300169629,
-8.28807624222333));
#37878=CARTESIAN_POINT('Ctrl Pts',(95.2646654131152,-0.844771405355678,
-8.2903784161469));
#37879=CARTESIAN_POINT('Ctrl Pts',(95.2408248836876,-0.809964347957286,
-8.29268059007048));
#37880=CARTESIAN_POINT('Ctrl Pts',(95.2185615998193,-0.774253562276169,
-8.29498276399405));
#37881=CARTESIAN_POINT('Ctrl Pts',(95.1894520055427,-0.727561147598254,
-8.29799289265546));
#37882=CARTESIAN_POINT('Ctrl Pts',(95.1629181506182,-0.679126695490427,
-8.30100302131687));
#37883=CARTESIAN_POINT('Ctrl Pts',(95.1391719819818,-0.629265335254224,
-8.30401314997828));
#37884=CARTESIAN_POINT('Ctrl Pts',(95.1154680169781,-0.57949259270458,-8.3070179287929));
#37885=CARTESIAN_POINT('Ctrl Pts',(95.0945421312549,-0.528298447719727,
-8.31002270760752));
#37886=CARTESIAN_POINT('Ctrl Pts',(95.0765615775312,-0.476024601965427,
-8.31302748642213));
#37887=CARTESIAN_POINT('Ctrl Pts',(95.0585988125865,-0.423802472521088,
-8.31602929250593));
#37888=CARTESIAN_POINT('Ctrl Pts',(95.0435757782425,-0.370503255274074,
-8.31903109858972));
#37889=CARTESIAN_POINT('Ctrl Pts',(95.0316118275887,-0.316488992270534,
-8.32203290467351));
#37890=CARTESIAN_POINT('Ctrl Pts',(95.0196549878109,-0.262506833104415,
-8.32503292660828));
#37891=CARTESIAN_POINT('Ctrl Pts',(95.0107537419261,-0.207810985136718,
-8.32803294854305));
#37892=CARTESIAN_POINT('Ctrl Pts',(95.0049770843418,-0.152776792365372,
-8.33103297047782));
#37893=CARTESIAN_POINT('Ctrl Pts',(94.999201578658,-0.0977535737447509,
-8.33403239419009));
#37894=CARTESIAN_POINT('Ctrl Pts',(94.9965494790006,-0.0423926692451935,
-8.33703181790235));
#37895=CARTESIAN_POINT('Ctrl Pts',(94.9970380211664,0.0129245999948381,
-8.34003124161461));
#37896=CARTESIAN_POINT('Ctrl Pts',(94.9975270124759,0.0682927254517481,
-8.34303342286254));
#37897=CARTESIAN_POINT('Ctrl Pts',(95.0011624095153,0.123616606271708,-8.34603560411046));
#37898=CARTESIAN_POINT('Ctrl Pts',(95.0079092850023,0.178515571519108,-8.34903778535839));
#37899=CARTESIAN_POINT('Ctrl Pts',(95.0146592315174,0.233439525556841,-8.35204133313258));
#37900=CARTESIAN_POINT('Ctrl Pts',(95.024523385504,0.287937657889964,-8.35504488090677));
#37901=CARTESIAN_POINT('Ctrl Pts',(95.0374154282645,0.341638364431615,-8.35804842868096));
#37902=CARTESIAN_POINT('Ctrl Pts',(95.050331802586,0.395440422019282,-8.36105764514609));
#37903=CARTESIAN_POINT('Ctrl Pts',(95.0662873289335,0.448441540391401,-8.36406686161122));
#37904=CARTESIAN_POINT('Ctrl Pts',(95.0851457684338,0.500285308109187,-8.36707607807635));
#37905=CARTESIAN_POINT('Ctrl Pts',(95.0995732475221,0.539947915112886,-8.3693782519981));
#37906=CARTESIAN_POINT('Ctrl Pts',(95.1156987231514,0.578933439619426,-8.37168042591986));
#37907=CARTESIAN_POINT('Ctrl Pts',(95.1334428963189,0.617091772109208,-8.37398259984161));
#37908=CARTESIAN_POINT('Ctrl Pts',(95.1566436821995,0.666984392819094,-8.37699272850269));
#37909=CARTESIAN_POINT('Ctrl Pts',(95.182710845181,0.715671604914427,-8.38000285716377));
#37910=CARTESIAN_POINT('Ctrl Pts',(95.2114962629664,0.762803711718899,-8.38301298582484));
#37911=CARTESIAN_POINT('Ctrl Pts',(95.2402305209534,0.809852051489189,-8.38601776463913));
#37912=CARTESIAN_POINT('Ctrl Pts',(95.2716731733469,0.855350323806835,-8.38902254345341));
#37913=CARTESIAN_POINT('Ctrl Pts',(95.3056294220346,0.898971745569833,-8.39202732226769));
#37914=CARTESIAN_POINT('Ctrl Pts',(95.3395520766398,0.942550011162923,-8.39502912835115));
#37915=CARTESIAN_POINT('Ctrl Pts',(95.3759830785269,0.984254689808661,-8.39803093443462));
#37916=CARTESIAN_POINT('Ctrl Pts',(95.4146844217983,1.02378800172987,-8.40103274051808));
#37917=CARTESIAN_POINT('Ctrl Pts',(95.4533627625966,1.06329781669037,-8.40403276245252));
#37918=CARTESIAN_POINT('Ctrl Pts',(95.4943084014814,1.1006384462905,-8.40703278438696));
#37919=CARTESIAN_POINT('Ctrl Pts',(95.5372446760263,1.13554701937008,-8.4100328063214));
#37920=CARTESIAN_POINT('Ctrl Pts',(95.5801723888186,1.17044863146918,-8.41303223003334));
#37921=CARTESIAN_POINT('Ctrl Pts',(95.6250895394138,1.20291881720026,-8.41603165374527));
#37922=CARTESIAN_POINT('Ctrl Pts',(95.6716861786677,1.23273478874661,-8.4190310774572));
#37923=CARTESIAN_POINT('Ctrl Pts',(95.7183256567825,1.26257817176033,-8.42203325870481));
#37924=CARTESIAN_POINT('Ctrl Pts',(95.7666472625621,1.28976218020096,-8.42503543995242));
#37925=CARTESIAN_POINT('Ctrl Pts',(95.8163130897231,1.31410806950236,-8.42803762120003));
#37926=CARTESIAN_POINT('Ctrl Pts',(95.8660015236662,1.33846504051217,-8.4310411689739));
#37927=CARTESIAN_POINT('Ctrl Pts',(95.9170349112087,1.35998111164486,-8.43404471674778));
#37928=CARTESIAN_POINT('Ctrl Pts',(95.9690548597294,1.37852553411864,-8.43704826452165));
#37929=CARTESIAN_POINT('Ctrl Pts',(96.0211729871483,1.39710495606895,-8.44005748098647));
#37930=CARTESIAN_POINT('Ctrl Pts',(96.074280887155,1.41270137636238,-8.4430666974513));
#37931=CARTESIAN_POINT('Ctrl Pts',(96.1280056151919,1.42523415691089,-8.44607591391612));
#37932=CARTESIAN_POINT('Ctrl Pts',(96.1691072339771,1.43482224766995,-8.44837808784047));
#37933=CARTESIAN_POINT('Ctrl Pts',(96.2105695565938,1.44261826540528,-8.45068026176483));
#37934=CARTESIAN_POINT('Ctrl Pts',(96.2522235336151,1.44860660591372,-8.45298243568918));
#37935=CARTESIAN_POINT('Ctrl Pts',(96.3066867645409,1.45643645543342,-8.4559925643501));
#37936=CARTESIAN_POINT('Ctrl Pts',(96.3617066105067,1.46120700645383,-8.45900269301103));
#37937=CARTESIAN_POINT('Ctrl Pts',(96.4169092576931,1.46285124249404,-8.46201282167196));
#37938=CARTESIAN_POINT('Ctrl Pts',(96.4720137942209,1.46449255626352,-8.46501760048609));
#37939=CARTESIAN_POINT('Ctrl Pts',(96.5272999636119,1.46301856605602,-8.46802237930021));
#37940=CARTESIAN_POINT('Ctrl Pts',(96.5823876392997,1.45841386752898,-8.47102715811434));
#37941=CARTESIAN_POINT('Ctrl Pts',(96.6374208148589,1.45381372458827,-8.47402896419764));
#37942=CARTESIAN_POINT('Ctrl Pts',(96.6922553620343,1.44608905273922,-8.47703077028094));
#37943=CARTESIAN_POINT('Ctrl Pts',(96.74651183676,1.43527648262532,-8.48003257636424));
#37944=CARTESIAN_POINT('Ctrl Pts',(96.8007360636878,1.42447033905457,-8.48303259829852));
#37945=CARTESIAN_POINT('Ctrl Pts',(96.8543823822712,1.41058003795155,-8.4860326202328));
#37946=CARTESIAN_POINT('Ctrl Pts',(96.9070794635753,1.39369365977409,-8.48903264216708));
#37947=CARTESIAN_POINT('Ctrl Pts',(96.9597660367627,1.37681064884258,-8.49203206587885));
#37948=CARTESIAN_POINT('Ctrl Pts',(97.0115032459361,1.3569329083871,-8.49503148959061));
#37949=CARTESIAN_POINT('Ctrl Pts',(97.0619351453074,1.33419829876907,-8.49803091330237));
#37950=CARTESIAN_POINT('Ctrl Pts',(97.1124134095059,1.31144278797029,-8.50103309454981));
#37951=CARTESIAN_POINT('Ctrl Pts',(97.1615834838807,1.28582537815449,-8.50403527579725));
#37952=CARTESIAN_POINT('Ctrl Pts',(97.2091110343805,1.25753140959865,-8.50703745704469));
#37953=CARTESIAN_POINT('Ctrl Pts',(97.2566602183662,1.2292245622564,-8.51004100481839));
#37954=CARTESIAN_POINT('Ctrl Pts',(97.3025649496152,1.19823902353762,-8.51304455259209));
#37955=CARTESIAN_POINT('Ctrl Pts',(97.3465198981824,1.16480351628688,-8.51604810036579));
#37956=CARTESIAN_POINT('Ctrl Pts',(97.3905578043177,1.13130490514315,-8.51905731683044));
#37957=CARTESIAN_POINT('Ctrl Pts',(97.4326381741408,1.09534743242449,-8.52206653329509));
#37958=CARTESIAN_POINT('Ctrl Pts',(97.4724896956406,1.05719938890008,-8.52507574975974));
#37959=CARTESIAN_POINT('Ctrl Pts',(97.5029777428691,1.02801457213837,-8.52737792368541));
#37960=CARTESIAN_POINT('Ctrl Pts',(97.5321619678664,0.997548474543418,-8.52968009761107));
#37961=CARTESIAN_POINT('Ctrl Pts',(97.5599369337489,0.965934153484868,-8.53198227153674));
#37962=CARTESIAN_POINT('Ctrl Pts',(97.5959137013808,0.924984289230303,-8.53496426534808));
#37963=CARTESIAN_POINT('Ctrl Pts',(97.6296825206123,0.881927048582567,-8.53794625915942));
#37964=CARTESIAN_POINT('Ctrl Pts',(97.6609847719527,0.83703215139049,-8.54092825297077));
#37965=CARTESIAN_POINT('Ctrl Pts',(97.692240926784,0.792203367591167,-8.5439058554205));
#37966=CARTESIAN_POINT('Ctrl Pts',(97.7210373999692,0.745542722705404,-8.54688345787024));
#37967=CARTESIAN_POINT('Ctrl Pts',(97.7471547911784,0.697354053073913,-8.54986106031997));
#37968=CARTESIAN_POINT('Ctrl Pts',(97.7732445159323,0.649216430258924,-8.5528355085609));
#37969=CARTESIAN_POINT('Ctrl Pts',(97.7966605255636,0.599554460627301,-8.55580995680183));
#37970=CARTESIAN_POINT('Ctrl Pts',(97.8172272417484,0.548700053470984,-8.55878440504276));
#37971=CARTESIAN_POINT('Ctrl Pts',(97.8377852922579,0.497867073545964,-8.56175760001591));
#37972=CARTESIAN_POINT('Ctrl Pts',(97.8554962169165,0.445843146258828,-8.56473079498905));
#37973=CARTESIAN_POINT('Ctrl Pts',(97.8702318258466,0.392981827642424,-8.56770398996219));
#37974=CARTESIAN_POINT('Ctrl Pts',(97.8849638022446,0.340133540074315,-8.57067645200153));
#37975=CARTESIAN_POINT('Ctrl Pts',(97.8967217797702,0.286448791372774,-8.57364891404087));
#37976=CARTESIAN_POINT('Ctrl Pts',(97.9054276944835,0.232295403278304,-8.57662137608021));
#37977=CARTESIAN_POINT('Ctrl Pts',(97.9141388930535,0.178109148017274,-8.57959564218774));
#37978=CARTESIAN_POINT('Ctrl Pts',(97.919794254375,0.123454219241105,-8.58256990829528));
#37979=CARTESIAN_POINT('Ctrl Pts',(97.9223673234851,0.068705747808685,-8.58554417440281));
#37980=CARTESIAN_POINT('Ctrl Pts',(97.9234633550916,0.0453849380947507,
-8.58681110098756));
#37981=CARTESIAN_POINT('Ctrl Pts',(97.9240007683061,0.0220471905637543,
-8.58807802757232));
#37982=CARTESIAN_POINT('Ctrl Pts',(97.9239803911309,-0.00127850362627049,
-8.58934495415707));
#37983=CARTESIAN_POINT('Origin',(96.460480949577,-8.32667268468867E-16,
1.18130019239114E-14));
#37984=CARTESIAN_POINT('',(97.9239808950412,0.000399532766094337,-9.16065504589061));
#37985=CARTESIAN_POINT('',(97.9239808729693,0.000473530088810134,-9.08934495421004));
#37986=CARTESIAN_POINT('',(97.923980949577,-1.01189432752408E-15,1.19922289829666E-14));
#37987=CARTESIAN_POINT('Ctrl Pts',(97.9239808950409,0.000399533638512916,
-9.1606550458429));
#37988=CARTESIAN_POINT('Ctrl Pts',(97.9239748177392,0.0226608147838017,
-9.15943762742574));
#37989=CARTESIAN_POINT('Ctrl Pts',(97.9234608417589,0.0449144548143451,
-9.15822020900858));
#37990=CARTESIAN_POINT('Ctrl Pts',(97.9224398574859,0.0671446318459906,
-9.15700279059142));
#37991=CARTESIAN_POINT('Ctrl Pts',(97.9199154218029,0.122109878251946,-9.15399266146905));
#37992=CARTESIAN_POINT('Ctrl Pts',(97.9142815808914,0.177048047496928,-9.15098253234669));
#37993=CARTESIAN_POINT('Ctrl Pts',(97.9055426216486,0.231579390079305,-9.14797240322433));
#37994=CARTESIAN_POINT('Ctrl Pts',(97.8968191939719,0.286013815269212,-9.14496762394028));
#37995=CARTESIAN_POINT('Ctrl Pts',(97.8850016826745,0.340042331438279,-9.14196284465623));
#37996=CARTESIAN_POINT('Ctrl Pts',(97.8701462548443,0.393288668951429,-9.13895806537219));
#37997=CARTESIAN_POINT('Ctrl Pts',(97.8553055239727,0.446482328128939,-9.13595625881414));
#37998=CARTESIAN_POINT('Ctrl Pts',(97.8374329715623,0.498894835391729,-9.1329544522561));
#37999=CARTESIAN_POINT('Ctrl Pts',(97.8166357481785,0.550160351379524,-9.12995264569806));
#38000=CARTESIAN_POINT('Ctrl Pts',(97.7958508857723,0.601395397343536,-9.12695262328508));
#38001=CARTESIAN_POINT('Ctrl Pts',(97.7721449959489,0.651484314848645,-9.12395260087211));
#38002=CARTESIAN_POINT('Ctrl Pts',(97.7456742438721,0.700078885768492,-9.12095257845913));
#38003=CARTESIAN_POINT('Ctrl Pts',(97.7192087701952,0.748663766688898,-9.11795315426557));
#38004=CARTESIAN_POINT('Ctrl Pts',(97.6899797816649,0.795754429287383,-9.114953730072));
#38005=CARTESIAN_POINT('Ctrl Pts',(97.6581894545535,0.841027102480651,-9.11195430587844));
#38006=CARTESIAN_POINT('Ctrl Pts',(97.6263699008356,0.886341397347103,-9.10895212414827));
#38007=CARTESIAN_POINT('Ctrl Pts',(97.5919846081353,0.929833930480223,-9.10594994241811));
#38008=CARTESIAN_POINT('Ctrl Pts',(97.5552783364075,0.971211064490668,-9.10294776068794));
#38009=CARTESIAN_POINT('Ctrl Pts',(97.5185553567869,1.0126070324684,-9.09994421243025));
#38010=CARTESIAN_POINT('Ctrl Pts',(97.4795096651337,1.05188530668701,-9.09694066417256));
#38011=CARTESIAN_POINT('Ctrl Pts',(97.4384231939164,1.08878887610795,-9.09393711591487));
#38012=CARTESIAN_POINT('Ctrl Pts',(97.3972591789663,1.12576209474541,-9.09092789897022));
#38013=CARTESIAN_POINT('Ctrl Pts',(97.3540471035433,1.1603513245554,-9.08791868202556));
#38014=CARTESIAN_POINT('Ctrl Pts',(97.3091013852761,1.19234039020483,-9.08490946508091));
#38015=CARTESIAN_POINT('Ctrl Pts',(97.2747161311802,1.21681329203075,-9.08260729496858));
#38016=CARTESIAN_POINT('Ctrl Pts',(97.2393168890532,1.23976519452232,-9.08030512485625));
#38017=CARTESIAN_POINT('Ctrl Pts',(97.2030541301642,1.26111748916295,-9.07800295474392));
#38018=CARTESIAN_POINT('Ctrl Pts',(97.1556399234842,1.28903599680548,-9.0749928260923));
#38019=CARTESIAN_POINT('Ctrl Pts',(97.106549428113,1.3143355000925,-9.07198269744068));
#38020=CARTESIAN_POINT('Ctrl Pts',(97.0561030366792,1.33681209575469,-9.06897256878906));
#38021=CARTESIAN_POINT('Ctrl Pts',(97.0057463026643,1.35924874418782,-9.06596778998226));
#38022=CARTESIAN_POINT('Ctrl Pts',(96.9540389333658,1.37887222826887,-9.06296301117545));
#38023=CARTESIAN_POINT('Ctrl Pts',(96.9013267540754,1.39552399716242,-9.05995823236864));
#38024=CARTESIAN_POINT('Ctrl Pts',(96.8486667247321,1.41215929189612,-9.05695642629144));
#38025=CARTESIAN_POINT('Ctrl Pts',(96.7950043557571,1.42582853717711,-9.05395462021423));
#38026=CARTESIAN_POINT('Ctrl Pts',(96.7407045939896,1.43642158126091,-9.05095281413702));
#38027=CARTESIAN_POINT('Ctrl Pts',(96.686437105726,1.44700832928305,-9.0479527922076));
#38028=CARTESIAN_POINT('Ctrl Pts',(96.6315334928645,1.45452239912856,-9.04495277027818));
#38029=CARTESIAN_POINT('Ctrl Pts',(96.5763707253807,1.45890431826908,-9.04195274834876));
#38030=CARTESIAN_POINT('Ctrl Pts',(96.5212189576633,1.46328536363025,-9.03895332464061));
#38031=CARTESIAN_POINT('Ctrl Pts',(96.4658086641142,1.46453545685631,-9.03595390093245));
#38032=CARTESIAN_POINT('Ctrl Pts',(96.4105214799486,1.46264701872818,-9.03295447722429));
#38033=CARTESIAN_POINT('Ctrl Pts',(96.3551834671884,1.46075684445347,-9.02995229597849));
#38034=CARTESIAN_POINT('Ctrl Pts',(96.2999693188758,1.45572239218327,-9.02695011473269));
#38035=CARTESIAN_POINT('Ctrl Pts',(96.2452587000085,1.44758821261113,-9.02394793348689));
#38036=CARTESIAN_POINT('Ctrl Pts',(96.1905231780621,1.43945033053805,-9.02094438571373));
#38037=CARTESIAN_POINT('Ctrl Pts',(96.1362921604736,1.42821001594495,-9.01794083794056));
#38038=CARTESIAN_POINT('Ctrl Pts',(96.0829349476038,1.41396296500086,-9.0149372901674));
#38039=CARTESIAN_POINT('Ctrl Pts',(96.0294770319419,1.39968902513713,-9.01192807370148));
#38040=CARTESIAN_POINT('Ctrl Pts',(95.9768967183659,1.38239717819773,-9.00891885723555));
#38041=CARTESIAN_POINT('Ctrl Pts',(95.9255468559991,1.36223264001712,-9.00590964076962));
#38042=CARTESIAN_POINT('Ctrl Pts',(95.8862621062263,1.34680594167364,-9.00360746681184));
#38043=CARTESIAN_POINT('Ctrl Pts',(95.8476971975314,1.32969892730821,-9.00130529285405));
#38044=CARTESIAN_POINT('Ctrl Pts',(95.8100001843338,1.31099466972547,-8.99900311889627));
#38045=CARTESIAN_POINT('Ctrl Pts',(95.7607107484999,1.28653855965879,-8.99599299034906));
#38046=CARTESIAN_POINT('Ctrl Pts',(95.7126988815147,1.25924749918696,-8.99298286180186));
#38047=CARTESIAN_POINT('Ctrl Pts',(95.6663104191203,1.22927841376727,-8.98997273325465));
#38048=CARTESIAN_POINT('Ctrl Pts',(95.6200044021485,1.19936259189157,-8.98696795455753));
#38049=CARTESIAN_POINT('Ctrl Pts',(95.5753165039784,1.1667784748072,-8.98396317586041));
#38050=CARTESIAN_POINT('Ctrl Pts',(95.5325684727805,1.13172906890532,-8.9809583971633));
#38051=CARTESIAN_POINT('Ctrl Pts',(95.4898627337063,1.09671433860767,-8.97795659119893));
#38052=CARTESIAN_POINT('Ctrl Pts',(95.4490934661905,1.05923948422606,-8.97495478523457));
#38053=CARTESIAN_POINT('Ctrl Pts',(95.4105523308054,1.01954997203883,-8.9719529792702));
#38054=CARTESIAN_POINT('Ctrl Pts',(95.3720341026954,0.979884049674879,-8.96895295745657));
#38055=CARTESIAN_POINT('Ctrl Pts',(95.3357417490241,0.938006456621444,-8.96595293564295));
#38056=CARTESIAN_POINT('Ctrl Pts',(95.3019310545548,0.894200419785157,-8.96295291382932));
#38057=CARTESIAN_POINT('Ctrl Pts',(95.2681271021593,0.850403118159582,-8.95995349023969));
#38058=CARTESIAN_POINT('Ctrl Pts',(95.2368041486956,0.804678554277653,-8.95695406665006));
#38059=CARTESIAN_POINT('Ctrl Pts',(95.2081770659551,0.757342216613798,-8.95395464306043));
#38060=CARTESIAN_POINT('Ctrl Pts',(95.1795236647701,0.709962360063037,-8.95095246193648));
#38061=CARTESIAN_POINT('Ctrl Pts',(95.1535713598329,0.660968222178031,-8.94795028081252));
#38062=CARTESIAN_POINT('Ctrl Pts',(95.130490286213,0.610702124905847,-8.94494809968857));
#38063=CARTESIAN_POINT('Ctrl Pts',(95.1073987066075,0.560413147636743,-8.94194455203929));
#38064=CARTESIAN_POINT('Ctrl Pts',(95.0871811566967,0.50885154937697,-8.93894100439001));
#38065=CARTESIAN_POINT('Ctrl Pts',(95.0699592726423,0.456378917101341,-8.93593745674073));
#38066=CARTESIAN_POINT('Ctrl Pts',(95.0527048851785,0.40380725155866,-8.93292824040049));
#38067=CARTESIAN_POINT('Ctrl Pts',(95.0384575942161,0.350321628757899,-8.92991902406025));
#38068=CARTESIAN_POINT('Ctrl Pts',(95.0272885729733,0.296296914673333,-8.92690980772));
#38069=CARTESIAN_POINT('Ctrl Pts',(95.0187438100355,0.254965775212202,-8.92460763282959));
#38070=CARTESIAN_POINT('Ctrl Pts',(95.0119996768107,0.213319403626447,-8.92230545793917));
#38071=CARTESIAN_POINT('Ctrl Pts',(95.0070674939591,0.171527190348247,-8.92000328304876));
#38072=CARTESIAN_POINT('Ctrl Pts',(95.0006185897725,0.116883235068071,-8.91699315432163));
#38073=CARTESIAN_POINT('Ctrl Pts',(94.9972420918849,0.0617602724040382,
-8.9139830255945));
#38074=CARTESIAN_POINT('Ctrl Pts',(94.9969955342547,0.00653369260061267,
-8.91097289686737));
#38075=CARTESIAN_POINT('Ctrl Pts',(94.9967494148268,-0.0485947340357235,
-8.90796811798572));
#38076=CARTESIAN_POINT('Ctrl Pts',(94.9996221986122,-0.103825888511681,
-8.90496333910406));
#38077=CARTESIAN_POINT('Ctrl Pts',(95.0056196641916,-0.158779376137817,
-8.9019585602224));
#38078=CARTESIAN_POINT('Ctrl Pts',(95.0116111962741,-0.213678496407335,
-8.89895675407081));
#38079=CARTESIAN_POINT('Ctrl Pts',(95.0207212293115,-0.268299971587273,
-8.89595494791922));
#38080=CARTESIAN_POINT('Ctrl Pts',(95.032903540841,-0.322265406251912,-8.89295314176763));
#38081=CARTESIAN_POINT('Ctrl Pts',(95.0450786117127,-0.376198766112767,
-8.88995311976443));
#38082=CARTESIAN_POINT('Ctrl Pts',(95.0603222256967,-0.429476344186914,
-8.88695309776122));
#38083=CARTESIAN_POINT('Ctrl Pts',(95.0785369323875,-0.481729159750651,
-8.88395307575802));
#38084=CARTESIAN_POINT('Ctrl Pts',(95.0967480069588,-0.533971555796207,
-8.88095365197682));
#38085=CARTESIAN_POINT('Ctrl Pts',(95.1179288239113,-0.585189096742762,
-8.87795422819562));
#38086=CARTESIAN_POINT('Ctrl Pts',(95.1419325582224,-0.635029439991598,
-8.87495480441441));
#38087=CARTESIAN_POINT('Ctrl Pts',(95.1659583604917,-0.684915604220037,
-8.87195262309731));
#38088=CARTESIAN_POINT('Ctrl Pts',(95.1928120354714,-0.733421564348278,
-8.8689504417802));
#38089=CARTESIAN_POINT('Ctrl Pts',(95.2222998404152,-0.780217784285143,
-8.8659482604631));
#38090=CARTESIAN_POINT('Ctrl Pts',(95.2518010675552,-0.827035304825718,
-8.86294471261949));
#38091=CARTESIAN_POINT('Ctrl Pts',(95.2839385077947,-0.872141102954705,
-8.85994116477589));
#38092=CARTESIAN_POINT('Ctrl Pts',(95.3184757837967,-0.915235735387955,
-8.85693761693229));
#38093=CARTESIAN_POINT('Ctrl Pts',(95.3530782430878,-0.958411701678599,
-8.85392840039822));
#38094=CARTESIAN_POINT('Ctrl Pts',(95.3900892320945,-0.999568526048704,
-8.85091918386416));
#38095=CARTESIAN_POINT('Ctrl Pts',(95.4292336792077,-1.03844177369548,-8.84790996733009));
#38096=CARTESIAN_POINT('Ctrl Pts',(95.4591807777146,-1.06818139354997,-8.84560779395378));
#38097=CARTESIAN_POINT('Ctrl Pts',(95.4903757469049,-1.09658518088179,-8.84330562057747));
#38098=CARTESIAN_POINT('Ctrl Pts',(95.5226829035798,-1.12355110027266,-8.84100344720117));
#38099=CARTESIAN_POINT('Ctrl Pts',(95.5649250296687,-1.15880947285163,-8.83799331854705));
#38100=CARTESIAN_POINT('Ctrl Pts',(95.6092470880068,-1.19175635038038,-8.83498318989293));
#38101=CARTESIAN_POINT('Ctrl Pts',(95.6553661155136,-1.22213843486369,-8.83197306123881));
#38102=CARTESIAN_POINT('Ctrl Pts',(95.7014031765153,-1.2524665218232,-8.82896828243136));
#38103=CARTESIAN_POINT('Ctrl Pts',(95.7492304312742,-1.28023857365049,-8.82596350362391));
#38104=CARTESIAN_POINT('Ctrl Pts',(95.7985324464156,-1.30524190446156,-8.82295872481646));
#38105=CARTESIAN_POINT('Ctrl Pts',(95.8477856853823,-1.33022049861977,-8.81995691873976));
#38106=CARTESIAN_POINT('Ctrl Pts',(95.8985103257694,-1.3524355602715,-8.81695511266306));
#38107=CARTESIAN_POINT('Ctrl Pts',(95.9503641954715,-1.37171904819494,-8.81395330658636));
#38108=CARTESIAN_POINT('Ctrl Pts',(96.0021872453858,-1.39099107481361,-8.81095328465859));
#38109=CARTESIAN_POINT('Ctrl Pts',(96.05513770031,-1.40733479755419,-8.80795326273082));
#38110=CARTESIAN_POINT('Ctrl Pts',(96.1088532824566,-1.42063022413133,-8.80495324080305));
#38111=CARTESIAN_POINT('Ctrl Pts',(96.1625581533932,-1.43392299952051,-8.80195381709769));
#38112=CARTESIAN_POINT('Ctrl Pts',(96.217027336194,-1.44416855909082,-8.79895439339232));
#38113=CARTESIAN_POINT('Ctrl Pts',(96.2718855098507,-1.45129735413334,-8.79595496968695));
#38114=CARTESIAN_POINT('Ctrl Pts',(96.3267941176565,-1.4584327030709,-8.7929527884457));
#38115=CARTESIAN_POINT('Ctrl Pts',(96.38209190596,-1.4624454945538,-8.78995060720445));
#38116=CARTESIAN_POINT('Ctrl Pts',(96.437397019156,-1.46331793611516,-8.78694842596319));
#38117=CARTESIAN_POINT('Ctrl Pts',(96.492727306014,-1.46419077479258,-8.78394487819557));
#38118=CARTESIAN_POINT('Ctrl Pts',(96.5480643958186,-1.46192043578959,-8.78094133042795));
#38119=CARTESIAN_POINT('Ctrl Pts',(96.6030283411271,-1.45654127684809,-8.77793778266033));
#38120=CARTESIAN_POINT('Ctrl Pts',(96.6580960216373,-1.45115196564887,-8.77492856620149));
#38121=CARTESIAN_POINT('Ctrl Pts',(96.7127886276902,-1.44264219491228,-8.77191934974266));
#38122=CARTESIAN_POINT('Ctrl Pts',(96.7667343899895,-1.43109785837151,-8.76891013328383));
#38123=CARTESIAN_POINT('Ctrl Pts',(96.8080051100655,-1.42226596756989,-8.76660795930709));
#38124=CARTESIAN_POINT('Ctrl Pts',(96.8488388658894,-1.41165905690412,-8.76430578533036));
#38125=CARTESIAN_POINT('Ctrl Pts',(96.8890760631564,-1.39933501300291,-8.76200361135362));
#38126=CARTESIAN_POINT('Ctrl Pts',(96.9416868308212,-1.38322113195709,-8.75899348270548));
#38127=CARTESIAN_POINT('Ctrl Pts',(96.9934981260025,-1.36410225986774,-8.75598335405734));
#38128=CARTESIAN_POINT('Ctrl Pts',(97.0441431948968,-1.34207698489628,-8.75297322540921));
#38129=CARTESIAN_POINT('Ctrl Pts',(97.0946982532261,-1.32009085504767,-8.74996844660827));
#38130=CARTESIAN_POINT('Ctrl Pts',(97.1440907181985,-1.2952087821968,-8.74696366780734));
#38131=CARTESIAN_POINT('Ctrl Pts',(97.1919701081049,-1.26757873954884,-8.7439588890064));
#38132=CARTESIAN_POINT('Ctrl Pts',(97.2398021292832,-1.23997603225283,-8.74095708293653));
#38133=CARTESIAN_POINT('Ctrl Pts',(97.2861235855885,-1.20963100336278,-8.73795527686666));
#38134=CARTESIAN_POINT('Ctrl Pts',(97.3306067764798,-1.17673841415872,-8.73495347079679));
#38135=CARTESIAN_POINT('Ctrl Pts',(97.3750635284043,-1.14386537494774,-8.73195344887615));
#38136=CARTESIAN_POINT('Ctrl Pts',(97.4176837567095,-1.10844808996118,-8.72895342695551));
#38137=CARTESIAN_POINT('Ctrl Pts',(97.4581690174657,-1.07072441327945,-8.72595340503488));
#38138=CARTESIAN_POINT('Ctrl Pts',(97.4986462052135,-1.0330082589293,-8.72295398133694));
#38139=CARTESIAN_POINT('Ctrl Pts',(97.5369888847219,-0.992986986064892,
-8.719954557639));
#38140=CARTESIAN_POINT('Ctrl Pts',(97.5729337331488,-0.950936934987414,
-8.71695513394106));
#38141=CARTESIAN_POINT('Ctrl Pts',(97.6089116276557,-0.908848224980831,
-8.71395295270764));
#38142=CARTESIAN_POINT('Ctrl Pts',(97.6424869429693,-0.864727412699082,
-8.71095077147421));
#38143=CARTESIAN_POINT('Ctrl Pts',(97.673436133015,-0.818884590751871,-8.70794859024079));
#38144=CARTESIAN_POINT('Ctrl Pts',(97.7043994104438,-0.773020902171533,
-8.70494504248123));
#38145=CARTESIAN_POINT('Ctrl Pts',(97.7327339090918,-0.725434095993351,
-8.70194149472166));
#38146=CARTESIAN_POINT('Ctrl Pts',(97.7582608027001,-0.676461161359394,
-8.6989379469621));
#38147=CARTESIAN_POINT('Ctrl Pts',(97.7838358740242,-0.627395798553031,
-8.69592873051161));
#38148=CARTESIAN_POINT('Ctrl Pts',(97.8065925373085,-0.576939563854436,
-8.69291951406113));
#38149=CARTESIAN_POINT('Ctrl Pts',(97.826399597581,-0.525450756051471,-8.68991029761064));
#38150=CARTESIAN_POINT('Ctrl Pts',(97.8415528112552,-0.486059705802819,
-8.68760812357577));
#38151=CARTESIAN_POINT('Ctrl Pts',(97.8549806423813,-0.446064760952756,
-8.6853059495409));
#38152=CARTESIAN_POINT('Ctrl Pts',(97.8666443708632,-0.405631215066805,
-8.68300377550604));
#38153=CARTESIAN_POINT('Ctrl Pts',(97.8855156283708,-0.340212009061028,
-8.6792789872356));
#38154=CARTESIAN_POINT('Ctrl Pts',(97.8998320831828,-0.273424344156363,
-8.67555419896517));
#38155=CARTESIAN_POINT('Ctrl Pts',(97.9094335351068,-0.205836476083635,
-8.67182941069473));
#38156=CARTESIAN_POINT('Ctrl Pts',(97.9190349870308,-0.138248608010908,
-8.66810462242429));
#38157=CARTESIAN_POINT('Ctrl Pts',(97.9239212489841,-0.0698603808178389,
-8.66437983415386));
#38158=CARTESIAN_POINT('Ctrl Pts',(97.9239804054011,-0.00126206278290129,
-8.66065504588342));
#38159=CARTESIAN_POINT('Ctrl Pts',(97.9239803911303,-0.0012785042514516,
-8.58934495419103));
#38160=CARTESIAN_POINT('Ctrl Pts',(97.9239200622951,-0.0703367154818267,
-8.59309582578319));
#38161=CARTESIAN_POINT('Ctrl Pts',(97.9189678486473,-0.139181005785864,
-8.59684669737536));
#38162=CARTESIAN_POINT('Ctrl Pts',(97.9092372158365,-0.2072137325898,-8.60059756896753));
#38163=CARTESIAN_POINT('Ctrl Pts',(97.9002572469804,-0.269998114631265,
-8.60405908177312));
#38164=CARTESIAN_POINT('Ctrl Pts',(97.8872083114429,-0.332091715069842,
-8.60752059457871));
#38165=CARTESIAN_POINT('Ctrl Pts',(97.8702152329669,-0.393041346724699,
-8.61098210738429));
#38166=CARTESIAN_POINT('Ctrl Pts',(97.8554380660434,-0.446043095769913,
-8.61399223604393));
#38167=CARTESIAN_POINT('Ctrl Pts',(97.8376366364107,-0.498321683240691,
-8.61700236470357));
#38168=CARTESIAN_POINT('Ctrl Pts',(97.8169002182971,-0.549507977599035,
-8.62001249336321));
#38169=CARTESIAN_POINT('Ctrl Pts',(97.7962006546411,-0.600603299489819,
-8.62301727217607));
#38170=CARTESIAN_POINT('Ctrl Pts',(97.7725766509802,-0.650609695299955,
-8.62602205098893));
#38171=CARTESIAN_POINT('Ctrl Pts',(97.7461672626046,-0.699173050462825,
-8.62902682980179));
#38172=CARTESIAN_POINT('Ctrl Pts',(97.7197840019434,-0.747688360231573,
-8.63202863588384));
#38173=CARTESIAN_POINT('Ctrl Pts',(97.6906210664925,-0.794762995788685,
-8.63503044196589));
#38174=CARTESIAN_POINT('Ctrl Pts',(97.6588648612092,-0.840064432255704,
-8.63803224804794));
#38175=CARTESIAN_POINT('Ctrl Pts',(97.6271275304969,-0.885338943428206,
-8.64103226998098));
#38176=CARTESIAN_POINT('Ctrl Pts',(97.5928002875123,-0.928841912857858,
-8.64403229191403));
#38177=CARTESIAN_POINT('Ctrl Pts',(97.5561133566788,-0.970268972248528,
-8.64703231384707));
#38178=CARTESIAN_POINT('Ctrl Pts',(97.519433741441,-1.01168777083333,-8.65003173755762));
#38179=CARTESIAN_POINT('Ctrl Pts',(97.4803957227518,-1.05103108631773,-8.65303116126817));
#38180=CARTESIAN_POINT('Ctrl Pts',(97.439268887824,-1.08802868617618,-8.65603058497872));
#38181=CARTESIAN_POINT('Ctrl Pts',(97.3981042427277,-1.12506029996945,-8.65903276622497));
#38182=CARTESIAN_POINT('Ctrl Pts',(97.3548473382227,-1.1597415356758,-8.66203494747123));
#38183=CARTESIAN_POINT('Ctrl Pts',(97.3098025097481,-1.19184107054108,-8.66503712871748));
#38184=CARTESIAN_POINT('Ctrl Pts',(97.2647371778672,-1.22395521640227,-8.66804067649002));
#38185=CARTESIAN_POINT('Ctrl Pts',(97.2178827472799,-1.25348503680048,-8.67104422426255));
#38186=CARTESIAN_POINT('Ctrl Pts',(97.1695715731776,-1.28024323373403,-8.67404777203509));
#38187=CARTESIAN_POINT('Ctrl Pts',(97.1211692198638,-1.30705193226152,-8.67705698849862));
#38188=CARTESIAN_POINT('Ctrl Pts',(97.0713051076994,-1.33107832783885,-8.68006620496214));
#38189=CARTESIAN_POINT('Ctrl Pts',(97.0203341002193,-1.35218219915658,-8.68307542142567));
#38190=CARTESIAN_POINT('Ctrl Pts',(96.9813391903137,-1.36832752571337,-8.68537759536107));
#38191=CARTESIAN_POINT('Ctrl Pts',(96.9416969107454,-1.38276330684513,-8.68767976929647));
#38192=CARTESIAN_POINT('Ctrl Pts',(96.9015715221215,-1.39544665136734,-8.68998194323187));
#38193=CARTESIAN_POINT('Ctrl Pts',(96.8491069448719,-1.41203032398191,-8.69299207189151));
#38194=CARTESIAN_POINT('Ctrl Pts',(96.7955955896307,-1.42568596254133,-8.69600220055116));
#38195=CARTESIAN_POINT('Ctrl Pts',(96.7413953930831,-1.43628664459072,-8.6990123292108));
#38196=CARTESIAN_POINT('Ctrl Pts',(96.6872915255573,-1.44686848624104,-8.70201710802362));
#38197=CARTESIAN_POINT('Ctrl Pts',(96.6325017603913,-1.45440604574695,-8.70502188683643));
#38198=CARTESIAN_POINT('Ctrl Pts',(96.5773986573295,-1.45882229884722,-8.70802666564925));
#38199=CARTESIAN_POINT('Ctrl Pts',(96.5223500696595,-1.46323418279668,-8.71102847173122));
#38200=CARTESIAN_POINT('Ctrl Pts',(96.4669892820208,-1.46453083556759,-8.71403027781319));
#38201=CARTESIAN_POINT('Ctrl Pts',(96.4116966438851,-1.46268668603982,-8.71703208389516));
#38202=CARTESIAN_POINT('Ctrl Pts',(96.3564368694002,-1.46084363259806,-8.7200321058281));
#38203=CARTESIAN_POINT('Ctrl Pts',(96.3012456909032,-1.45586349447276,-8.72303212776103));
#38204=CARTESIAN_POINT('Ctrl Pts',(96.2465038187545,-1.4477727851721,-8.72603214969396));
#38205=CARTESIAN_POINT('Ctrl Pts',(96.1917728624664,-1.43968368920783,-8.72903157340438));
#38206=CARTESIAN_POINT('Ctrl Pts',(96.1374915567438,-1.42848533106342,-8.73203099711479));
#38207=CARTESIAN_POINT('Ctrl Pts',(96.0840335299944,-1.41425584329343,-8.73503042082521));
#38208=CARTESIAN_POINT('Ctrl Pts',(96.0305263563324,-1.40001327357046,-8.73803260207128));
#38209=CARTESIAN_POINT('Ctrl Pts',(95.9778444852455,-1.38273414292416,-8.74103478331735));
#38210=CARTESIAN_POINT('Ctrl Pts',(95.9263479434552,-1.36254694663021,-8.74403696456342));
#38211=CARTESIAN_POINT('Ctrl Pts',(95.8748279615823,-1.34235056157267,-8.74704051233575));
#38212=CARTESIAN_POINT('Ctrl Pts',(95.8244948653259,-1.31924369291081,-8.75004406010807));
#38213=CARTESIAN_POINT('Ctrl Pts',(95.7756871193749,-1.29340235816901,-8.7530476078804));
#38214=CARTESIAN_POINT('Ctrl Pts',(95.7267872570173,-1.26751225225669,-8.75605682434369));
#38215=CARTESIAN_POINT('Ctrl Pts',(95.679418948962,-1.23887764455704,-8.75906604080697));
#38216=CARTESIAN_POINT('Ctrl Pts',(95.6338935303719,-1.20771912645777,-8.76207525727026));
#38217=CARTESIAN_POINT('Ctrl Pts',(95.5990647191515,-1.1838815829843,-8.76437743120665));
#38218=CARTESIAN_POINT('Ctrl Pts',(95.5653139779917,-1.15856776108484,-8.76667960514303));
#38219=CARTESIAN_POINT('Ctrl Pts',(95.5327669807653,-1.13189179786391,-8.76898177907942));
#38220=CARTESIAN_POINT('Ctrl Pts',(95.4902112694213,-1.09701255592482,-8.77199190775025));
#38221=CARTESIAN_POINT('Ctrl Pts',(95.4495359100341,-1.0596567429178,-8.77500203642108));
#38222=CARTESIAN_POINT('Ctrl Pts',(95.411042778776,-1.02005479052148,-8.7780121650919));
#38223=CARTESIAN_POINT('Ctrl Pts',(95.372618060658,-0.980523221952778,-8.78101694391595));
#38224=CARTESIAN_POINT('Ctrl Pts',(95.3363682390082,-0.938753811825842,
-8.78402172273999));
#38225=CARTESIAN_POINT('Ctrl Pts',(95.3025613889011,-0.895016503202071,
-8.78702650156404));
#38226=CARTESIAN_POINT('Ctrl Pts',(95.2687879850711,-0.851322465398916,
-8.79002830765726));
#38227=CARTESIAN_POINT('Ctrl Pts',(95.2374530863764,-0.805664801623698,
-8.79303011375049));
#38228=CARTESIAN_POINT('Ctrl Pts',(95.208785930777,-0.758348092838164,-8.79603191984371));
#38229=CARTESIAN_POINT('Ctrl Pts',(95.1801358137459,-0.711059507141787,
-8.7990319417879));
#38230=CARTESIAN_POINT('Ctrl Pts',(95.154150570165,-0.662114281668448,-8.80203196373209));
#38231=CARTESIAN_POINT('Ctrl Pts',(95.1310160129044,-0.61184575847036,-8.80503198567627));
#38232=CARTESIAN_POINT('Ctrl Pts',(95.1078860688147,-0.561587259120174,
-8.80803140939792));
#38233=CARTESIAN_POINT('Ctrl Pts',(95.0876059028056,-0.51000646556631,-8.81103083311956));
#38234=CARTESIAN_POINT('Ctrl Pts',(95.0703142258555,-0.457458992978983,
-8.81403025684121));
#38235=CARTESIAN_POINT('Ctrl Pts',(95.0530066517137,-0.404863210603937,
-8.8170324380984));
#38236=CARTESIAN_POINT('Ctrl Pts',(95.0386932211769,-0.351299476376848,
-8.82003461935559));
#38237=CARTESIAN_POINT('Ctrl Pts',(95.0274630331812,-0.297139531682706,
-8.82303680061277));
#38238=CARTESIAN_POINT('Ctrl Pts',(95.0162277334534,-0.24295493458509,-8.82604034839616));
#38239=CARTESIAN_POINT('Ctrl Pts',(95.0080785517375,-0.188174109318222,
-8.82904389617956));
#38240=CARTESIAN_POINT('Ctrl Pts',(95.0030530043974,-0.133176704454972,
-8.83204744396295));
#38241=CARTESIAN_POINT('Ctrl Pts',(94.9980179721828,-0.0780755012498627,
-8.83505666043708));
#38242=CARTESIAN_POINT('Ctrl Pts',(94.9961183693583,-0.0227574309915909,
-8.83806587691121));
#38243=CARTESIAN_POINT('Ctrl Pts',(94.997339557011,0.0323962244713164,-8.84107509338534));
#38244=CARTESIAN_POINT('Ctrl Pts',(94.9982738155799,0.0745910297559468,
-8.84337726723256));
#38245=CARTESIAN_POINT('Ctrl Pts',(95.0010335501691,0.116689555092574,-8.84567944107978));
#38246=CARTESIAN_POINT('Ctrl Pts',(95.0055918355963,0.158524181184871,-8.847981614927));
#38247=CARTESIAN_POINT('Ctrl Pts',(95.0115518657483,0.213223615191785,-8.85099174357379));
#38248=CARTESIAN_POINT('Ctrl Pts',(95.0206135077032,0.267701392552597,-8.85400187222059));
#38249=CARTESIAN_POINT('Ctrl Pts',(95.0327487126871,0.321578776888731,-8.85701200086738));
#38250=CARTESIAN_POINT('Ctrl Pts',(95.0448623499927,0.375360405933311,-8.86001677966749));
#38251=CARTESIAN_POINT('Ctrl Pts',(95.0600385946801,0.428543248514046,-8.86302155846759));
#38252=CARTESIAN_POINT('Ctrl Pts',(95.0781978373417,0.480755288716801,-8.8660263372677));
#38253=CARTESIAN_POINT('Ctrl Pts',(95.0963391144416,0.532915673756977,-8.86902814333706));
#38254=CARTESIAN_POINT('Ctrl Pts',(95.1174573707341,0.584106662664619,-8.87202994940641));
#38255=CARTESIAN_POINT('Ctrl Pts',(95.1414227661909,0.633969840640893,-8.87503175547577));
#38256=CARTESIAN_POINT('Ctrl Pts',(95.1653739176115,0.68380338201401,-8.8780317773962));
#38257=CARTESIAN_POINT('Ctrl Pts',(95.1921686257863,0.732310201650655,-8.88103179931664));
#38258=CARTESIAN_POINT('Ctrl Pts',(95.2216292352011,0.779152539486286,-8.88403182123707));
#38259=CARTESIAN_POINT('Ctrl Pts',(95.2510839699935,0.825985536678473,-8.88703124493512));
#38260=CARTESIAN_POINT('Ctrl Pts',(95.2832032692917,0.871154264424761,-8.89003066863317));
#38261=CARTESIAN_POINT('Ctrl Pts',(95.317765086957,0.91434824181847,-8.89303009233122));
#38262=CARTESIAN_POINT('Ctrl Pts',(95.3523586792113,0.957581929822697,-8.89603227356523));
#38263=CARTESIAN_POINT('Ctrl Pts',(95.3893989454749,0.998836827102428,-8.89903445479925));
#38264=CARTESIAN_POINT('Ctrl Pts',(95.4286232256451,1.03783519287118,-8.90203663603327));
#38265=CARTESIAN_POINT('Ctrl Pts',(95.4678653598388,1.0768513098323,-8.90504018379369));
#38266=CARTESIAN_POINT('Ctrl Pts',(95.5092930939115,1.11360849667038,-8.90804373155411));
#38267=CARTESIAN_POINT('Ctrl Pts',(95.5526089607629,1.14786789393499,-8.91104727931453));
#38268=CARTESIAN_POINT('Ctrl Pts',(95.5960065790295,1.18219195005124,-8.91405649576631));
#38269=CARTESIAN_POINT('Ctrl Pts',(95.6412990155778,1.21400849501656,-8.91706571221808));
#38270=CARTESIAN_POINT('Ctrl Pts',(95.688158937957,1.24312145841316,-8.92007492866986));
#38271=CARTESIAN_POINT('Ctrl Pts',(95.7240087009461,1.26539406973398,-8.92237710270476));
#38272=CARTESIAN_POINT('Ctrl Pts',(95.7607752599711,1.28608518851768,-8.92467927673965));
#38273=CARTESIAN_POINT('Ctrl Pts',(95.7983035175063,1.30512577878773,-8.92698145077455));
#38274=CARTESIAN_POINT('Ctrl Pts',(95.8473723027826,1.33002164917598,-8.92999157942976));
#38275=CARTESIAN_POINT('Ctrl Pts',(95.8979501531717,1.35219872387525,-8.93300170808497));
#38276=CARTESIAN_POINT('Ctrl Pts',(95.949704541023,1.3714735544168,-8.93601183674018));
#38277=CARTESIAN_POINT('Ctrl Pts',(96.0013669467394,1.39071412815159,-8.93901661554832));
#38278=CARTESIAN_POINT('Ctrl Pts',(96.0542012493329,1.40706251119737,-8.94202139435647));
#38279=CARTESIAN_POINT('Ctrl Pts',(96.1078523771949,1.42038211053918,-8.94502617316461));
#38280=CARTESIAN_POINT('Ctrl Pts',(96.1614504261514,1.4336885323434,-8.94802797924176));
#38281=CARTESIAN_POINT('Ctrl Pts',(96.2158631895059,1.44397197970279,-8.95102978531892));
#38282=CARTESIAN_POINT('Ctrl Pts',(96.2707195411358,1.45114536069492,-8.95403159139607));
#38283=CARTESIAN_POINT('Ctrl Pts',(96.3255432884229,1.45831447812658,-8.95703161332405));
#38284=CARTESIAN_POINT('Ctrl Pts',(96.3808095788004,1.46237712468836,-8.96003163525204));
#38285=CARTESIAN_POINT('Ctrl Pts',(96.4361384588475,1.46329754087987,-8.96303165718002));
#38286=CARTESIAN_POINT('Ctrl Pts',(96.4914563059789,1.46421777353478,-8.96603108088536));
#38287=CARTESIAN_POINT('Ctrl Pts',(96.5468361902465,1.46199701140092,-8.9690305045907));
#38288=CARTESIAN_POINT('Ctrl Pts',(96.6018967503953,1.45665157854544,-8.97202992829604));
#38289=CARTESIAN_POINT('Ctrl Pts',(96.6570079307514,1.45130123133895,-8.97503210953689));
#38290=CARTESIAN_POINT('Ctrl Pts',(96.7117986736951,1.44282052530622,-8.97803429077774));
#38291=CARTESIAN_POINT('Ctrl Pts',(96.7658928473922,1.43127768887555,-8.98103647201859));
#38292=CARTESIAN_POINT('Ctrl Pts',(96.8200116435546,1.41972959840232,-8.98404001978561));
#38293=CARTESIAN_POINT('Ctrl Pts',(96.8734327281375,1.40511673864492,-8.98704356755263));
#38294=CARTESIAN_POINT('Ctrl Pts',(96.9257935150648,1.38755773443815,-8.99004711531964));
#38295=CARTESIAN_POINT('Ctrl Pts',(96.9782531241647,1.36996559056631,-8.99305633177754));
#38296=CARTESIAN_POINT('Ctrl Pts',(97.0296479464591,1.34941639112559,-8.99606554823543));
#38297=CARTESIAN_POINT('Ctrl Pts',(97.0796349145283,1.32607715374524,-8.99907476469333));
#38298=CARTESIAN_POINT('Ctrl Pts',(97.1178769947014,1.30822168017775,-9.00137693866959));
#38299=CARTESIAN_POINT('Ctrl Pts',(97.1552954661095,1.28873424402383,-9.00367911264585));
#38300=CARTESIAN_POINT('Ctrl Pts',(97.1917477645958,1.26770702264061,-9.00598128662211));
#38301=CARTESIAN_POINT('Ctrl Pts',(97.2394097189393,1.24021359953267,-9.0089914153521));
#38302=CARTESIAN_POINT('Ctrl Pts',(97.2856191558644,1.20997075436872,-9.01200154408208));
#38303=CARTESIAN_POINT('Ctrl Pts',(97.3300407405297,1.17715675250085,-9.01501167281207));
#38304=CARTESIAN_POINT('Ctrl Pts',(97.3743833755269,1.14440107035689,-9.01801645169545));
#38305=CARTESIAN_POINT('Ctrl Pts',(97.4169440427174,1.10908361129906,-9.02102123057883));
#38306=CARTESIAN_POINT('Ctrl Pts',(97.4574143320345,1.07142712348618,-9.02402600946221));
#38307=CARTESIAN_POINT('Ctrl Pts',(97.497844582707,1.03380789052766,-9.02702781561483));
#38308=CARTESIAN_POINT('Ctrl Pts',(97.5361881675456,0.993854570880955,-9.03002962176745));
#38309=CARTESIAN_POINT('Ctrl Pts',(97.5721693628588,0.951830405994109,-9.03303142792007));
#38310=CARTESIAN_POINT('Ctrl Pts',(97.6081291724419,0.909831218527945,-9.03603144992361));
#38311=CARTESIAN_POINT('Ctrl Pts',(97.6417290327405,0.865764025757706,-9.03903147192715));
#38312=CARTESIAN_POINT('Ctrl Pts',(97.6727313891479,0.819927510064312,-9.0420314939307));
#38313=CARTESIAN_POINT('Ctrl Pts',(97.7037275634962,0.774100134451781,-9.04503091771155));
#38314=CARTESIAN_POINT('Ctrl Pts',(97.7321269668841,0.726504573794474,-9.0480303414924));
#38315=CARTESIAN_POINT('Ctrl Pts',(97.7577348968595,0.677469147828813,-9.05102976527325));
#38316=CARTESIAN_POINT('Ctrl Pts',(97.78336636961,0.628388640905758,-9.05403194658895));
#38317=CARTESIAN_POINT('Ctrl Pts',(97.8062009967092,0.577866093130214,-9.05703412790464));
#38318=CARTESIAN_POINT('Ctrl Pts',(97.8260904043397,0.526253804796457,-9.06003630922034));
#38319=CARTESIAN_POINT('Ctrl Pts',(97.8459888651845,0.474618023701381,-9.06303985706194));
#38320=CARTESIAN_POINT('Ctrl Pts',(97.8629392722567,0.421892016905816,-9.06604340490354));
#38321=CARTESIAN_POINT('Ctrl Pts',(97.8768428614345,0.368444276165705,-9.06904695274514));
#38322=CARTESIAN_POINT('Ctrl Pts',(97.89077269129,0.314895661837429,-9.07205616927627));
#38323=CARTESIAN_POINT('Ctrl Pts',(97.9016441120435,0.26062311155624,-9.0750653858074));
#38324=CARTESIAN_POINT('Ctrl Pts',(97.9094095547582,0.206005211311661,-9.07807460233852));
#38325=CARTESIAN_POINT('Ctrl Pts',(97.9153504351482,0.164220290036205,-9.08037677571558));
#38326=CARTESIAN_POINT('Ctrl Pts',(97.9194744872999,0.122233465437668,-9.08267894909264));
#38327=CARTESIAN_POINT('Ctrl Pts',(97.9217810157308,0.0802145040429385,
-9.0849811224697));
#38328=CARTESIAN_POINT('Ctrl Pts',(97.9232383780006,0.0536651460853008,
-9.08643573303216));
#38329=CARTESIAN_POINT('Ctrl Pts',(97.923972265548,0.0270757141546565,-9.08789034359461));
#38330=CARTESIAN_POINT('Ctrl Pts',(97.923980872969,0.000473531057436198,
-9.08934495415708));
#38331=CARTESIAN_POINT('Origin',(96.460480949577,-8.32667268468867E-16,
1.18130019239114E-14));
#38332=CARTESIAN_POINT('',(97.9239806795947,0.000888953301123027,-9.66065504580791));
#38333=CARTESIAN_POINT('',(97.9239807107692,0.000836056531580603,-9.58934495412282));
#38334=CARTESIAN_POINT('',(97.923980949577,-1.01189432752408E-15,1.19922289829666E-14));
#38335=CARTESIAN_POINT('Ctrl Pts',(97.9239806795947,0.000888953301123711,
-9.66065504580791));
#38336=CARTESIAN_POINT('Ctrl Pts',(97.9239428755536,0.0631264227740048,
-9.65728431017794));
#38337=CARTESIAN_POINT('Ctrl Pts',(97.9199308592474,0.125216815453647,-9.65391357454797));
#38338=CARTESIAN_POINT('Ctrl Pts',(97.9120250762094,0.186686631655774,-9.650542838918));
#38339=CARTESIAN_POINT('Ctrl Pts',(97.9040582848518,0.248630805701209,-9.64714609158046));
#38340=CARTESIAN_POINT('Ctrl Pts',(97.8921375250518,0.30994452224196,-9.64374934424291));
#38341=CARTESIAN_POINT('Ctrl Pts',(97.8763950474731,0.370161474736446,-9.64035259690536));
#38342=CARTESIAN_POINT('Ctrl Pts',(97.8619494022101,0.425417880864817,-9.63723566649584));
#38343=CARTESIAN_POINT('Ctrl Pts',(97.8442864177926,0.479750852825148,-9.63411873608632));
#38344=CARTESIAN_POINT('Ctrl Pts',(97.8235433666888,0.532816194439787,-9.6310018056768));
#38345=CARTESIAN_POINT('Ctrl Pts',(97.8035109438714,0.58406359072966,-9.62799165699888));
#38346=CARTESIAN_POINT('Ctrl Pts',(97.7805422755616,0.634287334492359,-9.62498150832096));
#38347=CARTESIAN_POINT('Ctrl Pts',(97.7547633097597,0.683129140148358,-9.62197135964303));
#38348=CARTESIAN_POINT('Ctrl Pts',(97.7290301577865,0.731884145188208,-9.61896656053719));
#38349=CARTESIAN_POINT('Ctrl Pts',(97.7004968642633,0.779261622706428,-9.61596176143135));
#38350=CARTESIAN_POINT('Ctrl Pts',(97.6693373955263,0.824923234663004,-9.61295696232551));
#38351=CARTESIAN_POINT('Ctrl Pts',(97.6382087521334,0.870539674639368,-9.60995513579817));
#38352=CARTESIAN_POINT('Ctrl Pts',(97.6044593762844,0.914443177580305,-9.60695330927082));
#38353=CARTESIAN_POINT('Ctrl Pts',(97.5683081725724,0.956321647768353,-9.60395148274347));
#38354=CARTESIAN_POINT('Ctrl Pts',(97.5321784541071,0.998175228902307,-9.60095144025032));
#38355=CARTESIAN_POINT('Ctrl Pts',(97.493650081473,1.03800576375584,-9.59795139775717));
#38356=CARTESIAN_POINT('Ctrl Pts',(97.4529827248317,1.07553357740064,-9.59495135526402));
#38357=CARTESIAN_POINT('Ctrl Pts',(97.4123234764008,1.11305390879352,-9.59195191091586));
#38358=CARTESIAN_POINT('Ctrl Pts',(97.3695264788022,1.1482720728127,-9.5889524665677));
#38359=CARTESIAN_POINT('Ctrl Pts',(97.324887132431,1.18094631590257,-9.58595302221953));
#38360=CARTESIAN_POINT('Ctrl Pts',(97.2802067476131,1.21365059751875,-9.58295082038169));
#38361=CARTESIAN_POINT('Ctrl Pts',(97.2336810572276,1.24380597317031,-9.57994861854386));
#38362=CARTESIAN_POINT('Ctrl Pts',(97.1856361206834,1.27121289633863,-9.57694641670602));
#38363=CARTESIAN_POINT('Ctrl Pts',(97.1375693152027,1.29863229450026,-9.5739428483358));
#38364=CARTESIAN_POINT('Ctrl Pts',(97.0879823587091,1.32330051070059,-9.57093927996559));
#38365=CARTESIAN_POINT('Ctrl Pts',(97.0372247609889,1.34506461777794,-9.56793571159537));
#38366=CARTESIAN_POINT('Ctrl Pts',(96.9863713717002,1.36686979886287,-9.56492647478263));
#38367=CARTESIAN_POINT('Ctrl Pts',(96.9343434254315,1.38575974152273,-9.5619172379699));
#38368=CARTESIAN_POINT('Ctrl Pts',(96.8815080919921,1.40163062015273,-9.55890800115716));
#38369=CARTESIAN_POINT('Ctrl Pts',(96.8410900402114,1.4137715484391,-9.55660599071452));
#38370=CARTESIAN_POINT('Ctrl Pts',(96.8001998904651,1.42414674629186,-9.55430398027188));
#38371=CARTESIAN_POINT('Ctrl Pts',(96.7590053466449,1.432730063325,-9.55200196982924));
#38372=CARTESIAN_POINT('Ctrl Pts',(96.7051389254407,1.44395369946123,-9.54899183662664));
#38373=CARTESIAN_POINT('Ctrl Pts',(96.650525486727,1.45215886526455,-9.54598170342403));
#38374=CARTESIAN_POINT('Ctrl Pts',(96.5955339178958,1.45725527816793,-9.54297157022142));
#38375=CARTESIAN_POINT('Ctrl Pts',(96.5406400802778,1.46234263370801,-9.53996678663834));
#38376=CARTESIAN_POINT('Ctrl Pts',(96.4853699677669,1.46433215218327,-9.53696200305525));
#38377=CARTESIAN_POINT('Ctrl Pts',(96.4301019985479,1.46318466686005,-9.53395721947217));
#38378=CARTESIAN_POINT('Ctrl Pts',(96.3748887052482,1.46203831672989,-9.53095540848437));
#38379=CARTESIAN_POINT('Ctrl Pts',(96.3196780764452,1.45776112139514,-9.52795359749657));
#38380=CARTESIAN_POINT('Ctrl Pts',(96.2648511060458,1.45036588980848,-9.52495178650877));
#38381=CARTESIAN_POINT('Ctrl Pts',(96.2100567201579,1.44297505332166,-9.52195175954339));
#38382=CARTESIAN_POINT('Ctrl Pts',(96.1556460630646,1.43246992399667,-9.51895173257801));
#38383=CARTESIAN_POINT('Ctrl Pts',(96.1019952497374,1.4189151676582,-9.51595170561264));
#38384=CARTESIAN_POINT('Ctrl Pts',(96.0483551325816,1.40536311368317,-9.51295227675194));
#38385=CARTESIAN_POINT('Ctrl Pts',(95.9954750700827,1.38876276943336,-9.50995284789125));
#38386=CARTESIAN_POINT('Ctrl Pts',(95.9437189400153,1.36922944588326,-9.50695341903056));
#38387=CARTESIAN_POINT('Ctrl Pts',(95.8919152253086,1.34967816337534,-9.50395123249187));
#38388=CARTESIAN_POINT('Ctrl Pts',(95.8412380026789,1.32718870102126,-9.50094904595318));
#38389=CARTESIAN_POINT('Ctrl Pts',(95.7920325524046,1.30192510933525,-9.4979468594145));
#38390=CARTESIAN_POINT('Ctrl Pts',(95.7428047035116,1.27665001750948,-9.49494330626234));
#38391=CARTESIAN_POINT('Ctrl Pts',(95.6950504186494,1.24859854699928,-9.49193975311019));
#38392=CARTESIAN_POINT('Ctrl Pts',(95.6490887462701,1.21797986125091,-9.48893619995803));
#38393=CARTESIAN_POINT('Ctrl Pts',(95.6030403279506,1.18730338720749,-9.4859269780382));
#38394=CARTESIAN_POINT('Ctrl Pts',(95.558791703991,1.15405033685307,-9.48291775611838));
#38395=CARTESIAN_POINT('Ctrl Pts',(95.5166304482771,1.1184714932424,-9.47990853419856));
#38396=CARTESIAN_POINT('Ctrl Pts',(95.4843759858983,1.09125274813422,-9.47760640079293));
#38397=CARTESIAN_POINT('Ctrl Pts',(95.4533425452679,1.062673672895,-9.4753042673873));
#38398=CARTESIAN_POINT('Ctrl Pts',(95.423643678839,1.03286045718122,-9.47300213398168));
#38399=CARTESIAN_POINT('Ctrl Pts',(95.3848113592478,0.993878621850589,-9.46999201302764));
#38400=CARTESIAN_POINT('Ctrl Pts',(95.3480988934569,0.952621871770907,-9.4669818920736));
#38401=CARTESIAN_POINT('Ctrl Pts',(95.3137834545098,0.909349825318449,-9.46397177111957));
#38402=CARTESIAN_POINT('Ctrl Pts',(95.2795290061742,0.866154688520976,-9.4609670002098));
#38403=CARTESIAN_POINT('Ctrl Pts',(95.2476634554643,0.820951774086749,-9.45796222930003));
#38404=CARTESIAN_POINT('Ctrl Pts',(95.2184263725026,0.774036612550378,-9.45495745839026));
#38405=CARTESIAN_POINT('Ctrl Pts',(95.1892182159837,0.727167867708177,-9.45195566032611));
#38406=CARTESIAN_POINT('Ctrl Pts',(95.1626336536143,0.678590677608588,-9.44895386226196));
#38407=CARTESIAN_POINT('Ctrl Pts',(95.1388701321584,0.628631129743169,-9.44595206419781));
#38408=CARTESIAN_POINT('Ctrl Pts',(95.1151207355842,0.578701277506215,-9.44295205038279));
#38409=CARTESIAN_POINT('Ctrl Pts',(95.0941892827754,0.527391172060683,-9.43995203656777));
#38410=CARTESIAN_POINT('Ctrl Pts',(95.0762271233534,0.475051149441075,-9.43695202275275));
#38411=CARTESIAN_POINT('Ctrl Pts',(95.0582685462166,0.422721565259672,-9.43395260724582));
#38412=CARTESIAN_POINT('Ctrl Pts',(95.0432782577514,0.369362971065246,-9.43095319173889));
#38413=CARTESIAN_POINT('Ctrl Pts',(95.0313585046755,0.315343126576124,-9.42795377623196));
#38414=CARTESIAN_POINT('Ctrl Pts',(95.0194277933504,0.261273619739118,-9.42495160325659));
#38415=CARTESIAN_POINT('Ctrl Pts',(95.0105733711451,0.206542164902607,-9.42194943028122));
#38416=CARTESIAN_POINT('Ctrl Pts',(95.0048465025647,0.151527577263318,-9.41894725730585));
#38417=CARTESIAN_POINT('Ctrl Pts',(94.9991170273292,0.0964879490536366,
-9.4159437178543));
#38418=CARTESIAN_POINT('Ctrl Pts',(94.9965179682838,0.041165459602171,-9.41294017840274));
#38419=CARTESIAN_POINT('Ctrl Pts',(94.9970484736826,-0.0140583959776044,
-9.40993663895119));
#38420=CARTESIAN_POINT('Ctrl Pts',(94.9975799803276,-0.0693864779779125,
-9.40692743078704));
#38421=CARTESIAN_POINT('Ctrl Pts',(95.0012528155677,-0.124615025982781,
-9.40391822262288));
#38422=CARTESIAN_POINT('Ctrl Pts',(95.0080140725138,-0.179366164686339,
-9.40090901445873));
#38423=CARTESIAN_POINT('Ctrl Pts',(95.0131868711568,-0.221254325164286,
-9.39860677568386));
#38424=CARTESIAN_POINT('Ctrl Pts',(95.0201663132098,-0.262863105816736,
-9.39630453690899));
#38425=CARTESIAN_POINT('Ctrl Pts',(95.0289087496575,-0.304028430278557,
-9.39400229813412));
#38426=CARTESIAN_POINT('Ctrl Pts',(95.0403393128094,-0.357851279749002,
-9.39099216636315));
#38427=CARTESIAN_POINT('Ctrl Pts',(95.0548334808039,-0.411141685750961,
-9.38798203459218));
#38428=CARTESIAN_POINT('Ctrl Pts',(95.0723252594524,-0.463525651905658,
-9.3849719028212));
#38429=CARTESIAN_POINT('Ctrl Pts',(95.0897859506098,-0.515816517975453,
-9.38196712084606));
#38430=CARTESIAN_POINT('Ctrl Pts',(95.1102335139627,-0.567203644328016,
-9.37896233887091));
#38431=CARTESIAN_POINT('Ctrl Pts',(95.1335513319142,-0.617324906163024,
-9.37595755689577));
#38432=CARTESIAN_POINT('Ctrl Pts',(95.1568460809952,-0.66739658184479,-9.3729557476227));
#38433=CARTESIAN_POINT('Ctrl Pts',(95.1830052378704,-0.71620439737557,-9.36995393834964));
#38434=CARTESIAN_POINT('Ctrl Pts',(95.211863576753,-0.763404811539821,-9.36695212907658));
#38435=CARTESIAN_POINT('Ctrl Pts',(95.2407047636744,-0.810577172125566,
-9.36395210392964));
#38436=CARTESIAN_POINT('Ctrl Pts',(95.2722416779248,-0.856143575256737,
-9.36095207878271));
#38437=CARTESIAN_POINT('Ctrl Pts',(95.3062635977552,-0.899785838271265,
-9.35795205363577));
#38438=CARTESIAN_POINT('Ctrl Pts',(95.3402787336102,-0.943419399012564,
-9.35495262669426));
#38439=CARTESIAN_POINT('Ctrl Pts',(95.3767775664702,-0.985129165322661,
-9.35195319975275));
#38440=CARTESIAN_POINT('Ctrl Pts',(95.4155079522929,-1.02462855950198,-9.34895377281124));
#38441=CARTESIAN_POINT('Ctrl Pts',(95.4542739450643,-1.06416426762112,-9.34595158833353));
#38442=CARTESIAN_POINT('Ctrl Pts',(95.4952752190651,-1.10148516581086,-9.34294940385581));
#38443=CARTESIAN_POINT('Ctrl Pts',(95.5382225146415,-1.13634133480671,-9.3399472193781));
#38444=CARTESIAN_POINT('Ctrl Pts',(95.5811893589277,-1.171213369601,-9.33694366836886));
#38445=CARTESIAN_POINT('Ctrl Pts',(95.6261035615186,-1.20361812924814,-9.33394011735962));
#38446=CARTESIAN_POINT('Ctrl Pts',(95.672645142244,-1.2333478790203,-9.33093656635038));
#38447=CARTESIAN_POINT('Ctrl Pts',(95.7192745617813,-1.26313373831563,-9.3279273466821));
#38448=CARTESIAN_POINT('Ctrl Pts',(95.7675370334016,-1.29023424317224,-9.32491812701381));
#38449=CARTESIAN_POINT('Ctrl Pts',(95.8170871659795,-1.31448723433442,-9.32190890734553));
#38450=CARTESIAN_POINT('Ctrl Pts',(95.8549945867329,-1.33304154070413,-9.31960675899254));
#38451=CARTESIAN_POINT('Ctrl Pts',(95.893655098805,-1.34993021289996,-9.31730461063955));
#38452=CARTESIAN_POINT('Ctrl Pts',(95.9329074541082,-1.3651001636799,-9.31500246228656));
#38453=CARTESIAN_POINT('Ctrl Pts',(95.9842311014382,-1.38493533529771,-9.31199233335907));
#38454=CARTESIAN_POINT('Ctrl Pts',(96.0367827540384,-1.40191373683392,-9.30898220443158));
#38455=CARTESIAN_POINT('Ctrl Pts',(96.0902131217131,-1.41588628980189,-9.30597207550409));
#38456=CARTESIAN_POINT('Ctrl Pts',(96.1435485289823,-1.42983400971417,-9.30296729640061));
#38457=CARTESIAN_POINT('Ctrl Pts',(96.1977590452854,-1.44078635018952,-9.29996251729713));
#38458=CARTESIAN_POINT('Ctrl Pts',(96.2524776626869,-1.44864311776329,-9.29695773819365));
#38459=CARTESIAN_POINT('Ctrl Pts',(96.3071421453374,-1.45649211240387,-9.29395593180725));
#38460=CARTESIAN_POINT('Ctrl Pts',(96.3623132131176,-1.46125152620082,-9.29095412542086));
#38461=CARTESIAN_POINT('Ctrl Pts',(96.4176128629549,-1.46287203033942,-9.28795231903446));
#38462=CARTESIAN_POINT('Ctrl Pts',(96.4728796452205,-1.46449157132479,-9.2849522967839));
#38463=CARTESIAN_POINT('Ctrl Pts',(96.5282743312317,-1.46297588500209,-9.28195227453333));
#38464=CARTESIAN_POINT('Ctrl Pts',(96.5834152975203,-1.45832760245967,-9.27895225228277));
#38465=CARTESIAN_POINT('Ctrl Pts',(96.6385452686007,-1.45368024679317,-9.27595282824205));
#38466=CARTESIAN_POINT('Ctrl Pts',(96.6934210944778,-1.44590157976285,-9.27295340420133));
#38467=CARTESIAN_POINT('Ctrl Pts',(96.7476649886759,-1.43504619357248,-9.26995398016062));
#38468=CARTESIAN_POINT('Ctrl Pts',(96.8019587525819,-1.42418082736597,-9.26695179856713));
#38469=CARTESIAN_POINT('Ctrl Pts',(96.855618905139,-1.41023319464999,-9.26394961697364));
#38470=CARTESIAN_POINT('Ctrl Pts',(96.9082780824478,-1.39330900298271,-9.26094743538014));
#38471=CARTESIAN_POINT('Ctrl Pts',(96.9609612292185,-1.37637710774338,-9.25794388725036));
#38472=CARTESIAN_POINT('Ctrl Pts',(97.0126419988178,-1.35646614290013,-9.25494033912057));
#38473=CARTESIAN_POINT('Ctrl Pts',(97.0629715724583,-1.33373059473796,-9.25193679099078));
#38474=CARTESIAN_POINT('Ctrl Pts',(97.113396134891,-1.31095213696813,-9.24892757415791));
#38475=CARTESIAN_POINT('Ctrl Pts',(97.1624639377061,-1.28533869149056,-9.24591835732504));
#38476=CARTESIAN_POINT('Ctrl Pts',(97.2098504483552,-1.25709092920955,-9.24290914049218));
#38477=CARTESIAN_POINT('Ctrl Pts',(97.2461030261194,-1.23548026016615,-9.24060696914111));
#38478=CARTESIAN_POINT('Ctrl Pts',(97.2813720575643,-1.21232872965131,-9.23830479779005));
#38479=CARTESIAN_POINT('Ctrl Pts',(97.3155249713475,-1.18774238403558,-9.23600262643899));
#38480=CARTESIAN_POINT('Ctrl Pts',(97.3620994697563,-1.15421386222258,-9.23286314391614));
#38481=CARTESIAN_POINT('Ctrl Pts',(97.4068089063882,-1.11786234322615,-9.22972366139329));
#38482=CARTESIAN_POINT('Ctrl Pts',(97.4492910382359,-1.07892856972385,-9.22658417887044));
#38483=CARTESIAN_POINT('Ctrl Pts',(97.4896602430355,-1.04193123913399,-9.22360084429148));
#38484=CARTESIAN_POINT('Ctrl Pts',(97.5280179674677,-1.00260282258903,-9.22061750971251));
#38485=CARTESIAN_POINT('Ctrl Pts',(97.5640836833129,-0.961193662115265,
-9.21763417513355));
#38486=CARTESIAN_POINT('Ctrl Pts',(97.6001148729103,-0.919824143248592,
-9.21465369654529));
#38487=CARTESIAN_POINT('Ctrl Pts',(97.6338580477706,-0.876378227201588,
-9.21167321795702));
#38488=CARTESIAN_POINT('Ctrl Pts',(97.6650693991479,-0.831143138791571,
-9.20869273936876));
#38489=CARTESIAN_POINT('Ctrl Pts',(97.6962636541565,-0.78593282840995,-9.20571389337116));
#38490=CARTESIAN_POINT('Ctrl Pts',(97.7249285295215,-0.738935728421387,
-9.20273504737357));
#38491=CARTESIAN_POINT('Ctrl Pts',(97.7508619298017,-0.690470257052557,
-9.19975620137597));
#38492=CARTESIAN_POINT('Ctrl Pts',(97.7767917451654,-0.642011485332505,
-9.19677776716065));
#38493=CARTESIAN_POINT('Ctrl Pts',(97.7999905834695,-0.592085218786595,
-9.19379933294532));
#38494=CARTESIAN_POINT('Ctrl Pts',(97.8203021533147,-0.541034697469037,
-9.19082089873));
#38495=CARTESIAN_POINT('Ctrl Pts',(97.8406324961992,-0.489936992528979,
-9.18783971168645));
#38496=CARTESIAN_POINT('Ctrl Pts',(97.8580700469041,-0.437713458661016,
-9.18485852464291));
#38497=CARTESIAN_POINT('Ctrl Pts',(97.8725072188332,-0.384725960822175,
-9.18187733759937));
#38498=CARTESIAN_POINT('Ctrl Pts',(97.8869521583396,-0.331709954319111,
-9.17889454659897));
#38499=CARTESIAN_POINT('Ctrl Pts',(97.8983933956118,-0.277929690946204,
-9.17591175559857));
#38500=CARTESIAN_POINT('Ctrl Pts',(97.9067744264917,-0.223757521960541,
-9.17292896459817));
#38501=CARTESIAN_POINT('Ctrl Pts',(97.9151698002279,-0.169492645568799,
-9.16994106900585));
#38502=CARTESIAN_POINT('Ctrl Pts',(97.9204944698832,-0.114835059200487,
-9.16695317341352));
#38503=CARTESIAN_POINT('Ctrl Pts',(97.9227438919018,-0.0601609300440481,
-9.16396527782119));
#38504=CARTESIAN_POINT('Ctrl Pts',(97.9235745889996,-0.039970125455074,
-9.16286186717766));
#38505=CARTESIAN_POINT('Ctrl Pts',(97.9239864032088,-0.0197770426895552,
-9.16175845653414));
#38506=CARTESIAN_POINT('Ctrl Pts',(97.9239808950412,0.000399532766103907,
-9.16065504589061));
#38507=CARTESIAN_POINT('Ctrl Pts',(97.9239808729693,0.000473530088800385,
-9.08934495421004));
#38508=CARTESIAN_POINT('Ctrl Pts',(97.9239992748646,-0.0563996718694793,
-9.09245478771451));
#38509=CARTESIAN_POINT('Ctrl Pts',(97.920697403407,-0.113405113933069,-9.09556462121898));
#38510=CARTESIAN_POINT('Ctrl Pts',(97.9140598623374,-0.170119353332748,
-9.09867445472345));
#38511=CARTESIAN_POINT('Ctrl Pts',(97.9077000961744,-0.224460154678947,
-9.10165414459454));
#38512=CARTESIAN_POINT('Ctrl Pts',(97.8982783612853,-0.278533039653128,
-9.10463383446563));
#38513=CARTESIAN_POINT('Ctrl Pts',(97.885834129519,-0.331964700577071,-9.10761352433672));
#38514=CARTESIAN_POINT('Ctrl Pts',(97.8734012327862,-0.385347692392875,
-9.11059050010824));
#38515=CARTESIAN_POINT('Ctrl Pts',(97.8579514115358,-0.438090095080488,
-9.11356747587975));
#38516=CARTESIAN_POINT('Ctrl Pts',(97.8395755182899,-0.489826929176552,
-9.11654445165126));
#38517=CARTESIAN_POINT('Ctrl Pts',(97.8212087994914,-0.541537932862495,
-9.11951994112183));
#38518=CARTESIAN_POINT('Ctrl Pts',(97.7999190831797,-0.592243856755905,
-9.1224954305924));
#38519=CARTESIAN_POINT('Ctrl Pts',(97.775846883691,-0.641595440579602,-9.12547092006297));
#38520=CARTESIAN_POINT('Ctrl Pts',(97.7517767951269,-0.690942696694307,
-9.12844614860874));
#38521=CARTESIAN_POINT('Ctrl Pts',(97.7249249455963,-0.738935366394723,
-9.1314213771545));
#38522=CARTESIAN_POINT('Ctrl Pts',(97.6954787067503,-0.785246961010896,
-9.13439660570027));
#38523=CARTESIAN_POINT('Ctrl Pts',(97.6660034720907,-0.83160415881513,-9.13737476396391));
#38524=CARTESIAN_POINT('Ctrl Pts',(97.6339290411011,-0.876276524932001,
-9.14035292222756));
#38525=CARTESIAN_POINT('Ctrl Pts',(97.5994862869263,-0.918966316841838,
-9.1433310804912));
#38526=CARTESIAN_POINT('Ctrl Pts',(97.5650233597422,-0.961681112024216,
-9.14631098305248));
#38527=CARTESIAN_POINT('Ctrl Pts',(97.5281897118012,-1.00241062525302,-9.14929088561375));
#38528=CARTESIAN_POINT('Ctrl Pts',(97.4892544620633,-1.04089255449666,-9.15227078817503));
#38529=CARTESIAN_POINT('Ctrl Pts',(97.4502516700871,-1.07944123958886,-9.15525586006975));
#38530=CARTESIAN_POINT('Ctrl Pts',(97.4091404096045,-1.11573421150836,-9.15824093196448));
#38531=CARTESIAN_POINT('Ctrl Pts',(97.3662230882605,-1.14954922826867,-9.1612260038592));
#38532=CARTESIAN_POINT('Ctrl Pts',(97.353020138166,-1.15995197393756,-9.16214432201188));
#38533=CARTESIAN_POINT('Ctrl Pts',(97.3396464633258,-1.17012051846723,-9.16306264016456));
#38534=CARTESIAN_POINT('Ctrl Pts',(97.3261113723403,-1.18004924523795,-9.16398095831724));
#38535=CARTESIAN_POINT('Ctrl Pts',(97.2817450868536,-1.21259433318003,-9.16699108698006));
#38536=CARTESIAN_POINT('Ctrl Pts',(97.2354476357177,-1.2427022656766,-9.17000121564287));
#38537=CARTESIAN_POINT('Ctrl Pts',(97.1875172822922,-1.27013795349643,-9.17301134430569));
#38538=CARTESIAN_POINT('Ctrl Pts',(97.1396721146441,-1.29752488034895,-9.17601612311956));
#38539=CARTESIAN_POINT('Ctrl Pts',(97.0902002586328,-1.32224872737416,-9.17902090193344));
#38540=CARTESIAN_POINT('Ctrl Pts',(97.039429842127,-1.3441169702876,-9.18202568074732));
#38541=CARTESIAN_POINT('Ctrl Pts',(96.9887096545592,-1.36596357818815,-9.18502748682906));
#38542=CARTESIAN_POINT('Ctrl Pts',(96.9366939340987,-1.38495997056865,-9.18802929291081));
#38543=CARTESIAN_POINT('Ctrl Pts',(96.8837347003823,-1.40095985396772,-9.19103109899255));
#38544=CARTESIAN_POINT('Ctrl Pts',(96.8308069434604,-1.4169502276929,-9.19403112092399));
#38545=CARTESIAN_POINT('Ctrl Pts',(96.7769372893349,-1.42994747006969,-9.19703114285542));
#38546=CARTESIAN_POINT('Ctrl Pts',(96.7224948162786,-1.43985450086322,-9.20003116478686));
#38547=CARTESIAN_POINT('Ctrl Pts',(96.6680631994037,-1.44975955613073,-9.20303058849452));
#38548=CARTESIAN_POINT('Ctrl Pts',(96.6130595097337,-1.45657552908113,-9.20603001220218));
#38549=CARTESIAN_POINT('Ctrl Pts',(96.5578626856738,-1.46025650057611,-9.20902943590984));
#38550=CARTESIAN_POINT('Ctrl Pts',(96.5026151161637,-1.4639408561889,-9.21203161715126));
#38551=CARTESIAN_POINT('Ctrl Pts',(96.4471745856018,-1.46448441691308,-9.21503379839268));
#38552=CARTESIAN_POINT('Ctrl Pts',(96.3919233144981,-1.46189332739171,-9.2180359796341));
#38553=CARTESIAN_POINT('Ctrl Pts',(96.3366468942619,-1.45930105846482,-9.22103952740072));
#38554=CARTESIAN_POINT('Ctrl Pts',(96.2815604314095,-1.45357134975233,-9.22404307516733));
#38555=CARTESIAN_POINT('Ctrl Pts',(96.2270409776931,-1.4447622743991,-9.22704662293395));
#38556=CARTESIAN_POINT('Ctrl Pts',(96.1724186277122,-1.43593657340336,-9.23005583938989));
#38557=CARTESIAN_POINT('Ctrl Pts',(96.1183659416231,-1.42402000980274,-9.23306505584582));
#38558=CARTESIAN_POINT('Ctrl Pts',(96.0652485831776,-1.40912157976177,-9.23607427230176));
#38559=CARTESIAN_POINT('Ctrl Pts',(96.0246116263725,-1.39772367000578,-9.23837644625611));
#38560=CARTESIAN_POINT('Ctrl Pts',(95.9845218841768,-1.38458157294644,-9.24067862021046));
#38561=CARTESIAN_POINT('Ctrl Pts',(95.9451350145213,-1.36976305148794,-9.24298079416481));
#38562=CARTESIAN_POINT('Ctrl Pts',(95.8936360546815,-1.35038759849686,-9.24599092330318));
#38563=CARTESIAN_POINT('Ctrl Pts',(95.8431230973883,-1.32806308925686,-9.24900105244154));
#38564=CARTESIAN_POINT('Ctrl Pts',(95.7939560062024,-1.30291087563944,-9.25201118157991));
#38565=CARTESIAN_POINT('Ctrl Pts',(95.7448762987437,-1.27780336456836,-9.25501596087356));
#38566=CARTESIAN_POINT('Ctrl Pts',(95.6971381768513,-1.24987836108153,-9.2580207401672));
#38567=CARTESIAN_POINT('Ctrl Pts',(95.6510821726361,-1.2193054866958,-9.26102551946084));
#38568=CARTESIAN_POINT('Ctrl Pts',(95.6050717331857,-1.18876285909018,-9.26402732602457));
#38569=CARTESIAN_POINT('Ctrl Pts',(95.5607405525931,-1.15557784058576,-9.26702913258829));
#38570=CARTESIAN_POINT('Ctrl Pts',(95.51840349777,-1.1199653230332,-9.27003093915201));
#38571=CARTESIAN_POINT('Ctrl Pts',(95.4760916063315,-1.08437397207996,-9.27303096156675));
#38572=CARTESIAN_POINT('Ctrl Pts',(95.4357718948095,-1.04635832108944,-9.2760309839815));
#38573=CARTESIAN_POINT('Ctrl Pts',(95.3977273334798,-1.00617443888841,-9.27903100639624));
#38574=CARTESIAN_POINT('Ctrl Pts',(95.3596903584748,-0.965998569606039,
-9.28203043058766));
#38575=CARTESIAN_POINT('Ctrl Pts',(95.3239279955571,-0.923655711047762,
-9.28502985477908));
#38576=CARTESIAN_POINT('Ctrl Pts',(95.2906857537411,-0.87943814438493,-9.2880292789705));
#38577=CARTESIAN_POINT('Ctrl Pts',(95.2574129505596,-0.835179926155239,
-9.29103146069252));
#38578=CARTESIAN_POINT('Ctrl Pts',(95.2266652153427,-0.789043979490932,
-9.29403364241454));
#38579=CARTESIAN_POINT('Ctrl Pts',(95.198646245614,-0.741353781857565,-9.29703582413656));
#38580=CARTESIAN_POINT('Ctrl Pts',(95.1706145222937,-0.693641876741469,
-9.30003937238275));
#38581=CARTESIAN_POINT('Ctrl Pts',(95.1453142821186,-0.644374780994861,
-9.30304292062894));
#38582=CARTESIAN_POINT('Ctrl Pts',(95.1229029069058,-0.593900016638946,
-9.30604646887513));
#38583=CARTESIAN_POINT('Ctrl Pts',(95.10044923407,-0.543329989831342,-9.30905568580296));
#38584=CARTESIAN_POINT('Ctrl Pts',(95.0808955049108,-0.491548236500181,
-9.31206490273079));
#38585=CARTESIAN_POINT('Ctrl Pts',(95.0643502294876,-0.438920565048586,
-9.31507411965861));
#38586=CARTESIAN_POINT('Ctrl Pts',(95.0516924385786,-0.398658312277413,
-9.31737628977653));
#38587=CARTESIAN_POINT('Ctrl Pts',(95.040794441548,-0.357901351132589,-9.31967845989445));
#38588=CARTESIAN_POINT('Ctrl Pts',(95.0316845359028,-0.316817073832236,
-9.32198063001236));
#38589=CARTESIAN_POINT('Ctrl Pts',(95.0197731751921,-0.263098663837841,
-9.32499075764263));
#38590=CARTESIAN_POINT('Ctrl Pts',(95.0108704732858,-0.208594704812133,
-9.32800088527289));
#38591=CARTESIAN_POINT('Ctrl Pts',(95.0050714228735,-0.153672898003324,
-9.33101101290315));
#38592=CARTESIAN_POINT('Ctrl Pts',(94.9992826790039,-0.0988487026837372,
-9.33401579069047));
#38593=CARTESIAN_POINT('Ctrl Pts',(94.9965866949739,-0.0436086542901982,
-9.33702056847778));
#38594=CARTESIAN_POINT('Ctrl Pts',(94.9970274737238,0.0116693621642374,
-9.3400253462651));
#38595=CARTESIAN_POINT('Ctrl Pts',(94.9974678163966,0.0668926902181632,
-9.3430271513247));
#38596=CARTESIAN_POINT('Ctrl Pts',(95.0010387701615,0.122153386418911,-9.34602895638431));
#38597=CARTESIAN_POINT('Ctrl Pts',(95.007732399473,0.177070325494678,-9.34903076144392));
#38598=CARTESIAN_POINT('Ctrl Pts',(95.0144220503785,0.23195462429809,-9.3520307823594));
#38599=CARTESIAN_POINT('Ctrl Pts',(95.0242306343782,0.286495047751098,-9.35503080327488));
#38600=CARTESIAN_POINT('Ctrl Pts',(95.037098300903,0.340314685921306,-9.35803082419035));
#38601=CARTESIAN_POINT('Ctrl Pts',(95.0499634015649,0.394123592246064,-9.36103024688997));
#38602=CARTESIAN_POINT('Ctrl Pts',(95.0658862505955,0.447211485372616,-9.36402966958959));
#38603=CARTESIAN_POINT('Ctrl Pts',(95.0847561999249,0.499213043894782,-9.36702909228921));
#38604=CARTESIAN_POINT('Ctrl Pts',(95.1036434975602,0.551262410650516,-9.37003127254275));
#38605=CARTESIAN_POINT('Ctrl Pts',(95.1254831280923,0.602222949951803,-9.37303345279627));
#38606=CARTESIAN_POINT('Ctrl Pts',(95.1501154700795,0.651747313106343,-9.3760356330498));
#38607=CARTESIAN_POINT('Ctrl Pts',(95.1747590242363,0.701294218800918,-9.37903917983819));
#38608=CARTESIAN_POINT('Ctrl Pts',(95.2021975617758,0.749403185655384,-9.38204272662658));
#38609=CARTESIAN_POINT('Ctrl Pts',(95.2322260165785,0.795752517787265,-9.38504627341497));
#38610=CARTESIAN_POINT('Ctrl Pts',(95.2623111453174,0.842189326917629,-9.38805548892059));
#38611=CARTESIAN_POINT('Ctrl Pts',(95.2949956433555,0.886859439794644,-9.39106470442622));
#38612=CARTESIAN_POINT('Ctrl Pts',(95.3300324259056,0.929472100350025,-9.39407391993184));
#38613=CARTESIAN_POINT('Ctrl Pts',(95.3568371027837,0.962072656507588,-9.39637610190787));
#38614=CARTESIAN_POINT('Ctrl Pts',(95.3850176700251,0.99346963244608,-9.3986782838839));
#38615=CARTESIAN_POINT('Ctrl Pts',(95.4144493917181,1.02354786403143,-9.40098046585993));
#38616=CARTESIAN_POINT('Ctrl Pts',(95.4529317014846,1.06287549281125,-9.40399059489228));
#38617=CARTESIAN_POINT('Ctrl Pts',(95.4937158506339,1.10011250776548,-9.40700072392464));
#38618=CARTESIAN_POINT('Ctrl Pts',(95.5365457828554,1.13497843930852,-9.41001085295699));
#38619=CARTESIAN_POINT('Ctrl Pts',(95.5792995939972,1.16978240408632,-9.41301563212629));
#38620=CARTESIAN_POINT('Ctrl Pts',(95.624091566403,1.20222331764116,-9.41602041129558));
#38621=CARTESIAN_POINT('Ctrl Pts',(95.6706292539979,1.23205785131656,-9.41902519046488));
#38622=CARTESIAN_POINT('Ctrl Pts',(95.7171209001088,1.26186286856612,-9.42202699689317));
#38623=CARTESIAN_POINT('Ctrl Pts',(95.765354397691,1.28906633037508,-9.42502880332147));
#38624=CARTESIAN_POINT('Ctrl Pts',(95.8150062078859,1.31346663750505,-9.42803060974977));
#38625=CARTESIAN_POINT('Ctrl Pts',(95.8646285069314,1.33785244201956,-9.43103063201838));
#38626=CARTESIAN_POINT('Ctrl Pts',(95.915666974697,1.3594381616923,-9.43403065428699));
#38627=CARTESIAN_POINT('Ctrl Pts',(95.9677732366186,1.37806798075832,-9.4370306765556));
#38628=CARTESIAN_POINT('Ctrl Pts',(96.019869108044,1.39669408485694,-9.44003010059054));
#38629=CARTESIAN_POINT('Ctrl Pts',(96.0730318537501,1.41236528124424,-9.44302952462549));
#38630=CARTESIAN_POINT('Ctrl Pts',(96.1268950493132,1.42497463035143,-9.44602894866044));
#38631=CARTESIAN_POINT('Ctrl Pts',(96.180807763926,1.4375955718452,-9.44903113021146));
#38632=CARTESIAN_POINT('Ctrl Pts',(96.2354216996206,1.44714892160888,-9.45203331176249));
#38633=CARTESIAN_POINT('Ctrl Pts',(96.2903587257388,1.4535785768084,-9.45503549331352));
#38634=CARTESIAN_POINT('Ctrl Pts',(96.3453207577788,1.46001115862165,-9.4580390413804));
#38635=CARTESIAN_POINT('Ctrl Pts',(96.4006056453079,1.4633171799797,-9.46104258944727));
#38636=CARTESIAN_POINT('Ctrl Pts',(96.4558319117699,1.46349261578167,-9.46404613751415));
#38637=CARTESIAN_POINT('Ctrl Pts',(96.511162408129,1.46366838268796,-9.4670553542515));
#38638=CARTESIAN_POINT('Ctrl Pts',(96.5664335337557,1.46070178940326,-9.47006457098885));
#38639=CARTESIAN_POINT('Ctrl Pts',(96.6212667661651,1.45464090798523,-9.47307378772619));
#38640=CARTESIAN_POINT('Ctrl Pts',(96.6632163851004,1.45000409095428,-9.47537595905329));
#38641=CARTESIAN_POINT('Ctrl Pts',(96.7049097565665,1.44355731388188,-9.47767813038039));
#38642=CARTESIAN_POINT('Ctrl Pts',(96.7461822746122,1.43534212049711,-9.4799803017075));
#38643=CARTESIAN_POINT('Ctrl Pts',(96.8001468599256,1.42460060228424,-9.48299043355479));
#38644=CARTESIAN_POINT('Ctrl Pts',(96.8536182130661,1.41078892260863,-9.48600056540209));
#38645=CARTESIAN_POINT('Ctrl Pts',(96.9062215244966,1.39396828868893,-9.48901069724939));
#38646=CARTESIAN_POINT('Ctrl Pts',(96.9587313454702,1.37717754963149,-9.49201547926995));
#38647=CARTESIAN_POINT('Ctrl Pts',(97.0103756873712,1.35738862849228,-9.49502026129052));
#38648=CARTESIAN_POINT('Ctrl Pts',(97.0607909640459,1.33471350353864,-9.49802504331108));
#38649=CARTESIAN_POINT('Ctrl Pts',(97.1111563633747,1.31206081176646,-9.50102685261064));
#38650=CARTESIAN_POINT('Ctrl Pts',(97.1602946269448,1.28652778816772,-9.50402866191019));
#38651=CARTESIAN_POINT('Ctrl Pts',(97.2078601292047,1.25827525281991,-9.50703047120975));
#38652=CARTESIAN_POINT('Ctrl Pts',(97.2553973605972,1.23003950955129,-9.51003049636432));
#38653=CARTESIAN_POINT('Ctrl Pts',(97.3013632303254,1.1990877274236,-9.51303052151888));
#38654=CARTESIAN_POINT('Ctrl Pts',(97.3454368876451,1.16562654297076,-9.51603054667344));
#38655=CARTESIAN_POINT('Ctrl Pts',(97.3895017563951,1.13217203089258,-9.51902997360376));
#38656=CARTESIAN_POINT('Ctrl Pts',(97.4316747416874,1.09620942940807,-9.52202940053408));
#38657=CARTESIAN_POINT('Ctrl Pts',(97.4716660655663,1.05798719803303,-9.5250288274644));
#38658=CARTESIAN_POINT('Ctrl Pts',(97.5116941552569,1.01972982725206,-9.52803101190197));
#38659=CARTESIAN_POINT('Ctrl Pts',(97.5495361938056,0.979209041925372,-9.53103319633955));
#38660=CARTESIAN_POINT('Ctrl Pts',(97.5849385841689,0.936710882827834,-9.53403538077712));
#38661=CARTESIAN_POINT('Ctrl Pts',(97.620357088769,0.894193379686126,-9.53703893173008));
#38662=CARTESIAN_POINT('Ctrl Pts',(97.6533334165546,0.84969713362517,-9.54004248268305));
#38663=CARTESIAN_POINT('Ctrl Pts',(97.6836557588033,0.803539442761955,-9.54304603363601));
#38664=CARTESIAN_POINT('Ctrl Pts',(97.7140353287283,0.757294638002065,-9.54605525322236));
#38665=CARTESIAN_POINT('Ctrl Pts',(97.7417506419836,0.709382582729455,-9.54906447280871));
#38666=CARTESIAN_POINT('Ctrl Pts',(97.7666351367122,0.660146566626753,-9.55207369239506));
#38667=CARTESIAN_POINT('Ctrl Pts',(97.7856725641079,0.622479453348951,-9.55437584078172));
#38668=CARTESIAN_POINT('Ctrl Pts',(97.803054121417,0.584038015309721,-9.55667798916839));
#38669=CARTESIAN_POINT('Ctrl Pts',(97.8187246641583,0.544982808720181,-9.55898013755506));
#38670=CARTESIAN_POINT('Ctrl Pts',(97.8417157589475,0.487682817804549,-9.56235774308225));
#38671=CARTESIAN_POINT('Ctrl Pts',(97.8611038616657,0.428859176734495,-9.56573534860944));
#38672=CARTESIAN_POINT('Ctrl Pts',(97.8767107744066,0.368951667923016,-9.56911295413663));
#38673=CARTESIAN_POINT('Ctrl Pts',(97.8922917856593,0.309143582595085,-9.57248495413433));
#38674=CARTESIAN_POINT('Ctrl Pts',(97.9041039701687,0.24825547473603,-9.57585695413203));
#38675=CARTESIAN_POINT('Ctrl Pts',(97.9120173549428,0.186746656992054,-9.57922895412973));
#38676=CARTESIAN_POINT('Ctrl Pts',(97.9199307397169,0.125237839248078,-9.58260095412743));
#38677=CARTESIAN_POINT('Ctrl Pts',(97.9239451362168,0.0631085786241471,
-9.58597295412512));
#38678=CARTESIAN_POINT('Ctrl Pts',(97.9239807107692,0.000836056531596055,
-9.58934495412282));
#38679=CARTESIAN_POINT('Origin',(96.460480949577,-8.32667268468867E-16,
1.18130019239114E-14));
#38680=CARTESIAN_POINT('',(97.9239803647431,-0.00130836102040465,-10.1606550458429));
#38681=CARTESIAN_POINT('',(97.9239804027775,-0.00126510151654843,-10.0893449541571));
#38682=CARTESIAN_POINT('',(97.923980949577,-1.01189432752408E-15,1.19922289829666E-14));
#38683=CARTESIAN_POINT('Ctrl Pts',(97.9239803647431,-0.00130836102040465,
-10.1606550458429));
#38684=CARTESIAN_POINT('Ctrl Pts',(97.9240294293408,0.0535740521494451,
-10.1576764399972));
#38685=CARTESIAN_POINT('Ctrl Pts',(97.9209869965176,0.108513542155505,-10.1546978341516));
#38686=CARTESIAN_POINT('Ctrl Pts',(97.9148604658852,0.163133296855682,-10.151719228306));
#38687=CARTESIAN_POINT('Ctrl Pts',(97.9087364944472,0.217730235614312,-10.1487418666932));
#38688=CARTESIAN_POINT('Ctrl Pts',(97.8995310384136,0.272007171166325,-10.1457645050805));
#38689=CARTESIAN_POINT('Ctrl Pts',(97.887303411852,0.325591632489809,-10.1427871434677));
#38690=CARTESIAN_POINT('Ctrl Pts',(97.8750758843932,0.379175659520625,-10.139809805986));
#38691=CARTESIAN_POINT('Ctrl Pts',(97.859826357819,0.432066701307455,-10.1368324685043));
#38692=CARTESIAN_POINT('Ctrl Pts',(97.8416648848964,0.483904109112112,-10.1338551310225));
#38693=CARTESIAN_POINT('Ctrl Pts',(97.8234839976644,0.535796930234749,-10.130874610817));
#38694=CARTESIAN_POINT('Ctrl Pts',(97.802385134747,0.586633364343026,-10.1278940906115));
#38695=CARTESIAN_POINT('Ctrl Pts',(97.7785271432923,0.636071129067042,-10.1249135704061));
#38696=CARTESIAN_POINT('Ctrl Pts',(97.754653594347,0.685541131524163,-10.1219311066415));
#38697=CARTESIAN_POINT('Ctrl Pts',(97.7280176005758,0.733610182794539,-10.118948642877));
#38698=CARTESIAN_POINT('Ctrl Pts',(97.6988231611858,0.779962061223371,-10.1159661791125));
#38699=CARTESIAN_POINT('Ctrl Pts',(97.6695774261019,0.826395381591766,-10.1129784750504));
#38700=CARTESIAN_POINT('Ctrl Pts',(97.6377645955694,0.87110507949753,-10.1099907709883));
#38701=CARTESIAN_POINT('Ctrl Pts',(97.6036299865693,0.913806614784328,-10.1070030669263));
#38702=CARTESIAN_POINT('Ctrl Pts',(97.5960047456357,0.923345598951333,-10.1063356515382));
#38703=CARTESIAN_POINT('Ctrl Pts',(97.5882637899108,0.932784517046882,-10.1056682361502));
#38704=CARTESIAN_POINT('Ctrl Pts',(97.5804100987424,0.94212045453311,-10.1050008207621));
#38705=CARTESIAN_POINT('Ctrl Pts',(97.5449812473275,0.984235879614959,-10.1019900376656));
#38706=CARTESIAN_POINT('Ctrl Pts',(97.5070992123615,1.02443828878907,-10.0989792545691));
#38707=CARTESIAN_POINT('Ctrl Pts',(97.4669984367473,1.06242872608957,-10.0959684714726));
#38708=CARTESIAN_POINT('Ctrl Pts',(97.42696889155,1.10035168153606,-10.0929630363857));
#38709=CARTESIAN_POINT('Ctrl Pts',(97.384728807109,1.13607010244594,-10.0899576012988));
#38710=CARTESIAN_POINT('Ctrl Pts',(97.3405516921868,1.16931934816897,-10.086952166212));
#38711=CARTESIAN_POINT('Ctrl Pts',(97.296418264805,1.20253571311719,-10.0839497032537));
#38712=CARTESIAN_POINT('Ctrl Pts',(97.2503520213352,1.23328742422046,-10.0809472402954));
#38713=CARTESIAN_POINT('Ctrl Pts',(97.2026606000705,1.26134912549753,-10.0779447773372));
#38714=CARTESIAN_POINT('Ctrl Pts',(97.1549975280862,1.28939414601698,-10.0749440991373));
#38715=CARTESIAN_POINT('Ctrl Pts',(97.1057116471631,1.31475205899299,-10.0719434209374));
#38716=CARTESIAN_POINT('Ctrl Pts',(97.0551387920655,1.33724130222144,-10.0689427427376));
#38717=CARTESIAN_POINT('Ctrl Pts',(97.0045760499692,1.35972604829932,-10.0659426645802));
#38718=CARTESIAN_POINT('Ctrl Pts',(96.9527273268401,1.3793430495183,-10.0629425864228));
#38719=CARTESIAN_POINT('Ctrl Pts',(96.8999501221443,1.39595812844189,-10.0599425082655));
#38720=CARTESIAN_POINT('Ctrl Pts',(96.8471245503528,1.41258843407401,-10.0569396807191));
#38721=CARTESIAN_POINT('Ctrl Pts',(96.7933693015709,1.42621116223602,-10.0539368531727));
#38722=CARTESIAN_POINT('Ctrl Pts',(96.7390573629085,1.43674195036386,-10.0509340256263));
#38723=CARTESIAN_POINT('Ctrl Pts',(96.6847207719484,1.4472775184375,-10.0479298350904));
#38724=CARTESIAN_POINT('Ctrl Pts',(96.6298275113632,1.45471827768085,-10.0449256445546));
#38725=CARTESIAN_POINT('Ctrl Pts',(96.5747578178983,1.45903154433572,-10.0419214540188));
#38726=CARTESIAN_POINT('Ctrl Pts',(96.519584466998,1.46335292983294,-10.0389116087086));
#38727=CARTESIAN_POINT('Ctrl Pts',(96.4642345488208,1.46453505141985,-10.0359017633985));
#38728=CARTESIAN_POINT('Ctrl Pts',(96.409089269428,1.46259739682917,-10.0328919180884));
#38729=CARTESIAN_POINT('Ctrl Pts',(96.3670048878966,1.46111866653769,-10.0305949403638));
#38730=CARTESIAN_POINT('Ctrl Pts',(96.3250397233806,1.45782404885631,-10.0282979626392));
#38731=CARTESIAN_POINT('Ctrl Pts',(96.2833598762869,1.45274236373714,-10.0260009849147));
#38732=CARTESIAN_POINT('Ctrl Pts',(96.2287299609898,1.44608178201755,-10.0229903285115));
#38733=CARTESIAN_POINT('Ctrl Pts',(96.1743619734304,1.43632147095853,-10.0199796721084));
#38734=CARTESIAN_POINT('Ctrl Pts',(96.1206343740473,1.42349448720419,-10.0169690157053));
#38735=CARTESIAN_POINT('Ctrl Pts',(96.0670019208968,1.41069021876177,-10.0139636908751));
#38736=CARTESIAN_POINT('Ctrl Pts',(96.014008114684,1.3948301767368,-10.0109583660449));
#38737=CARTESIAN_POINT('Ctrl Pts',(95.9620240141196,1.375998885717,-10.0079530412147));
#38738=CARTESIAN_POINT('Ctrl Pts',(95.9100911476214,1.35718615428754,-10.004950678348));
#38739=CARTESIAN_POINT('Ctrl Pts',(95.8591665093319,1.33540815386084,-10.0019483154814));
#38740=CARTESIAN_POINT('Ctrl Pts',(95.8096068943097,1.31079945612587,-9.99894595261475));
#38741=CARTESIAN_POINT('Ctrl Pts',(95.7600765691199,1.28620530218085,-9.99594536415061));
#38742=CARTESIAN_POINT('Ctrl Pts',(95.7119101400558,1.25878400119002,-9.99294477568647));
#38743=CARTESIAN_POINT('Ctrl Pts',(95.6654431201801,1.22871766481477,-9.98994418722233));
#38744=CARTESIAN_POINT('Ctrl Pts',(95.6189852290236,1.19865723514804,-9.98694418824143));
#38745=CARTESIAN_POINT('Ctrl Pts',(95.5742265269607,1.16595308872611,-9.98394418926053));
#38746=CARTESIAN_POINT('Ctrl Pts',(95.5314746688416,1.13083136689526,-9.98094419027963));
#38747=CARTESIAN_POINT('Ctrl Pts',(95.4886833860961,1.09567725674667,-9.97794142477946));
#38748=CARTESIAN_POINT('Ctrl Pts',(95.4479030533949,1.05810145297181,-9.97493865927928));
#38749=CARTESIAN_POINT('Ctrl Pts',(95.4094080591436,1.01837028088799,-9.97193589377911));
#38750=CARTESIAN_POINT('Ctrl Pts',(95.3708954707516,0.978620949668397,-9.9689317558647));
#38751=CARTESIAN_POINT('Ctrl Pts',(95.3346706487805,0.936714686469186,-9.96592761795029));
#38752=CARTESIAN_POINT('Ctrl Pts',(95.3009686515576,0.892952115592899,-9.96292348003587));
#38753=CARTESIAN_POINT('Ctrl Pts',(95.2672030338939,0.84910693257838,-9.95991367110507));
#38754=CARTESIAN_POINT('Ctrl Pts',(95.2359700532083,0.803398878601056,-9.95690386217427));
#38755=CARTESIAN_POINT('Ctrl Pts',(95.2074615959471,0.756157886574571,-9.95389405324347));
#38756=CARTESIAN_POINT('Ctrl Pts',(95.1856987455871,0.720094951603775,-9.951596418518));
#38757=CARTESIAN_POINT('Ctrl Pts',(95.1655227269374,0.683139315342153,-9.94929878379252));
#38758=CARTESIAN_POINT('Ctrl Pts',(95.1470001770739,0.645445977805055,-9.94700114906704));
#38759=CARTESIAN_POINT('Ctrl Pts',(95.1227375337846,0.596071566085913,-9.94399148289449));
#38760=CARTESIAN_POINT('Ctrl Pts',(95.1012116407638,0.545223123099354,-9.94098181672195));
#38761=CARTESIAN_POINT('Ctrl Pts',(95.0826017297944,0.493235345136,-9.9379721505494));
#38762=CARTESIAN_POINT('Ctrl Pts',(95.0640249644206,0.441340161159751,-9.93496784480966));
#38763=CARTESIAN_POINT('Ctrl Pts',(95.0483540511211,0.388310162559924,-9.93196353906993));
#38764=CARTESIAN_POINT('Ctrl Pts',(95.0357210892669,0.334502003654749,-9.92895923333019));
#38765=CARTESIAN_POINT('Ctrl Pts',(95.0231006533233,0.280747196940334,-9.92595790643783));
#38766=CARTESIAN_POINT('Ctrl Pts',(95.013512322027,0.226216270114416,-9.92295657954548));
#38767=CARTESIAN_POINT('Ctrl Pts',(95.0070384973276,0.17128131246392,-9.91995525265312));
#38768=CARTESIAN_POINT('Ctrl Pts',(95.0005685323207,0.116379107019746,-9.91695571515101));
#38769=CARTESIAN_POINT('Ctrl Pts',(94.9972094552371,0.0610738718124895,
-9.9139561776489));
#38770=CARTESIAN_POINT('Ctrl Pts',(94.9969922291307,0.00574587908985627,
-9.91095664014679));
#38771=CARTESIAN_POINT('Ctrl Pts',(94.9967750466643,-0.0495709984394848,
-9.9079577052409));
#38772=CARTESIAN_POINT('Ctrl Pts',(94.9996984637714,-0.104910096399853,
-9.90495877033501));
#38773=CARTESIAN_POINT('Ctrl Pts',(95.0057413464022,-0.159890390439509,
-9.90195983542912));
#38774=CARTESIAN_POINT('Ctrl Pts',(95.0117897796947,-0.214921186371307,
-9.89895814586558));
#38775=CARTESIAN_POINT('Ctrl Pts',(95.0209633453419,-0.26959199365133,-9.89595645630205));
#38776=CARTESIAN_POINT('Ctrl Pts',(95.0331890750857,-0.323527672712909,
-9.89295476673851));
#38777=CARTESIAN_POINT('Ctrl Pts',(95.0454203610206,-0.377487863762713,
-9.88995171300602));
#38778=CARTESIAN_POINT('Ctrl Pts',(95.0607064300513,-0.430711751943461,
-9.88694865927353));
#38779=CARTESIAN_POINT('Ctrl Pts',(95.0789240932648,-0.482838381631814,
-9.88394560554103));
#38780=CARTESIAN_POINT('Ctrl Pts',(95.0971761588704,-0.535063447696359,
-9.88093688081602));
#38781=CARTESIAN_POINT('Ctrl Pts',(95.1183706749341,-0.586186626761002,
-9.87792815609101));
#38782=CARTESIAN_POINT('Ctrl Pts',(95.1423363114514,-0.635867095375006,
-9.874919431366));
#38783=CARTESIAN_POINT('Ctrl Pts',(95.1607047920133,-0.673944728797587,
-9.87261339198383));
#38784=CARTESIAN_POINT('Ctrl Pts',(95.1807001516218,-0.711175248614454,
-9.87030735260166));
#38785=CARTESIAN_POINT('Ctrl Pts',(95.2022278909176,-0.74741654408645,-9.86800131321949));
#38786=CARTESIAN_POINT('Ctrl Pts',(95.2303296931089,-0.794725074839264,
-9.8649910639001));
#38787=CARTESIAN_POINT('Ctrl Pts',(95.2611623134059,-0.840545858886474,
-9.8619808145807));
#38788=CARTESIAN_POINT('Ctrl Pts',(95.294543180829,-0.884545854892223,-9.85897056526131));
#38789=CARTESIAN_POINT('Ctrl Pts',(95.3278647364916,-0.928467670867626,
-9.8559656646102));
#38790=CARTESIAN_POINT('Ctrl Pts',(95.3637252372699,-0.970574701818236,
-9.85296076395909));
#38791=CARTESIAN_POINT('Ctrl Pts',(95.4018979789767,-1.01056140058635,-9.84995586330798));
#38792=CARTESIAN_POINT('Ctrl Pts',(95.4400329645613,-1.05050854907286,-9.84695393476187));
#38793=CARTESIAN_POINT('Ctrl Pts',(95.4804752977666,-1.08833913973975,-9.84395200621574));
#38794=CARTESIAN_POINT('Ctrl Pts',(95.5229582040928,-1.12378082903198,-9.84095007766962));
#38795=CARTESIAN_POINT('Ctrl Pts',(95.5654158670453,-1.15920145884675,-9.83794993287162));
#38796=CARTESIAN_POINT('Ctrl Pts',(95.6099112951568,-1.19223566320698,-9.83494978807362));
#38797=CARTESIAN_POINT('Ctrl Pts',(95.6561427654742,-1.22264971909135,-9.83194964327562));
#38798=CARTESIAN_POINT('Ctrl Pts',(95.7023650200588,-1.25305771226978,-9.82895009652333));
#38799=CARTESIAN_POINT('Ctrl Pts',(95.75032218867,-1.28084630417462,-9.82595054977104));
#38800=CARTESIAN_POINT('Ctrl Pts',(95.799683462524,-1.30582500018356,-9.82295100301875));
#38801=CARTESIAN_POINT('Ctrl Pts',(95.8490901032074,-1.33082665354655,-9.81994869945094));
#38802=CARTESIAN_POINT('Ctrl Pts',(95.8999029551621,-1.3530130125462,-9.81694639588313));
#38803=CARTESIAN_POINT('Ctrl Pts',(95.9517678242792,-1.37224021444855,-9.81394409231532));
#38804=CARTESIAN_POINT('Ctrl Pts',(96.0036562965077,-1.39147616643153,-9.81094042243335));
#38805=CARTESIAN_POINT('Ctrl Pts',(96.0565972346435,-1.40775012135957,-9.80793675255138));
#38806=CARTESIAN_POINT('Ctrl Pts',(96.110220888847,-1.42096802914683,-9.80493308266941));
#38807=CARTESIAN_POINT('Ctrl Pts',(96.1639457109321,-1.43421087420756,-9.80192374598007));
#38808=CARTESIAN_POINT('Ctrl Pts',(96.2183553017883,-1.44438605707627,-9.79891440929072));
#38809=CARTESIAN_POINT('Ctrl Pts',(96.2730704726965,-1.45145084765397,-9.79590507260138));
#38810=CARTESIAN_POINT('Ctrl Pts',(96.3149104119537,-1.45685319591917,-9.79360387419156));
#38811=CARTESIAN_POINT('Ctrl Pts',(96.356928825872,-1.4604378223726,-9.79130267578174));
#38812=CARTESIAN_POINT('Ctrl Pts',(96.3989561765355,-1.46220619349741,-9.78900147737192));
#38813=CARTESIAN_POINT('Ctrl Pts',(96.4539318564525,-1.46451938724857,-9.78599129602081));
#38814=CARTESIAN_POINT('Ctrl Pts',(96.5091536315192,-1.46373268468115,-9.7829811146697));
#38815=CARTESIAN_POINT('Ctrl Pts',(96.5642428293329,-1.45981701672145,-9.77997093331859));
#38816=CARTESIAN_POINT('Ctrl Pts',(96.6192341581163,-1.45590830516413,-9.77696609972243));
#38817=CARTESIAN_POINT('Ctrl Pts',(96.6740928545523,-1.44888169680325,-9.77396126612626));
#38818=CARTESIAN_POINT('Ctrl Pts',(96.7284391581908,-1.43876010802235,-9.77095643253009));
#38819=CARTESIAN_POINT('Ctrl Pts',(96.7827317185529,-1.42864852852097,-9.76795457042585));
#38820=CARTESIAN_POINT('Ctrl Pts',(96.8365123732653,-1.41544812780354,-9.76495270832161));
#38821=CARTESIAN_POINT('Ctrl Pts',(96.889407276111,-1.39923352461482,-9.76195084621737));
#38822=CARTESIAN_POINT('Ctrl Pts',(96.9422707610342,-1.38302855239467,-9.75895076712559));
#38823=CARTESIAN_POINT('Ctrl Pts',(96.994249032978,-1.36381308075201,-9.75595068803382));
#38824=CARTESIAN_POINT('Ctrl Pts',(97.0449814957135,-1.34171210084955,-9.75295060894204));
#38825=CARTESIAN_POINT('Ctrl Pts',(97.0957038597974,-1.31961552030177,-9.749951127037));
#38826=CARTESIAN_POINT('Ctrl Pts',(97.1451804232903,-1.29463478298976,-9.74695164513195));
#38827=CARTESIAN_POINT('Ctrl Pts',(97.1930709028164,-1.26694285996356,-9.74395216322691));
#38828=CARTESIAN_POINT('Ctrl Pts',(97.2410054281509,-1.23922546813551,-9.74094992263984));
#38829=CARTESIAN_POINT('Ctrl Pts',(97.2873504969757,-1.20879217377013,-9.73794768205278));
#38830=CARTESIAN_POINT('Ctrl Pts',(97.3317921040487,-1.17586101308499,-9.73494544146571));
#38831=CARTESIAN_POINT('Ctrl Pts',(97.3762539503339,-1.14291485517552,-9.7319418336242));
#38832=CARTESIAN_POINT('Ctrl Pts',(97.4188102003654,-1.10746890187683,-9.7289382257827));
#38833=CARTESIAN_POINT('Ctrl Pts',(97.4591800696255,-1.0697814345063,-9.72593461794119));
#38834=CARTESIAN_POINT('Ctrl Pts',(97.4996261347469,-1.03202283415745,-9.72292534095855));
#38835=CARTESIAN_POINT('Ctrl Pts',(97.537877209595,-0.992014650837638,-9.71991606397592));
#38836=CARTESIAN_POINT('Ctrl Pts',(97.5736903348873,-0.950051111497216,
-9.71690678699328));
#38837=CARTESIAN_POINT('Ctrl Pts',(97.6010828327383,-0.917954327097042,
-9.71460507183697));
#38838=CARTESIAN_POINT('Ctrl Pts',(97.6270498305126,-0.884714358085679,
-9.71230335668067));
#38839=CARTESIAN_POINT('Ctrl Pts',(97.6514998639153,-0.850474100539441,
-9.71000164152436));
#38840=CARTESIAN_POINT('Ctrl Pts',(97.683736559021,-0.8053292647564,-9.70696689353479));
#38841=CARTESIAN_POINT('Ctrl Pts',(97.7134696579605,-0.758255660224419,
-9.70393214554522));
#38842=CARTESIAN_POINT('Ctrl Pts',(97.7404646736664,-0.709558958837252,
-9.70089739755565));
#38843=CARTESIAN_POINT('Ctrl Pts',(97.767415230793,-0.660942456927828,-9.6978676475474));
#38844=CARTESIAN_POINT('Ctrl Pts',(97.7916363977639,-0.610708606457505,
-9.69483789753914));
#38845=CARTESIAN_POINT('Ctrl Pts',(97.8129364109217,-0.55919269941482,-9.69180814753089));
#38846=CARTESIAN_POINT('Ctrl Pts',(97.8342065427992,-0.507749062809193,
-9.68878264788665));
#38847=CARTESIAN_POINT('Ctrl Pts',(97.8525634604831,-0.455027415355879,
-9.68575714824241));
#38848=CARTESIAN_POINT('Ctrl Pts',(97.8678619595953,-0.401386276097912,
-9.68273164859817));
#38849=CARTESIAN_POINT('Ctrl Pts',(97.8831479351127,-0.347789048330475,
-9.6797086256761));
#38850=CARTESIAN_POINT('Ctrl Pts',(97.8953803175433,-0.293274317348441,
-9.67668560275404));
#38851=CARTESIAN_POINT('Ctrl Pts',(97.9044632059323,-0.238217323742553,
-9.67366257983197));
#38852=CARTESIAN_POINT('Ctrl Pts',(97.9135431559158,-0.183178141626121,
-9.67064053488813));
#38853=CARTESIAN_POINT('Ctrl Pts',(97.9194755451615,-0.127597553509319,
-9.66761848994428));
#38854=CARTESIAN_POINT('Ctrl Pts',(97.9222156394325,-0.0718606044574211,
-9.66459644500044));
#38855=CARTESIAN_POINT('Ctrl Pts',(97.9234068642987,-0.0476295988393163,
-9.66328264528126));
#38856=CARTESIAN_POINT('Ctrl Pts',(97.923995414332,-0.0233691259645077,
-9.66196884556208));
#38857=CARTESIAN_POINT('Ctrl Pts',(97.9239806795951,0.000888952655002563,
-9.6606550458429));
#38858=CARTESIAN_POINT('Ctrl Pts',(97.9239807107695,0.000836055898965084,
-9.58934495415708));
#38859=CARTESIAN_POINT('Ctrl Pts',(97.9240126572801,-0.0550856961044943,
-9.59237306577497));
#38860=CARTESIAN_POINT('Ctrl Pts',(97.920835028295,-0.111014615602546,-9.59540117739287));
#38861=CARTESIAN_POINT('Ctrl Pts',(97.9144717574115,-0.166562242818737,
-9.59842928901076));
#38862=CARTESIAN_POINT('Ctrl Pts',(97.9081069032638,-0.222123691003714,
-9.60145815406203));
#38863=CARTESIAN_POINT('Ctrl Pts',(97.8985548953864,-0.277303148660256,
-9.6044870191133));
#38864=CARTESIAN_POINT('Ctrl Pts',(97.8858913123318,-0.331719079570828,
-9.60751588416457));
#38865=CARTESIAN_POINT('Ctrl Pts',(97.8732102931455,-0.386209934247392,
-9.610548919575));
#38866=CARTESIAN_POINT('Ctrl Pts',(97.8574092691731,-0.439934663777601,
-9.61358195498544));
#38867=CARTESIAN_POINT('Ctrl Pts',(97.8386142670535,-0.49252493262916,-9.61661499039588));
#38868=CARTESIAN_POINT('Ctrl Pts',(97.8198043156689,-0.545157030997792,
-9.61965043823754));
#38869=CARTESIAN_POINT('Ctrl Pts',(97.7979958479512,-0.596652400285083,
-9.62268588607919));
#38870=CARTESIAN_POINT('Ctrl Pts',(97.7733625727979,-0.646663817921657,
-9.62572133392085));
#38871=CARTESIAN_POINT('Ctrl Pts',(97.7486806606055,-0.696773980335626,
-9.62876277508634));
#38872=CARTESIAN_POINT('Ctrl Pts',(97.7211630645337,-0.745393897980012,
-9.63180421625184));
#38873=CARTESIAN_POINT('Ctrl Pts',(97.6910282055441,-0.792203067926339,
-9.63484565741733));
#38874=CARTESIAN_POINT('Ctrl Pts',(97.6806765153304,-0.808282586553376,
-9.63589042941243));
#38875=CARTESIAN_POINT('Ctrl Pts',(97.6700163442168,-0.824148714008224,
-9.63693520140752));
#38876=CARTESIAN_POINT('Ctrl Pts',(97.6590576291842,-0.839789374249164,
-9.63797997340262));
#38877=CARTESIAN_POINT('Ctrl Pts',(97.6274840396244,-0.884852302285955,
-9.64099010753408));
#38878=CARTESIAN_POINT('Ctrl Pts',(97.5932992289051,-0.928226826130445,
-9.64400024166554));
#38879=CARTESIAN_POINT('Ctrl Pts',(97.5567102281248,-0.969594564163086,
-9.64701037579701));
#38880=CARTESIAN_POINT('Ctrl Pts',(97.5201862576479,-1.0108887785548,-9.65001515996176));
#38881=CARTESIAN_POINT('Ctrl Pts',(97.4812669239856,-1.05018289288802,-9.65301994412652));
#38882=CARTESIAN_POINT('Ctrl Pts',(97.4402012041658,-1.08718925341837,-9.65602472829128));
#38883=CARTESIAN_POINT('Ctrl Pts',(97.3991761130537,-1.12415900140154,-9.65902653964811));
#38884=CARTESIAN_POINT('Ctrl Pts',(97.3560092328158,-1.1588451274842,-9.66202835100494));
#38885=CARTESIAN_POINT('Ctrl Pts',(97.3109870062691,-1.19099609467454,-9.66503016236177));
#38886=CARTESIAN_POINT('Ctrl Pts',(97.2659915403011,-1.22312795178188,-9.66803018948412));
#38887=CARTESIAN_POINT('Ctrl Pts',(97.2191433427515,-1.25272733040001,-9.67103021660648));
#38888=CARTESIAN_POINT('Ctrl Pts',(97.1707608078467,-1.27958382802237,-9.67403024372883));
#38889=CARTESIAN_POINT('Ctrl Pts',(97.1223879222096,-1.30643496946541,-9.67702967253478));
#38890=CARTESIAN_POINT('Ctrl Pts',(97.0724817684151,-1.33054406012878,-9.68002910134072));
#38891=CARTESIAN_POINT('Ctrl Pts',(97.021386499642,-1.35174598719816,-9.68302853014666));
#38892=CARTESIAN_POINT('Ctrl Pts',(96.970244259382,-1.3729674050357,-9.68603071630439));
#38893=CARTESIAN_POINT('Ctrl Pts',(96.9179112090179,-1.39127611706288,-9.68903290246212));
#38894=CARTESIAN_POINT('Ctrl Pts',(96.8647513203896,-1.40655526634507,-9.69203508861985));
#38895=CARTESIAN_POINT('Ctrl Pts',(96.8115672362733,-1.42184136986442,-9.69503864120932));
#38896=CARTESIAN_POINT('Ctrl Pts',(96.7575560796247,-1.4340950448615,-9.69804219379879));
#38897=CARTESIAN_POINT('Ctrl Pts',(96.7030935938257,-1.44325027450219,-9.70104574638826));
#38898=CARTESIAN_POINT('Ctrl Pts',(96.6485283232801,-1.45242278242067,-9.70405496745554));
#38899=CARTESIAN_POINT('Ctrl Pts',(96.5935105482571,-1.45848510557856,-9.70706418852281));
#38900=CARTESIAN_POINT('Ctrl Pts',(96.538421570746,-1.46142311107078,-9.71007340959008));
#38901=CARTESIAN_POINT('Ctrl Pts',(96.496277054823,-1.46367076250384,-9.71237554281011));
#38902=CARTESIAN_POINT('Ctrl Pts',(96.454090998094,-1.46409093678363,-9.71467767603014));
#38903=CARTESIAN_POINT('Ctrl Pts',(96.412032562978,-1.46269785117637,-9.71697980925017));
#38904=CARTESIAN_POINT('Ctrl Pts',(96.3570391548051,-1.46087632535857,-9.71998995814154));
#38905=CARTESIAN_POINT('Ctrl Pts',(96.302033080692,-1.45594525977901,-9.72300010703291));
#38906=CARTESIAN_POINT('Ctrl Pts',(96.2473941183345,-1.44790408948626,-9.72601025592429));
#38907=CARTESIAN_POINT('Ctrl Pts',(96.1928522608653,-1.43987721003852,-9.72901505515016));
#38908=CARTESIAN_POINT('Ctrl Pts',(96.1386767386452,-1.42875127113368,-9.73201985437604));
#38909=CARTESIAN_POINT('Ctrl Pts',(96.085244512539,-1.41457762824069,-9.73502465360192));
#38910=CARTESIAN_POINT('Ctrl Pts',(96.0318651467173,-1.40041800727509,-9.73802648019212));
#38911=CARTESIAN_POINT('Ctrl Pts',(95.9792281282806,-1.38321678979531,-9.74102830678232));
#38912=CARTESIAN_POINT('Ctrl Pts',(95.9277006400562,-1.363076443853,-9.74403013337251));
#38913=CARTESIAN_POINT('Ctrl Pts',(95.876203776431,-1.34294806802687,-9.74703017587155));
#38914=CARTESIAN_POINT('Ctrl Pts',(95.825815626866,-1.31988421793841,-9.7500302183706));
#38915=CARTESIAN_POINT('Ctrl Pts',(95.7768863807261,-1.29403659741045,-9.75303026086964));
#38916=CARTESIAN_POINT('Ctrl Pts',(95.727966890969,-1.26819413084046,-9.75602970516689));
#38917=CARTESIAN_POINT('Ctrl Pts',(95.6805061936124,-1.23956924273064,-9.75902914946414));
#38918=CARTESIAN_POINT('Ctrl Pts',(95.6348306210236,-1.20835995670149,-9.76202859376139));
#38919=CARTESIAN_POINT('Ctrl Pts',(95.5891130586785,-1.17712197983742,-9.76503079546107));
#38920=CARTESIAN_POINT('Ctrl Pts',(95.5451843367288,-1.14329515699568,-9.76803299716075));
#38921=CARTESIAN_POINT('Ctrl Pts',(95.503341200612,-1.10712047716194,-9.77103519886043));
#38922=CARTESIAN_POINT('Ctrl Pts',(95.4614790191512,-1.07092933204171,-9.77403876704383));
#38923=CARTESIAN_POINT('Ctrl Pts',(95.4217046957669,-1.03238856778564,-9.77704233522723));
#38924=CARTESIAN_POINT('Ctrl Pts',(95.3842788277877,-0.991776811110299,
-9.78004590341063));
#38925=CARTESIAN_POINT('Ctrl Pts',(95.346782329318,-0.951088411501984,-9.7830551399594));
#38926=CARTESIAN_POINT('Ctrl Pts',(95.3116434760072,-0.908321620881624,
-9.78606437650817));
#38927=CARTESIAN_POINT('Ctrl Pts',(95.2790824481551,-0.863788070557825,
-9.78907361305693));
#38928=CARTESIAN_POINT('Ctrl Pts',(95.2541738599928,-0.829720722639403,
-9.7913756237372));
#38929=CARTESIAN_POINT('Ctrl Pts',(95.230772976813,-0.79462017121957,-9.79367763441747));
#38930=CARTESIAN_POINT('Ctrl Pts',(95.2089603081028,-0.758635837516282,
-9.79597964509773));
#38931=CARTESIAN_POINT('Ctrl Pts',(95.1804384897308,-0.711583427572393,
-9.79898970917496));
#38932=CARTESIAN_POINT('Ctrl Pts',(95.1545139061549,-0.662821427610296,
-9.80199977325219));
#38933=CARTESIAN_POINT('Ctrl Pts',(95.131394539733,-0.612667581293462,-9.80500983732941));
#38934=CARTESIAN_POINT('Ctrl Pts',(95.1083162632534,-0.562602873174066,
-9.80801455163378));
#38935=CARTESIAN_POINT('Ctrl Pts',(95.0880335290975,-0.51115170356423,-9.81101926593814));
#38936=CARTESIAN_POINT('Ctrl Pts',(95.0707092966997,-0.458657827643519,
-9.8140239802425));
#38937=CARTESIAN_POINT('Ctrl Pts',(95.0534022035883,-0.406215885197136,
-9.81702572190957));
#38938=CARTESIAN_POINT('Ctrl Pts',(95.0390479788662,-0.352733779004543,
-9.82002746357664));
#38939=CARTESIAN_POINT('Ctrl Pts',(95.0277614316403,-0.298575003848839,
-9.82302920524371));
#38940=CARTESIAN_POINT('Ctrl Pts',(95.0164815920401,-0.244448415399853,
-9.82602916296758));
#38941=CARTESIAN_POINT('Ctrl Pts',(95.0082659239144,-0.18964647106752,-9.82902912069145));
#38942=CARTESIAN_POINT('Ctrl Pts',(95.0031787151428,-0.134545336274049,
-9.83202907841532));
#38943=CARTESIAN_POINT('Ctrl Pts',(94.9980925202735,-0.0794551833708021,
-9.83502843823487));
#38944=CARTESIAN_POINT('Ctrl Pts',(94.9961335950115,-0.0240664840386528,
-9.83802779805443));
#38945=CARTESIAN_POINT('Ctrl Pts',(94.9973143978304,0.0312392677565819,
-9.84102715787398));
#38946=CARTESIAN_POINT('Ctrl Pts',(94.9984962866418,0.0865958846348152,
-9.84402927622553));
#38947=CARTESIAN_POINT('Ctrl Pts',(95.0028236613408,0.141868872408044,-9.84703139457709));
#38948=CARTESIAN_POINT('Ctrl Pts',(95.0102568295359,0.196678040591868,-9.85003351292864));
#38949=CARTESIAN_POINT('Ctrl Pts',(95.017693382345,0.251512165546761,-9.85303699826282));
#38950=CARTESIAN_POINT('Ctrl Pts',(95.0282384469924,0.305881530527964,-9.85604048359699));
#38951=CARTESIAN_POINT('Ctrl Pts',(95.0418010573405,0.359415655424122,-9.85904396893116));
#38952=CARTESIAN_POINT('Ctrl Pts',(95.0553892722402,0.413050846208539,-9.86205312447876));
#38953=CARTESIAN_POINT('Ctrl Pts',(95.072006254042,0.465847141931595,-9.86506228002635));
#38954=CARTESIAN_POINT('Ctrl Pts',(95.0915113107741,0.517449879733214,-9.86807143557394));
#38955=CARTESIAN_POINT('Ctrl Pts',(95.1064370725862,0.556937597398208,-9.87037411736439));
#38956=CARTESIAN_POINT('Ctrl Pts',(95.1230529646099,0.595726717173825,-9.87267679915484));
#38957=CARTESIAN_POINT('Ctrl Pts',(95.1412777538414,0.633668034826621,-9.8749794809453));
#38958=CARTESIAN_POINT('Ctrl Pts',(95.1651021765784,0.683266961841729,-9.87798967018303));
#38959=CARTESIAN_POINT('Ctrl Pts',(95.1917777436817,0.731624607382276,-9.88099985942075));
#38960=CARTESIAN_POINT('Ctrl Pts',(95.2211519553535,0.778393148785941,-9.88401004865848));
#38961=CARTESIAN_POINT('Ctrl Pts',(95.2504739534409,0.825078557637538,-9.88701488719024));
#38962=CARTESIAN_POINT('Ctrl Pts',(95.2824847979448,0.870180024375918,-9.89001972572201));
#38963=CARTESIAN_POINT('Ctrl Pts',(95.316985604283,0.913373223436577,-9.89302456425377));
#38964=CARTESIAN_POINT('Ctrl Pts',(95.351452271939,0.956523682658692,-9.89602642948611));
#38965=CARTESIAN_POINT('Ctrl Pts',(95.3884036927349,0.997769204124672,-9.89902829471845));
#38966=CARTESIAN_POINT('Ctrl Pts',(95.4275981411842,1.03681500477504,-9.9020301599508));
#38967=CARTESIAN_POINT('Ctrl Pts',(95.4667692858438,1.07583759001698,-9.90503024036822));
#38968=CARTESIAN_POINT('Ctrl Pts',(95.5081804414227,1.11266267479681,-9.90803032078565));
#38969=CARTESIAN_POINT('Ctrl Pts',(95.551551666227,1.14703086613607,-9.91103040120308));
#38970=CARTESIAN_POINT('Ctrl Pts',(95.5949142316723,1.18139219563296,-9.91402988263411));
#38971=CARTESIAN_POINT('Ctrl Pts',(95.6402356754912,1.21329727807385,-9.91702936406515));
#38972=CARTESIAN_POINT('Ctrl Pts',(95.6872032737517,1.24252721743639,-9.92002884549619));
#38973=CARTESIAN_POINT('Ctrl Pts',(95.7342140256209,1.27178401312992,-9.92303108283667));
#38974=CARTESIAN_POINT('Ctrl Pts',(95.7828735043524,1.29836047552374,-9.92603332017715));
#38975=CARTESIAN_POINT('Ctrl Pts',(95.832841582506,1.32208209839733,-9.92903555751764));
#38976=CARTESIAN_POINT('Ctrl Pts',(95.8828323910048,1.34581451217376,-9.93203916056786));
#38977=CARTESIAN_POINT('Ctrl Pts',(95.9341324955781,1.36668929823868,-9.93504276361809));
#38978=CARTESIAN_POINT('Ctrl Pts',(95.9863818843884,1.38458019861157,-9.93804636666831));
#38979=CARTESIAN_POINT('Ctrl Pts',(96.038729848288,1.40250485243388,-9.9410556363961));
#38980=CARTESIAN_POINT('Ctrl Pts',(96.0920301643488,1.41743423200839,-9.94406490612388));
#38981=CARTESIAN_POINT('Ctrl Pts',(96.1459088968136,1.42929236813893,-9.94707417585166));
#38982=CARTESIAN_POINT('Ctrl Pts',(96.1871193648072,1.43836235395923,-9.94937588949873));
#38983=CARTESIAN_POINT('Ctrl Pts',(96.2286679205669,1.44563660279784,-9.9516776031458));
#38984=CARTESIAN_POINT('Ctrl Pts',(96.2703854375572,1.45110163197136,-9.95397931679287));
#38985=CARTESIAN_POINT('Ctrl Pts',(96.3249448203917,1.45824895617449,-9.95698956488781));
#38986=CARTESIAN_POINT('Ctrl Pts',(96.3800224167897,1.46232997560268,-9.95999981298275));
#38987=CARTESIAN_POINT('Ctrl Pts',(96.4352435718802,1.46328238039245,-9.96301006107769));
#38988=CARTESIAN_POINT('Ctrl Pts',(96.4903666159433,1.46423309305151,-9.96601496088659));
#38989=CARTESIAN_POINT('Ctrl Pts',(96.5456321888077,1.46206621312329,-9.96901986069548));
#38990=CARTESIAN_POINT('Ctrl Pts',(96.6006599733415,1.45677111836295,-9.97202476050438));
#38991=CARTESIAN_POINT('Ctrl Pts',(96.6556333349422,1.45148126049503,-9.97502668844256));
#38992=CARTESIAN_POINT('Ctrl Pts',(96.7103688510263,1.44306936687821,-9.97802861638075));
#38993=CARTESIAN_POINT('Ctrl Pts',(96.7644875417311,1.43157683759092,-9.98103054431893));
#38994=CARTESIAN_POINT('Ctrl Pts',(96.8185740792824,1.42009113627848,-9.98403068874298));
#38995=CARTESIAN_POINT('Ctrl Pts',(96.8720440023069,1.40552853651072,-9.98703083316703));
#38996=CARTESIAN_POINT('Ctrl Pts',(96.9245270922357,1.38798178211517,-9.99003097759107));
#38997=CARTESIAN_POINT('Ctrl Pts',(96.9769997243323,1.37043852410319,-9.99303052420339));
#38998=CARTESIAN_POINT('Ctrl Pts',(97.0284854133109,1.34991245971505,-9.99603007081569));
#38999=CARTESIAN_POINT('Ctrl Pts',(97.0786299477101,1.32654591556683,-9.99902961742801));
#39000=CARTESIAN_POINT('Ctrl Pts',(97.1288205748707,1.30315789293534,-10.0020319212179));
#39001=CARTESIAN_POINT('Ctrl Pts',(97.1776671048263,1.27692439770182,-10.0050342250078));
#39002=CARTESIAN_POINT('Ctrl Pts',(97.224837531989,1.24803496141875,-10.0080365287977));
#39003=CARTESIAN_POINT('Ctrl Pts',(97.2720294290388,1.21913237594506,-10.0110401991032));
#39004=CARTESIAN_POINT('Ctrl Pts',(97.3175432678237,1.18757174105362,-10.0140438694086));
#39005=CARTESIAN_POINT('Ctrl Pts',(97.361076588278,1.15358560391186,-10.0170475397141));
#39006=CARTESIAN_POINT('Ctrl Pts',(97.4046920445891,1.11953534392202,-10.0200568771507));
#39007=CARTESIAN_POINT('Ctrl Pts',(97.4463191197987,1.0830507887586,-10.0230662145873));
#39008=CARTESIAN_POINT('Ctrl Pts',(97.4856898648184,1.04440362413652,-10.0260755520238));
#39009=CARTESIAN_POINT('Ctrl Pts',(97.5157961484908,1.01485065274464,-10.0283767522294));
#39010=CARTESIAN_POINT('Ctrl Pts',(97.5445837589622,0.984033929331002,-10.0306779524349));
#39011=CARTESIAN_POINT('Ctrl Pts',(97.571949066195,0.952087640788239,-10.0329791526404));
#39012=CARTESIAN_POINT('Ctrl Pts',(97.6074588746238,0.910633452953977,-10.0359652392851));
#39013=CARTESIAN_POINT('Ctrl Pts',(97.6407275751511,0.867094924415226,-10.0389513259298));
#39014=CARTESIAN_POINT('Ctrl Pts',(97.6714995489266,0.821745825684147,-10.0419374125744));
#39015=CARTESIAN_POINT('Ctrl Pts',(97.7022257692905,0.776464154411317,-10.0449190593462));
#39016=CARTESIAN_POINT('Ctrl Pts',(97.7304623148778,0.729377683712454,-10.0479007061181));
#39017=CARTESIAN_POINT('Ctrl Pts',(97.7559932347603,0.680793778569701,-10.0508823528899));
#39018=CARTESIAN_POINT('Ctrl Pts',(97.7814966803646,0.632262155433588,-10.0538607910584));
#39019=CARTESIAN_POINT('Ctrl Pts',(97.8043000205057,0.582236763687155,-10.056839229227));
#39020=CARTESIAN_POINT('Ctrl Pts',(97.8242314826978,0.531052477079951,-10.0598176673955));
#39021=CARTESIAN_POINT('Ctrl Pts',(97.8441534630728,0.47989253991768,-10.0627946886582));
#39022=CARTESIAN_POINT('Ctrl Pts',(97.8612060710213,0.427575297084985,-10.0657717099209));
#39023=CARTESIAN_POINT('Ctrl Pts',(97.875265199105,0.374456642733757,-10.0687487311836));
#39024=CARTESIAN_POINT('Ctrl Pts',(97.889320627778,0.321351965616041,-10.0717249690958));
#39025=CARTESIAN_POINT('Ctrl Pts',(97.9003840081287,0.267446816066161,-10.0747012070081));
#39026=CARTESIAN_POINT('Ctrl Pts',(97.9083815176956,0.213110757217513,-10.0776774449203));
#39027=CARTESIAN_POINT('Ctrl Pts',(97.9163831135109,0.158746935896923,-10.0806552035119));
#39028=CARTESIAN_POINT('Ctrl Pts',(97.9213156428349,0.103952298681166,-10.0836329621035));
#39029=CARTESIAN_POINT('Ctrl Pts',(97.9231569701812,0.0491030421626044,
-10.0866107206951));
#39030=CARTESIAN_POINT('Ctrl Pts',(97.9237205505487,0.0323151721445975,
-10.0875221318491));
#39031=CARTESIAN_POINT('Ctrl Pts',(97.9239949143218,0.015522197232046,-10.0884335430031));
#39032=CARTESIAN_POINT('Ctrl Pts',(97.9239804027775,-0.00126510151654843,
-10.0893449541571));
#39033=CARTESIAN_POINT('Origin',(96.460480949577,-8.32667268468867E-16,
1.18130019239114E-14));
#39034=CARTESIAN_POINT('',(97.0954317298417,1.32103105766813,-10.4999624929899));
#39035=CARTESIAN_POINT('Ctrl Pts',(97.9232424573285,-0.00127078615709219,
-10.0893452975919));
#39036=CARTESIAN_POINT('Ctrl Pts',(97.9243963473812,-0.140165259671045,
-10.096889861224));
#39037=CARTESIAN_POINT('Ctrl Pts',(97.8427247309318,-0.762515797147353,
-10.1307677034719));
#39038=CARTESIAN_POINT('Ctrl Pts',(96.9603351573397,-1.65300340041201,-10.1909788243355));
#39039=CARTESIAN_POINT('Ctrl Pts',(95.3490596299417,-1.32199308459857,-10.2699786601832));
#39040=CARTESIAN_POINT('Ctrl Pts',(94.7462060275777,0.208822451170032,-10.3489784960306));
#39041=CARTESIAN_POINT('Ctrl Pts',(95.6701133225779,1.50956345563644,-10.425639773633));
#39042=CARTESIAN_POINT('Ctrl Pts',(96.6979102974993,1.50901532054598,-10.4759677726193));
#39043=CARTESIAN_POINT('Ctrl Pts',(97.0954317298416,1.32103105766813,-10.4999624929899));
#39044=CARTESIAN_POINT('',(95.8264738550018,1.31904027763685,-10.5));
#39045=CARTESIAN_POINT('Origin',(96.460480949577,-2.11854640757359E-15,
-10.5));
#39046=CARTESIAN_POINT('Ctrl Pts',(95.8264738550018,1.31904027763685,-10.5));
#39047=CARTESIAN_POINT('Ctrl Pts',(95.389985305394,1.10923861968599,-10.4736667213841));
#39048=CARTESIAN_POINT('Ctrl Pts',(94.7489680295834,0.225931430401009,-10.4210001641525));
#39049=CARTESIAN_POINT('Ctrl Pts',(95.3368678391471,-1.31284583226671,-10.3420003283048));
#39050=CARTESIAN_POINT('Ctrl Pts',(96.945745154454,-1.65698344561198,-10.2630004924574));
#39051=CARTESIAN_POINT('Ctrl Pts',(97.8393255414646,-0.771433645423267,
-10.202552200022));
#39052=CARTESIAN_POINT('Ctrl Pts',(97.9242498774361,-0.1446116846944,-10.1684371862026));
#39053=CARTESIAN_POINT('Ctrl Pts',(97.923091047352,-0.00131502666372312,
-10.160655450999));
#39054=CARTESIAN_POINT('Origin',(96.460480949577,-7.19464945638997E-16,
0.924367114736168));
#39055=CARTESIAN_POINT('',(95.7870390291235,-0.966214801312794,-10.4999999999999));
#39056=CARTESIAN_POINT('Ctrl Pts',(95.7870390291235,-0.966214801312794,
-10.4999999999999));
#39057=CARTESIAN_POINT('Ctrl Pts',(95.8544328204863,-1.01318759061422,-10.4940933826723));
#39058=CARTESIAN_POINT('Ctrl Pts',(95.9265691194591,-1.05298970580012,-10.4879796024791));
#39059=CARTESIAN_POINT('Ctrl Pts',(96.0554830599743,-1.10743282480879,-10.4778357939815));
#39060=CARTESIAN_POINT('Ctrl Pts',(96.1102754510535,-1.12596123198284,-10.4737357746006));
#39061=CARTESIAN_POINT('Ctrl Pts',(96.1769942019014,-1.14317726828716,-10.468999148222));
#39062=CARTESIAN_POINT('Ctrl Pts',(96.1878131566054,-1.14580595743389,-10.4682386528551));
#39063=CARTESIAN_POINT('Ctrl Pts',(96.2048531906659,-1.14969115664634,-10.4670523381136));
#39064=CARTESIAN_POINT('Ctrl Pts',(96.2110496912719,-1.15105141364629,-10.4666233064918));
#39065=CARTESIAN_POINT('Ctrl Pts',(96.2226437963609,-1.15349853120499,-10.4658248528591));
#39066=CARTESIAN_POINT('Ctrl Pts',(96.2280385893279,-1.15459773247405,-10.4654550574637));
#39067=CARTESIAN_POINT('Ctrl Pts',(96.2401001084916,-1.1569673301482,-10.4646320323687));
#39068=CARTESIAN_POINT('Ctrl Pts',(96.246770542536,-1.15821802060255,-10.4641794217779));
#39069=CARTESIAN_POINT('Ctrl Pts',(96.263714378522,-1.1612435848658,-10.4630359371115));
#39070=CARTESIAN_POINT('Ctrl Pts',(96.274001356937,-1.16293986064668,-10.4623474742393));
#39071=CARTESIAN_POINT('Ctrl Pts',(96.3548783104421,-1.17517532307434,-10.4569766409464));
#39072=CARTESIAN_POINT('Ctrl Pts',(96.4262750274982,-1.17941544920117,-10.4524975226811));
#39073=CARTESIAN_POINT('Ctrl Pts',(96.5497825983152,-1.17551838631524,-10.4448125440057));
#39074=CARTESIAN_POINT('Ctrl Pts',(96.601771553668,-1.17040794904005,-10.4415932459585));
#39075=CARTESIAN_POINT('Ctrl Pts',(96.6881374820688,-1.15607887547855,-10.4360515066784));
#39076=CARTESIAN_POINT('Ctrl Pts',(96.7227452443597,-1.14872223958326,-10.4337764625604));
#39077=CARTESIAN_POINT('Ctrl Pts',(96.7615628452717,-1.1386251872194,-10.4311094906997));
#39078=CARTESIAN_POINT('Ctrl Pts',(96.7661524950613,-1.13740165701946,-10.4307923009737));
#39079=CARTESIAN_POINT('Ctrl Pts',(96.7746719986907,-1.13507519880498,-10.4301998464747));
#39080=CARTESIAN_POINT('Ctrl Pts',(96.7786037828066,-1.13397953423189,-10.4299249650611));
#39081=CARTESIAN_POINT('Ctrl Pts',(96.7855076302119,-1.13201691859115,-10.4294395959154));
#39082=CARTESIAN_POINT('Ctrl Pts',(96.7884821506178,-1.13115863551943,-10.4292295890975));
#39083=CARTESIAN_POINT('Ctrl Pts',(96.7943229246815,-1.12944833415548,-10.4288154131124));
#39084=CARTESIAN_POINT('Ctrl Pts',(96.7971893854899,-1.12859710816218,-10.4286112916624));
#39085=CARTESIAN_POINT('Ctrl Pts',(96.8049184708953,-1.12626980804266,-10.4280586412863));
#39086=CARTESIAN_POINT('Ctrl Pts',(96.8097747654666,-1.12477318355665,-10.4277089822683));
#39087=CARTESIAN_POINT('Ctrl Pts',(96.8291389597203,-1.11866798158017,-10.4263054554145));
#39088=CARTESIAN_POINT('Ctrl Pts',(96.8435658790611,-1.11380997684799,-10.4252389078994));
#39089=CARTESIAN_POINT('Ctrl Pts',(96.9301100207214,-1.08278756005178,-10.4187301073203));
#39090=CARTESIAN_POINT('Ctrl Pts',(96.9996200957762,-1.04990869045323,-10.413046761696));
#39091=CARTESIAN_POINT('Ctrl Pts',(97.1236429017441,-0.975660603296374,
-10.4024873564727));
#39092=CARTESIAN_POINT('Ctrl Pts',(97.1787381628072,-0.935845439251295,
-10.3976122234331));
#39093=CARTESIAN_POINT('Ctrl Pts',(97.2414089403017,-0.88174232736521,-10.3918796147378));
#39094=CARTESIAN_POINT('Ctrl Pts',(97.2525263581025,-0.871769559373845,
-10.3908541924939));
#39095=CARTESIAN_POINT('Ctrl Pts',(97.2686268689341,-0.856764426683987,
-10.3893557592327));
#39096=CARTESIAN_POINT('Ctrl Pts',(97.2737587148631,-0.851894588580639,
-10.3888760717168));
#39097=CARTESIAN_POINT('Ctrl Pts',(97.2827930595554,-0.843165448093971,
-10.3880277521992));
#39098=CARTESIAN_POINT('Ctrl Pts',(97.2867130062517,-0.839324591167573,
-10.3876583536494));
#39099=CARTESIAN_POINT('Ctrl Pts',(97.2949060595357,-0.831183820705522,
-10.3868833974825));
#39100=CARTESIAN_POINT('Ctrl Pts',(97.2991731141308,-0.826878022056163,
-10.3864781093615));
#39101=CARTESIAN_POINT('Ctrl Pts',(97.3103903347578,-0.815382785178269,
-10.385408034293));
#39102=CARTESIAN_POINT('Ctrl Pts',(97.3172826109272,-0.80813734758312,-10.3847457259154));
#39103=CARTESIAN_POINT('Ctrl Pts',(97.3475906889598,-0.775452621156036,
-10.3818100475003));
#39104=CARTESIAN_POINT('Ctrl Pts',(97.3699731455309,-0.749075933191025,
-10.379579532275));
#39105=CARTESIAN_POINT('Ctrl Pts',(97.4528343737023,-0.642227973803992,
-10.3709885142502));
#39106=CARTESIAN_POINT('Ctrl Pts',(97.5040530417584,-0.555137170636209,
-10.3649501606482));
#39107=CARTESIAN_POINT('Ctrl Pts',(97.5520536274543,-0.442752743614256,
-10.3572000895141));
#39108=CARTESIAN_POINT('Ctrl Pts',(97.5599834921799,-0.42267593765064,-10.3558154250398));
#39109=CARTESIAN_POINT('Ctrl Pts',(97.5719878230905,-0.389655297475727,
-10.3535205560766));
#39110=CARTESIAN_POINT('Ctrl Pts',(97.5763983259937,-0.376838362017642,
-10.3526255996791));
#39111=CARTESIAN_POINT('Ctrl Pts',(97.5820623258186,-0.359406579672633,
-10.351399133887));
#39112=CARTESIAN_POINT('Ctrl Pts',(97.5835105443611,-0.354855464003163,
-10.3510780794959));
#39113=CARTESIAN_POINT('Ctrl Pts',(97.5858802805173,-0.347248606473874,
-10.3505398544353));
#39114=CARTESIAN_POINT('Ctrl Pts',(97.5868171454956,-0.344197649506389,
-10.3503235540892));
#39115=CARTESIAN_POINT('Ctrl Pts',(97.5885622074047,-0.338431329294745,
-10.3499138704001));
#39116=CARTESIAN_POINT('Ctrl Pts',(97.5893730286879,-0.33571678845484,-10.3497206413114));
#39117=CARTESIAN_POINT('Ctrl Pts',(97.5912690164379,-0.329284691960429,
-10.349261959504));
#39118=CARTESIAN_POINT('Ctrl Pts',(97.5923456507548,-0.32556467510609,-10.3489960287361));
#39119=CARTESIAN_POINT('Ctrl Pts',(97.5960487638755,-0.312529164963181,
-10.3480620536682));
#39120=CARTESIAN_POINT('Ctrl Pts',(97.5985786550422,-0.303186967959959,
-10.3473889344492));
#39121=CARTESIAN_POINT('Ctrl Pts',(97.6191712142058,-0.223252113596779,
-10.3416035584047));
#39122=CARTESIAN_POINT('Ctrl Pts',(97.6307600479905,-0.15116091643948,-10.3362245342904));
#39123=CARTESIAN_POINT('Ctrl Pts',(97.6394621080441,-0.0208403352663324,
-10.3266425998832));
#39124=CARTESIAN_POINT('Ctrl Pts',(97.6390662658986,0.0369986000578744,
-10.322437653745));
#39125=CARTESIAN_POINT('Ctrl Pts',(97.6327439017465,0.115472762149749,-10.3168608650334));
#39126=CARTESIAN_POINT('Ctrl Pts',(97.630503176332,0.136317535264723,-10.3153913038444));
#39127=CARTESIAN_POINT('Ctrl Pts',(97.6256336464841,0.172499027029182,-10.3128608564475));
#39128=CARTESIAN_POINT('Ctrl Pts',(97.6232552394847,0.187863547373732,-10.3117927216581));
#39129=CARTESIAN_POINT('Ctrl Pts',(97.6193416384434,0.21020926217041,-10.3102479267851));
#39130=CARTESIAN_POINT('Ctrl Pts',(97.6180461034964,0.217230173878387,-10.3097638116526));
#39131=CARTESIAN_POINT('Ctrl Pts',(97.6156502914679,0.229583295954162,-10.3089140995947));
#39132=CARTESIAN_POINT('Ctrl Pts',(97.6145767434501,0.234920408880118,-10.3085476710602));
#39133=CARTESIAN_POINT('Ctrl Pts',(97.6122587266158,0.246044819460985,-10.3077852557351));
#39134=CARTESIAN_POINT('Ctrl Pts',(97.6110075523271,0.251830576791391,-10.3073894926348));
#39135=CARTESIAN_POINT('Ctrl Pts',(97.6076239740772,0.266925351739846,-10.3063588146737));
#39136=CARTESIAN_POINT('Ctrl Pts',(97.6054218443306,0.276218425295059,-10.3057261275267));
#39137=CARTESIAN_POINT('Ctrl Pts',(97.5956113847424,0.315483983633561,-10.3030594832556));
#39138=CARTESIAN_POINT('Ctrl Pts',(97.5869368786744,0.345179010834586,-10.3010596485522));
#39139=CARTESIAN_POINT('Ctrl Pts',(97.547397980448,0.463069430320239,-10.2931337270882));
#39140=CARTESIAN_POINT('Ctrl Pts',(97.5072630980035,0.547785210173771,-10.2874971016047));
#39141=CARTESIAN_POINT('Ctrl Pts',(97.4420020619828,0.651585577764651,-10.2798142703053));
#39142=CARTESIAN_POINT('Ctrl Pts',(97.4255496640518,0.675714136159123,-10.2779637442871));
#39143=CARTESIAN_POINT('Ctrl Pts',(97.3983104963319,0.712635510535071,-10.2749872081784));
#39144=CARTESIAN_POINT('Ctrl Pts',(97.3881180466705,0.725853274181756,-10.2738906294118));
#39145=CARTESIAN_POINT('Ctrl Pts',(97.3744323299601,0.742841992305386,-10.272433478883));
#39146=CARTESIAN_POINT('Ctrl Pts',(97.3711898349455,0.746813681537597,-10.2720893151264));
#39147=CARTESIAN_POINT('Ctrl Pts',(97.3658513982501,0.753266194593324,-10.2715241822711));
#39148=CARTESIAN_POINT('Ctrl Pts',(97.3637709005156,0.75575979859333,-10.2713043034189));
#39149=CARTESIAN_POINT('Ctrl Pts',(97.359675432883,0.760627398716923,-10.2708721093703));
#39150=CARTESIAN_POINT('Ctrl Pts',(97.3576613078154,0.763002072540364,-10.27065985779));
#39151=CARTESIAN_POINT('Ctrl Pts',(97.3531416538762,0.768288151389158,-10.270184287716));
#39152=CARTESIAN_POINT('Ctrl Pts',(97.3506312644098,0.771195327094181,-10.2699206247326));
#39153=CARTESIAN_POINT('Ctrl Pts',(97.3418921451673,0.781216211562879,-10.2690045975254));
#39154=CARTESIAN_POINT('Ctrl Pts',(97.3355921982093,0.788266930284467,-10.2683474316679));
#39155=CARTESIAN_POINT('Ctrl Pts',(97.276907786255,0.852374250616028,-10.2622608328277));
#39156=CARTESIAN_POINT('Ctrl Pts',(97.2191032641449,0.904204020466417,-10.256530893841));
#39157=CARTESIAN_POINT('Ctrl Pts',(97.0933804315891,0.996334927992151,-10.2451102858897));
#39158=CARTESIAN_POINT('Ctrl Pts',(97.0256430012394,1.03626305308206,-10.2394527221208));
#39159=CARTESIAN_POINT('Ctrl Pts',(96.9424876350059,1.07468022866367,-10.2331302766877));
#39160=CARTESIAN_POINT('Ctrl Pts',(96.9304562243289,1.07999597408983,-10.2322292109008));
#39161=CARTESIAN_POINT('Ctrl Pts',(96.9121499761785,1.08772021213893,-10.2308782264583));
#39162=CARTESIAN_POINT('Ctrl Pts',(96.9059397625232,1.09027822993904,-10.2304233460956));
#39163=CARTESIAN_POINT('Ctrl Pts',(96.8946617679668,1.09481124239496,-10.2296033276849));
#39164=CARTESIAN_POINT('Ctrl Pts',(96.889601582798,1.09680450553919,-10.2292375921824));
#39165=CARTESIAN_POINT('Ctrl Pts',(96.8786931441526,1.10101441187411,-10.2284537654709));
#39166=CARTESIAN_POINT('Ctrl Pts',(96.8728406540623,1.10321967508768,-10.228036058337));
#39167=CARTESIAN_POINT('Ctrl Pts',(96.856970520403,1.1090557297753,-10.2269107840463));
#39168=CARTESIAN_POINT('Ctrl Pts',(96.8469205608273,1.11259742517426,-10.226206133973));
#39169=CARTESIAN_POINT('Ctrl Pts',(96.7940470706375,1.13042763136496,-10.2225381149314));
#39170=CARTESIAN_POINT('Ctrl Pts',(96.7504735294051,1.1423825970985,-10.2196509506409));
#39171=CARTESIAN_POINT('Ctrl Pts',(96.6291979447398,1.16826704834721,-10.2118497624505));
#39172=CARTESIAN_POINT('Ctrl Pts',(96.5506246965517,1.17693956619396,-10.2070614215352));
#39173=CARTESIAN_POINT('Ctrl Pts',(96.4319188657766,1.17807812333763,-10.1995940008165));
#39174=CARTESIAN_POINT('Ctrl Pts',(96.3920717450702,1.17643669864132,-10.197044697995));
#39175=CARTESIAN_POINT('Ctrl Pts',(96.3457644474222,1.17216869514144,-10.1939543964287));
#39176=CARTESIAN_POINT('Ctrl Pts',(96.3391449464109,1.17150198250603,-10.193509574419));
#39177=CARTESIAN_POINT('Ctrl Pts',(96.3289477913203,1.17038758031127,-10.1928191065292));
#39178=CARTESIAN_POINT('Ctrl Pts',(96.3253658202838,1.16997947026224,-10.1925755673221));
#39179=CARTESIAN_POINT('Ctrl Pts',(96.3187527039388,1.16919523441498,-10.1921240024915));
#39180=CARTESIAN_POINT('Ctrl Pts',(96.3157210921172,1.16882375693528,-10.191916233542));
#39181=CARTESIAN_POINT('Ctrl Pts',(96.3088014968668,1.1679485331352,-10.1914402719191));
#39182=CARTESIAN_POINT('Ctrl Pts',(96.3049145869711,1.16743716667682,-10.1911716704924));
#39183=CARTESIAN_POINT('Ctrl Pts',(96.2947177621872,1.16604383335837,-10.1904638917223));
#39184=CARTESIAN_POINT('Ctrl Pts',(96.2884124258897,1.16513006754865,-10.1900230702317));
#39185=CARTESIAN_POINT('Ctrl Pts',(96.2360481625204,1.15710714948915,-10.1863375570663));
#39186=CARTESIAN_POINT('Ctrl Pts',(96.1904459829458,1.14732172480013,-10.1829709595529));
#39187=CARTESIAN_POINT('Ctrl Pts',(96.0682801739044,1.11341990657611,-10.1737106503624));
#39188=CARTESIAN_POINT('Ctrl Pts',(95.9933936369627,1.08413893770357,-10.1677827019961));
#39189=CARTESIAN_POINT('Ctrl Pts',(95.9219746556536,1.04742829986771,-10.1620534757847));
#39190=CARTESIAN_POINT('Ctrl Pts',(95.9218881615534,1.04738382680279,-10.1620465370855));
#39191=CARTESIAN_POINT('Ctrl Pts',(95.9218016730735,1.04733934308113,-10.1620395986893));
#39192=CARTESIAN_POINT('',(97.1451453741165,-0.958295198918411,-10.5));
#39193=CARTESIAN_POINT('Origin',(96.460480949577,-2.11854640757359E-15,
-10.5));
#39194=CARTESIAN_POINT('',(97.6382309406263,0.000145201367806521,-10.4243671147812));
#39195=CARTESIAN_POINT('Ctrl Pts',(97.6382309406263,0.000145201367822534,
-10.4243671147812));
#39196=CARTESIAN_POINT('Ctrl Pts',(97.6382368014081,-0.0473924754352446,
-10.4276037988433));
#39197=CARTESIAN_POINT('Ctrl Pts',(97.6353602115632,-0.0950271641440371,
-10.4308404829053));
#39198=CARTESIAN_POINT('Ctrl Pts',(97.6295919559438,-0.142388613631584,
-10.4340771669673));
#39199=CARTESIAN_POINT('Ctrl Pts',(97.6238335157924,-0.189669471200782,
-10.4373083433732));
#39200=CARTESIAN_POINT('Ctrl Pts',(97.6151932243682,-0.236677487308967,
-10.440539519779));
#39201=CARTESIAN_POINT('Ctrl Pts',(97.6037137770981,-0.283043750289888,
-10.4437706961849));
#39202=CARTESIAN_POINT('Ctrl Pts',(97.5922494600277,-0.329348901371691,
-10.4469976138191));
#39203=CARTESIAN_POINT('Ctrl Pts',(97.5779535327664,-0.37501346219832,-10.4502245314534));
#39204=CARTESIAN_POINT('Ctrl Pts',(97.5609199362858,-0.419677374933826,
-10.4534514490876));
#39205=CARTESIAN_POINT('Ctrl Pts',(97.5439022631352,-0.464299534994062,
-10.4566753501378));
#39206=CARTESIAN_POINT('Ctrl Pts',(97.5241521862377,-0.507922406356242,
-10.4598992511881));
#39207=CARTESIAN_POINT('Ctrl Pts',(97.5018131201261,-0.550202120206348,
-10.4631231522383));
#39208=CARTESIAN_POINT('Ctrl Pts',(97.4794789809893,-0.592472509088109,
-10.4663463422436));
#39209=CARTESIAN_POINT('Ctrl Pts',(97.454557220798,-0.633399850627232,-10.4695695322489));
#39210=CARTESIAN_POINT('Ctrl Pts',(97.4272380850568,-0.672663142664198,
-10.4727927222543));
#39211=CARTESIAN_POINT('Ctrl Pts',(97.3999245324198,-0.711918410616832,
-10.4760152535489));
#39212=CARTESIAN_POINT('Ctrl Pts',(97.370214886659,-0.749509870604237,-10.4792377848436));
#39213=CARTESIAN_POINT('Ctrl Pts',(97.3383422154285,-0.785146266893978,
-10.4824603161383));
#39214=CARTESIAN_POINT('Ctrl Pts',(97.3064421588081,-0.820813282412446,
-10.4856856162714));
#39215=CARTESIAN_POINT('Ctrl Pts',(97.2723757229821,-0.854521483376949,
-10.4889109164044));
#39216=CARTESIAN_POINT('Ctrl Pts',(97.236414587066,-0.886014702312063,-10.4921362165375));
#39217=CARTESIAN_POINT('Ctrl Pts',(97.2071883058683,-0.911609824628666,
-10.4947574776917));
#39218=CARTESIAN_POINT('Ctrl Pts',(97.1767113679881,-0.935742531375487,
-10.4973787388458));
#39219=CARTESIAN_POINT('Ctrl Pts',(97.1451453741165,-0.958295198918386,
-10.5));
#39220=CARTESIAN_POINT('Ctrl Pts',(95.9218016730721,1.04733934308042,-10.2615611054409));
#39221=CARTESIAN_POINT('Ctrl Pts',(95.9280836198898,1.05057034417782,-10.262040901113));
#39222=CARTESIAN_POINT('Ctrl Pts',(95.9343926980404,1.05374382729346,-10.2625206967852));
#39223=CARTESIAN_POINT('Ctrl Pts',(95.9407277584678,1.05685934865135,-10.2630004924573));
#39224=CARTESIAN_POINT('Ctrl Pts',(95.9841897259695,1.07823352330357,-10.2662921522843));
#39225=CARTESIAN_POINT('Ctrl Pts',(96.0290697844585,1.09697019344544,-10.2695838121113));
#39226=CARTESIAN_POINT('Ctrl Pts',(96.0750142256799,1.11288385165212,-10.2728754719383));
#39227=CARTESIAN_POINT('Ctrl Pts',(96.1193341606865,1.12823483380984,-10.2760507450664));
#39228=CARTESIAN_POINT('Ctrl Pts',(96.164643883886,1.14095891506093,-10.2792260181944));
#39229=CARTESIAN_POINT('Ctrl Pts',(96.2106024746863,1.15093692715382,-10.2824012913225));
#39230=CARTESIAN_POINT('Ctrl Pts',(96.2565163429393,1.16090522959048,-10.2855734745756));
#39231=CARTESIAN_POINT('Ctrl Pts',(96.3030772877012,1.16813263488393,-10.2887456578286));
#39232=CARTESIAN_POINT('Ctrl Pts',(96.3499301376088,1.17255003324939,-10.2919178410817));
#39233=CARTESIAN_POINT('Ctrl Pts',(96.3967578963307,1.17696506595808,-10.2950883255301));
#39234=CARTESIAN_POINT('Ctrl Pts',(96.4438766976299,1.17857302092982,-10.2982588099785));
#39235=CARTESIAN_POINT('Ctrl Pts',(96.4909248041402,1.17735646013403,-10.3014292944269));
#39236=CARTESIAN_POINT('Ctrl Pts',(96.5379683002796,1.17614001855231,-10.304599468191));
#39237=CARTESIAN_POINT('Ctrl Pts',(96.584940559731,1.1720996274432,-10.3077696419551));
#39238=CARTESIAN_POINT('Ctrl Pts',(96.6314811217072,1.16526992736938,-10.3109398157192));
#39239=CARTESIAN_POINT('Ctrl Pts',(96.678069400412,1.15843322499627,-10.3141132397733));
#39240=CARTESIAN_POINT('Ctrl Pts',(96.724224547625,1.14880159031184,-10.3172866638273));
#39241=CARTESIAN_POINT('Ctrl Pts',(96.7695944703289,1.13646112726673,-10.3204600878813));
#39242=CARTESIAN_POINT('Ctrl Pts',(96.8149924393552,1.12411303571833,-10.3236354736507));
#39243=CARTESIAN_POINT('Ctrl Pts',(96.8596036908615,1.1090529615634,-10.3268108594201));
#39244=CARTESIAN_POINT('Ctrl Pts',(96.9030930134713,1.09141633824824,-10.3299862451895));
#39245=CARTESIAN_POINT('Ctrl Pts',(96.9466605320552,1.07374800340354,-10.3331673404611));
#39246=CARTESIAN_POINT('Ctrl Pts',(96.9891015976539,1.05349412008248,-10.3363484357327));
#39247=CARTESIAN_POINT('Ctrl Pts',(97.0301043730256,1.03083665920392,-10.3395295310043));
#39248=CARTESIAN_POINT('Ctrl Pts',(97.0407201660206,1.02497054618352,-10.3403531301045));
#39249=CARTESIAN_POINT('Ctrl Pts',(97.0512397004402,1.0189435435138,-10.3411767292047));
#39250=CARTESIAN_POINT('Ctrl Pts',(97.0616578984223,1.01275926985492,-10.3420003283049));
#39251=CARTESIAN_POINT('Ctrl Pts',(97.1032960737916,0.988042723713015,-10.3452919881319));
#39252=CARTESIAN_POINT('Ctrl Pts',(97.1435148709796,0.960690062866965,-10.3485836479588));
#39253=CARTESIAN_POINT('Ctrl Pts',(97.1819585355496,0.930894814379747,-10.3518753077858));
#39254=CARTESIAN_POINT('Ctrl Pts',(97.2186428708157,0.902463110558934,-10.3550163286543));
#39255=CARTESIAN_POINT('Ctrl Pts',(97.2537105004253,0.871807916615277,-10.3581573495228));
#39256=CARTESIAN_POINT('Ctrl Pts',(97.2868787612889,0.839143443815064,-10.3612983703912));
#39257=CARTESIAN_POINT('Ctrl Pts',(97.3200145729144,0.806510927386065,-10.36443631833));
#39258=CARTESIAN_POINT('Ctrl Pts',(97.351254286152,0.7718734167847,-10.3675742662687));
#39259=CARTESIAN_POINT('Ctrl Pts',(97.380349063542,0.735484680608969,-10.3707122142075));
#39260=CARTESIAN_POINT('Ctrl Pts',(97.4094288083644,0.699114745612872,-10.3738485408445));
#39261=CARTESIAN_POINT('Ctrl Pts',(97.4363654556145,0.66099582000426,-10.3769848674815));
#39262=CARTESIAN_POINT('Ctrl Pts',(97.4609497080266,0.621415582252544,-10.3801211941184));
#39263=CARTESIAN_POINT('Ctrl Pts',(97.4855326067524,0.581837523913344,-10.3832573480594));
#39264=CARTESIAN_POINT('Ctrl Pts',(97.5077630698396,0.540798798312993,-10.3863935020003));
#39265=CARTESIAN_POINT('Ctrl Pts',(97.5274760904889,0.498614512193911,-10.3895296559413));
#39266=CARTESIAN_POINT('Ctrl Pts',(97.5472123600316,0.45638047530423,-10.3926695085599));
#39267=CARTESIAN_POINT('Ctrl Pts',(97.5644250256606,0.412998700993198,-10.3958093611785));
#39268=CARTESIAN_POINT('Ctrl Pts',(97.5789967832024,0.36880535846057,-10.398949213797));
#39269=CARTESIAN_POINT('Ctrl Pts',(97.5935786471709,0.32458136507679,-10.4020912441001));
#39270=CARTESIAN_POINT('Ctrl Pts',(97.6055158193112,0.279545235778642,-10.4052332744031));
#39271=CARTESIAN_POINT('Ctrl Pts',(97.6147416237034,0.234045633723838,-10.4083753047062));
#39272=CARTESIAN_POINT('Ctrl Pts',(97.6239861174384,0.188453860014178,-10.4115237000348));
#39273=CARTESIAN_POINT('Ctrl Pts',(97.6305082170572,0.142397304832613,-10.4146720953635));
#39274=CARTESIAN_POINT('Ctrl Pts',(97.6342930436276,0.0962300907233125,
-10.4178204906922));
#39275=CARTESIAN_POINT('Ctrl Pts',(97.6355671860971,0.0806881346777844,
-10.4188803818456));
#39276=CARTESIAN_POINT('Ctrl Pts',(97.6365315514698,0.0651336273818042,
-10.419940272999));
#39277=CARTESIAN_POINT('Ctrl Pts',(97.6371868971856,0.0495799895370037,
-10.4210001641524));
#39278=CARTESIAN_POINT('Ctrl Pts',(97.6378808416011,0.0331102700276012,
-10.4221224810136));
#39279=CARTESIAN_POINT('Ctrl Pts',(97.6382289083969,0.0166288424470303,
-10.4232447978749));
#39280=CARTESIAN_POINT('Ctrl Pts',(97.6382309406262,0.000145202030728477,
-10.4243671147361));
#39281=CARTESIAN_POINT('Ctrl Pts',(96.9698189919063,1.05966857234488,0.166148582192736));
#39282=CARTESIAN_POINT('Ctrl Pts',(97.3204778808345,0.89112161655769,0.139815303576882));
#39283=CARTESIAN_POINT('Ctrl Pts',(97.8354473421669,0.181504183543753,0.0871487463451743));
#39284=CARTESIAN_POINT('Ctrl Pts',(97.3631507055241,-1.05469178959263,0.00814891049761157));
#39285=CARTESIAN_POINT('Ctrl Pts',(96.0706374094237,-1.33116003884258,-0.0708509253499507));
#39286=CARTESIAN_POINT('Ctrl Pts',(95.1324539764634,-0.40140754516674,-0.149850761197514));
#39287=CARTESIAN_POINT('Ctrl Pts',(95.398731272582,0.893221222269588,-0.228850597045076));
#39288=CARTESIAN_POINT('Ctrl Pts',(96.6284070005896,1.37714878342488,-0.307850432892638));
#39289=CARTESIAN_POINT('Ctrl Pts',(97.7056520100152,0.611901250598986,-0.386850268740201));
#39290=CARTESIAN_POINT('Ctrl Pts',(97.6533122610813,-0.708562065134396,
-0.465850104587763));
#39291=CARTESIAN_POINT('Ctrl Pts',(96.5188040922679,-1.38616440608763,-0.544849940435326));
#39292=CARTESIAN_POINT('Ctrl Pts',(95.3313961518403,-0.806251887258617,
-0.623849776282889));
#39293=CARTESIAN_POINT('Ctrl Pts',(95.1682969837761,0.505111073403053,-0.702849612130451));
#39294=CARTESIAN_POINT('Ctrl Pts',(96.177480216103,1.35822699414563,-0.781849447978014));
#39295=CARTESIAN_POINT('Ctrl Pts',(97.4434024291193,0.97915193147552,-0.860849283825576));
#39296=CARTESIAN_POINT('Ctrl Pts',(97.8176113252564,-0.288219083786204,
-0.939849119673137));
#39297=CARTESIAN_POINT('Ctrl Pts',(96.9606204994759,-1.29411465266134,-1.0188489555207));
#39298=CARTESIAN_POINT('Ctrl Pts',(95.6498993457129,-1.12597967087778,-1.09784879136826));
#39299=CARTESIAN_POINT('Ctrl Pts',(95.0745440861015,0.0636531236609935,
-1.17684862721583));
#39300=CARTESIAN_POINT('Ctrl Pts',(95.7565216816914,1.19553919527067,-1.25584846306339));
#39301=CARTESIAN_POINT('Ctrl Pts',(97.0771366259267,1.24282277813268,-1.33484829891095));
#39302=CARTESIAN_POINT('Ctrl Pts',(97.8383167123646,0.162607750675068,-1.41384813475851));
#39303=CARTESIAN_POINT('Ctrl Pts',(97.3495133703376,-1.06512629046087,-1.49284797060608));
#39304=CARTESIAN_POINT('Ctrl Pts',(96.054172839641,-1.32656940567028,-1.57184780645364));
#39305=CARTESIAN_POINT('Ctrl Pts',(95.1274382145455,-0.38453833712907,-1.6508476423012));
#39306=CARTESIAN_POINT('Ctrl Pts',(95.4100504255828,0.906348928056774,-1.72984747814876));
#39307=CARTESIAN_POINT('Ctrl Pts',(96.6456214547034,1.37498933072291,-1.80884731399633));
#39308=CARTESIAN_POINT('Ctrl Pts',(97.713231564224,0.596228616712231,-1.88784714984389));
#39309=CARTESIAN_POINT('Ctrl Pts',(97.6443364803891,-0.723435379256512,
-1.96684698569145));
#39310=CARTESIAN_POINT('Ctrl Pts',(96.5014383643424,-1.38679311943509,-2.04584682153901));
#39311=CARTESIAN_POINT('Ctrl Pts',(95.3213833600239,-0.792041253569239,
-2.12484665738657));
#39312=CARTESIAN_POINT('Ctrl Pts',(95.1747266322779,0.521256655997792,-2.20384649323414));
#39313=CARTESIAN_POINT('Ctrl Pts',(96.1945163159272,1.36166643475577,-2.2828463290817));
#39314=CARTESIAN_POINT('Ctrl Pts',(97.4555912033766,0.966761733141859,-2.36184616492926));
#39315=CARTESIAN_POINT('Ctrl Pts',(97.8138942557399,-0.305196803040322,
-2.44084600077682));
#39316=CARTESIAN_POINT('Ctrl Pts',(96.9443701307973,-1.300278403337,-2.51984583662439));
#39317=CARTESIAN_POINT('Ctrl Pts',(95.6358579415274,-1.11573722734368,-2.59884567247195));
#39318=CARTESIAN_POINT('Ctrl Pts',(95.0754502194629,0.0810095212020413,
-2.67784550831951));
#39319=CARTESIAN_POINT('Ctrl Pts',(95.7715532499494,1.20426379608938,-2.75684534416707));
#39320=CARTESIAN_POINT('Ctrl Pts',(97.092656898466,1.23500050021526,-2.83584518001464));
#39321=CARTESIAN_POINT('Ctrl Pts',(97.8402455627935,0.145335054276059,-2.9148450158622));
#39322=CARTESIAN_POINT('Ctrl Pts',(97.3361009371651,-1.076179493961,-2.99384485170976));
#39323=CARTESIAN_POINT('Ctrl Pts',(96.037586984105,-1.32137555594659,-3.07284468755733));
#39324=CARTESIAN_POINT('Ctrl Pts',(95.1227257567579,-0.36780933915736,-3.15184452340489));
#39325=CARTESIAN_POINT('Ctrl Pts',(95.4214865433566,0.919436397870225,-3.23084435925245));
#39326=CARTESIAN_POINT('Ctrl Pts',(96.66283121266,1.37256221604562,-3.30984419510002));
#39327=CARTESIAN_POINT('Ctrl Pts',(97.7206021345964,0.580488815526218,-3.38884403094757));
#39328=CARTESIAN_POINT('Ctrl Pts',(97.6351812239852,-0.738208595988316,
-3.46784386679515));
#39329=CARTESIAN_POINT('Ctrl Pts',(96.4840630015917,-1.38719737337863,-3.54684370264269));
#39330=CARTESIAN_POINT('Ctrl Pts',(95.3115509564625,-0.777709802437698,
-3.62584353849027));
#39331=CARTESIAN_POINT('Ctrl Pts',(95.1813572215973,0.53732220725129,-3.70484337433782));
#39332=CARTESIAN_POINT('Ctrl Pts',(96.2115945754469,1.36489129188303,-3.78384321018539));
#39333=CARTESIAN_POINT('Ctrl Pts',(97.4676236019706,0.954220280446444,-3.86284304603295));
#39334=CARTESIAN_POINT('Ctrl Pts',(97.809964906937,-0.322126861211645,-3.94184288188052));
#39335=CARTESIAN_POINT('Ctrl Pts',(96.9280437706806,-1.30623798528726,-4.02084271772807));
#39336=CARTESIAN_POINT('Ctrl Pts',(95.6219459721774,-1.10531975353869,-4.09984255357564));
#39337=CARTESIAN_POINT('Ctrl Pts',(95.0765736886995,0.098353236737004,-4.1788423894232));
#39338=CARTESIAN_POINT('Ctrl Pts',(95.7866929376608,1.21279939845126,-4.25784222527076));
#39339=CARTESIAN_POINT('Ctrl Pts',(97.1080779610953,1.22698442392656,-4.33684206111833));
#39340=CARTESIAN_POINT('Ctrl Pts',(97.8419578912489,0.128039546681841,-4.41584189696589));
#39341=CARTESIAN_POINT('Ctrl Pts',(97.3225510936281,-1.08706381258025,-4.49484173281344));
#39342=CARTESIAN_POINT('Ctrl Pts',(96.0210674930154,-1.31597434628425,-4.57384156866102));
#39343=CARTESIAN_POINT('Ctrl Pts',(95.1182232301301,-0.351022621025214,
-4.65284140450857));
#39344=CARTESIAN_POINT('Ctrl Pts',(95.433085708698,0.932379581986348,-4.73184124035615));
#39345=CARTESIAN_POINT('Ctrl Pts',(96.6800092161049,1.36991970789569,-4.81084107620369));
#39346=CARTESIAN_POINT('Ctrl Pts',(97.7277749565514,0.564657919250789,-4.88984091205127));
#39347=CARTESIAN_POINT('Ctrl Pts',(97.6258416240571,-0.752865966996209,
-4.96884074789882));
#39348=CARTESIAN_POINT('Ctrl Pts',(96.4666839381626,-1.38738393706227,-5.04784058374639));
#39349=CARTESIAN_POINT('Ctrl Pts',(95.3018988523223,-0.763256306758528,
-5.12684041959395));
#39350=CARTESIAN_POINT('Ctrl Pts',(95.188188541403,0.553303437535439,-5.20584025544151));
#39351=CARTESIAN_POINT('Ctrl Pts',(96.2287118922362,1.3679019591861,-5.28484009128907));
#39352=CARTESIAN_POINT('Ctrl Pts',(97.4794979515607,0.941529083753663,-5.36383992713664));
#39353=CARTESIAN_POINT('Ctrl Pts',(97.8058237861511,-0.339006368619123,
-5.4428397629842));
#39354=CARTESIAN_POINT('Ctrl Pts',(96.911644036809,-1.31199258176452,-5.52183959883176));
#39355=CARTESIAN_POINT('Ctrl Pts',(95.6081655925459,-1.09472882398092,-5.60083943467933));
#39356=CARTESIAN_POINT('Ctrl Pts',(95.077914331903,0.115681517883201,-5.67983927052688));
#39357=CARTESIAN_POINT('Ctrl Pts',(95.8019383616594,1.22114467848177,-5.75883910637445));
#39358=CARTESIAN_POINT('Ctrl Pts',(97.1233973975418,1.21877579927701,-5.83783894222201));
#39359=CARTESIAN_POINT('Ctrl Pts',(97.8434534271231,0.110723946082075,-5.91683877806957));
#39360=CARTESIAN_POINT('Ctrl Pts',(97.3088659670429,-1.0977775403174,-5.99583861391714));
#39361=CARTESIAN_POINT('Ctrl Pts',(96.0046169582537,-1.31036662323974,-6.0748384497647));
#39362=CARTESIAN_POINT('Ctrl Pts',(95.1139313414852,-0.334180817572524,
-6.15383828561227));
#39363=CARTESIAN_POINT('Ctrl Pts',(95.4448461012445,0.9451764495261,-6.23283812145983));
#39364=CARTESIAN_POINT('Ctrl Pts',(96.6971527693917,1.36706222081932,-6.31183795730738));
#39365=CARTESIAN_POINT('Ctrl Pts',(97.7347489044381,0.548738412268767,-6.39083779315495));
#39366=CARTESIAN_POINT('Ctrl Pts',(97.6163191462674,-0.767405192162125,
-6.46983762900251));
#39367=CARTESIAN_POINT('Ctrl Pts',(96.4493039013101,-1.3873527811908,-6.54883746485007));
#39368=CARTESIAN_POINT('Ctrl Pts',(95.2924285622943,-0.748683034700886,
-6.62783730069764));
#39369=CARTESIAN_POINT('Ctrl Pts',(95.1952195196663,0.569197838950488,-6.7068371365452));
#39370=CARTESIAN_POINT('Ctrl Pts',(96.2458655801085,1.37069796420425,-6.78583697239276));
#39371=CARTESIAN_POINT('Ctrl Pts',(97.4912123887268,0.928690134670386,-6.86483680824032));
#39372=CARTESIAN_POINT('Ctrl Pts',(97.8014715432413,-0.355832676393984,
-6.94383664408789));
#39373=CARTESIAN_POINT('Ctrl Pts',(96.8951735027615,-1.31754128971044,-7.02283647993545));
#39374=CARTESIAN_POINT('Ctrl Pts',(95.5945189651623,-1.08396610068519,-7.10183631578301));
#39375=CARTESIAN_POINT('Ctrl Pts',(95.079471938689,0.132991645346109,-7.18083615163058));
#39376=CARTESIAN_POINT('Ctrl Pts',(95.8172871295089,1.22929832657175,-7.25983598747813));
#39377=CARTESIAN_POINT('Ctrl Pts',(97.1386128037557,1.21037591443069,-7.3388358233257));
#39378=CARTESIAN_POINT('Ctrl Pts',(97.8447319357241,0.093390969781441,-7.41783565917326));
#39379=CARTESIAN_POINT('Ctrl Pts',(97.2950477049903,-1.10831899588724,-7.49683549502083));
#39380=CARTESIAN_POINT('Ctrl Pts',(95.9882379613722,-1.30455326682254,-7.57583533086838));
#39381=CARTESIAN_POINT('Ctrl Pts',(95.1098507643406,-0.317286571751796,
-7.65483516671596));
#39382=CARTESIAN_POINT('Ctrl Pts',(95.4567658754601,0.957824992300916,-7.7338350025635));
#39383=CARTESIAN_POINT('Ctrl Pts',(96.7142591822142,1.36399020323693,-7.81283483841108));
#39384=CARTESIAN_POINT('Ctrl Pts',(97.7415228838485,0.532732792797828,-7.89183467425863));
#39385=CARTESIAN_POINT('Ctrl Pts',(97.6066152849611,-0.781823989871474,
-7.9708345101062));
#39386=CARTESIAN_POINT('Ctrl Pts',(96.4319256184501,-1.38710391065599,-8.04983434595377));
#39387=CARTESIAN_POINT('Ctrl Pts',(95.2831415725345,-0.733992273215962,
-8.12883418180132));
#39388=CARTESIAN_POINT('Ctrl Pts',(95.2024490530263,0.585002917208061,-8.2078340176489));
#39389=CARTESIAN_POINT('Ctrl Pts',(96.2630529471728,1.373278868185,-8.28683385349645));
#39390=CARTESIAN_POINT('Ctrl Pts',(97.502765075134,0.915705447950804,-8.36583368934401));
#39391=CARTESIAN_POINT('Ctrl Pts',(97.7969088612167,-0.37260314394072,-8.44483352519157));
#39392=CARTESIAN_POINT('Ctrl Pts',(96.878634753188,-1.32288323852336,-8.52383336103914));
#39393=CARTESIAN_POINT('Ctrl Pts',(95.5810082316452,-1.07303327233716,-8.6028331968867));
#39394=CARTESIAN_POINT('Ctrl Pts',(95.08124626447,0.150280902113239,-8.68183303273427));
#39395=CARTESIAN_POINT('Ctrl Pts',(95.8327368328608,1.23725906429836,-8.76083286858181));
#39396=CARTESIAN_POINT('Ctrl Pts',(97.1537217914135,1.20178608537639,-8.8398327044294));
#39397=CARTESIAN_POINT('Ctrl Pts',(97.8457932175932,0.0760433421147284,
-8.91883254027695));
#39398=CARTESIAN_POINT('Ctrl Pts',(97.2810984736349,-1.11868653349764,-8.99783237612451));
#39399=CARTESIAN_POINT('Ctrl Pts',(95.9719330772361,-1.29853517268555,-9.07683221197208));
#39400=CARTESIAN_POINT('Ctrl Pts',(95.1059821301293,-0.300342567425433,
-9.15583204781964));
#39401=CARTESIAN_POINT('Ctrl Pts',(95.4688431783388,0.970323289634254,-9.2348318836672));
#39402=CARTESIAN_POINT('Ctrl Pts',(96.7313257356152,1.36070401097439,-9.31383171951477));
#39403=CARTESIAN_POINT('Ctrl Pts',(97.7480958995279,0.516643820744214,-9.39283155536233));
#39404=CARTESIAN_POINT('Ctrl Pts',(97.5967314297322,-0.796120585216384,
-9.47183139120988));
#39405=CARTESIAN_POINT('Ctrl Pts',(96.4145520785679,-1.38663640568844,-9.55083122705745));
#39406=CARTESIAN_POINT('Ctrl Pts',(95.2740388257579,-0.719188212344122,
-9.62983106290501));
#39407=CARTESIAN_POINT('Ctrl Pts',(95.2098770186021,0.600719896472962,-9.70883089875258));
#39408=CARTESIAN_POINT('Ctrl Pts',(96.2802693077949,1.37563698476155,-9.78783073460014));
#39409=CARTESIAN_POINT('Ctrl Pts',(97.5141581063061,0.902591373346843,-9.86683057044771));
#39410=CARTESIAN_POINT('Ctrl Pts',(97.7921287736904,-0.389343271126291,
-9.94583040629525));
#39411=CARTESIAN_POINT('Ctrl Pts',(96.8620454838072,-1.32796229432384,-10.0248302421428));
#39412=CARTESIAN_POINT('Ctrl Pts',(95.5676058319486,-1.06204074913918,-10.1038300779904));
#39413=CARTESIAN_POINT('Ctrl Pts',(95.0832953624497,0.167760296979913,-10.182829913838));
#39414=CARTESIAN_POINT('Ctrl Pts',(95.8481704737817,1.24460472281043,-10.2618297496855));
#39415=CARTESIAN_POINT('Ctrl Pts',(97.1689462680908,1.19384435828083,-10.3408295855331));
#39416=CARTESIAN_POINT('Ctrl Pts',(97.846259559098,0.0568453784873504,-10.4198356323639));
#39417=CARTESIAN_POINT('Ctrl Pts',(97.4604426383845,-0.730656199282666,
-10.4725084005789));
#39418=CARTESIAN_POINT('Ctrl Pts',(97.1437425383552,-0.956805267514262,
-10.4988478901781));
#39419=CARTESIAN_POINT('Ctrl Pts',(97.0116446152009,1.14668602409723,0.110406857325715));
#39420=CARTESIAN_POINT('Ctrl Pts',(97.39109877441,0.964298394937262,0.0840735787098607));
#39421=CARTESIAN_POINT('Ctrl Pts',(97.9483562977128,0.196408873506787,0.0314070214781526));
#39422=CARTESIAN_POINT('Ctrl Pts',(97.4372757895234,-1.14130055983423,-0.0475928143694103));
#39423=CARTESIAN_POINT('Ctrl Pts',(96.0386243891912,-1.44047172126636,-0.126592650216973));
#39424=CARTESIAN_POINT('Ctrl Pts',(95.0233995739129,-0.434370173866093,
-0.205592486064536));
#39425=CARTESIAN_POINT('Ctrl Pts',(95.3115429254873,0.966570415254535,-0.284592321912098));
#39426=CARTESIAN_POINT('Ctrl Pts',(96.6421966867455,1.4902369516927,-0.363592157759661));
#39427=CARTESIAN_POINT('Ctrl Pts',(97.807902482949,0.662149119546701,-0.442591993607223));
#39428=CARTESIAN_POINT('Ctrl Pts',(97.7512647188651,-0.766747489261799,
-0.521591829454785));
#39429=CARTESIAN_POINT('Ctrl Pts',(96.5235934494195,-1.49999291575139,-0.600591665302348));
#39430=CARTESIAN_POINT('Ctrl Pts',(95.238678405485,-0.872459366210753,-0.679591501149911));
#39431=CARTESIAN_POINT('Ctrl Pts',(95.0621859233619,0.546589588107095,-0.758591336997473));
#39432=CARTESIAN_POINT('Ctrl Pts',(96.1542408719215,1.46976135027951,-0.837591172845036));
#39433=CARTESIAN_POINT('Ctrl Pts',(97.5241175929496,1.05955754902332,-0.916591008692599));
#39434=CARTESIAN_POINT('Ctrl Pts',(97.9290556297016,-0.3118869464293,-0.995590844540159));
#39435=CARTESIAN_POINT('Ctrl Pts',(97.0016907645461,-1.40038425646847,-1.07459068038772));
#39436=CARTESIAN_POINT('Ctrl Pts',(95.5833363207763,-1.21844243163316,-1.15359051623528));
#39437=CARTESIAN_POINT('Ctrl Pts',(94.9607342616933,0.0688801661171027,
-1.23259035208285));
#39438=CARTESIAN_POINT('Ctrl Pts',(95.6987142282786,1.29371401800065,-1.31159018793041));
#39439=CARTESIAN_POINT('Ctrl Pts',(97.1277749169594,1.34488041573305,-1.39059002377797));
#39440=CARTESIAN_POINT('Ctrl Pts',(97.9514612937366,0.175960710712014,-1.46958985962553));
#39441=CARTESIAN_POINT('Ctrl Pts',(97.4225185889493,-1.15259191698711,-1.5485896954731));
#39442=CARTESIAN_POINT('Ctrl Pts',(96.0208077882696,-1.43550411626438,-1.62758953132066));
#39443=CARTESIAN_POINT('Ctrl Pts',(95.0179719296082,-0.416115706762684,
-1.70658936716822));
#39444=CARTESIAN_POINT('Ctrl Pts',(95.3237915802923,0.980776136880604,-1.78558920301579));
#39445=CARTESIAN_POINT('Ctrl Pts',(96.6608247507084,1.4879001698935,-1.86458903886335));
#39446=CARTESIAN_POINT('Ctrl Pts',(97.8161044520424,0.645189486405023,-1.94358887471091));
#39447=CARTESIAN_POINT('Ctrl Pts',(97.7415518685047,-0.782842164409236,
-2.02258871055847));
#39448=CARTESIAN_POINT('Ctrl Pts',(96.5048016894009,-1.50067325753703,-2.10158854640604));
#39449=CARTESIAN_POINT('Ctrl Pts',(95.2278433871241,-0.857081789230136,
-2.1805883822536));
#39450=CARTESIAN_POINT('Ctrl Pts',(95.0691435592389,0.564061007374844,-2.25958821810116));
#39451=CARTESIAN_POINT('Ctrl Pts',(96.1726759355667,1.47348322953618,-2.33858805394872));
#39452=CARTESIAN_POINT('Ctrl Pts',(97.5373072802312,1.04614989720104,-2.41758788979629));
#39453=CARTESIAN_POINT('Ctrl Pts',(97.9250333233159,-0.330258835431031,
-2.49658772564385));
#39454=CARTESIAN_POINT('Ctrl Pts',(96.9841059544115,-1.40705415962521,-2.57558756149141));
#39455=CARTESIAN_POINT('Ctrl Pts',(95.5681418700222,-1.20735890310389,-2.65458739733897));
#39456=CARTESIAN_POINT('Ctrl Pts',(94.9617148045619,0.087661829562074,-2.73358723318654));
#39457=CARTESIAN_POINT('Ctrl Pts',(95.7149801530134,1.30315506219667,-2.81258706903409));
#39458=CARTESIAN_POINT('Ctrl Pts',(97.1445696772038,1.33641579103944,-2.89158690488166));
#39459=CARTESIAN_POINT('Ctrl Pts',(97.9535485367549,0.157269621746915,-2.97058674072922));
#39460=CARTESIAN_POINT('Ctrl Pts',(97.408004758805,-1.16455278315403,-3.04958657657678));
#39461=CARTESIAN_POINT('Ctrl Pts',(96.0028599418983,-1.4298837600088,-3.12858641242435));
#39462=CARTESIAN_POINT('Ctrl Pts',(95.0128724960447,-0.398012963440909,
-3.20758624827191));
#39463=CARTESIAN_POINT('Ctrl Pts',(95.3361668047384,0.994938318450894,-3.28658608411947));
#39464=CARTESIAN_POINT('Ctrl Pts',(96.6794477328763,1.48527374635697,-3.36558591996704));
#39465=CARTESIAN_POINT('Ctrl Pts',(97.8240802760465,0.628157170345926,-3.44458575581459));
#39466=CARTESIAN_POINT('Ctrl Pts',(97.7316448043156,-0.798828522407786,
-3.52358559166216));
#39467=CARTESIAN_POINT('Ctrl Pts',(96.4859995033687,-1.5011107078487,-3.60258542750972));
#39468=CARTESIAN_POINT('Ctrl Pts',(95.2172035700704,-0.841573473567619,
-3.68158526335729));
#39469=CARTESIAN_POINT('Ctrl Pts',(95.0763186367137,0.581445823318793,-3.76058509920484));
#39470=CARTESIAN_POINT('Ctrl Pts',(96.1911566209602,1.47697290422696,-3.83958493505241));
#39471=CARTESIAN_POINT('Ctrl Pts',(97.5503277506541,1.03257857037017,-3.91858477089997));
#39472=CARTESIAN_POINT('Ctrl Pts',(97.9207813057759,-0.348579149535705,
-3.99758460674753));
#39473=CARTESIAN_POINT('Ctrl Pts',(96.9664389126037,-1.41350312820859,-4.0765844425951));
#39474=CARTESIAN_POINT('Ctrl Pts',(95.5530874829827,-1.19608597123602,-4.15558427844266));
#39475=CARTESIAN_POINT('Ctrl Pts',(94.9629305304085,0.106429769584916,-4.23458411429023));
#39476=CARTESIAN_POINT('Ctrl Pts',(95.731363075713,1.31239158783408,-4.31358395013778));
#39477=CARTESIAN_POINT('Ctrl Pts',(97.1612570806572,1.32774145371525,-4.39258378598535));
#39478=CARTESIAN_POINT('Ctrl Pts',(97.9554014775327,0.138553848385749,-4.47158362183291));
#39479=CARTESIAN_POINT('Ctrl Pts',(97.3933422344856,-1.1763308960171,-4.55058345768047));
#39480=CARTESIAN_POINT('Ctrl Pts',(95.9849839096634,-1.42403901591176,-4.62958329352804));
#39481=CARTESIAN_POINT('Ctrl Pts',(95.0080002326859,-0.379847760117011,
-4.7085831293756));
#39482=CARTESIAN_POINT('Ctrl Pts',(95.3487184658291,1.00894436592707,-4.78758296522316));
#39483=CARTESIAN_POINT('Ctrl Pts',(96.6980363529281,1.48241424175037,-4.86658280107073));
#39484=CARTESIAN_POINT('Ctrl Pts',(97.8318421130057,0.611026278686286,-4.94558263691828));
#39485=CARTESIAN_POINT('Ctrl Pts',(97.7215382587522,-0.814689521708318,
-5.02458247276585));
#39486=CARTESIAN_POINT('Ctrl Pts',(96.4671933127673,-1.50131259169636,-5.10358230861341));
#39487=CARTESIAN_POINT('Ctrl Pts',(95.2067588581957,-0.825933091350775,
-5.18258214446097));
#39488=CARTESIAN_POINT('Ctrl Pts',(95.0837109281827,0.598739394056823,-5.26158198030854));
#39489=CARTESIAN_POINT('Ctrl Pts',(96.2096795709132,1.48023080033689,-5.3405818161561));
#39490=CARTESIAN_POINT('Ctrl Pts',(97.5631771934661,1.01884520292257,-5.41958165200366));
#39491=CARTESIAN_POINT('Ctrl Pts',(97.9163001260439,-0.366844761768566,
-5.49858148785122));
#39492=CARTESIAN_POINT('Ctrl Pts',(96.9486924717633,-1.41973027840158,-5.57758132369879));
#39493=CARTESIAN_POINT('Ctrl Pts',(95.5381754914957,-1.18462533984329,-5.65658115954635));
#39494=CARTESIAN_POINT('Ctrl Pts',(94.9643812640292,0.125181007783859,-5.73558099539391));
#39495=CARTESIAN_POINT('Ctrl Pts',(95.747860417511,1.32142216232493,-5.81458083124147));
#39496=CARTESIAN_POINT('Ctrl Pts',(97.1778345126287,1.31885875641881,-5.89358066708904));
#39497=CARTESIAN_POINT('Ctrl Pts',(97.9570198232402,0.119816332029419,-5.9725805029366));
#39498=CARTESIAN_POINT('Ctrl Pts',(97.3785333179971,-1.18792440948235,-6.05158033878416));
#39499=CARTESIAN_POINT('Ctrl Pts',(95.9671824962854,-1.41797080004694,-6.13058017463173));
#39500=CARTESIAN_POINT('Ctrl Pts',(95.0033559043983,-0.361622947997633,
-6.20958001047928));
#39501=CARTESIAN_POINT('Ctrl Pts',(95.3614445937175,1.02279208165916,-6.28857984632685));
#39502=CARTESIAN_POINT('Ctrl Pts',(96.7165876938569,1.47932210466145,-6.36757968217441));
#39503=CARTESIAN_POINT('Ctrl Pts',(97.8393887448333,0.593799499820503,-6.44657951802197));
#39504=CARTESIAN_POINT('Ctrl Pts',(97.7112338178343,-0.830422673312564,
-6.52557935386954));
#39505=CARTESIAN_POINT('Ctrl Pts',(96.4483860688072,-1.50127887737916,-6.6045791897171));
#39506=CARTESIAN_POINT('Ctrl Pts',(95.1965108905739,-0.810163097005384,
-6.68357902556466));
#39507=CARTESIAN_POINT('Ctrl Pts',(95.0913192735848,0.615939005746443,-6.76257886141222));
#39508=CARTESIAN_POINT('Ctrl Pts',(96.2282418786556,1.48325640660785,-6.84157869725979));
#39509=CARTESIAN_POINT('Ctrl Pts',(97.5758535922281,1.00495195001113,-6.92057853310735));
#39510=CARTESIAN_POINT('Ctrl Pts',(97.9115904873431,-0.385052805742064,
-6.9995783689549));
#39511=CARTESIAN_POINT('Ctrl Pts',(96.9308694168058,-1.42573463298888,-7.07857820480248));
#39512=CARTESIAN_POINT('Ctrl Pts',(95.5234082356713,-1.17297880742125,-7.15757804065002));
#39513=CARTESIAN_POINT('Ctrl Pts',(94.9660667777636,0.143912601562404,-7.23657787649761));
#39514=CARTESIAN_POINT('Ctrl Pts',(95.7644695895102,1.33024536851806,-7.31557771234515));
#39515=CARTESIAN_POINT('Ctrl Pts',(97.1942993716535,1.30976909309513,-7.39457754819273));
#39516=CARTESIAN_POINT('Ctrl Pts',(97.958403319913,0.101060013121175,-7.47357738404029));
#39517=CARTESIAN_POINT('Ctrl Pts',(97.363580333275,-1.19933150420143,-7.55257721988785));
#39518=CARTESIAN_POINT('Ctrl Pts',(95.9494584953071,-1.41168006468811,-7.63157705573541));
#39519=CARTESIAN_POINT('Ctrl Pts',(94.9989402400067,-0.343341387068236,
-7.71057689158298));
#39520=CARTESIAN_POINT('Ctrl Pts',(95.3743431913168,1.03647929255094,-7.78957672743054));
#39521=CARTESIAN_POINT('Ctrl Pts',(96.7350988444355,1.47599782033385,-7.8685765632781));
#39522=CARTESIAN_POINT('Ctrl Pts',(97.8467189872506,0.576479537113928,-7.94757639912566));
#39523=CARTESIAN_POINT('Ctrl Pts',(97.7007330986187,-0.846025508245198,
-8.02657623497322));
#39524=CARTESIAN_POINT('Ctrl Pts',(96.429580722873,-1.50100957019055,-8.1055760708208));
#39525=CARTESIAN_POINT('Ctrl Pts',(95.1864612754006,-0.794265965281614,
-8.18457590666833));
#39526=CARTESIAN_POINT('Ctrl Pts',(95.0991424789539,0.633041959274281,-8.26357574251592));
#39527=CARTESIAN_POINT('Ctrl Pts',(96.2468406312449,1.48604924825804,-8.34257557836346));
#39528=CARTESIAN_POINT('Ctrl Pts',(97.5883549576452,0.990900991836843,-8.42157541421104));
#39529=CARTESIAN_POINT('Ctrl Pts',(97.9066531287706,-0.403200424021302,
-8.50057525005859));
#39530=CARTESIAN_POINT('Ctrl Pts',(96.9129725446261,-1.43151524987712,-8.57957508590616));
#39531=CARTESIAN_POINT('Ctrl Pts',(95.5087880329934,-1.16114820132636,-8.65857492175372));
#39532=CARTESIAN_POINT('Ctrl Pts',(94.9679868069389,0.162621610793496,-8.73757475760129));
#39533=CARTESIAN_POINT('Ctrl Pts',(95.7811879855942,1.33885982300962,-8.81657459344884));
#39534=CARTESIAN_POINT('Ctrl Pts',(97.2106490732843,1.30047388779886,-8.89557442929642));
#39535=CARTESIAN_POINT('Ctrl Pts',(97.9595517517141,0.0822878397116671,
-8.97457426514396));
#39536=CARTESIAN_POINT('Ctrl Pts',(97.3484856243634,-1.21055039923371,-9.05357410099154));
#39537=CARTESIAN_POINT('Ctrl Pts',(95.9318146930359,-1.40516777903702,-9.1325739368391));
#39538=CARTESIAN_POINT('Ctrl Pts',(94.9947539227958,-0.325005981583586,
-9.21157377268665));
#39539=CARTESIAN_POINT('Ctrl Pts',(95.3874122534566,1.05000392020451,-9.29057360853423));
#39540=CARTESIAN_POINT('Ctrl Pts',(96.7535668624323,1.47244177381299,-9.36957344438178));
#39541=CARTESIAN_POINT('Ctrl Pts',(97.8538317632754,0.559069377109707,-9.44857328022934));
#39542=CARTESIAN_POINT('Ctrl Pts',(97.69003760481,-0.86149610584715,-9.52757311607691));
#39543=CARTESIAN_POINT('Ctrl Pts',(96.4107805093987,-1.50050367483187,-9.60657295192447));
#39544=CARTESIAN_POINT('Ctrl Pts',(95.1766110328037,-0.778246230295927,
-9.68557278777204));
#39545=CARTESIAN_POINT('Ctrl Pts',(95.1071804113186,0.650049579330621,-9.76457262361959));
#39546=CARTESIAN_POINT('Ctrl Pts',(96.2654707582736,1.48860100773463,-9.84357245946716));
#39547=CARTESIAN_POINT('Ctrl Pts',(97.6006835573209,0.976710020754203,-9.92257229531473));
#39548=CARTESIAN_POINT('Ctrl Pts',(97.9014805118753,-0.421315210461393,
-10.0015721311623));
#39549=CARTESIAN_POINT('Ctrl Pts',(96.8950210040736,-1.43701138560673,-10.0805719670098));
#39550=CARTESIAN_POINT('Ctrl Pts',(95.49428506025,-1.14925299838305,-10.1595718028574));
#39551=CARTESIAN_POINT('Ctrl Pts',(94.9702041719499,0.181536371810648,-10.238571638705));
#39552=CARTESIAN_POINT('Ctrl Pts',(95.7978890002384,1.34680868945089,-10.3175714745525));
#39553=CARTESIAN_POINT('Ctrl Pts',(97.2271237476169,1.29188000504595,-10.3965713104001));
#39554=CARTESIAN_POINT('Ctrl Pts',(97.9600563880694,0.0615133851726164,
-10.4755773572309));
#39555=CARTESIAN_POINT('Ctrl Pts',(97.5425571034927,-0.790655940926349,
-10.5282501254459));
#39556=CARTESIAN_POINT('Ctrl Pts',(97.1998503478036,-1.03537583040079,-10.5545896150451));
#39557=CARTESIAN_POINT('Ctrl Pts',(97.0534702384955,1.23370347584956,0.0546651324586929));
#39558=CARTESIAN_POINT('Ctrl Pts',(97.4617196679856,1.03747517331684,0.0283318538428387));
#39559=CARTESIAN_POINT('Ctrl Pts',(98.0612652532588,0.21131356346982,-0.0243347033888694));
#39560=CARTESIAN_POINT('Ctrl Pts',(97.5114008735226,-1.22790933007582,-0.103334539236432));
#39561=CARTESIAN_POINT('Ctrl Pts',(96.0066113689587,-1.54978340369014,-0.182334375083995));
#39562=CARTESIAN_POINT('Ctrl Pts',(94.9143451713624,-0.467332802565443,
-0.261334210931557));
#39563=CARTESIAN_POINT('Ctrl Pts',(95.2243545783925,1.03991960823948,-0.340334046779121));
#39564=CARTESIAN_POINT('Ctrl Pts',(96.6559863729016,1.60332511996053,-0.419333882626682));
#39565=CARTESIAN_POINT('Ctrl Pts',(97.9101529558824,0.712396988494417,-0.498333718474245));
#39566=CARTESIAN_POINT('Ctrl Pts',(97.8492171766492,-0.824932913389202,
-0.577333554321806));
#39567=CARTESIAN_POINT('Ctrl Pts',(96.5283828065708,-1.61382142541515,-0.656333390169371));
#39568=CARTESIAN_POINT('Ctrl Pts',(95.1459606591299,-0.938666845162889,
-0.735333226016932));
#39569=CARTESIAN_POINT('Ctrl Pts',(94.9560748629476,0.588068102811137,-0.814333061864496));
#39570=CARTESIAN_POINT('Ctrl Pts',(96.1310015277402,1.58129570641339,-0.893332897712057));
#39571=CARTESIAN_POINT('Ctrl Pts',(97.6048327567796,1.13996316657112,-0.97233273355962));
#39572=CARTESIAN_POINT('Ctrl Pts',(98.0404999341466,-0.335554809072396,
-1.05133256940718));
#39573=CARTESIAN_POINT('Ctrl Pts',(97.0427610296164,-1.50665386027559,-1.13033240525474));
#39574=CARTESIAN_POINT('Ctrl Pts',(95.5167732958396,-1.31090519238855,-1.20933224110231));
#39575=CARTESIAN_POINT('Ctrl Pts',(94.8469244372853,0.0741072085732126,
-1.28833207694987));
#39576=CARTESIAN_POINT('Ctrl Pts',(95.6409067748658,1.39188884073063,-1.36733191279743));
#39577=CARTESIAN_POINT('Ctrl Pts',(97.178413207992,1.44693805333341,-1.44633174864499));
#39578=CARTESIAN_POINT('Ctrl Pts',(98.0646058751086,0.18931367074896,-1.52533158449256));
#39579=CARTESIAN_POINT('Ctrl Pts',(97.4955238075608,-1.24005754351337,-1.60433142034012));
#39580=CARTESIAN_POINT('Ctrl Pts',(95.9874427368982,-1.54443882685847,-1.68333125618768));
#39581=CARTESIAN_POINT('Ctrl Pts',(94.9085056446709,-0.447693076396299,
-1.76233109203524));
#39582=CARTESIAN_POINT('Ctrl Pts',(95.2375327350021,1.05520334570443,-1.84133092788281));
#39583=CARTESIAN_POINT('Ctrl Pts',(96.676028046713,1.60081100906409,-1.92033076373037));
#39584=CARTESIAN_POINT('Ctrl Pts',(97.918977339861,0.694150356097816,-1.99933059957793));
#39585=CARTESIAN_POINT('Ctrl Pts',(97.83876725662,-0.842248949561958,-2.07833043542549));
#39586=CARTESIAN_POINT('Ctrl Pts',(96.5081650144597,-1.61455339563897,-2.15733027127306));
#39587=CARTESIAN_POINT('Ctrl Pts',(95.1343034142239,-0.922122324891032,
-2.23633010712062));
#39588=CARTESIAN_POINT('Ctrl Pts',(94.9635604862002,0.606865358751896,-2.31532994296818));
#39589=CARTESIAN_POINT('Ctrl Pts',(96.1508355552055,1.5853000243166,-2.39432977881574));
#39590=CARTESIAN_POINT('Ctrl Pts',(97.6190233570862,1.12553806126023,-2.47332961466331));
#39591=CARTESIAN_POINT('Ctrl Pts',(98.0361723908918,-0.355320867821741,
-2.55232945051087));
#39592=CARTESIAN_POINT('Ctrl Pts',(97.0238417780262,-1.51382991591343,-2.63132928635843));
#39593=CARTESIAN_POINT('Ctrl Pts',(95.5004257985166,-1.2989805788641,-2.71032912220599));
#39594=CARTESIAN_POINT('Ctrl Pts',(94.8479793896609,0.0943141379221071,
-2.78932895805356));
#39595=CARTESIAN_POINT('Ctrl Pts',(95.6584070560774,1.40204632830397,-2.86832879390112));
#39596=CARTESIAN_POINT('Ctrl Pts',(97.1964824559416,1.43783108186362,-2.94732862974868));
#39597=CARTESIAN_POINT('Ctrl Pts',(98.0668515107163,0.16920418921777,-3.02632846559624));
#39598=CARTESIAN_POINT('Ctrl Pts',(97.4799085804449,-1.25292607234706,-3.10532830144381));
#39599=CARTESIAN_POINT('Ctrl Pts',(95.9681328996918,-1.53839196407101,-3.18432813729137));
#39600=CARTESIAN_POINT('Ctrl Pts',(94.9030192353312,-0.428216587724458,
-3.26332797313893));
#39601=CARTESIAN_POINT('Ctrl Pts',(95.2508470661204,1.07044023903157,-3.34232780898649));
#39602=CARTESIAN_POINT('Ctrl Pts',(96.6960642530924,1.59798527666832,-3.42132764483406));
#39603=CARTESIAN_POINT('Ctrl Pts',(97.9275584174969,0.675825525165635,-3.50032748068162));
#39604=CARTESIAN_POINT('Ctrl Pts',(97.8281083846458,-0.859448448827256,
-3.57932731652918));
#39605=CARTESIAN_POINT('Ctrl Pts',(96.4879360051457,-1.61502404231877,-3.65832715237675));
#39606=CARTESIAN_POINT('Ctrl Pts',(95.1228561836784,-0.905437144697542,
-3.7373269882243));
#39607=CARTESIAN_POINT('Ctrl Pts',(94.9712800518301,0.625569439386297,-3.81632682407187));
#39608=CARTESIAN_POINT('Ctrl Pts',(96.1707186664732,1.58905451657091,-3.89532665991943));
#39609=CARTESIAN_POINT('Ctrl Pts',(97.6330318993376,1.11093686029388,-3.97432649576699));
#39610=CARTESIAN_POINT('Ctrl Pts',(98.0315977046149,-0.375031437859765,
-4.05332633161456));
#39611=CARTESIAN_POINT('Ctrl Pts',(97.0048340545268,-1.5207682711299,-4.13232616746212));
#39612=CARTESIAN_POINT('Ctrl Pts',(95.4842289937883,-1.28685218893334,-4.21132600330968));
#39613=CARTESIAN_POINT('Ctrl Pts',(94.8492873721174,0.114506302432829,-4.29032583915724));
#39614=CARTESIAN_POINT('Ctrl Pts',(95.6760332137652,1.41198377721691,-4.36932567500481));
#39615=CARTESIAN_POINT('Ctrl Pts',(97.2144362002192,1.42849848350396,-4.44832551085237));
#39616=CARTESIAN_POINT('Ctrl Pts',(98.0688450638164,0.149068150089657,-4.52732534669993));
#39617=CARTESIAN_POINT('Ctrl Pts',(97.464133375343,-1.26559797945395,-4.60632518254749));
#39618=CARTESIAN_POINT('Ctrl Pts',(95.9489003263115,-1.53210368553927,-4.68532501839506));
#39619=CARTESIAN_POINT('Ctrl Pts',(94.8977772352419,-0.408672899208807,
-4.76432485424261));
#39620=CARTESIAN_POINT('Ctrl Pts',(95.2643512229599,1.0855091498678,-4.84332469009019));
#39621=CARTESIAN_POINT('Ctrl Pts',(96.7160634897512,1.59490877560504,-4.92232452593774));
#39622=CARTESIAN_POINT('Ctrl Pts',(97.93590926946,0.657394638121783,-5.00132436178531));
#39623=CARTESIAN_POINT('Ctrl Pts',(97.8172348934474,-0.876513076420429,
-5.08032419763286));
#39624=CARTESIAN_POINT('Ctrl Pts',(96.4677026873718,-1.61524124633046,-5.15932403348044));
#39625=CARTESIAN_POINT('Ctrl Pts',(95.1116188640692,-0.888609875943022,
-5.23832386932799));
#39626=CARTESIAN_POINT('Ctrl Pts',(94.9792333149623,0.644175350578207,-5.31732370517556));
#39627=CARTESIAN_POINT('Ctrl Pts',(96.1906472495902,1.59255964148767,-5.39632354102312));
#39628=CARTESIAN_POINT('Ctrl Pts',(97.6468564353717,1.09616132209147,-5.47532337687068));
#39629=CARTESIAN_POINT('Ctrl Pts',(98.0267764659365,-0.394683154918008,
-5.55432321271824));
#39630=CARTESIAN_POINT('Ctrl Pts',(96.9857409067177,-1.52746797503865,-5.6333230485658));
#39631=CARTESIAN_POINT('Ctrl Pts',(95.4681853904451,-1.27452185570567,-5.71232288441337));
#39632=CARTESIAN_POINT('Ctrl Pts',(94.8508481961557,0.134680497684516,-5.79132272026093));
#39633=CARTESIAN_POINT('Ctrl Pts',(95.6937824733625,1.42169964616808,-5.8703225561085));
#39634=CARTESIAN_POINT('Ctrl Pts',(97.2322716277157,1.41894171356061,-5.94932239195605));
#39635=CARTESIAN_POINT('Ctrl Pts',(98.070586219357,0.128908717976762,-6.02832222780363));
#39636=CARTESIAN_POINT('Ctrl Pts',(97.4482006689514,-1.27807127864728,-6.10732206365118));
#39637=CARTESIAN_POINT('Ctrl Pts',(95.9297480343168,-1.52557497685415,-6.18632189949874));
#39638=CARTESIAN_POINT('Ctrl Pts',(94.8927804673116,-0.389065078422743,
-6.26532173534631));
#39639=CARTESIAN_POINT('Ctrl Pts',(95.2780430861903,1.10040771379221,-6.34432157119387));
#39640=CARTESIAN_POINT('Ctrl Pts',(96.7360226183224,1.59158198850359,-6.42332140704143));
#39641=CARTESIAN_POINT('Ctrl Pts',(97.9440285852282,0.638860587372241,-6.50232124288899));
#39642=CARTESIAN_POINT('Ctrl Pts',(97.8061484894015,-0.893440154463006,
-6.58132107873655));
#39643=CARTESIAN_POINT('Ctrl Pts',(96.4474682363038,-1.61520497356751,-6.66032091458412));
#39644=CARTESIAN_POINT('Ctrl Pts',(95.1005932188536,-0.871643159309884,
-6.73932075043168));
#39645=CARTESIAN_POINT('Ctrl Pts',(94.9874190275034,0.6626801725424,-6.81832058627924));
#39646=CARTESIAN_POINT('Ctrl Pts',(96.2106181772027,1.59581484901143,-6.89732042212681));
#39647=CARTESIAN_POINT('Ctrl Pts',(97.6604947957295,1.08121376535188,-6.97632025797437));
#39648=CARTESIAN_POINT('Ctrl Pts',(98.0217094314449,-0.414272935090146,
-7.05532009382193));
#39649=CARTESIAN_POINT('Ctrl Pts',(96.9665653308501,-1.53392797626733,-7.1343199296695));
#39650=CARTESIAN_POINT('Ctrl Pts',(95.4522975061803,-1.2619915141573,-7.21331976551705));
#39651=CARTESIAN_POINT('Ctrl Pts',(94.8526616168382,0.154833557778703,-7.29231960136462));
#39652=CARTESIAN_POINT('Ctrl Pts',(95.7116520495115,1.43119241046437,-7.37131943721218));
#39653=CARTESIAN_POINT('Ctrl Pts',(97.2499859395508,1.40916227175958,-7.45031927305975));
#39654=CARTESIAN_POINT('Ctrl Pts',(98.0720747041024,0.108729056460906,-7.5293191089073));
#39655=CARTESIAN_POINT('Ctrl Pts',(97.4321129615595,-1.29034401251561,-7.60831894475487));
#39656=CARTESIAN_POINT('Ctrl Pts',(95.9106790292421,-1.51880686255369,-7.68731878060243));
#39657=CARTESIAN_POINT('Ctrl Pts',(94.8880297156727,-0.369396202384675,
-7.76631861644999));
#39658=CARTESIAN_POINT('Ctrl Pts',(95.2919205071734,1.11513359280096,-7.84531845229756));
#39659=CARTESIAN_POINT('Ctrl Pts',(96.7559385066569,1.58800543743075,-7.92431828814511));
#39660=CARTESIAN_POINT('Ctrl Pts',(97.9519150906526,0.620226281430028,-8.00331812399269));
#39661=CARTESIAN_POINT('Ctrl Pts',(97.7948509122765,-0.910227026618923,
-8.08231795984023));
#39662=CARTESIAN_POINT('Ctrl Pts',(96.427235827296,-1.61491522972511,-8.16131779568782));
#39663=CARTESIAN_POINT('Ctrl Pts',(95.0897809782665,-0.854539657347264,
-8.24031763153535));
#39664=CARTESIAN_POINT('Ctrl Pts',(94.9958359048817,0.681081001340498,-8.31931746738295));
#39665=CARTESIAN_POINT('Ctrl Pts',(96.2306283153171,1.59881962833109,-8.39831730323048));
#39666=CARTESIAN_POINT('Ctrl Pts',(97.6739448401565,1.06609653572288,-8.47731713907807));
#39667=CARTESIAN_POINT('Ctrl Pts',(98.0163973963242,-0.433797704101884,
-8.55631697492561));
#39668=CARTESIAN_POINT('Ctrl Pts',(96.9473103360644,-1.54014726123087,-8.63531681077318));
#39669=CARTESIAN_POINT('Ctrl Pts',(95.4365678343412,-1.24926313031556,-8.71431664662074));
#39670=CARTESIAN_POINT('Ctrl Pts',(94.8547273494079,0.174962319473753,-8.7933164824683));
#39671=CARTESIAN_POINT('Ctrl Pts',(95.7296391383274,1.44046058172089,-8.87231631831587));
#39672=CARTESIAN_POINT('Ctrl Pts',(97.2675763551547,1.39916169022134,-8.95131615416344));
#39673=CARTESIAN_POINT('Ctrl Pts',(98.0733102858353,0.088532337308607,-9.03031599001099));
#39674=CARTESIAN_POINT('Ctrl Pts',(97.4158727750917,-1.30241426496977,-9.10931582585856));
#39675=CARTESIAN_POINT('Ctrl Pts',(95.8916963088359,-1.51180038538851,-9.18831566170613));
#39676=CARTESIAN_POINT('Ctrl Pts',(94.8835257154617,-0.349669395741739,
-9.26731549755368));
#39677=CARTESIAN_POINT('Ctrl Pts',(95.3059813285748,1.12968455077475,-9.34631533340124));
#39678=CARTESIAN_POINT('Ctrl Pts',(96.775807989249,1.58417953665158,-9.42531516924881));
#39679=CARTESIAN_POINT('Ctrl Pts',(97.959567627023,0.601494933475199,-9.50431500509637));
#39680=CARTESIAN_POINT('Ctrl Pts',(97.7833437798875,-0.926871626477916,
-9.58331484094394));
#39681=CARTESIAN_POINT('Ctrl Pts',(96.4070089402296,-1.61437094397529,-9.66231467679148));
#39682=CARTESIAN_POINT('Ctrl Pts',(95.0791832398496,-0.837304248247735,
-9.74131451263906));
#39683=CARTESIAN_POINT('Ctrl Pts',(95.004483804035,0.699379262188282,-9.8203143484866));
#39684=CARTESIAN_POINT('Ctrl Pts',(96.2506722087523,1.6015650307077,-9.89931418433419));
#39685=CARTESIAN_POINT('Ctrl Pts',(97.6872090083356,1.05082866816156,-9.97831402018174));
#39686=CARTESIAN_POINT('Ctrl Pts',(98.0108322500603,-0.453287149796495,
-10.0573138560293));
#39687=CARTESIAN_POINT('Ctrl Pts',(96.9279965243397,-1.54606047688962,-10.1363136918769));
#39688=CARTESIAN_POINT('Ctrl Pts',(95.4209642885513,-1.23646524762692,-10.2153135277244));
#39689=CARTESIAN_POINT('Ctrl Pts',(94.85711298145,0.195312446641386,-10.294313363572));
#39690=CARTESIAN_POINT('Ctrl Pts',(95.747607526695,1.44901265609136,-10.3733131994195));
#39691=CARTESIAN_POINT('Ctrl Pts',(97.2853012271431,1.38991565181107,-10.4523130352671));
#39692=CARTESIAN_POINT('Ctrl Pts',(98.0738532170406,0.0661813918578819,
-10.5313190820979));
#39693=CARTESIAN_POINT('Ctrl Pts',(97.6246715686008,-0.850655682570031,
-10.583991850313));
#39694=CARTESIAN_POINT('Ctrl Pts',(97.2559581572523,-1.11394639328732,-10.6103313399122));
#39695=CARTESIAN_POINT('Ctrl Pts',(97.0952958617901,1.3207209276019,-0.00107659240832891));
#39696=CARTESIAN_POINT('Ctrl Pts',(97.5323405615611,1.1106519516964,-0.027409871024183));
#39697=CARTESIAN_POINT('Ctrl Pts',(98.1741742088046,0.226218253432855,-0.0800764282558911));
#39698=CARTESIAN_POINT('Ctrl Pts',(97.5855259575219,-1.31451810031743,-0.159076264103454));
#39699=CARTESIAN_POINT('Ctrl Pts',(95.9745983487262,-1.65909508611393,-0.238076099951017));
#39700=CARTESIAN_POINT('Ctrl Pts',(94.8052907688116,-0.500295431264796,
-0.317075935798579));
#39701=CARTESIAN_POINT('Ctrl Pts',(95.1371662312978,1.11326880122442,-0.396075771646142));
#39702=CARTESIAN_POINT('Ctrl Pts',(96.6697760590574,1.71641328822836,-0.475075607493704));
#39703=CARTESIAN_POINT('Ctrl Pts',(98.012403428816,0.762644857442132,-0.554075443341267));
#39704=CARTESIAN_POINT('Ctrl Pts',(97.9471696344331,-0.883118337516605,
-0.633075279188829));
#39705=CARTESIAN_POINT('Ctrl Pts',(96.5331721637222,-1.72764993507891,-0.712075115036392));
#39706=CARTESIAN_POINT('Ctrl Pts',(95.0532429127743,-1.00487432411502,-0.791074950883953));
#39707=CARTESIAN_POINT('Ctrl Pts',(94.8499638025334,0.629546617515179,-0.870074786731518));
#39708=CARTESIAN_POINT('Ctrl Pts',(96.1077621835587,1.69283006254727,-0.949074622579079));
#39709=CARTESIAN_POINT('Ctrl Pts',(97.6855479206097,1.22036878411891,-1.02807445842664));
#39710=CARTESIAN_POINT('Ctrl Pts',(98.1519442385918,-0.359222671715493,
-1.1070742942742));
#39711=CARTESIAN_POINT('Ctrl Pts',(97.0838312946866,-1.61292346408271,-1.18607413012177));
#39712=CARTESIAN_POINT('Ctrl Pts',(95.4502102709029,-1.40336795314393,-1.26507396596933));
#39713=CARTESIAN_POINT('Ctrl Pts',(94.7331146128772,0.0793342510293227,
-1.34407380181689));
#39714=CARTESIAN_POINT('Ctrl Pts',(95.5830993214529,1.49006366346062,-1.42307363766445));
#39715=CARTESIAN_POINT('Ctrl Pts',(97.2290514990247,1.54899569093378,-1.50207347351202));
#39716=CARTESIAN_POINT('Ctrl Pts',(98.1777504564805,0.202666630785906,-1.58107330935958));
#39717=CARTESIAN_POINT('Ctrl Pts',(97.5685290261725,-1.32752317003962,-1.66007314520714));
#39718=CARTESIAN_POINT('Ctrl Pts',(95.9540776855269,-1.65337353745256,-1.7390729810547));
#39719=CARTESIAN_POINT('Ctrl Pts',(94.7990393597335,-0.479270446029912,
-1.81807281690227));
#39720=CARTESIAN_POINT('Ctrl Pts',(95.1512738897119,1.12963055452827,-1.89707265274983));
#39721=CARTESIAN_POINT('Ctrl Pts',(96.6912313427176,1.71372184823468,-1.97607248859739));
#39722=CARTESIAN_POINT('Ctrl Pts',(98.0218502276797,0.743111225790608,-2.05507232444495));
#39723=CARTESIAN_POINT('Ctrl Pts',(97.9359826447353,-0.90165573471468,-2.13407216029252));
#39724=CARTESIAN_POINT('Ctrl Pts',(96.5115283395184,-1.7284335337409,-2.21307199614008));
#39725=CARTESIAN_POINT('Ctrl Pts',(95.0407634413237,-0.987162860551926,
-2.29207183198764));
#39726=CARTESIAN_POINT('Ctrl Pts',(94.8579774131613,0.649669710128945,-2.37107166783521));
#39727=CARTESIAN_POINT('Ctrl Pts',(96.1289951748448,1.69711681909701,-2.45007150368276));
#39728=CARTESIAN_POINT('Ctrl Pts',(97.7007394339408,1.20492622531942,-2.52907133953033));
#39729=CARTESIAN_POINT('Ctrl Pts',(98.147311458468,-0.38038290021245,-2.60807117537789));
#39730=CARTESIAN_POINT('Ctrl Pts',(97.0635776016403,-1.62060567220166,-2.68707101122545));
#39731=CARTESIAN_POINT('Ctrl Pts',(95.4327097270115,-1.39060225462431,-2.76607084707302));
#39732=CARTESIAN_POINT('Ctrl Pts',(94.7342439747597,0.100966446282139,-2.84507068292058));
#39733=CARTESIAN_POINT('Ctrl Pts',(95.6018339591418,1.50093759441126,-2.92407051876814));
#39734=CARTESIAN_POINT('Ctrl Pts',(97.248395234679,1.5392463726878,-3.0030703546157));
#39735=CARTESIAN_POINT('Ctrl Pts',(98.1801544846778,0.181138756688628,-3.08207019046326));
#39736=CARTESIAN_POINT('Ctrl Pts',(97.5518124020847,-1.34129936154011,-3.16107002631083));
#39737=CARTESIAN_POINT('Ctrl Pts',(95.9334058574854,-1.64690016813321,-3.24006986215839));
#39738=CARTESIAN_POINT('Ctrl Pts',(94.7931659746178,-0.458420212008008,
-3.31906969800596));
#39739=CARTESIAN_POINT('Ctrl Pts',(95.1655273275025,1.14594215961223,-3.39806953385351));
#39740=CARTESIAN_POINT('Ctrl Pts',(96.7126807733086,1.71069680697967,-3.47706936970108));
#39741=CARTESIAN_POINT('Ctrl Pts',(98.0310365589472,0.723493879985343,-3.55606920554864));
#39742=CARTESIAN_POINT('Ctrl Pts',(97.9245719649759,-0.920068375246725,
-3.63506904139621));
#39743=CARTESIAN_POINT('Ctrl Pts',(96.4898725069229,-1.72893737678884,-3.71406887724376));
#39744=CARTESIAN_POINT('Ctrl Pts',(95.028508797286,-0.969300815827463,-3.79306871309133));
#39745=CARTESIAN_POINT('Ctrl Pts',(94.8662414669465,0.6696930554538,-3.87206854893889));
#39746=CARTESIAN_POINT('Ctrl Pts',(96.1502807119863,1.70113612891485,-3.95106838478645));
#39747=CARTESIAN_POINT('Ctrl Pts',(97.715736048021,1.18929515021761,-4.03006822063402));
#39748=CARTESIAN_POINT('Ctrl Pts',(98.1424141034539,-0.401483726183824,
-4.10906805648158));
#39749=CARTESIAN_POINT('Ctrl Pts',(97.0432291964499,-1.62803341405123,-4.18806789232914));
#39750=CARTESIAN_POINT('Ctrl Pts',(95.4153705045938,-1.37761840663066,-4.26706772817671));
#39751=CARTESIAN_POINT('Ctrl Pts',(94.7356442138263,0.122582835280742,-4.34606756402426));
#39752=CARTESIAN_POINT('Ctrl Pts',(95.6207033518175,1.51157596659972,-4.42506739987183));
#39753=CARTESIAN_POINT('Ctrl Pts',(97.2676153197811,1.52925551329267,-4.50406723571939));
#39754=CARTESIAN_POINT('Ctrl Pts',(98.1822886501,0.159582451793565,-4.58306707156695));
#39755=CARTESIAN_POINT('Ctrl Pts',(97.5349245162006,-1.35486506289079,-4.66206690741451));
#39756=CARTESIAN_POINT('Ctrl Pts',(95.9128167429594,-1.64016835516679,-4.74106674326208));
#39757=CARTESIAN_POINT('Ctrl Pts',(94.7875542377978,-0.437498038300601,
-4.82006657910964));
#39758=CARTESIAN_POINT('Ctrl Pts',(95.1799839800908,1.16207393380852,-4.8990664149572));
#39759=CARTESIAN_POINT('Ctrl Pts',(96.7340906265743,1.70740330945973,-4.97806625080476));
#39760=CARTESIAN_POINT('Ctrl Pts',(98.0399764259145,0.703762997557278,-5.05706608665234));
#39761=CARTESIAN_POINT('Ctrl Pts',(97.9129315281424,-0.938336631132538,
-5.13606592249989));
#39762=CARTESIAN_POINT('Ctrl Pts',(96.4682120619765,-1.72916990096455,-5.21506575834745));
#39763=CARTESIAN_POINT('Ctrl Pts',(95.0164788699425,-0.951286660535266,
-5.29406559419502));
#39764=CARTESIAN_POINT('Ctrl Pts',(94.8747557017422,0.689611307099592,-5.37306543004258));
#39765=CARTESIAN_POINT('Ctrl Pts',(96.171614928267,1.70488848263846,-5.45206526589014));
#39766=CARTESIAN_POINT('Ctrl Pts',(97.7305356772772,1.17347744126039,-5.5310651017377));
#39767=CARTESIAN_POINT('Ctrl Pts',(98.1372528058293,-0.422521548067451,
-5.61006493758527));
#39768=CARTESIAN_POINT('Ctrl Pts',(97.0227893416717,-1.6352056716757,-5.68906477343282));
#39769=CARTESIAN_POINT('Ctrl Pts',(95.3981952893951,-1.36441837156804,-5.76806460928039));
#39770=CARTESIAN_POINT('Ctrl Pts',(94.7373151282815,0.144179987585173,-5.84706444512795));
#39771=CARTESIAN_POINT('Ctrl Pts',(95.6397045292144,1.52197713001124,-5.92606428097553));
#39772=CARTESIAN_POINT('Ctrl Pts',(97.2867087428023,1.51902467070241,-6.00506411682307));
#39773=CARTESIAN_POINT('Ctrl Pts',(98.1841526154742,0.138001103924106,-6.08406395267065));
#39774=CARTESIAN_POINT('Ctrl Pts',(97.5178680199056,-1.36821814781222,-6.1630637885182));
#39775=CARTESIAN_POINT('Ctrl Pts',(95.8923135723485,-1.63317915366136,-6.24206362436576));
#39776=CARTESIAN_POINT('Ctrl Pts',(94.7822050302246,-0.416507208847854,
-6.32106346021333));
#39777=CARTESIAN_POINT('Ctrl Pts',(95.1946415786631,1.17802334592527,-6.40006329606089));
#39778=CARTESIAN_POINT('Ctrl Pts',(96.7554575427877,1.70384187234572,-6.47906313190846));
#39779=CARTESIAN_POINT('Ctrl Pts',(98.0486684256232,0.683921674923979,-6.55806296775601));
#39780=CARTESIAN_POINT('Ctrl Pts',(97.9010631609685,-0.956457635613447,
-6.63706280360359));
#39781=CARTESIAN_POINT('Ctrl Pts',(96.4465504038007,-1.72913106975587,-6.71606263945113));
#39782=CARTESIAN_POINT('Ctrl Pts',(95.0046755471332,-0.933123221614384,
-6.79506247529871));
#39783=CARTESIAN_POINT('Ctrl Pts',(94.883518781422,0.709421339338357,-6.87406231114626));
#39784=CARTESIAN_POINT('Ctrl Pts',(96.1929944757499,1.70837329141502,-6.95306214699383));
#39785=CARTESIAN_POINT('Ctrl Pts',(97.7451359992307,1.15747558069262,-7.03206198284139));
#39786=CARTESIAN_POINT('Ctrl Pts',(98.1318283755469,-0.443493064438228,
-7.11106181868895));
#39787=CARTESIAN_POINT('Ctrl Pts',(97.0022612448941,-1.64212131954578,-7.19006165453652));
#39788=CARTESIAN_POINT('Ctrl Pts',(95.3811867766894,-1.35100422089335,-7.26906149038407));
#39789=CARTESIAN_POINT('Ctrl Pts',(94.7392564559124,0.165754513994999,-7.34806132623165));
#39790=CARTESIAN_POINT('Ctrl Pts',(95.658834509513,1.53213945241069,-7.4270611620792));
#39791=CARTESIAN_POINT('Ctrl Pts',(97.3056725074482,1.50855545042403,-7.50606099792676));
#39792=CARTESIAN_POINT('Ctrl Pts',(98.1857460882916,0.116398099800639,-7.58506083377433));
#39793=CARTESIAN_POINT('Ctrl Pts',(97.500645589844,-1.3813565208298,-7.66406066962188));
#39794=CARTESIAN_POINT('Ctrl Pts',(95.871899563177,-1.62593366041925,-7.74306050546945));
#39795=CARTESIAN_POINT('Ctrl Pts',(94.7771191913385,-0.395451017701117,
-7.82206034131702));
#39796=CARTESIAN_POINT('Ctrl Pts',(95.2094978230301,1.19378789305098,-7.90106017716457));
#39797=CARTESIAN_POINT('Ctrl Pts',(96.7767781688782,1.70001305452767,-7.98006001301215));
#39798=CARTESIAN_POINT('Ctrl Pts',(98.0571111940546,0.663973025746128,-8.05905984885969));
#39799=CARTESIAN_POINT('Ctrl Pts',(97.8889687259342,-0.974428544992647,
-8.13805968470727));
#39800=CARTESIAN_POINT('Ctrl Pts',(96.4248909317188,-1.72882088925967,-8.21705952055483));
#39801=CARTESIAN_POINT('Ctrl Pts',(94.9931006811322,-0.914813349412916,
-8.29605935640239));
#39802=CARTESIAN_POINT('Ctrl Pts',(94.8925293308096,0.729120043406717,-8.37505919224995));
#39803=CARTESIAN_POINT('Ctrl Pts',(96.2144159993889,1.71159000840414,-8.45405902809752));
#39804=CARTESIAN_POINT('Ctrl Pts',(97.7595347226678,1.14129207960892,-8.53305886394508));
#39805=CARTESIAN_POINT('Ctrl Pts',(98.1261416638778,-0.464394984182465,
-8.61205869979263));
#39806=CARTESIAN_POINT('Ctrl Pts',(96.9816481275025,-1.64877927258462,-8.69105853564022));
#39807=CARTESIAN_POINT('Ctrl Pts',(95.3643476356891,-1.33737805930476,-8.77005837148776));
#39808=CARTESIAN_POINT('Ctrl Pts',(94.741467891877,0.187303028154009,-8.84905820733534));
#39809=CARTESIAN_POINT('Ctrl Pts',(95.6780902910606,1.54206134043216,-8.92805804318289));
#39810=CARTESIAN_POINT('Ctrl Pts',(97.3245036370254,1.49784949264381,-9.00705787903045));
#39811=CARTESIAN_POINT('Ctrl Pts',(98.187068819956,0.0947768349055472,-9.08605771487802));
#39812=CARTESIAN_POINT('Ctrl Pts',(97.4832599258204,-1.39427813070584,-9.16505755072557));
#39813=CARTESIAN_POINT('Ctrl Pts',(95.8515779246356,-1.61843299173998,-9.24405738657315));
#39814=CARTESIAN_POINT('Ctrl Pts',(94.7722975081282,-0.374332809899895,
-9.32305722242069));
#39815=CARTESIAN_POINT('Ctrl Pts',(95.2245504036924,1.209365181345,-9.40205705826827));
#39816=CARTESIAN_POINT('Ctrl Pts',(96.7980491160662,1.69591729949016,-9.48105689411583));
#39817=CARTESIAN_POINT('Ctrl Pts',(98.0653034907704,0.643920489840692,-9.56005672996339));
#39818=CARTESIAN_POINT('Ctrl Pts',(97.8766499549651,-0.992247147108681,
-9.63905656581095));
#39819=CARTESIAN_POINT('Ctrl Pts',(96.4032373710603,-1.72823821311873,-9.71805640165851));
#39820=CARTESIAN_POINT('Ctrl Pts',(94.9817554468956,-0.896362266199541,
-9.79705623750608));
#39821=CARTESIAN_POINT('Ctrl Pts',(94.9017871967514,0.748708945045941,-9.87605607335364));
#39822=CARTESIAN_POINT('Ctrl Pts',(96.2358736592311,1.71452905368079,-9.9550559092012));
#39823=CARTESIAN_POINT('Ctrl Pts',(97.7737344593502,1.12494731556893,-10.0340557450487));
#39824=CARTESIAN_POINT('Ctrl Pts',(98.1201839882452,-0.485259089131598,
-10.1130555808963));
#39825=CARTESIAN_POINT('Ctrl Pts',(96.9609720446059,-1.65510956817251,-10.1920554167438));
#39826=CARTESIAN_POINT('Ctrl Pts',(95.3476435168528,-1.32367749687079,-10.2710552525914));
#39827=CARTESIAN_POINT('Ctrl Pts',(94.74402179095,0.209088521472124,-10.350055088439));
#39828=CARTESIAN_POINT('Ctrl Pts',(95.6973260531519,1.55121662273183,-10.4290549242865));
#39829=CARTESIAN_POINT('Ctrl Pts',(97.343478706669,1.48795129857621,-10.5080547601341));
#39830=CARTESIAN_POINT('Ctrl Pts',(98.187650046012,0.0708493985431469,-10.587060806965));
#39831=CARTESIAN_POINT('Ctrl Pts',(97.706786033709,-0.910655424213715,-10.6397335751801));
#39832=CARTESIAN_POINT('Ctrl Pts',(97.3120659667008,-1.19251695617385,-10.6660730647792));
#39833=CARTESIAN_POINT('Ctrl Pts',(97.0960530345221,1.32073705981523,-10.5));
#39834=CARTESIAN_POINT('Ctrl Pts',(97.1327523794304,1.29890511060011,-10.5));
#39835=CARTESIAN_POINT('Ctrl Pts',(97.1683327868718,1.27542981429671,-10.5));
#39836=CARTESIAN_POINT('Ctrl Pts',(97.2026700353434,1.25031220514833,-10.5));
#39837=CARTESIAN_POINT('Ctrl Pts',(97.2492821414819,1.2162155691137,-10.5));
#39838=CARTESIAN_POINT('Ctrl Pts',(97.2936053051564,1.17909352994033,-10.5));
#39839=CARTESIAN_POINT('Ctrl Pts',(97.3355049529323,1.1392708471789,-10.5));
#39840=CARTESIAN_POINT('Ctrl Pts',(97.3718456384346,1.10473156900102,-10.5));
#39841=CARTESIAN_POINT('Ctrl Pts',(97.406362784151,1.06815959411897,-10.5));
#39842=CARTESIAN_POINT('Ctrl Pts',(97.4389410516463,1.0297508894014,-10.5));
#39843=CARTESIAN_POINT('Ctrl Pts',(97.4537854365593,1.01224984834946,-10.5));
#39844=CARTESIAN_POINT('Ctrl Pts',(97.4682268999763,0.99436732143761,-10.5));
#39845=CARTESIAN_POINT('Ctrl Pts',(97.482252575178,0.976121347465687,-10.5));
#39846=CARTESIAN_POINT('Ctrl Pts',(97.4887615062686,0.967653891492528,-10.5));
#39847=CARTESIAN_POINT('Ctrl Pts',(97.4951808738737,0.959108159795724,-10.5));
#39848=CARTESIAN_POINT('Ctrl Pts',(97.5015092969713,0.950485946835754,-10.5));
#39849=CARTESIAN_POINT('Ctrl Pts',(97.5079891070103,0.941657475471821,-10.5));
#39850=CARTESIAN_POINT('Ctrl Pts',(97.514369012319,0.932754939898317,-10.5));
#39851=CARTESIAN_POINT('Ctrl Pts',(97.5206439889312,0.923786412192149,-10.5));
#39852=CARTESIAN_POINT('Ctrl Pts',(97.5532336246143,0.877207585110972,-10.5));
#39853=CARTESIAN_POINT('Ctrl Pts',(97.5830328074137,0.828801651694975,-10.5));
#39854=CARTESIAN_POINT('Ctrl Pts',(97.6099076639557,0.778871925525369,-10.5));
#39855=CARTESIAN_POINT('Ctrl Pts',(97.6363426534309,0.729759410869599,-10.5));
#39856=CARTESIAN_POINT('Ctrl Pts',(97.6599484872081,0.679171459866346,-10.5));
#39857=CARTESIAN_POINT('Ctrl Pts',(97.6805502395513,0.627383924127521,-10.5));
#39858=CARTESIAN_POINT('Ctrl Pts',(97.6987863703601,0.58154295583198,-10.5));
#39859=CARTESIAN_POINT('Ctrl Pts',(97.7146681957523,0.534761436162482,-10.5));
#39860=CARTESIAN_POINT('Ctrl Pts',(97.728040262327,0.487232253208875,-10.5));
#39861=CARTESIAN_POINT('Ctrl Pts',(97.7323205078086,0.472018705665731,-10.5));
#39862=CARTESIAN_POINT('Ctrl Pts',(97.7363446754649,0.456722195966646,-10.5));
#39863=CARTESIAN_POINT('Ctrl Pts',(97.7400979971882,0.441388713975437,-10.5));
#39864=CARTESIAN_POINT('Ctrl Pts',(97.7528828129849,0.389158780803246,-10.5));
#39865=CARTESIAN_POINT('Ctrl Pts',(97.7625536024157,0.336421827194652,-10.5));
#39866=CARTESIAN_POINT('Ctrl Pts',(97.7689618062189,0.283432905893329,-10.5));
#39867=CARTESIAN_POINT('Ctrl Pts',(97.7751646173992,0.232142359654773,-10.5));
#39868=CARTESIAN_POINT('Ctrl Pts',(97.7783106242714,0.180614917104041,-10.5));
#39869=CARTESIAN_POINT('Ctrl Pts',(97.7782188386079,0.129087102186097,-10.5));
#39870=CARTESIAN_POINT('Ctrl Pts',(97.7781750834699,0.104523280682375,-10.5));
#39871=CARTESIAN_POINT('Ctrl Pts',(97.7773948438647,0.0799595271486894,
-10.5));
#39872=CARTESIAN_POINT('Ctrl Pts',(97.7758546340163,0.0554226938714613,
-10.5));
#39873=CARTESIAN_POINT('Ctrl Pts',(97.7740586174852,0.0268106458234052,
-10.5));
#39874=CARTESIAN_POINT('Ctrl Pts',(97.7712292013864,-0.00176488002858206,
-10.5));
#39875=CARTESIAN_POINT('Ctrl Pts',(97.7673856184957,-0.0302588563087463,
-10.5));
#39876=CARTESIAN_POINT('Ctrl Pts',(97.7658297121615,-0.0417933956804935,
-10.5));
#39877=CARTESIAN_POINT('Ctrl Pts',(97.764107082079,-0.0533166512022675,
-10.5));
#39878=CARTESIAN_POINT('Ctrl Pts',(97.762222928785,-0.0648035136284369,
-10.5));
#39879=CARTESIAN_POINT('Ctrl Pts',(97.7537235936656,-0.1166202599317,-10.5));
#39880=CARTESIAN_POINT('Ctrl Pts',(97.7419297521137,-0.167796425585881,
-10.5));
#39881=CARTESIAN_POINT('Ctrl Pts',(97.7270294698183,-0.218079862035151,
-10.5));
#39882=CARTESIAN_POINT('Ctrl Pts',(97.7120073204257,-0.268774558910008,
-10.5));
#39883=CARTESIAN_POINT('Ctrl Pts',(97.6938269971693,-0.318562860100363,
-10.5));
#39884=CARTESIAN_POINT('Ctrl Pts',(97.6726356487453,-0.367160875033588,
-10.5));
#39885=CARTESIAN_POINT('Ctrl Pts',(97.6591336259524,-0.398124997381542,
-10.5));
#39886=CARTESIAN_POINT('Ctrl Pts',(97.644408373247,-0.428605353314649,-10.5));
#39887=CARTESIAN_POINT('Ctrl Pts',(97.6284904320524,-0.458520380816364,
-10.5));
#39888=CARTESIAN_POINT('Ctrl Pts',(97.6201510508066,-0.474192810828878,
-10.5));
#39889=CARTESIAN_POINT('Ctrl Pts',(97.6114842266502,-0.489709957087109,
-10.5));
#39890=CARTESIAN_POINT('Ctrl Pts',(97.6024938431448,-0.505059230819634,
-10.5));
#39891=CARTESIAN_POINT('Ctrl Pts',(97.5966859477238,-0.514975045486983,
-10.5));
#39892=CARTESIAN_POINT('Ctrl Pts',(97.5907474448757,-0.524813128712183,
-10.5));
#39893=CARTESIAN_POINT('Ctrl Pts',(97.5846829146721,-0.534565759424631,
-10.5));
#39894=CARTESIAN_POINT('Ctrl Pts',(97.557451153234,-0.578358321097343,-10.5));
#39895=CARTESIAN_POINT('Ctrl Pts',(97.5276624401207,-0.620462600956481,
-10.5));
#39896=CARTESIAN_POINT('Ctrl Pts',(97.4954500652803,-0.660602101447504,
-10.5));
#39897=CARTESIAN_POINT('Ctrl Pts',(97.4703422909784,-0.691888634151548,
-10.5));
#39898=CARTESIAN_POINT('Ctrl Pts',(97.4437612066321,-0.721980945035717,
-10.5));
#39899=CARTESIAN_POINT('Ctrl Pts',(97.4157584644867,-0.75072877166702,-10.5));
#39900=CARTESIAN_POINT('Ctrl Pts',(97.4049420135528,-0.761833021907868,
-10.5));
#39901=CARTESIAN_POINT('Ctrl Pts',(97.3939097361129,-0.772739659318788,
-10.5));
#39902=CARTESIAN_POINT('Ctrl Pts',(97.3826861942266,-0.783419204631785,
-10.5));
#39903=CARTESIAN_POINT('Ctrl Pts',(97.346908313003,-0.81746295905454,-10.5));
#39904=CARTESIAN_POINT('Ctrl Pts',(97.3091533165845,-0.849241353705008,
-10.5));
#39905=CARTESIAN_POINT('Ctrl Pts',(97.2695300366762,-0.878485320260425,
-10.5));
#39906=CARTESIAN_POINT('Ctrl Pts',(97.2299067567679,-0.907729286815843,
-10.5));
#39907=CARTESIAN_POINT('Ctrl Pts',(97.1884145438752,-0.93443952153388,-10.5));
#39908=CARTESIAN_POINT('Ctrl Pts',(97.1451453741165,-0.958295198918411,
-10.5));
#39909=CARTESIAN_POINT('',(97.1458324630994,-0.958883592186423,0.000494446711454889));
#39910=CARTESIAN_POINT('Ctrl Pts',(97.1466202729343,-0.959424520989747,
9.31828399164392E-15));
#39911=CARTESIAN_POINT('Ctrl Pts',(97.1772000435651,-0.942816385269717,
2.8509622347868E-15));
#39912=CARTESIAN_POINT('Ctrl Pts',(97.206909689724,-0.924824757093772,9.99012851391334E-15));
#39913=CARTESIAN_POINT('Ctrl Pts',(97.2356432203996,-0.905478322627354,
6.69603261727048E-15));
#39914=CARTESIAN_POINT('Ctrl Pts',(97.2754551973134,-0.8786727131449,1.91303236758859E-15));
#39915=CARTESIAN_POINT('Ctrl Pts',(97.3133946513639,-0.849268561702089,
2.31792913122294E-14));
#39916=CARTESIAN_POINT('Ctrl Pts',(97.3494001049585,-0.817569258176344,
2.5954932647565E-14));
#39917=CARTESIAN_POINT('Ctrl Pts',(97.3839689672423,-0.787134733717629,
2.87388746824356E-14));
#39918=CARTESIAN_POINT('Ctrl Pts',(97.4167554059431,-0.754583690540391,
5.09432319230377E-15));
#39919=CARTESIAN_POINT('Ctrl Pts',(97.447687563878,-0.720145741968749,1.92866556059101E-14));
#39920=CARTESIAN_POINT('Ctrl Pts',(97.4644376227941,-0.701497263943401,
2.70598459029195E-14));
#39921=CARTESIAN_POINT('Ctrl Pts',(97.4806436126852,-0.682294876652444,
1.24190508234713E-14));
#39922=CARTESIAN_POINT('Ctrl Pts',(97.4962913478694,-0.662571287839571,
1.84921522539128E-14));
#39923=CARTESIAN_POINT('Ctrl Pts',(97.5025355811585,-0.654700583971173,
2.10484807325984E-14));
#39924=CARTESIAN_POINT('Ctrl Pts',(97.5086857564786,-0.646753256969243,
2.79135666469497E-14));
#39925=CARTESIAN_POINT('Ctrl Pts',(97.5147378717323,-0.638736474398883,
2.78388423424758E-14));
#39926=CARTESIAN_POINT('Ctrl Pts',(97.5456685520257,-0.597764925068949,
2.75219226050856E-14));
#39927=CARTESIAN_POINT('Ctrl Pts',(97.574069340512,-0.554946070203035,1.1374087770192E-14));
#39928=CARTESIAN_POINT('Ctrl Pts',(97.5998669969729,-0.510609758068244,
9.35362898246694E-15));
#39929=CARTESIAN_POINT('Ctrl Pts',(97.6262338873721,-0.465295150342756,
7.24263366321213E-15));
#39930=CARTESIAN_POINT('Ctrl Pts',(97.6498822495387,-0.41839459509935,2.45765135840765E-14));
#39931=CARTESIAN_POINT('Ctrl Pts',(97.6707026342043,-0.370215921141815,
9.78384040450919E-15));
#39932=CARTESIAN_POINT('Ctrl Pts',(97.6902204920045,-0.325051313359365,
-4.4286697064792E-15));
#39933=CARTESIAN_POINT('Ctrl Pts',(97.7072533202619,-0.278762428188124,
2.28542419073914E-14));
#39934=CARTESIAN_POINT('Ctrl Pts',(97.7216779303715,-0.231578653933733,
1.02001740387436E-15));
#39935=CARTESIAN_POINT('Ctrl Pts',(97.7245628026305,-0.222142061860196,
-3.40706245095146E-15));
#39936=CARTESIAN_POINT('Ctrl Pts',(97.7273405894162,-0.212678180277356,
1.20348809539547E-14));
#39937=CARTESIAN_POINT('Ctrl Pts',(97.7300098441781,-0.203192277103622,
1.16434639707563E-14));
#39938=CARTESIAN_POINT('Ctrl Pts',(97.7447154730192,-0.150931933398112,
9.82772154440629E-15));
#39939=CARTESIAN_POINT('Ctrl Pts',(97.7561395027148,-0.09797517174401,4.93265201506828E-16));
#39940=CARTESIAN_POINT('Ctrl Pts',(97.7641794825515,-0.0446542022561014,
-2.91433543964104E-16));
#39941=CARTESIAN_POINT('Ctrl Pts',(97.7721731219472,0.00835943844565992,
-1.07340161594935E-15));
#39942=CARTESIAN_POINT('Ctrl Pts',(97.7768222245354,0.0617341894820306,
1.98200327771534E-14));
#39943=CARTESIAN_POINT('Ctrl Pts',(97.777982886155,0.115169799540912,2.12746487093796E-14));
#39944=CARTESIAN_POINT('Ctrl Pts',(97.7783979164878,0.134277348761075,2.1813788991162E-14));
#39945=CARTESIAN_POINT('Ctrl Pts',(97.7783664526014,0.153392845938293,9.27618377225713E-15));
#39946=CARTESIAN_POINT('Ctrl Pts',(97.7778803285128,0.172502974242189,1.77219350305791E-14));
#39947=CARTESIAN_POINT('Ctrl Pts',(97.7774094242059,0.191014794440757,2.59186172024163E-14));
#39948=CARTESIAN_POINT('Ctrl Pts',(97.7765118801322,0.209521582396939,1.00647601749991E-14));
#39949=CARTESIAN_POINT('Ctrl Pts',(97.7751951538298,0.228013923914682,1.25871535416877E-14));
#39950=CARTESIAN_POINT('Ctrl Pts',(97.7742947580553,0.24065924445855,1.426827868324E-14));
#39951=CARTESIAN_POINT('Ctrl Pts',(97.7731983350769,0.25329781108981,1.89882289688263E-14));
#39952=CARTESIAN_POINT('Ctrl Pts',(97.7719080551977,0.265926612846937,7.67441665772139E-15));
#39953=CARTESIAN_POINT('Ctrl Pts',(97.770904685478,0.275747239738408,-1.27219627523598E-15));
#39954=CARTESIAN_POINT('Ctrl Pts',(97.7697845744754,0.285556547529046,1.18323679014023E-14));
#39955=CARTESIAN_POINT('Ctrl Pts',(97.7685502311383,0.2953453042908,1.36418654150816E-14));
#39956=CARTESIAN_POINT('Ctrl Pts',(97.76175934138,0.349199338287771,2.41200680770917E-14));
#39957=CARTESIAN_POINT('Ctrl Pts',(97.7515083176503,0.402502016329768,3.80654692591887E-14));
#39958=CARTESIAN_POINT('Ctrl Pts',(97.7380513471759,0.455014629129198,2.81302758864399E-14));
#39959=CARTESIAN_POINT('Ctrl Pts',(97.7245943767015,0.507527241928628,1.81950825136911E-14));
#39960=CARTESIAN_POINT('Ctrl Pts',(97.7079310928974,0.559250673400171,1.81745979355416E-14));
#39961=CARTESIAN_POINT('Ctrl Pts',(97.6882615948245,0.609952423015609,8.90953977261688E-15));
#39962=CARTESIAN_POINT('Ctrl Pts',(97.6741507870948,0.646325625714142,2.17032712502928E-15));
#39963=CARTESIAN_POINT('Ctrl Pts',(97.6584916710932,0.682173182980464,3.58040368876852E-14));
#39964=CARTESIAN_POINT('Ctrl Pts',(97.6413425828207,0.71740732801415,2.72143418911241E-14));
#39965=CARTESIAN_POINT('Ctrl Pts',(97.6343564201633,0.731760946374833,2.37222638421511E-14));
#39966=CARTESIAN_POINT('Ctrl Pts',(97.6271228439595,0.746012728042026,7.49441688733765E-15));
#39967=CARTESIAN_POINT('Ctrl Pts',(97.6196452280311,0.760156545554777,1.99978922310606E-14));
#39968=CARTESIAN_POINT('Ctrl Pts',(97.6146240899864,0.769653965707259,2.81848743562857E-14));
#39969=CARTESIAN_POINT('Ctrl Pts',(97.6094929748939,0.779102355169158,3.56241109591605E-14));
#39970=CARTESIAN_POINT('Ctrl Pts',(97.6042599031689,0.788487808932253,3.17662562920873E-14));
#39971=CARTESIAN_POINT('Ctrl Pts',(97.5764823540215,0.838306522849914,1.14908850691008E-14));
#39972=CARTESIAN_POINT('Ctrl Pts',(97.5457904930518,0.88644061665542,2.43775865153609E-14));
#39973=CARTESIAN_POINT('Ctrl Pts',(97.5123991020691,0.93263343166495,2.61735078055381E-14));
#39974=CARTESIAN_POINT('Ctrl Pts',(97.4844179100545,0.971341912756621,2.76234915115376E-14));
#39975=CARTESIAN_POINT('Ctrl Pts',(97.4545399996545,1.00868751676431,1.11804510128399E-14));
#39976=CARTESIAN_POINT('Ctrl Pts',(97.4228654712748,1.04451118656265,2.90045765183322E-14));
#39977=CARTESIAN_POINT('Ctrl Pts',(97.4142291322117,1.0542788255675,3.37850636592315E-14));
#39978=CARTESIAN_POINT('Ctrl Pts',(97.4054591001408,1.06393325519369,3.00163047873623E-14));
#39979=CARTESIAN_POINT('Ctrl Pts',(97.396557125927,1.07347108761765,2.89213097914853E-14));
#39980=CARTESIAN_POINT('Ctrl Pts',(97.3879421590792,1.08270141205566,2.79854433512853E-14));
#39981=CARTESIAN_POINT('Ctrl Pts',(97.3792090872826,1.09181661488917,2.79116941233197E-14));
#39982=CARTESIAN_POINT('Ctrl Pts',(97.3703634096788,1.10081055725528,2.57571741713036E-14));
#39983=CARTESIAN_POINT('Ctrl Pts',(97.3290717691756,1.14279429796123,1.54378006085243E-14));
#39984=CARTESIAN_POINT('Ctrl Pts',(97.285307623798,1.18216180934031,1.40986011756825E-14));
#39985=CARTESIAN_POINT('Ctrl Pts',(97.2392696854532,1.21863191240908,1.55708779203678E-14));
#39986=CARTESIAN_POINT('Ctrl Pts',(97.1932317471084,1.25510201547784,1.69060522755085E-14));
#39987=CARTESIAN_POINT('Ctrl Pts',(97.1449194813229,1.28867583838664,2.09837577252251E-15));
#39988=CARTESIAN_POINT('Ctrl Pts',(97.0944880441522,1.31904027763685,1.16850973341798E-14));
#39989=CARTESIAN_POINT('Ctrl Pts',(97.1453218036553,-0.958169122381499,
0.000494446711454821));
#39990=CARTESIAN_POINT('Ctrl Pts',(97.1415381744624,-0.960873429781328,
0.00032963114095207));
#39991=CARTESIAN_POINT('Ctrl Pts',(97.1377385268835,-0.963555325660809,
0.000164815570449321));
#39992=CARTESIAN_POINT('Ctrl Pts',(97.1339231275304,-0.966214621837944,
-5.34294830600857E-14));
#39993=CARTESIAN_POINT('Ctrl Pts',(95.6089494686613,-1.19245765552795,0.166027734467303));
#39994=CARTESIAN_POINT('Ctrl Pts',(95.2142463808146,-0.910612241588899,
0.139688080028275));
#39995=CARTESIAN_POINT('Ctrl Pts',(94.7334030913231,0.0708416381760633,
0.0870151469733932));
#39996=CARTESIAN_POINT('Ctrl Pts',(95.5775313502033,1.48787114334542,0.00800893530265735));
#39997=CARTESIAN_POINT('Ctrl Pts',(97.2235943441107,1.55113222293223,-0.070990900544905));
#39998=CARTESIAN_POINT('Ctrl Pts',(98.1768471138565,0.209077371665153,-0.149990736392467));
#39999=CARTESIAN_POINT('Ctrl Pts',(97.5732580287732,-1.32360584827862,-0.228990572240029));
#40000=CARTESIAN_POINT('Ctrl Pts',(95.960016997387,-1.65501977806249,-0.307990408087592));
#40001=CARTESIAN_POINT('Ctrl Pts',(94.8008678817747,-0.485232819228974,
-0.386990243935154));
#40002=CARTESIAN_POINT('Ctrl Pts',(95.1472986348494,1.12488635124402,-0.465990079782718));
#40003=CARTESIAN_POINT('Ctrl Pts',(96.6850760631179,1.71443609477336,-0.544989915630279));
#40004=CARTESIAN_POINT('Ctrl Pts',(98.0190902033242,0.748668362857634,-0.623989751477842));
#40005=CARTESIAN_POINT('Ctrl Pts',(97.9391262882993,-0.89631367659507,-0.702989587325403));
#40006=CARTESIAN_POINT('Ctrl Pts',(96.5177214247813,-1.72814452071155,-0.781989423172969));
#40007=CARTESIAN_POINT('Ctrl Pts',(95.0443887169318,-0.992193356934267,
-0.860989259020528));
#40008=CARTESIAN_POINT('Ctrl Pts',(94.8557454082464,0.64388558250149,-0.939989094868094));
#40009=CARTESIAN_POINT('Ctrl Pts',(96.1229310831989,1.69582536089387,-1.01898893071566));
#40010=CARTESIAN_POINT('Ctrl Pts',(97.6963444937537,1.20929961996931,-1.09798876656322));
#40011=CARTESIAN_POINT('Ctrl Pts',(98.1485728720161,-0.374312516833932,
-1.17698860241079));
#40012=CARTESIAN_POINT('Ctrl Pts',(97.0693509649446,-1.61834525395207,-1.25598843825835));
#40013=CARTESIAN_POINT('Ctrl Pts',(95.4377574197567,-1.394202544772,-1.33498827410591));
#40014=CARTESIAN_POINT('Ctrl Pts',(94.7339866801775,0.0947716969215828,
-1.41398810995347));
#40015=CARTESIAN_POINT('Ctrl Pts',(95.5965051021273,1.49776829191394,-1.49298794580103));
#40016=CARTESIAN_POINT('Ctrl Pts',(97.2428291934931,1.54197774292137,-1.5719877816486));
#40017=CARTESIAN_POINT('Ctrl Pts',(98.1794008169382,0.187292874166953,-1.65098761749616));
#40018=CARTESIAN_POINT('Ctrl Pts',(97.5565548403935,-1.33730555798415,-1.72998745334372));
#40019=CARTESIAN_POINT('Ctrl Pts',(95.9393420249252,-1.64868988972742,-1.80898728919129));
#40020=CARTESIAN_POINT('Ctrl Pts',(94.7949105333028,-0.46436980861648,-1.88798712503885));
#40021=CARTESIAN_POINT('Ctrl Pts',(95.1614976001875,1.14123020841151,-1.96698696088641));
#40022=CARTESIAN_POINT('Ctrl Pts',(96.7065325602059,1.71149722047994,-2.04598679673397));
#40023=CARTESIAN_POINT('Ctrl Pts',(98.0283475672782,0.729080516688774,-2.12498663258154));
#40024=CARTESIAN_POINT('Ctrl Pts',(97.9277816690826,-0.914763755975596,
-2.20398646842909));
#40025=CARTESIAN_POINT('Ctrl Pts',(96.4960690380457,-1.72872716722286,-2.28298630427666));
#40026=CARTESIAN_POINT('Ctrl Pts',(95.032070613737,-0.974375719723946,-2.36198614012422));
#40027=CARTESIAN_POINT('Ctrl Pts',(94.8639372608783,0.663937030748207,-2.44098597597178));
#40028=CARTESIAN_POINT('Ctrl Pts',(96.1442008772341,1.69992089420785,-2.51998581181935));
#40029=CARTESIAN_POINT('Ctrl Pts',(97.7113962584065,1.19372317597498,-2.5989856476669));
#40030=CARTESIAN_POINT('Ctrl Pts',(98.1437514501881,-0.395429579693847,
-2.67798548351448));
#40031=CARTESIAN_POINT('Ctrl Pts',(97.0490304280756,-1.62584551605722,-2.75698531936203));
#40032=CARTESIAN_POINT('Ctrl Pts',(95.4203726982335,-1.38128163537028,-2.8359851552096));
#40033=CARTESIAN_POINT('Ctrl Pts',(94.7353093401365,0.116391789680825,-2.91498499105715));
#40034=CARTESIAN_POINT('Ctrl Pts',(95.615335210839,1.50847366931512,-2.99398482690473));
#40035=CARTESIAN_POINT('Ctrl Pts',(97.2620839311558,1.53205639277676,-3.07298466275228));
#40036=CARTESIAN_POINT('Ctrl Pts',(98.181612133017,0.16574552818808,-3.15198449859985));
#40037=CARTESIAN_POINT('Ctrl Pts',(97.5397166122691,-1.35093098087869,-3.23098433444741));
#40038=CARTESIAN_POINT('Ctrl Pts',(95.918730025002,-1.64203229762585,-3.30998417029497));
#40039=CARTESIAN_POINT('Ctrl Pts',(94.7892241299194,-0.443469021997726,
-3.38898400614253));
#40040=CARTESIAN_POINT('Ctrl Pts',(95.1758955430473,1.15741283216291,-3.4679838419901));
#40041=CARTESIAN_POINT('Ctrl Pts',(96.7279529225517,1.7082806778739,-3.54698367783766));
#40042=CARTESIAN_POINT('Ctrl Pts',(98.0373576281896,0.709382880517475,-3.62598351368522));
#40043=CARTESIAN_POINT('Ctrl Pts',(97.9162074305732,-0.933072635570782,
-3.70498334953278));
#40044=CARTESIAN_POINT('Ctrl Pts',(96.4744107401569,-1.7290373309037,-3.78398318538035));
#40045=CARTESIAN_POINT('Ctrl Pts',(95.0199768343608,-0.956405784575361,
-3.86298302122791));
#40046=CARTESIAN_POINT('Ctrl Pts',(94.8723795716142,0.683884598479127,-3.94198285707547));
#40047=CARTESIAN_POINT('Ctrl Pts',(96.1655203475008,1.7037495044598,-4.02098269292304));
#40048=CARTESIAN_POINT('Ctrl Pts',(97.7262516973936,1.1779594834696,-4.0999825287706));
#40049=CARTESIAN_POINT('Ctrl Pts',(98.1386658870132,-0.416484629352105,
-4.17898236461816));
#40050=CARTESIAN_POINT('Ctrl Pts',(97.028617525579,-1.63309061651,-4.25798220046572));
#40051=CARTESIAN_POINT('Ctrl Pts',(95.4031512018262,-1.36814397460409,-4.33698203631329));
#40052=CARTESIAN_POINT('Ctrl Pts',(94.7369027265695,0.137993622672245,-4.41598187216085));
#40053=CARTESIAN_POINT('Ctrl Pts',(95.6342979474299,1.51894232204099,-4.49498170800841));
#40054=CARTESIAN_POINT('Ctrl Pts',(97.2812128743889,1.52189462129242,-4.57398154385597));
#40055=CARTESIAN_POINT('Ctrl Pts',(98.1835533554055,0.144172171366491,-4.65298137970354));
#40056=CARTESIAN_POINT('Ctrl Pts',(97.5227090216212,-1.36434440435165,-4.7319812155511));
#40057=CARTESIAN_POINT('Ctrl Pts',(95.898203041084,-1.63511702466368,-4.81098105139866));
#40058=CARTESIAN_POINT('Ctrl Pts',(94.7837999937036,-0.422498642525088,
-4.88998088724622));
#40059=CARTESIAN_POINT('Ctrl Pts',(95.1904950734952,1.17341382524522,-4.96898072309378));
#40060=CARTESIAN_POINT('Ctrl Pts',(96.7493313110161,1.70479605801417,-5.04798055894135));
#40061=CARTESIAN_POINT('Ctrl Pts',(98.0461202328097,0.689573922210988,-5.12698039478891));
#40062=CARTESIAN_POINT('Ctrl Pts',(97.9044047476399,-0.951235089823737,
-5.20598023063647));
#40063=CARTESIAN_POINT('Ctrl Pts',(96.4527502562932,-1.72907616000729,-5.28498006648404));
#40064=CARTESIAN_POINT('Ctrl Pts',(95.0081091105889,-0.938285762461949,
-5.36397990233159));
#40065=CARTESIAN_POINT('Ctrl Pts',(94.8810711001165,0.703724845483841,-5.44297973817916));
#40066=CARTESIAN_POINT('Ctrl Pts',(96.1868861053805,1.70731074850284,-5.52197957402672));
#40067=CARTESIAN_POINT('Ctrl Pts',(97.7409085013552,1.16201093599497,-5.60097940987428));
#40068=CARTESIAN_POINT('Ctrl Pts',(98.1333169694285,-0.437474320859729,
-5.67997924572183));
#40069=CARTESIAN_POINT('Ctrl Pts',(97.0081154664765,-1.64007943912008,-5.7589790815694));
#40070=CARTESIAN_POINT('Ctrl Pts',(95.3860956301902,-1.35479161357392,-5.83797891741698));
#40071=CARTESIAN_POINT('Ctrl Pts',(94.738766590895,0.159573800583674,-5.91697875326452));
#40072=CARTESIAN_POINT('Ctrl Pts',(95.6533903353675,1.52917261000153,-5.9959785891121));
#40073=CARTESIAN_POINT('Ctrl Pts',(97.3002130217027,1.51149402174397,-6.07497842495966));
#40074=CARTESIAN_POINT('Ctrl Pts',(98.185224179278,0.122576189876859,-6.15397826080722));
#40075=CARTESIAN_POINT('Ctrl Pts',(97.5055347375172,-1.37754372382008,-6.23297809665479));
#40076=CARTESIAN_POINT('Ctrl Pts',(95.877764294382,-1.6279451558583,-6.31197793250235));
#40077=CARTESIAN_POINT('Ctrl Pts',(94.7786389758806,-0.401461961134109,
-6.39097776834991));
#40078=CARTESIAN_POINT('Ctrl Pts',(95.2052939004409,1.18923067670014,-6.46997760419747));
#40079=CARTESIAN_POINT('Ctrl Pts',(96.770664370736,1.70104390771143,-6.54897744004503));
#40080=CARTESIAN_POINT('Ctrl Pts',(98.0546340060357,0.669656750364228,-6.62797727589259));
#40081=CARTESIAN_POINT('Ctrl Pts',(97.8923754724572,-0.969248268540891,
-6.70697711174016));
#40082=CARTESIAN_POINT('Ctrl Pts',(96.4310909855927,-1.72884364843707,-6.78597694758772));
#40083=CARTESIAN_POINT('Ctrl Pts',(94.9964693048017,-0.920018496926357,
-6.86497678343529));
#40084=CARTESIAN_POINT('Ctrl Pts',(94.8900104824397,0.723454658270465,-6.94397661928285));
#40085=CARTESIAN_POINT('Ctrl Pts',(96.2082947979853,1.71060406747721,-7.02297645513041));
#40086=CARTESIAN_POINT('Ctrl Pts',(97.7553643702261,1.14588003632696,-7.10197629097797));
#40087=CARTESIAN_POINT('Ctrl Pts',(98.1277055368295,-0.458395360343963,
-7.18097612682554));
#40088=CARTESIAN_POINT('Ctrl Pts',(96.9875274681182,-1.64681088714457,-7.25997596267309));
#40089=CARTESIAN_POINT('Ctrl Pts',(95.3692086598241,-1.34122664764074,-7.33897579852067));
#40090=CARTESIAN_POINT('Ctrl Pts',(94.7409006406209,0.181128936878324,-7.41797563436821));
#40091=CARTESIAN_POINT('Ctrl Pts',(95.672609378519,1.53916292777684,-7.4969754702158));
#40092=CARTESIAN_POINT('Ctrl Pts',(97.3190813914398,1.50085622627801,-7.57597530606333));
#40093=CARTESIAN_POINT('Ctrl Pts',(98.1866243424353,0.100960972735917,-7.65497514191093));
#40094=CARTESIAN_POINT('Ctrl Pts',(97.4881964550856,-1.39052686793939,-7.73397497775846));
#40095=CARTESIAN_POINT('Ctrl Pts',(95.8574169923098,-1.62051781667803,-7.81297481360604));
#40096=CARTESIAN_POINT('Ctrl Pts',(94.7737418863601,-0.380362279070926,
-7.8919746494536));
#40097=CARTESIAN_POINT('Ctrl Pts',(95.2202897015312,1.20486090441735,-7.97097448530115));
#40098=CARTESIAN_POINT('Ctrl Pts',(96.7919487539561,1.69702481578656,-8.04997432114873));
#40099=CARTESIAN_POINT('Ctrl Pts',(98.0628976118138,0.64963449053567,-8.12897415699628));
#40100=CARTESIAN_POINT('Ctrl Pts',(97.8801214927624,-0.987109344936422,
-8.20797399284384));
#40101=CARTESIAN_POINT('Ctrl Pts',(96.4094363269932,-1.72833983270331,-8.28697382869141));
#40102=CARTESIAN_POINT('Ctrl Pts',(94.9850592436326,-0.901606854571692,
-8.36597366453896));
#40103=CARTESIAN_POINT('Ctrl Pts',(94.899196315702,0.743070940588966,-8.44497350038655));
#40104=CARTESIAN_POINT('Ctrl Pts',(96.2297430657699,1.71362894474065,-8.52397333623409));
#40105=CARTESIAN_POINT('Ctrl Pts',(97.7696170353154,1.1295693155191,-8.60297317208167));
#40106=CARTESIAN_POINT('Ctrl Pts',(98.1218324701197,-0.479244464040642,
-8.6819730079292));
#40107=CARTESIAN_POINT('Ctrl Pts',(96.9668567607269,-1.6532839055364,-8.76097284377679));
#40108=CARTESIAN_POINT('Ctrl Pts',(95.3524929419726,-1.32745120296166,-8.83997267962433));
#40109=CARTESIAN_POINT('Ctrl Pts',(94.743304538488,0.202655643903087,-8.91897251547192));
#40110=CARTESIAN_POINT('Ctrl Pts',(95.6919520655271,1.54891171752243,-8.99797235131946));
#40111=CARTESIAN_POINT('Ctrl Pts',(97.3378150134816,1.48998288477276,-9.07697218716705));
#40112=CARTESIAN_POINT('Ctrl Pts',(98.1877536431172,0.0793299502857095,
-9.15597202301459));
#40113=CARTESIAN_POINT('Ctrl Pts',(97.4706968598829,-1.40329187457507,-9.23497185886216));
#40114=CARTESIAN_POINT('Ctrl Pts',(95.8371643973225,-1.61283602471812,-9.31397169470972));
#40115=CARTESIAN_POINT('Ctrl Pts',(94.7691093572545,-0.359203198268218,
-9.39297153055729));
#40116=CARTESIAN_POINT('Ctrl Pts',(95.2354803915345,1.22030262709654,-9.47197136640485));
#40117=CARTESIAN_POINT('Ctrl Pts',(96.8131805937843,1.69273828970788,-9.55097120225241));
#40118=CARTESIAN_POINT('Ctrl Pts',(98.0709107886458,0.62951249234026,-9.62997103809997));
#40119=CARTESIAN_POINT('Ctrl Pts',(97.8676426968368,-1.00481985473004,-9.70897087394753));
#40120=CARTESIAN_POINT('Ctrl Pts',(96.3877936776409,-1.72755626495539,-9.78797070979509));
#40121=CARTESIAN_POINT('Ctrl Pts',(94.9738728583651,-0.883070483070808,
-9.86697054564266));
#40122=CARTESIAN_POINT('Ctrl Pts',(94.9086426046154,0.762603550204478,-9.94597038149023));
#40123=CARTESIAN_POINT('Ctrl Pts',(96.2511971856125,1.71632017390702,-10.0249702173378));
#40124=CARTESIAN_POINT('Ctrl Pts',(97.78372392326,1.11320856185152,-10.1039700531854));
#40125=CARTESIAN_POINT('Ctrl Pts',(98.1155814248733,-0.500268501807092,
-10.1829698890329));
#40126=CARTESIAN_POINT('Ctrl Pts',(96.9463371342804,-1.65900482028253,-10.2619697248805));
#40127=CARTESIAN_POINT('Ctrl Pts',(95.3354971295683,-1.31444738919156,-10.3409695607281));
#40128=CARTESIAN_POINT('Ctrl Pts',(94.7468801337304,0.226207046957059,-10.4199693965756));
#40129=CARTESIAN_POINT('Ctrl Pts',(95.3886793944715,1.11059179364519,-10.4726359538073));
#40130=CARTESIAN_POINT('Ctrl Pts',(95.8257004218783,1.32064939124249,-10.4989692324232));
#40131=CARTESIAN_POINT('Ctrl Pts',(95.6650518398339,-1.11389367580726,0.110290927349878));
#40132=CARTESIAN_POINT('Ctrl Pts',(95.296353403176,-0.850617388648033,0.0839512729108505));
#40133=CARTESIAN_POINT('Ctrl Pts',(94.8471900331093,0.0661743017727613,
0.0312783398559688));
#40134=CARTESIAN_POINT('Ctrl Pts',(95.6357036753152,1.38984411673286,-0.047727871814767));
#40135=CARTESIAN_POINT('Ctrl Pts',(97.1733173175222,1.44893729807126,-0.12672770766233));
#40136=CARTESIAN_POINT('Ctrl Pts',(98.0637659022104,0.195302500657018,-0.205727543509892));
#40137=CARTESIAN_POINT('Ctrl Pts',(97.4999437307949,-1.23640129007877,-0.284727379357454));
#40138=CARTESIAN_POINT('Ctrl Pts',(95.9929896061911,-1.545980316847,-0.363727215205017));
#40139=CARTESIAN_POINT('Ctrl Pts',(94.9102099676746,-0.453263699660661,
-0.442727051052579));
#40140=CARTESIAN_POINT('Ctrl Pts',(95.2338164480949,1.05077424497549,-0.521726886900142));
#40141=CARTESIAN_POINT('Ctrl Pts',(96.6702788199085,1.60148204398775,-0.600726722747705));
#40142=CARTESIAN_POINT('Ctrl Pts',(97.916402661141,0.699343033941837,-0.679726558595267));
#40143=CARTESIAN_POINT('Ctrl Pts',(97.8417070953685,-0.837260871503877,
-0.758726394442829));
#40144=CARTESIAN_POINT('Ctrl Pts',(96.5139501885348,-1.61428730284708,-0.837726230290392));
#40145=CARTESIAN_POINT('Ctrl Pts',(95.1376866557998,-0.926823606979764,
-0.916726066137954));
#40146=CARTESIAN_POINT('Ctrl Pts',(94.9614719386115,0.601463771033733,-0.995725901985518));
#40147=CARTESIAN_POINT('Ctrl Pts',(96.1451702467733,1.58409746125275,-1.07472573783308));
#40148=CARTESIAN_POINT('Ctrl Pts',(97.614920756842,1.12962602285743,-1.15372557368064));
#40149=CARTESIAN_POINT('Ctrl Pts',(98.0373544828796,-0.349651279728017,
-1.23272540952821));
#40150=CARTESIAN_POINT('Ctrl Pts',(97.0292361220251,-1.51172206014459,-1.31172524537577));
#40151=CARTESIAN_POINT('Ctrl Pts',(95.5051386221701,-1.30234678792709,-1.39072508122333));
#40152=CARTESIAN_POINT('Ctrl Pts',(94.8477351727468,0.088527750530259,-1.46972491707089));
#40153=CARTESIAN_POINT('Ctrl Pts',(95.6534273589836,1.39908920073889,-1.54872475291846));
#40154=CARTESIAN_POINT('Ctrl Pts',(97.1912848964821,1.44038595258563,-1.62772458876602));
#40155=CARTESIAN_POINT('Ctrl Pts',(98.0661513569051,0.174953254810515,-1.70672442461358));
#40156=CARTESIAN_POINT('Ctrl Pts',(97.4843410166729,-1.24919840696643,-1.78572426046114));
#40157=CARTESIAN_POINT('Ctrl Pts',(95.9736767853404,-1.5400674674034,-1.86472409630871));
#40158=CARTESIAN_POINT('Ctrl Pts',(94.9046451136471,-0.433775229380962,
-1.94372393215627));
#40159=CARTESIAN_POINT('Ctrl Pts',(95.247079927615,1.066041302093,-2.02272376800383));
#40160=CARTESIAN_POINT('Ctrl Pts',(96.6903216753514,1.59873679473359,-2.1017236038514));
#40161=CARTESIAN_POINT('Ctrl Pts',(97.9250501121554,0.681045715065119,-2.18072343969896));
#40162=CARTESIAN_POINT('Ctrl Pts',(97.8311099059914,-0.854495384314323,
-2.25972327554652));
#40163=CARTESIAN_POINT('Ctrl Pts',(96.4937243494543,-1.614831562227,-2.33872311139408));
#40164=CARTESIAN_POINT('Ctrl Pts',(95.1261801195442,-0.910179868466786,
-2.41772294724165));
#40165=CARTESIAN_POINT('Ctrl Pts',(94.9691240785406,0.620194147990309,-2.4967227830892));
#40166=CARTESIAN_POINT('Ctrl Pts',(96.1650386999228,1.58792316410799,-2.57572261893677));
#40167=CARTESIAN_POINT('Ctrl Pts',(97.6289808497757,1.11507581859951,-2.65472245478433));
#40168=CARTESIAN_POINT('Ctrl Pts',(98.03285071601,-0.36937706425566,-2.73372229063189));
#40169=CARTESIAN_POINT('Ctrl Pts',(97.0102543851032,-1.51872817435509,-2.81272212647946));
#40170=CARTESIAN_POINT('Ctrl Pts',(95.4888992770912,-1.29027716079902,-2.89172196232702));
#40171=CARTESIAN_POINT('Ctrl Pts',(94.8489706904667,0.108723423293354,-2.97072179817458));
#40172=CARTESIAN_POINT('Ctrl Pts',(95.671016863241,1.4090892641617,-3.04972163402214));
#40173=CARTESIAN_POINT('Ctrl Pts',(97.2092710534012,1.43111826150216,-3.12872146986971));
#40174=CARTESIAN_POINT('Ctrl Pts',(98.068216982451,0.154825535972839,-3.20772130571727));
#40175=CARTESIAN_POINT('Ctrl Pts',(97.4686121597758,-1.26192613136156,-3.28672114156483));
#40176=CARTESIAN_POINT('Ctrl Pts',(95.9544227881412,-1.53384850465562,-3.3657209774124));
#40177=CARTESIAN_POINT('Ctrl Pts',(94.8993333537387,-0.41425147193255,-3.44472081325996));
#40178=CARTESIAN_POINT('Ctrl Pts',(95.2605292752057,1.08115774851027,-3.52372064910751));
#40179=CARTESIAN_POINT('Ctrl Pts',(96.7103307767561,1.59573217108913,-3.60272048495509));
#40180=CARTESIAN_POINT('Ctrl Pts',(97.9334665534616,0.662645839599646,-3.68172032080264));
#40181=CARTESIAN_POINT('Ctrl Pts',(97.8202982255782,-0.871598000157872,
-3.76072015665021));
#40182=CARTESIAN_POINT('Ctrl Pts',(96.4734929886715,-1.61512129105799,-3.83971999249776));
#40183=CARTESIAN_POINT('Ctrl Pts',(95.114883127738,-0.893393866025624,-3.91871982834534));
#40184=CARTESIAN_POINT('Ctrl Pts',(94.9770101753713,0.638827488503664,-3.99771966419289));
#40185=CARTESIAN_POINT('Ctrl Pts',(96.1849535564308,1.5914995298825,-4.07671950004046));
#40186=CARTESIAN_POINT('Ctrl Pts',(97.6428575517804,1.10035070252706,-4.15571933588801));
#40187=CARTESIAN_POINT('Ctrl Pts',(98.0281002105038,-0.389044921264601,
-4.23471917173559));
#40188=CARTESIAN_POINT('Ctrl Pts',(96.9911863679787,-1.52549593800485,-4.31371900758313));
#40189=CARTESIAN_POINT('Ctrl Pts',(95.4728124031908,-1.27800506277145,-4.39271884343072));
#40190=CARTESIAN_POINT('Ctrl Pts',(94.8504590980947,0.128902039316688,-4.47171867927826));
#40191=CARTESIAN_POINT('Ctrl Pts',(95.6887302573114,1.41886819929748,-4.55071851512584));
#40192=CARTESIAN_POINT('Ctrl Pts',(97.2271397037416,1.42162598901859,-4.62971835097339));
#40193=CARTESIAN_POINT('Ctrl Pts',(98.0700303091814,0.134673519992983,-4.70871818682096));
#40194=CARTESIAN_POINT('Ctrl Pts',(97.4527250986499,-1.27445582372271,-4.78771802266851));
#40195=CARTESIAN_POINT('Ctrl Pts',(95.935248205745,-1.52738883811455,-4.86671785851608));
#40196=CARTESIAN_POINT('Ctrl Pts',(94.8942665817662,-0.394662706691651,
-4.94571769436365));
#40197=CARTESIAN_POINT('Ctrl Pts',(95.2741669289706,1.09610453082861,-5.02471753021121));
#40198=CARTESIAN_POINT('Ctrl Pts',(96.7303006696905,1.59247713221513,-5.10371736605877));
#40199=CARTESIAN_POINT('Ctrl Pts',(97.9416518419073,0.644141976355837,-5.18271720190633));
#40200=CARTESIAN_POINT('Ctrl Pts',(97.8092731515925,-0.888563837758662,
-5.26171703775389));
#40201=CARTESIAN_POINT('Ctrl Pts',(96.4532595859348,-1.61515756194168,-5.34071687360145));
#40202=CARTESIAN_POINT('Ctrl Pts',(95.1037972980699,-0.876467664961753,
-5.41971670944902));
#40203=CARTESIAN_POINT('Ctrl Pts',(94.9851290704841,0.657360579018497,-5.49871654529658));
#40204=CARTESIAN_POINT('Ctrl Pts',(96.2049116509347,1.59482614462572,-5.57771638114415));
#40205=CARTESIAN_POINT('Ctrl Pts',(97.6565487056463,1.08545291048562,-5.65671621699171));
#40206=CARTESIAN_POINT('Ctrl Pts',(98.0231037014517,-0.408651726184762,
-5.73571605283926));
#40207=CARTESIAN_POINT('Ctrl Pts',(96.9720350682498,-1.53202430844267,-5.81471588868683));
#40208=CARTESIAN_POINT('Ctrl Pts',(95.4568805222601,-1.26553240981001,-5.89371572453439));
#40209=CARTESIAN_POINT('Ctrl Pts',(94.8522001634278,0.149060426985132,-5.97271556038196));
#40210=CARTESIAN_POINT('Ctrl Pts',(95.7065647607682,1.42842447411204,-6.05171539622952));
#40211=CARTESIAN_POINT('Ctrl Pts',(97.2448880437637,1.411910623439,-6.13071523207708));
#40212=CARTESIAN_POINT('Ctrl Pts',(98.0715910523545,0.114500369950604,-6.20971506792465));
#40213=CARTESIAN_POINT('Ctrl Pts',(97.4366823265136,-1.28678551812544,-6.2887149037722));
#40214=CARTESIAN_POINT('Ctrl Pts',(95.9161560471369,-1.52068948131225,-6.36771473961977));
#40215=CARTESIAN_POINT('Ctrl Pts',(94.8894455928724,-0.375012007773534,
-6.44671457546733));
#40216=CARTESIAN_POINT('Ctrl Pts',(95.2879907487666,1.11087930352192,-6.5257144113149));
#40217=CARTESIAN_POINT('Ctrl Pts',(96.7502282203229,1.58897218889616,-6.60471424716245));
#40218=CARTESIAN_POINT('Ctrl Pts',(97.9496046929873,0.625537029121671,-6.68371408301002));
#40219=CARTESIAN_POINT('Ctrl Pts',(97.7980364141802,-0.90539023470551,-6.76271391885758));
#40220=CARTESIAN_POINT('Ctrl Pts',(96.4330273164332,-1.61494036918316,-6.84171375470514));
#40221=CARTESIAN_POINT('Ctrl Pts',(95.0929243702188,-0.859403921473622,
-6.92071359055271));
#40222=CARTESIAN_POINT('Ctrl Pts',(94.9934794897961,0.675790511172483,-6.99971342640027));
#40223=CARTESIAN_POINT('Ctrl Pts',(96.2249098514488,1.59790248629786,-7.07871326224784));
#40224=CARTESIAN_POINT('Ctrl Pts',(97.6700521628457,1.0703847803579,-7.15771309809539));
#40225=CARTESIAN_POINT('Ctrl Pts',(98.0178619729467,-0.428194402157172,
-7.23671293394296));
#40226=CARTESIAN_POINT('Ctrl Pts',(96.9528034912937,-1.53831226118359,-7.31571276979052));
#40227=CARTESIAN_POINT('Ctrl Pts',(95.4411061344594,-1.25286115922476,-7.39471260563808));
#40228=CARTESIAN_POINT('Ctrl Pts',(94.8541936132431,0.169195422880768,-7.47371244148564));
#40229=CARTESIAN_POINT('Ctrl Pts',(95.7245175748764,1.43775658895706,-7.55271227733321));
#40230=CARTESIAN_POINT('Ctrl Pts',(97.2625132882538,1.40197368937753,-7.63171211318077));
#40231=CARTESIAN_POINT('Ctrl Pts',(98.0728989670454,0.0943092515801678,
-7.71071194902833));
#40232=CARTESIAN_POINT('Ctrl Pts',(97.4204863609289,-1.29891327969378,-7.78971178487589));
#40233=CARTESIAN_POINT('Ctrl Pts',(95.8971493084129,-1.51375148556655,-7.86871162072345));
#40234=CARTESIAN_POINT('Ctrl Pts',(94.8848711436064,-0.355302458924759,
-7.94771145657102));
#40235=CARTESIAN_POINT('Ctrl Pts',(95.3019985652462,1.12547974801143,-8.02671129241858));
#40236=CARTESIAN_POINT('Ctrl Pts',(96.7701103014622,1.58521789115917,-8.10571112826615));
#40237=CARTESIAN_POINT('Ctrl Pts',(97.9573238586725,0.606833917531075,-8.1847109641137));
#40238=CARTESIAN_POINT('Ctrl Pts',(97.7865897767067,-0.922074550452794,
-8.26371079996127));
#40239=CARTESIAN_POINT('Ctrl Pts',(96.4127993551685,-1.61446974688726,-8.34271063580883));
#40240=CARTESIAN_POINT('Ctrl Pts',(95.0822660504723,-0.842205313300818,
-8.4217104716564));
#40241=CARTESIAN_POINT('Ctrl Pts',(95.0020601228529,0.694114392709185,-8.50071030750395));
#40242=CARTESIAN_POINT('Ctrl Pts',(96.2449450197681,1.60072807229517,-8.57971014335152));
#40243=CARTESIAN_POINT('Ctrl Pts',(97.6833658041586,1.05514867644134,-8.65870997919908));
#40244=CARTESIAN_POINT('Ctrl Pts',(98.0123758478541,-0.447669881765458,
-8.73770981504665));
#40245=CARTESIAN_POINT('Ctrl Pts',(96.9334946545137,-1.54435881069132,-8.8167096508942));
#40246=CARTESIAN_POINT('Ctrl Pts',(95.4254917163583,-1.23999329709286,-8.89570948674177));
#40247=CARTESIAN_POINT('Ctrl Pts',(94.8564391325024,0.189303862542906,-8.97470932258933));
#40248=CARTESIAN_POINT('Ctrl Pts',(95.7425858866791,1.44686308862524,-9.0537091584369));
#40249=CARTESIAN_POINT('Ctrl Pts',(97.2800126627773,1.39181672801171,-9.13270899428446));
#40250=CARTESIAN_POINT('Ctrl Pts',(98.073953864787,0.0741033692187827,-9.21170883013202));
#40251=CARTESIAN_POINT('Ctrl Pts',(97.4041397105173,-1.31083727556667,-9.29070866597957));
#40252=CARTESIAN_POINT('Ctrl Pts',(95.8782310370846,-1.50657580142939,-9.36970850182715));
#40253=CARTESIAN_POINT('Ctrl Pts',(94.8805438244351,-0.335537424767974,
-9.44870833767471));
#40254=CARTESIAN_POINT('Ctrl Pts',(95.3161884305613,1.13990410694458,-9.52770817352227));
#40255=CARTESIAN_POINT('Ctrl Pts',(96.7899433009825,1.58121377892249,-9.60670800936984));
#40256=CARTESIAN_POINT('Ctrl Pts',(97.9648090946936,0.588037638744514,-9.68570784521739));
#40257=CARTESIAN_POINT('Ctrl Pts',(97.7749331348131,-0.938618219540738,
-9.76470768106496));
#40258=CARTESIAN_POINT('Ctrl Pts',(96.3925826119331,-1.61373780378226,-9.84370751691252));
#40259=CARTESIAN_POINT('Ctrl Pts',(95.0718166699452,-0.824890193647276,
-9.92270735276009));
#40260=CARTESIAN_POINT('Ctrl Pts',(95.0108840516792,0.712360114242248,-10.0017071886077));
#40261=CARTESIAN_POINT('Ctrl Pts',(96.264985654588,1.60324199229448,-10.0807070244552));
#40262=CARTESIAN_POINT('Ctrl Pts',(97.6965432727204,1.03986583603414,-10.1597068603028));
#40263=CARTESIAN_POINT('Ctrl Pts',(98.0065366469945,-0.467308770072661,
-10.2387066961504));
#40264=CARTESIAN_POINT('Ctrl Pts',(96.9143269448493,-1.54970280821276,-10.3177065319979));
#40265=CARTESIAN_POINT('Ctrl Pts',(95.409615657477,-1.22784622767471,-10.3967063678455));
#40266=CARTESIAN_POINT('Ctrl Pts',(94.8597791529295,0.211303602992048,-10.475706203693));
#40267=CARTESIAN_POINT('Ctrl Pts',(95.4592940575998,1.03742147120277,-10.5283727609247));
#40268=CARTESIAN_POINT('Ctrl Pts',(95.8675223551553,1.2336396165048,-10.5547060395406));
#40269=CARTESIAN_POINT('Ctrl Pts',(95.7211542110066,-1.03532969608655,0.0545541202324537));
#40270=CARTESIAN_POINT('Ctrl Pts',(95.3784604255374,-0.790622535707167,
0.0282144657934261));
#40271=CARTESIAN_POINT('Ctrl Pts',(94.9609769748953,0.0615069653694607,
-0.0244584672614556));
#40272=CARTESIAN_POINT('Ctrl Pts',(95.6938760004271,1.2918170901203,-0.103464678932191));
#40273=CARTESIAN_POINT('Ctrl Pts',(97.1230402909337,1.34674237321029,-0.182464514779754));
#40274=CARTESIAN_POINT('Ctrl Pts',(97.9506846905642,0.181527629648881,-0.261464350627316));
#40275=CARTESIAN_POINT('Ctrl Pts',(97.426629432817,-1.1491967318789,-0.340464186474878));
#40276=CARTESIAN_POINT('Ctrl Pts',(96.0259622149947,-1.43694085563152,-0.419464022322441));
#40277=CARTESIAN_POINT('Ctrl Pts',(95.0195520535749,-0.421294580092347,
-0.498463858170003));
#40278=CARTESIAN_POINT('Ctrl Pts',(95.32033426134,0.976662138706952,-0.577463694017566));
#40279=CARTESIAN_POINT('Ctrl Pts',(96.6554815766994,1.48852799320213,-0.656463529865129));
#40280=CARTESIAN_POINT('Ctrl Pts',(97.8137151189575,0.65001770502604,-0.73546336571269));
#40281=CARTESIAN_POINT('Ctrl Pts',(97.7442879024379,-0.778208066412684,
-0.814463201560254));
#40282=CARTESIAN_POINT('Ctrl Pts',(96.5101789522881,-1.5004300849826,-0.893463037407817));
#40283=CARTESIAN_POINT('Ctrl Pts',(95.2309845946679,-0.86145385702526,-0.972462873255379));
#40284=CARTESIAN_POINT('Ctrl Pts',(95.0671984689766,0.559041959565974,-1.05146270910294));
#40285=CARTESIAN_POINT('Ctrl Pts',(96.1674094103476,1.47236956161164,-1.1304625449505));
#40286=CARTESIAN_POINT('Ctrl Pts',(97.5334970199301,1.04995242574554,-1.20946238079807));
#40287=CARTESIAN_POINT('Ctrl Pts',(97.9261360937432,-0.324990042622103,
-1.28846221664563));
#40288=CARTESIAN_POINT('Ctrl Pts',(96.9891212791054,-1.4050988663371,-1.36746205249319));
#40289=CARTESIAN_POINT('Ctrl Pts',(95.5725198245835,-1.2104910310822,-1.44646188834075));
#40290=CARTESIAN_POINT('Ctrl Pts',(94.9614836653162,0.0822838041389368,
-1.52546172418832));
#40291=CARTESIAN_POINT('Ctrl Pts',(95.7103496158398,1.30041010956386,-1.60446156003588));
#40292=CARTESIAN_POINT('Ctrl Pts',(97.1397405994712,1.3387941622499,-1.68346139588344));
#40293=CARTESIAN_POINT('Ctrl Pts',(97.9529018968721,0.162613635454076,-1.762461231731));
#40294=CARTESIAN_POINT('Ctrl Pts',(97.4121271929523,-1.16109125594871,-1.84146106757857));
#40295=CARTESIAN_POINT('Ctrl Pts',(96.0080115457559,-1.43144504507938,-1.92046090342613));
#40296=CARTESIAN_POINT('Ctrl Pts',(95.0143796939912,-0.403180650145441,
-1.99946073927369));
#40297=CARTESIAN_POINT('Ctrl Pts',(95.3326622550427,0.990852395774487,-2.07846057512125));
#40298=CARTESIAN_POINT('Ctrl Pts',(96.6741107904969,1.48597636898726,-2.15746041096882));
#40299=CARTESIAN_POINT('Ctrl Pts',(97.8217526570323,0.633010913441462,-2.23646024681638));
#40300=CARTESIAN_POINT('Ctrl Pts',(97.7344381429004,-0.794227012653048,
-2.31546008266394));
#40301=CARTESIAN_POINT('Ctrl Pts',(96.4913796608627,-1.50093595723113,-2.3944599185115));
#40302=CARTESIAN_POINT('Ctrl Pts',(95.2202896253514,-0.845984017209627,
-2.47345975435907));
#40303=CARTESIAN_POINT('Ctrl Pts',(95.074310896203,0.576451265232411,-2.55245959020663));
#40304=CARTESIAN_POINT('Ctrl Pts',(96.1858765226113,1.47592543400813,-2.63145942605419));
#40305=CARTESIAN_POINT('Ctrl Pts',(97.5465654411451,1.03642846122403,-2.71045926190175));
#40306=CARTESIAN_POINT('Ctrl Pts',(97.9219499818317,-0.343324548817473,
-2.78945909774932));
#40307=CARTESIAN_POINT('Ctrl Pts',(96.971478342131,-1.41161083265297,-2.86845893359688));
#40308=CARTESIAN_POINT('Ctrl Pts',(95.5574258559488,-1.19927268622775,-2.94745876944444));
#40309=CARTESIAN_POINT('Ctrl Pts',(94.9626320407967,0.101055056905879,-3.026458605292));
#40310=CARTESIAN_POINT('Ctrl Pts',(95.7266985156432,1.3097048590083,-3.10545844113957));
#40311=CARTESIAN_POINT('Ctrl Pts',(97.1564581756467,1.33018013022757,-3.18445827698713));
#40312=CARTESIAN_POINT('Ctrl Pts',(97.9548218318848,0.143905543757601,-3.26345811283469));
#40313=CARTESIAN_POINT('Ctrl Pts',(97.3975077072827,-1.17292128184443,-3.34245794868225));
#40314=CARTESIAN_POINT('Ctrl Pts',(95.9901155512801,-1.42566471168538,-3.42145778452982));
#40315=CARTESIAN_POINT('Ctrl Pts',(95.0094425775579,-0.385033921867376,
-3.50045762037738));
#40316=CARTESIAN_POINT('Ctrl Pts',(95.3451630073641,1.00490266485763,-3.57945745622494));
#40317=CARTESIAN_POINT('Ctrl Pts',(96.6927086309606,1.48318366430436,-3.65845729207251));
#40318=CARTESIAN_POINT('Ctrl Pts',(97.8295754787336,0.615908798681818,-3.73745712792006));
#40319=CARTESIAN_POINT('Ctrl Pts',(97.724389020583,-0.810123364744962,-3.81645696376764));
#40320=CARTESIAN_POINT('Ctrl Pts',(96.4725752371862,-1.50120525121228,-3.89545679961518));
#40321=CARTESIAN_POINT('Ctrl Pts',(95.2097894211152,-0.830381947475887,
-3.97445663546276));
#40322=CARTESIAN_POINT('Ctrl Pts',(95.0816407791284,0.593770378528202,-4.05345647131031));
#40323=CARTESIAN_POINT('Ctrl Pts',(96.2043867653607,1.47924955530519,-4.13245630715788));
#40324=CARTESIAN_POINT('Ctrl Pts',(97.5594634061673,1.02274192158454,-4.21145614300544));
#40325=CARTESIAN_POINT('Ctrl Pts',(97.9175345339944,-0.361605213177098,
-4.29045597885301));
#40326=CARTESIAN_POINT('Ctrl Pts',(96.9537552103785,-1.41790125949968,-4.36945581470056));
#40327=CARTESIAN_POINT('Ctrl Pts',(95.5424736045553,-1.18786615093881,-4.44845565054813));
#40328=CARTESIAN_POINT('Ctrl Pts',(94.9640154696202,0.119810455961133,-4.52745548639569));
#40329=CARTESIAN_POINT('Ctrl Pts',(95.7431625671928,1.31879407655398,-4.60645532224326));
#40330=CARTESIAN_POINT('Ctrl Pts',(97.1730665330944,1.32135735674475,-4.68545515809081));
#40331=CARTESIAN_POINT('Ctrl Pts',(97.9565072629573,0.125174868619475,-4.76445499393838));
#40332=CARTESIAN_POINT('Ctrl Pts',(97.3827411756789,-1.18456724309377,-4.84345482978594));
#40333=CARTESIAN_POINT('Ctrl Pts',(95.9722933704059,-1.41966065156544,-4.92245466563351));
#40334=CARTESIAN_POINT('Ctrl Pts',(95.0047331698288,-0.366826770858215,
-5.00145450148106));
#40335=CARTESIAN_POINT('Ctrl Pts',(95.3578387844463,1.01879523641201,-5.08045433732863));
#40336=CARTESIAN_POINT('Ctrl Pts',(96.7112700283648,1.48015820641608,-5.15945417317619));
#40337=CARTESIAN_POINT('Ctrl Pts',(97.8371834510051,0.598710030500683,-5.23845400902375));
#40338=CARTESIAN_POINT('Ctrl Pts',(97.7141415555451,-0.825892585693585,
-5.31745384487131));
#40339=CARTESIAN_POINT('Ctrl Pts',(96.4537689155765,-1.50123896387606,-5.39645368071888));
#40340=CARTESIAN_POINT('Ctrl Pts',(95.1994854855508,-0.814649567461558,
-5.47545351656644));
#40341=CARTESIAN_POINT('Ctrl Pts',(95.0891870408519,0.610996312553152,-5.554453352414));
#40342=CARTESIAN_POINT('Ctrl Pts',(96.2229371964889,1.48234154074859,-5.63345318826156));
#40343=CARTESIAN_POINT('Ctrl Pts',(97.5721889099376,1.00889488497626,-5.71245302410913));
#40344=CARTESIAN_POINT('Ctrl Pts',(97.9128904334748,-0.379829131509795,
-5.79145285995669));
#40345=CARTESIAN_POINT('Ctrl Pts',(96.935954670023,-1.42396917776525,-5.87045269580425));
#40346=CARTESIAN_POINT('Ctrl Pts',(95.5276654143301,-1.17627320604611,-5.94945253165182));
#40347=CARTESIAN_POINT('Ctrl Pts',(94.9656337359601,0.138547053386591,-6.02845236749938));
#40348=CARTESIAN_POINT('Ctrl Pts',(95.7597391861691,1.32767633822254,-6.10745220334694));
#40349=CARTESIAN_POINT('Ctrl Pts',(97.1895630658246,1.31232722513404,-6.18645203919449));
#40350=CARTESIAN_POINT('Ctrl Pts',(97.9579579254309,0.106424550024346,-6.26545187504207));
#40351=CARTESIAN_POINT('Ctrl Pts',(97.36782991551,-1.19602731243079,-6.34445171088962));
#40352=CARTESIAN_POINT('Ctrl Pts',(95.9545477998918,-1.41343380676619,-6.4234515467372));
#40353=CARTESIAN_POINT('Ctrl Pts',(95.000252209864,-0.348562054412959,-6.50245138258475));
#40354=CARTESIAN_POINT('Ctrl Pts',(95.3706875970921,1.03252793034369,-6.58145121843232));
#40355=CARTESIAN_POINT('Ctrl Pts',(96.72979206991,1.47690047008088,-6.66045105427987));
#40356=CARTESIAN_POINT('Ctrl Pts',(97.8445753799389,0.581417307879113,-6.73945089012744));
#40357=CARTESIAN_POINT('Ctrl Pts',(97.7036973559032,-0.841532200870129,
-6.818450725975));
#40358=CARTESIAN_POINT('Ctrl Pts',(96.4349636472737,-1.50103708992925,-6.89745056182257));
#40359=CARTESIAN_POINT('Ctrl Pts',(95.1893794356358,-0.798789346020887,
-6.97645039767013));
#40360=CARTESIAN_POINT('Ctrl Pts',(95.0969484971525,0.6281263640745,-7.0554502335177));
#40361=CARTESIAN_POINT('Ctrl Pts',(96.2415249049123,1.48520090511852,-7.13445006936525));
#40362=CARTESIAN_POINT('Ctrl Pts',(97.5847399554654,0.994889524388842,-7.21344990521282));
#40363=CARTESIAN_POINT('Ctrl Pts',(97.9080184090637,-0.39799344397038,-7.29244974106037));
#40364=CARTESIAN_POINT('Ctrl Pts',(96.9180795144695,-1.4298136352226,-7.37144957690794));
#40365=CARTESIAN_POINT('Ctrl Pts',(95.5130036090947,-1.16449567080877,-7.45044941275551));
#40366=CARTESIAN_POINT('Ctrl Pts',(94.9674865858653,0.157261908883212,-7.52944924860306));
#40367=CARTESIAN_POINT('Ctrl Pts',(95.7764257712339,1.33635025013728,-7.60844908445063));
#40368=CARTESIAN_POINT('Ctrl Pts',(97.2059451850679,1.30309115247707,-7.68744892029819));
#40369=CARTESIAN_POINT('Ctrl Pts',(97.9591735916556,0.0876575304244177,
-7.76644875614576));
#40370=CARTESIAN_POINT('Ctrl Pts',(97.3527762667723,-1.20729969144816,-7.84544859199331));
#40371=CARTESIAN_POINT('Ctrl Pts',(95.9368816245161,-1.40698515445507,-7.92444842784087));
#40372=CARTESIAN_POINT('Ctrl Pts',(94.9960004008529,-0.330242638778592,
-8.00344826368845));
#40373=CARTESIAN_POINT('Ctrl Pts',(95.3837074289611,1.04609859160552,-8.082448099536));
#40374=CARTESIAN_POINT('Ctrl Pts',(96.7482718489681,1.47341096653177,-8.16144793538358));
#40375=CARTESIAN_POINT('Ctrl Pts',(97.8517501055313,0.56403334452648,-8.24044777123112));
#40376=CARTESIAN_POINT('Ctrl Pts',(97.6930580606508,-0.857039755969165,
-8.31944760707869));
#40377=CARTESIAN_POINT('Ctrl Pts',(96.4161623833438,-1.50059966107122,-8.39844744292626));
#40378=CARTESIAN_POINT('Ctrl Pts',(95.179472857312,-0.782803772029945,-8.47744727877381));
#40379=CARTESIAN_POINT('Ctrl Pts',(95.1049239300038,0.645157844829405,-8.55644711462139));
#40380=CARTESIAN_POINT('Ctrl Pts',(96.2601469737666,1.48782719984968,-8.63544695046894));
#40381=CARTESIAN_POINT('Ctrl Pts',(97.5971145730019,0.980728037363569,-8.71444678631651));
#40382=CARTESIAN_POINT('Ctrl Pts',(97.9029192255884,-0.416095299490275,
-8.79344662216406));
#40383=CARTESIAN_POINT('Ctrl Pts',(96.9001325483008,-1.43543371584626,-8.87244645801162));
#40384=CARTESIAN_POINT('Ctrl Pts',(95.4984904907437,-1.15253539122406,-8.95144629385919));
#40385=CARTESIAN_POINT('Ctrl Pts',(94.9695737265171,0.175952081182726,-9.03044612970675));
#40386=CARTESIAN_POINT('Ctrl Pts',(95.7932197078309,1.34481445972806,-9.10944596555432));
#40387=CARTESIAN_POINT('Ctrl Pts',(97.2222103120731,1.29365057125066,-9.18844580140188));
#40388=CARTESIAN_POINT('Ctrl Pts',(97.9601540864565,0.0688767881518556,
-9.26744563724945));
#40389=CARTESIAN_POINT('Ctrl Pts',(97.3375825611522,-1.21838267655828,-9.34644547309699));
#40390=CARTESIAN_POINT('Ctrl Pts',(95.9192976768465,-1.40031557814065,-9.42544530894457));
#40391=CARTESIAN_POINT('Ctrl Pts',(94.9919782916159,-0.31187165126773,-9.50444514479212));
#40392=CARTESIAN_POINT('Ctrl Pts',(95.3968964695879,1.05950558679262,-9.58344498063969));
#40393=CARTESIAN_POINT('Ctrl Pts',(96.766706008181,1.4696892681371,-9.66244481648726));
#40394=CARTESIAN_POINT('Ctrl Pts',(97.8587074007407,0.546562785148768,-9.7414446523348));
#40395=CARTESIAN_POINT('Ctrl Pts',(97.68222357279,-0.872416584351429,-9.82044448818239));
#40396=CARTESIAN_POINT('Ctrl Pts',(96.3973715462248,-1.49991934260912,-9.89944432402992));
#40397=CARTESIAN_POINT('Ctrl Pts',(95.1697604815257,-0.766709904223744,
-9.97844415987751));
#40398=CARTESIAN_POINT('Ctrl Pts',(95.113125498743,0.662116678280016,-10.0574439957251));
#40399=CARTESIAN_POINT('Ctrl Pts',(96.2787741235636,1.49016381068195,-10.1364438315726));
#40400=CARTESIAN_POINT('Ctrl Pts',(97.6093626221807,0.966523110216778,-10.2154436674202));
#40401=CARTESIAN_POINT('Ctrl Pts',(97.8974918691158,-0.43434903833823,-10.2944435032678));
#40402=CARTESIAN_POINT('Ctrl Pts',(96.8823167554179,-1.44040079614298,-10.3734433391153));
#40403=CARTESIAN_POINT('Ctrl Pts',(95.4837341853858,-1.14124506615788,-10.4524431749629));
#40404=CARTESIAN_POINT('Ctrl Pts',(94.9726781721285,0.196400159027038,-10.5314430108104));
#40405=CARTESIAN_POINT('Ctrl Pts',(95.5299087207281,0.964251148760358,-10.5841095680422));
#40406=CARTESIAN_POINT('Ctrl Pts',(95.9093442884325,1.1466298417671,-10.610442846658));
#40407=CARTESIAN_POINT('Ctrl Pts',(95.7772565821794,-0.95676571636586,-0.00118268688497079));
#40408=CARTESIAN_POINT('Ctrl Pts',(95.4605674478988,-0.730627682766301,
-0.0275223413239983));
#40409=CARTESIAN_POINT('Ctrl Pts',(95.0747639166813,0.0568396289661587,
-0.0801952743788798));
#40410=CARTESIAN_POINT('Ctrl Pts',(95.7520483255391,1.19379006350773,-0.159201486049616));
#40411=CARTESIAN_POINT('Ctrl Pts',(97.0727632643449,1.24454744834932,-0.238201321897178));
#40412=CARTESIAN_POINT('Ctrl Pts',(97.8376034789184,0.167752758640745,-0.317201157744741));
#40413=CARTESIAN_POINT('Ctrl Pts',(97.3533151348387,-1.06199217367905,-0.396200993592303));
#40414=CARTESIAN_POINT('Ctrl Pts',(96.0589348237986,-1.32790139441603,-0.475200829439865));
#40415=CARTESIAN_POINT('Ctrl Pts',(95.1288941394749,-0.389325460524031,
-0.554200665287428));
#40416=CARTESIAN_POINT('Ctrl Pts',(95.4068520745854,0.902550032438413,-0.633200501134991));
#40417=CARTESIAN_POINT('Ctrl Pts',(96.6406843334901,1.37557394241651,-0.712200336982554));
#40418=CARTESIAN_POINT('Ctrl Pts',(97.7110275767741,0.600692376110241,-0.791200172830115));
#40419=CARTESIAN_POINT('Ctrl Pts',(97.6468687095074,-0.719155261321492,
-0.870200008677678));
#40420=CARTESIAN_POINT('Ctrl Pts',(96.5064077160413,-1.38657286711812,-0.949199844525241));
#40421=CARTESIAN_POINT('Ctrl Pts',(95.3242825335359,-0.796084107070757,
-1.0281996803728));
#40422=CARTESIAN_POINT('Ctrl Pts',(95.1729249993416,0.516620148098217,-1.10719951622037));
#40423=CARTESIAN_POINT('Ctrl Pts',(96.189648573922,1.36064166197053,-1.18619935206792));
#40424=CARTESIAN_POINT('Ctrl Pts',(97.4520732830183,0.970278828633655,-1.26519918791549));
#40425=CARTESIAN_POINT('Ctrl Pts',(97.8149177046067,-0.300328805516186,
-1.34419902376305));
#40426=CARTESIAN_POINT('Ctrl Pts',(96.9490064361857,-1.29847567252962,-1.42319885961061));
#40427=CARTESIAN_POINT('Ctrl Pts',(95.639901026997,-1.1186352742373,-1.50219869545818));
#40428=CARTESIAN_POINT('Ctrl Pts',(95.0752321578856,0.0760398577476157,
-1.58119853130574));
#40429=CARTESIAN_POINT('Ctrl Pts',(95.7672718726961,1.2017310183888,-1.6601983671533));
#40430=CARTESIAN_POINT('Ctrl Pts',(97.0881963024602,1.23720237191416,-1.73919820300086));
#40431=CARTESIAN_POINT('Ctrl Pts',(97.839652436839,0.150274016097634,-1.81819803884842));
#40432=CARTESIAN_POINT('Ctrl Pts',(97.3399133692319,-1.072984104931,-1.89719787469599));
#40433=CARTESIAN_POINT('Ctrl Pts',(96.0423463061713,-1.32282262275537,-1.97619771054355));
#40434=CARTESIAN_POINT('Ctrl Pts',(95.1241142743353,-0.372586070909921,
-2.05519754639111));
#40435=CARTESIAN_POINT('Ctrl Pts',(95.4182445824703,0.915663489455976,-2.13419738223868));
#40436=CARTESIAN_POINT('Ctrl Pts',(96.6578999056424,1.37321594324093,-2.21319721808624));
#40437=CARTESIAN_POINT('Ctrl Pts',(97.7184552019094,0.584976111817808,-2.2921970539338));
#40438=CARTESIAN_POINT('Ctrl Pts',(97.6377663798092,-0.733958640991776,
-2.37119688978136));
#40439=CARTESIAN_POINT('Ctrl Pts',(96.4890349722712,-1.38704035223526,-2.45019672562893));
#40440=CARTESIAN_POINT('Ctrl Pts',(95.3143991311586,-0.781788165952468,
-2.52919656147649));
#40441=CARTESIAN_POINT('Ctrl Pts',(95.1794977138653,0.532708382474514,-2.60819639732405));
#40442=CARTESIAN_POINT('Ctrl Pts',(96.2067143453001,1.36392770390827,-2.68719623317162));
#40443=CARTESIAN_POINT('Ctrl Pts',(97.4641500325143,0.957781103848562,-2.76619606901917));
#40444=CARTESIAN_POINT('Ctrl Pts',(97.8110492476535,-0.317272033379287,
-2.84519590486674));
#40445=CARTESIAN_POINT('Ctrl Pts',(96.9327022991588,-1.30449349095085,-2.9241957407143));
#40446=CARTESIAN_POINT('Ctrl Pts',(95.6259524348061,-1.10826821165649,-3.00319557656186));
#40447=CARTESIAN_POINT('Ctrl Pts',(95.0762933911271,0.0933866905184069,
-3.08219541240942));
#40448=CARTESIAN_POINT('Ctrl Pts',(95.7823801680448,1.21032045385489,-3.16119524825699));
#40449=CARTESIAN_POINT('Ctrl Pts',(97.1036452978925,1.22924199895298,-3.24019508410455));
#40450=CARTESIAN_POINT('Ctrl Pts',(97.8414266813184,0.132985551542359,-3.31919491995211));
#40451=CARTESIAN_POINT('Ctrl Pts',(97.3264032547896,-1.08391643232731,-3.39819475579968));
#40452=CARTESIAN_POINT('Ctrl Pts',(96.0258083144189,-1.31748091871516,-3.47719459164724));
#40453=CARTESIAN_POINT('Ctrl Pts',(95.1195518013773,-0.355816371802199,
-3.5561944274948));
#40454=CARTESIAN_POINT('Ctrl Pts',(95.4297967395223,0.928647581204988,-3.63519426334236));
#40455=CARTESIAN_POINT('Ctrl Pts',(96.675086485165,1.37063515751958,-3.71419409918992));
#40456=CARTESIAN_POINT('Ctrl Pts',(97.7256844040054,0.569171757763991,-3.79319393503749));
#40457=CARTESIAN_POINT('Ctrl Pts',(97.6284798155882,-0.748648729332052,
-3.87219377088505));
#40458=CARTESIAN_POINT('Ctrl Pts',(96.4716574857007,-1.38728921136657,-3.95119360673261));
#40459=CARTESIAN_POINT('Ctrl Pts',(95.3046957144924,-0.76737002892615,-4.03019344258017));
#40460=CARTESIAN_POINT('Ctrl Pts',(95.1862713828854,0.548713268552738,-4.10919327842774));
#40461=CARTESIAN_POINT('Ctrl Pts',(96.2238199742907,1.36699958072789,-4.1881931142753));
#40462=CARTESIAN_POINT('Ctrl Pts',(97.4760692605543,0.94513314064201,-4.26719295012286));
#40463=CARTESIAN_POINT('Ctrl Pts',(97.806968857485,-0.334165505089595,-4.34619278597042));
#40464=CARTESIAN_POINT('Ctrl Pts',(96.9163240527783,-1.31030658099452,-4.42519262181799));
#40465=CARTESIAN_POINT('Ctrl Pts',(95.6121348059199,-1.09772723910617,-4.50419245766555));
#40466=CARTESIAN_POINT('Ctrl Pts',(95.0775718411454,0.110718872605577,-4.58319229351311));
#40467=CARTESIAN_POINT('Ctrl Pts',(95.7975948770745,1.21871995381048,-4.66219212936068));
#40468=CARTESIAN_POINT('Ctrl Pts',(97.118993362447,1.22108872447091,-4.74119196520824));
#40469=CARTESIAN_POINT('Ctrl Pts',(97.8429842167332,0.115676217245968,-4.8201918010558));
#40470=CARTESIAN_POINT('Ctrl Pts',(97.3127572527077,-1.09467866246482,-4.89919163690336));
#40471=CARTESIAN_POINT('Ctrl Pts',(96.0093385350669,-1.31193246501631,-4.97819147275094));
#40472=CARTESIAN_POINT('Ctrl Pts',(95.1151997578914,-0.338990835024778,
-5.05719130859848));
#40473=CARTESIAN_POINT('Ctrl Pts',(95.4415106399219,0.941485941995406,-5.13619114444606));
#40474=CARTESIAN_POINT('Ctrl Pts',(96.6922393870391,1.36783928061704,-5.21519098029361));
#40475=CARTESIAN_POINT('Ctrl Pts',(97.7327150601027,0.553278084645531,-5.29419081614118));
#40476=CARTESIAN_POINT('Ctrl Pts',(97.6190099594978,-0.76322133362851,-5.37319065198874));
#40477=CARTESIAN_POINT('Ctrl Pts',(96.4542782452181,-1.38732036581045,-5.4521904878363));
#40478=CARTESIAN_POINT('Ctrl Pts',(95.2951736730316,-0.752831469961364,
-5.53119032368387));
#40479=CARTESIAN_POINT('Ctrl Pts',(95.1932450112196,0.564632046087808,-5.61019015953143));
#40480=CARTESIAN_POINT('Ctrl Pts',(96.2409627420432,1.36985693687148,-5.689189995379));
#40481=CARTESIAN_POINT('Ctrl Pts',(97.4878291142287,0.9323368594669,-5.76818983122655));
#40482=CARTESIAN_POINT('Ctrl Pts',(97.8026771654983,-0.351006536834826,
-5.84718966707411));
#40483=CARTESIAN_POINT('Ctrl Pts',(96.8998742717961,-1.31591404708784,-5.92618950292167));
#40484=CARTESIAN_POINT('Ctrl Pts',(95.5984503064001,-1.08701400228222,-6.00518933876924));
#40485=CARTESIAN_POINT('Ctrl Pts',(95.0790673084927,0.128033679788049,-6.0841891746168));
#40486=CARTESIAN_POINT('Ctrl Pts',(95.81291361157,1.22692820233305,-6.16318901046438));
#40487=CARTESIAN_POINT('Ctrl Pts',(97.1342380878854,1.21274382682907,-6.24218884631192));
#40488=CARTESIAN_POINT('Ctrl Pts',(97.8443247985074,0.0983487300980883,
-6.32118868215949));
#40489=CARTESIAN_POINT('Ctrl Pts',(97.2989775045063,-1.10526910673613,-6.40018851800705));
#40490=CARTESIAN_POINT('Ctrl Pts',(95.9929395526466,-1.30617813222014,-6.47918835385461));
#40491=CARTESIAN_POINT('Ctrl Pts',(95.1110588268558,-0.322112101052384,
-6.55818818970217));
#40492=CARTESIAN_POINT('Ctrl Pts',(95.4533844454178,0.954176557165478,-6.63718802554975));
#40493=CARTESIAN_POINT('Ctrl Pts',(96.7093559194969,1.3648287512656,-6.71618786139731));
#40494=CARTESIAN_POINT('Ctrl Pts',(97.7395460668907,0.537297586636558,-6.79518769724487));
#40495=CARTESIAN_POINT('Ctrl Pts',(97.6093582976261,-0.777674167034751,
-6.87418753309242));
#40496=CARTESIAN_POINT('Ctrl Pts',(96.4368999781142,-1.38713381067534,-6.95318736893999));
#40497=CARTESIAN_POINT('Ctrl Pts',(95.2858345010529,-0.738174770568153,
-7.03218720478755));
#40498=CARTESIAN_POINT('Ctrl Pts',(95.200417504509,0.580462216976517,-7.11118704063511));
#40499=CARTESIAN_POINT('Ctrl Pts',(96.2581399583757,1.37249932393917,-7.19018687648268));
#40500=CARTESIAN_POINT('Ctrl Pts',(97.4994277480854,0.919394268419785,-7.26918671233024));
#40501=CARTESIAN_POINT('Ctrl Pts',(97.7981748451804,-0.367792485783587,
-7.3481865481778));
#40502=CARTESIAN_POINT('Ctrl Pts',(96.8833555376452,-1.32131500926161,-7.42718638402537));
#40503=CARTESIAN_POINT('Ctrl Pts',(95.5849010837298,-1.07613018239279,-7.50618621987292));
#40504=CARTESIAN_POINT('Ctrl Pts',(95.0807795584877,0.145328394885655,-7.5851860557205));
#40505=CARTESIAN_POINT('Ctrl Pts',(95.8283339675914,1.23494391131751,-7.66418589156805));
#40506=CARTESIAN_POINT('Ctrl Pts',(97.1493770818821,1.2042086155766,-7.74318572741561));
#40507=CARTESIAN_POINT('Ctrl Pts',(97.8454482162656,0.0810058092686688,
-7.82218556326319));
#40508=CARTESIAN_POINT('Ctrl Pts',(97.2850661726159,-1.11568610320255,-7.90118539911075));
#40509=CARTESIAN_POINT('Ctrl Pts',(95.9766139406194,-1.30021882334358,-7.9801852349583));
#40510=CARTESIAN_POINT('Ctrl Pts',(95.1071296580992,-0.305182818632427,
-8.05918507080586));
#40511=CARTESIAN_POINT('Ctrl Pts',(95.4654162926759,0.966717435199593,-8.13818490665342));
#40512=CARTESIAN_POINT('Ctrl Pts',(96.7264333964741,1.36160404190438,-8.217184742501));
#40513=CARTESIAN_POINT('Ctrl Pts',(97.7461763523901,0.521232771521885,-8.29618457834855));
#40514=CARTESIAN_POINT('Ctrl Pts',(97.5995263445948,-0.792004961485537,
-8.37518441419613));
#40515=CARTESIAN_POINT('Ctrl Pts',(96.4195254115195,-1.38672957525517,-8.45418425004368));
#40516=CARTESIAN_POINT('Ctrl Pts',(95.2766796641515,-0.72340223075907,-8.53318408589125));
#40517=CARTESIAN_POINT('Ctrl Pts',(95.207787737155,0.596201296949623,-8.6121839217388));
#40518=CARTESIAN_POINT('Ctrl Pts',(96.2753489277647,1.37492632740421,-8.69118375758637));
#40519=CARTESIAN_POINT('Ctrl Pts',(97.5108633418452,0.906307398285803,-8.77018359343392));
#40520=CARTESIAN_POINT('Ctrl Pts',(97.7934626033228,-0.384520717215092,
-8.84918342928149));
#40521=CARTESIAN_POINT('Ctrl Pts',(96.866770442088,-1.32650862100118,-8.92818326512905));
#40522=CARTESIAN_POINT('Ctrl Pts',(95.5714892651293,-1.06507748535526,-9.00718310097661));
#40523=CARTESIAN_POINT('Ctrl Pts',(95.0827083205317,0.162600299822547,-9.0861829368242));
#40524=CARTESIAN_POINT('Ctrl Pts',(95.8438535289828,1.24276583083088,-9.16518277267173));
#40525=CARTESIAN_POINT('Ctrl Pts',(97.1644079613688,1.19548441448961,-9.24418260851932));
#40526=CARTESIAN_POINT('Ctrl Pts',(97.8463543081263,0.063650207084928,-9.32318244436686));
#40527=CARTESIAN_POINT('Ctrl Pts',(97.2710254117867,-1.12592807754988,-9.40218228021444));
#40528=CARTESIAN_POINT('Ctrl Pts',(95.9603643166085,-1.29405535485191,-9.48118211606198));
#40529=CARTESIAN_POINT('Ctrl Pts',(95.1034127587967,-0.288205877767486,
-9.56018195190957));
#40530=CARTESIAN_POINT('Ctrl Pts',(95.4776045086144,0.979107066640665,-9.63918178775711));
#40531=CARTESIAN_POINT('Ctrl Pts',(96.7434687153796,1.3581647573517,-9.71818162360469));
#40532=CARTESIAN_POINT('Ctrl Pts',(97.7526057067882,0.505087931553021,-9.79718145945224));
#40533=CARTESIAN_POINT('Ctrl Pts',(97.5895140107666,-0.806214949162121,
-9.8761812952998));
#40534=CARTESIAN_POINT('Ctrl Pts',(96.4021604805168,-1.38610088143599,-9.95518113114737));
#40535=CARTESIAN_POINT('Ctrl Pts',(95.2677042931061,-0.70852961480021,-10.0341809669949));
#40536=CARTESIAN_POINT('Ctrl Pts',(95.2153669458066,0.611873242317784,-10.1131808028425));
#40537=CARTESIAN_POINT('Ctrl Pts',(96.2925625925392,1.37708562906941,-10.1921806386901));
#40538=CARTESIAN_POINT('Ctrl Pts',(97.522181971641,0.893180384399409,-10.2711804745376));
#40539=CARTESIAN_POINT('Ctrl Pts',(97.788447091237,-0.401389306603797,-10.3501803103852));
#40540=CARTESIAN_POINT('Ctrl Pts',(96.8503065659866,-1.33109878407321,-10.4291801462327));
#40541=CARTESIAN_POINT('Ctrl Pts',(95.5578527132946,-1.05464390464104,-10.5081799820803));
#40542=CARTESIAN_POINT('Ctrl Pts',(95.0855771913276,0.181496715062028,-10.5871798179279));
#40543=CARTESIAN_POINT('Ctrl Pts',(95.6005233838565,0.891080826317942,-10.6398463751596));
#40544=CARTESIAN_POINT('Ctrl Pts',(95.9511662217095,1.05962006702942,-10.6661796537754));
#40545=CARTESIAN_POINT('',(95.7749081866277,-0.958725441828032,-10.5005139401467));
#40546=CARTESIAN_POINT('Ctrl Pts',(95.7743417034713,-0.959424604812491,
-10.5));
#40547=CARTESIAN_POINT('Ctrl Pts',(95.743761931704,-0.942816466443102,-10.5));
#40548=CARTESIAN_POINT('Ctrl Pts',(95.7140522834952,-0.924824833399416,
-10.5));
#40549=CARTESIAN_POINT('Ctrl Pts',(95.6853187497364,-0.905478391503427,
-10.5));
#40550=CARTESIAN_POINT('Ctrl Pts',(95.6455067847734,-0.878672782649827,
-10.5));
#40551=CARTESIAN_POINT('Ctrl Pts',(95.6075673391679,-0.849268629040611,
-10.5));
#40552=CARTESIAN_POINT('Ctrl Pts',(95.571561890951,-0.817569321508675,-10.5));
#40553=CARTESIAN_POINT('Ctrl Pts',(95.53699301791,-0.787134779187252,-10.5));
#40554=CARTESIAN_POINT('Ctrl Pts',(95.5042065672641,-0.754583714502893,
-10.5));
#40555=CARTESIAN_POINT('Ctrl Pts',(95.4732743966275,-0.720145741921755,
-10.5));
#40556=CARTESIAN_POINT('Ctrl Pts',(95.4565243447733,-0.701497266414933,
-10.5));
#40557=CARTESIAN_POINT('Ctrl Pts',(95.4403183608167,-0.682294881829244,
-10.5));
#40558=CARTESIAN_POINT('Ctrl Pts',(95.42467063047,-0.662571296003026,-10.5));
#40559=CARTESIAN_POINT('Ctrl Pts',(95.4184263768185,-0.654700565226925,
-10.5));
#40560=CARTESIAN_POINT('Ctrl Pts',(95.4122761815382,-0.646753210694079,
-10.5));
#40561=CARTESIAN_POINT('Ctrl Pts',(95.4062240468848,-0.638736400192628,
-10.5));
#40562=CARTESIAN_POINT('Ctrl Pts',(95.3752933609304,-0.597764831948361,
-10.5));
#40563=CARTESIAN_POINT('Ctrl Pts',(95.3468925649399,-0.554945957420721,
-10.5));
#40564=CARTESIAN_POINT('Ctrl Pts',(95.3210948996399,-0.51060962610373,-10.5));
#40565=CARTESIAN_POINT('Ctrl Pts',(95.2946242490595,-0.465116690186564,
-10.5));
#40566=CARTESIAN_POINT('Ctrl Pts',(95.2708935368424,-0.41802532548798,-10.5));
#40567=CARTESIAN_POINT('Ctrl Pts',(95.250013584509,-0.369646938464868,-10.5));
#40568=CARTESIAN_POINT('Ctrl Pts',(95.2305984415717,-0.324662482363928,
-10.5));
#40569=CARTESIAN_POINT('Ctrl Pts',(95.2136479739893,-0.27856414950988,-10.5));
#40570=CARTESIAN_POINT('Ctrl Pts',(95.1992838987357,-0.231578413904824,
-10.5));
#40571=CARTESIAN_POINT('Ctrl Pts',(95.1963990144411,-0.22214178757666,-10.5));
#40572=CARTESIAN_POINT('Ctrl Pts',(95.1936212162796,-0.212677871502264,
-10.5));
#40573=CARTESIAN_POINT('Ctrl Pts',(95.1909519508877,-0.203191933881503,
-10.5));
#40574=CARTESIAN_POINT('Ctrl Pts',(95.1762463098862,-0.150931565302911,
-10.5));
#40575=CARTESIAN_POINT('Ctrl Pts',(95.1648222691944,-0.0979747821329156,
-10.5));
#40576=CARTESIAN_POINT('Ctrl Pts',(95.1567822801157,-0.044653796014109,
-10.5));
#40577=CARTESIAN_POINT('Ctrl Pts',(95.1487886315547,0.0083598610667158,
-10.5));
#40578=CARTESIAN_POINT('Ctrl Pts',(95.1441395215139,0.0617346236555578,
-10.5));
#40579=CARTESIAN_POINT('Ctrl Pts',(95.1429788547342,0.115170238925761,-10.5));
#40580=CARTESIAN_POINT('Ctrl Pts',(95.1425638222925,0.134277802153374,-10.5));
#40581=CARTESIAN_POINT('Ctrl Pts',(95.1425952849307,0.153393312536775,-10.5));
#40582=CARTESIAN_POINT('Ctrl Pts',(95.1430814086749,0.172503453148985,-10.5));
#40583=CARTESIAN_POINT('Ctrl Pts',(95.1435523124352,0.191015276902803,-10.5));
#40584=CARTESIAN_POINT('Ctrl Pts',(95.1444498564248,0.209522067576187,-10.5));
#40585=CARTESIAN_POINT('Ctrl Pts',(95.145766583077,0.228014411035019,-10.5));
#40586=CARTESIAN_POINT('Ctrl Pts',(95.146666979761,0.240659742321974,-10.5));
#40587=CARTESIAN_POINT('Ctrl Pts',(95.1477634041437,0.253298319323364,-10.5));
#40588=CARTESIAN_POINT('Ctrl Pts',(95.1490536859085,0.265927131090289,-10.5));
#40589=CARTESIAN_POINT('Ctrl Pts',(95.1500570571513,0.275747766322456,-10.5));
#40590=CARTESIAN_POINT('Ctrl Pts',(95.1511771699739,0.285557082169919,-10.5));
#40591=CARTESIAN_POINT('Ctrl Pts',(95.1524115154242,0.295345846772921,-10.5));
#40592=CARTESIAN_POINT('Ctrl Pts',(95.1590576930707,0.348052217159999,-10.5));
#40593=CARTESIAN_POINT('Ctrl Pts',(95.1690182934861,0.400230513827266,-10.5));
#40594=CARTESIAN_POINT('Ctrl Pts',(95.1820544730012,0.451656851506956,-10.5));
#40595=CARTESIAN_POINT('Ctrl Pts',(95.1955365881926,0.504842357864085,-10.5));
#40596=CARTESIAN_POINT('Ctrl Pts',(95.2123083596628,0.557224436802563,-10.5));
#40597=CARTESIAN_POINT('Ctrl Pts',(95.2321614793495,0.608561995447114,-10.5));
#40598=CARTESIAN_POINT('Ctrl Pts',(95.2464121121572,0.645412259235966,-10.5));
#40599=CARTESIAN_POINT('Ctrl Pts',(95.2622515842379,0.681724527967293,-10.5));
#40600=CARTESIAN_POINT('Ctrl Pts',(95.2796192182905,0.717407656638586,-10.5));
#40601=CARTESIAN_POINT('Ctrl Pts',(95.2866053987556,0.731761297192127,-10.5));
#40602=CARTESIAN_POINT('Ctrl Pts',(95.2938389938601,0.746013100506293,-10.5));
#40603=CARTESIAN_POINT('Ctrl Pts',(95.3013166297465,0.760156939120319,-10.5));
#40604=CARTESIAN_POINT('Ctrl Pts',(95.3063377624319,0.7696543379561,-10.5));
#40605=CARTESIAN_POINT('Ctrl Pts',(95.3114688717837,0.779102706153686,-10.5));
#40606=CARTESIAN_POINT('Ctrl Pts',(95.3167019374426,0.788488138842627,-10.5));
#40607=CARTESIAN_POINT('Ctrl Pts',(95.3444794956177,0.838306814836282,-10.5));
#40608=CARTESIAN_POINT('Ctrl Pts',(95.3751713649573,0.886440870645454,-10.5));
#40609=CARTESIAN_POINT('Ctrl Pts',(95.4085627630981,0.932633649457067,-10.5));
#40610=CARTESIAN_POINT('Ctrl Pts',(95.4365439625058,0.971342102145167,-10.5));
#40611=CARTESIAN_POINT('Ctrl Pts',(95.4664218796374,1.00868767887304,-10.5));
#40612=CARTESIAN_POINT('Ctrl Pts',(95.4980964137371,1.0445113235797,-10.5));
#40613=CARTESIAN_POINT('Ctrl Pts',(95.5067327648042,1.05427896755563,-10.5));
#40614=CARTESIAN_POINT('Ctrl Pts',(95.5155028091272,1.06393340204177,-10.5));
#40615=CARTESIAN_POINT('Ctrl Pts',(95.5244047958277,1.07347123922404,-10.5));
#40616=CARTESIAN_POINT('Ctrl Pts',(95.5330197495047,1.0827015412082,-10.5));
#40617=CARTESIAN_POINT('Ctrl Pts',(95.5417528075879,1.09181672209954,-10.5));
#40618=CARTESIAN_POINT('Ctrl Pts',(95.5505984710309,1.10081064316732,-10.5));
#40619=CARTESIAN_POINT('Ctrl Pts',(95.5918901186315,1.14279435887975,-10.5));
#40620=CARTESIAN_POINT('Ctrl Pts',(95.6356542695399,1.18216184934901,-10.5));
#40621=CARTESIAN_POINT('Ctrl Pts',(95.6816922111834,1.2186319374679,-10.5));
#40622=CARTESIAN_POINT('Ctrl Pts',(95.7277301528269,1.25510202558684,-10.5));
#40623=CARTESIAN_POINT('Ctrl Pts',(95.7760424196809,1.28867583950039,-10.5));
#40624=CARTESIAN_POINT('Ctrl Pts',(95.8264738550018,1.31904027763685,-10.5));
#40625=CARTESIAN_POINT('Ctrl Pts',(95.7870390291235,-0.966214801312805,
-10.4999999999999));
#40626=CARTESIAN_POINT('Ctrl Pts',(95.7831492272154,-0.963503648819942,
-10.5001713133822));
#40627=CARTESIAN_POINT('Ctrl Pts',(95.7792757974046,-0.960769006609016,
-10.5003426267644));
#40628=CARTESIAN_POINT('Ctrl Pts',(95.7754190221833,-0.958011074119503,
-10.5005139401467));
#40629=CARTESIAN_POINT('Ctrl Pts',(95.8249089770643,1.32073714597366,1.47379938114645E-14));
#40630=CARTESIAN_POINT('Ctrl Pts',(95.7882096295246,1.29890519325284,2.47546172164436E-14));
#40631=CARTESIAN_POINT('Ctrl Pts',(95.7526292179146,1.27542989100163,4.25615003845605E-15));
#40632=CARTESIAN_POINT('Ctrl Pts',(95.7182919635207,1.25031227307591,9.89139326001975E-15));
#40633=CARTESIAN_POINT('Ctrl Pts',(95.6717202412518,1.21624517170915,1.73698872156513E-14));
#40634=CARTESIAN_POINT('Ctrl Pts',(95.6274334991323,1.17915789839703,9.97151118260645E-16));
#40635=CARTESIAN_POINT('Ctrl Pts',(95.585565943421,1.1393743846506,6.57807142090405E-15));
#40636=CARTESIAN_POINT('Ctrl Pts',(95.5491852857017,1.10480464749038,1.1427591481002E-14));
#40637=CARTESIAN_POINT('Ctrl Pts',(95.5146317052295,1.06819794712208,6.30435606573601E-15));
#40638=CARTESIAN_POINT('Ctrl Pts',(95.4820208735387,1.02975084482163,6.20337115009306E-15));
#40639=CARTESIAN_POINT('Ctrl Pts',(95.4671764842234,1.01224979609028,6.07670337588304E-15));
#40640=CARTESIAN_POINT('Ctrl Pts',(95.4527350160314,0.994367261227605,1.23663649028217E-14));
#40641=CARTESIAN_POINT('Ctrl Pts',(95.4387093357306,0.976121279115226,1.82250048386123E-14));
#40642=CARTESIAN_POINT('Ctrl Pts',(95.4322004051361,0.967653823087995,2.0923811005169E-14));
#40643=CARTESIAN_POINT('Ctrl Pts',(95.4257810378785,0.959108091365199,2.27073921460578E-14));
#40644=CARTESIAN_POINT('Ctrl Pts',(95.419452614983,0.950485878413156,8.29891710907305E-15));
#40645=CARTESIAN_POINT('Ctrl Pts',(95.4129727980227,0.941657397345356,-6.60253895520359E-15));
#40646=CARTESIAN_POINT('Ctrl Pts',(95.4065928858365,0.932754851908662,1.77479395350164E-16));
#40647=CARTESIAN_POINT('Ctrl Pts',(95.4003179024342,0.923786314242425,3.69843045078255E-15));
#40648=CARTESIAN_POINT('Ctrl Pts',(95.3677308770152,0.877211216563209,2.16423796791319E-14));
#40649=CARTESIAN_POINT('Ctrl Pts',(95.3379338541689,0.828809305904207,1.19539479630578E-14));
#40650=CARTESIAN_POINT('Ctrl Pts',(95.3110606737817,0.77888382467263,8.24340595784179E-15));
#40651=CARTESIAN_POINT('Ctrl Pts',(95.2843801273044,0.72931622220764,4.55946207774017E-15));
#40652=CARTESIAN_POINT('Ctrl Pts',(95.2605813437002,0.678245682189612,-5.6098006835629E-15));
#40653=CARTESIAN_POINT('Ctrl Pts',(95.2398443953752,0.625955786165572,-1.25247034965525E-14));
#40654=CARTESIAN_POINT('Ctrl Pts',(95.2218459942583,0.580571358898283,-1.84710252423929E-14));
#40655=CARTESIAN_POINT('Ctrl Pts',(95.2061547434338,0.534267750929017,7.33456568098874E-15));
#40656=CARTESIAN_POINT('Ctrl Pts',(95.1929214733713,0.487231932453229,-1.0692835505921E-14));
#40657=CARTESIAN_POINT('Ctrl Pts',(95.1889192493455,0.473006583624943,-1.60992812190512E-14));
#40658=CARTESIAN_POINT('Ctrl Pts',(95.1851406834792,0.458707962306186,1.6491895291636E-14));
#40659=CARTESIAN_POINT('Ctrl Pts',(95.1815985241459,0.444375806041165,1.71807013060743E-14));
#40660=CARTESIAN_POINT('Ctrl Pts',(95.168691449557,0.392151670274027,1.95643296332385E-14));
#40661=CARTESIAN_POINT('Ctrl Pts',(95.158897674096,0.339415368628355,-4.77953976795929E-15));
#40662=CARTESIAN_POINT('Ctrl Pts',(95.1523649309639,0.286422180494928,-6.99440505513849E-15));
#40663=CARTESIAN_POINT('Ctrl Pts',(95.1459203851088,0.234144442946058,-9.17936788277064E-15));
#40664=CARTESIAN_POINT('Ctrl Pts',(95.1426492616811,0.1816158105116,-1.2022342687055E-14));
#40665=CARTESIAN_POINT('Ctrl Pts',(95.1427428232365,0.129086762469465,9.96425164601078E-15));
#40666=CARTESIAN_POINT('Ctrl Pts',(95.1427865748878,0.10452290626488,2.02972138732121E-14));
#40667=CARTESIAN_POINT('Ctrl Pts',(95.1435668137101,0.0799591192207672,
8.29095392627298E-15));
#40668=CARTESIAN_POINT('Ctrl Pts',(95.1451070256586,0.0554222538728419,
1.63619118254132E-14));
#40669=CARTESIAN_POINT('Ctrl Pts',(95.1469030423967,0.0268102041407893,
2.57643491551798E-14));
#40670=CARTESIAN_POINT('Ctrl Pts',(95.1497324600441,-0.00176532152798841,
2.28418772120502E-14));
#40671=CARTESIAN_POINT('Ctrl Pts',(95.1535760456806,-0.0302592959787804,
2.42444953002519E-14));
#40672=CARTESIAN_POINT('Ctrl Pts',(95.1551319527013,-0.041793831458969,
2.50559662492533E-14));
#40673=CARTESIAN_POINT('Ctrl Pts',(95.1568545835752,-0.0533170828206849,
9.15937163043892E-15));
#40674=CARTESIAN_POINT('Ctrl Pts',(95.1587387377557,-0.064803940851461,
1.1671219546372E-14));
#40675=CARTESIAN_POINT('Ctrl Pts',(95.1672789468338,-0.116869833466758,
2.27889665739075E-14));
#40676=CARTESIAN_POINT('Ctrl Pts',(95.1791453848401,-0.168288980706651,
-1.08395901568713E-14));
#40677=CARTESIAN_POINT('Ctrl Pts',(95.194147378263,-0.218805534067158,-1.06858966120171E-15));
#40678=CARTESIAN_POINT('Ctrl Pts',(95.2092083821131,-0.269520794580306,
8.71771805315145E-15));
#40679=CARTESIAN_POINT('Ctrl Pts',(95.2274304072348,-0.319327333795833,
-1.20151378749622E-14));
#40680=CARTESIAN_POINT('Ctrl Pts',(95.2486662510227,-0.367940603828083,
-1.25316423904565E-14));
#40681=CARTESIAN_POINT('Ctrl Pts',(95.2620753394337,-0.398636800424634,
-1.2922186424885E-14));
#40682=CARTESIAN_POINT('Ctrl Pts',(95.2766869482097,-0.428856661622077,
2.14493485157268E-14));
#40683=CARTESIAN_POINT('Ctrl Pts',(95.2924713193047,-0.458520632581111,
2.45081732686003E-14));
#40684=CARTESIAN_POINT('Ctrl Pts',(95.3008107067378,-0.474193055963875,
2.60243438444447E-14));
#40685=CARTESIAN_POINT('Ctrl Pts',(95.3094775372499,-0.489710195447915,
2.29976605015753E-15));
#40686=CARTESIAN_POINT('Ctrl Pts',(95.3184679272418,-0.505059462317017,
1.29479760246909E-14));
#40687=CARTESIAN_POINT('Ctrl Pts',(95.3242758264827,-0.514975271918048,
1.99495353990142E-14));
#40688=CARTESIAN_POINT('Ctrl Pts',(95.3302143331834,-0.524813350049739,
1.92471923790151E-14));
#40689=CARTESIAN_POINT('Ctrl Pts',(95.3362788672618,-0.534565975662569,
1.7125190154843E-14));
#40690=CARTESIAN_POINT('Ctrl Pts',(95.3635106434983,-0.578358510253512,
8.19581166695719E-15));
#40691=CARTESIAN_POINT('Ctrl Pts',(95.3932993713737,-0.620462763195338,
1.21772296880902E-14));
#40692=CARTESIAN_POINT('Ctrl Pts',(95.4255117600527,-0.660602238459277,
1.63757896132211E-15));
#40693=CARTESIAN_POINT('Ctrl Pts',(95.4506195460652,-0.691888752651906,
-6.61641427583824E-15));
#40694=CARTESIAN_POINT('Ctrl Pts',(95.4772006416695,-0.721981045963318,
9.76424046132771E-15));
#40695=CARTESIAN_POINT('Ctrl Pts',(95.5052033941774,-0.750728856696811,
1.41830991395864E-14));
#40696=CARTESIAN_POINT('Ctrl Pts',(95.5160198476517,-0.761833099295801,
1.584519613144E-14));
#40697=CARTESIAN_POINT('Ctrl Pts',(95.5270521274395,-0.77273972936565,-1.46751849299723E-15));
#40698=CARTESIAN_POINT('Ctrl Pts',(95.5382756714544,-0.783419267701306,
1.94289029309402E-15));
#40699=CARTESIAN_POINT('Ctrl Pts',(95.5740535630002,-0.817463003247418,
1.30361735751359E-14));
#40700=CARTESIAN_POINT('Ctrl Pts',(95.6118085679276,-0.849241382244103,
-8.74677678469814E-15));
#40701=CARTESIAN_POINT('Ctrl Pts',(95.6514318537012,-0.878485337795217,
-1.27675647831893E-15));
#40702=CARTESIAN_POINT('Ctrl Pts',(95.6910551394747,-0.90772929334633,6.2769800476697E-15));
#40703=CARTESIAN_POINT('Ctrl Pts',(95.7325473555912,-0.934439521706132,
8.70022739947829E-15));
#40704=CARTESIAN_POINT('Ctrl Pts',(95.7758165250375,-0.958295198918397,
1.22124532708767E-14));
#40705=CARTESIAN_POINT('Origin',(96.460480949577,-2.11854640757359E-15,
-10.5));
#40706=CARTESIAN_POINT('Origin',(96.460480949577,-8.32667268468867E-16,
1.18130019239114E-14));
#40723=UNCERTAINTY_MEASURE_WITH_UNIT(LENGTH_MEASURE(0.01),#40735,
'DISTANCE_ACCURACY_VALUE',
'Maximum model space distance between geometric entities at asserted c
onnectivities');
#40724=UNCERTAINTY_MEASURE_WITH_UNIT(LENGTH_MEASURE(0.01),#40735,
'DISTANCE_ACCURACY_VALUE',
'Maximum model space distance between geometric entities at asserted c
onnectivities');
#40733=(
GEOMETRIC_REPRESENTATION_CONTEXT(3)
GLOBAL_UNCERTAINTY_ASSIGNED_CONTEXT((#40723))
GLOBAL_UNIT_ASSIGNED_CONTEXT((#40735,#40737,#40738))
REPRESENTATION_CONTEXT('','3D')
);
#40734=(
GEOMETRIC_REPRESENTATION_CONTEXT(3)
GLOBAL_UNCERTAINTY_ASSIGNED_CONTEXT((#40724))
GLOBAL_UNIT_ASSIGNED_CONTEXT((#40735,#40737,#40738))
REPRESENTATION_CONTEXT('','3D')
);
#40735=(
LENGTH_UNIT()
NAMED_UNIT(*)
SI_UNIT(.MILLI.,.METRE.)
);
#40737=(
NAMED_UNIT(*)
PLANE_ANGLE_UNIT()
SI_UNIT($,.RADIAN.)
);
#40738=(
NAMED_UNIT(*)
SI_UNIT($,.STERADIAN.)
SOLID_ANGLE_UNIT()
);
#40747=SHAPE_DEFINITION_REPRESENTATION(#40756,#40773);
#40756=PRODUCT_DEFINITION_SHAPE('',$,#40783);
#40773=SHAPE_REPRESENTATION('',(#3423),#40733);
#40774=PRODUCT_DEFINITION_CONTEXT('part definition',#40803,'design');
#40783=PRODUCT_DEFINITION('Screw (1)','Screw_right',#40792,#40774);
#40792=PRODUCT_DEFINITION_FORMATION('',$,#40813);
#40803=APPLICATION_CONTEXT(
'Core Data for Automotive Mechanical Design Process');
#40804=PRODUCT_CONTEXT('part definition',#40803,'mechanical');
#40813=PRODUCT('Screw (1)','Screw_right',$,(#40804));
#40815=PRESENTATION_STYLE_ASSIGNMENT((#40818));
#40818=SURFACE_STYLE_USAGE(.BOTH.,#40821);
#40821=SURFACE_SIDE_STYLE('',(#40824));
#40824=SURFACE_STYLE_FILL_AREA(#40827);
#40827=FILL_AREA_STYLE('Opaque(203,203,203)',(#40830));
#40830=FILL_AREA_STYLE_COLOUR('Opaque(203,203,203)',#40833);
#40833=COLOUR_RGB('Opaque(203,203,203)', 0.09019608, 0.27058824, 0.51372549);
ENDSEC;
END-ISO-10303-21;
